ISO-10303-21;
HEADER;
FILE_DESCRIPTION (('STEP AP214'),
    '1' );
FILE_NAME ('Injection Molded Chain Links 3.step',
    '2026-10-08T22:59:04',
    ( '' ),
    ( '' ),
    'SwSTEP 2.0',
    'SolidWorks 2020',
    '' );
FILE_SCHEMA (( 'AUTOMOTIVE_DESIGN' ));
ENDSEC;

DATA;
#4=DIRECTION ( 'NONE',  ( 0.000000000000000000, 0.000000000000000000, -1.000000000000000000 ) ) ;
#20=LINE ( 'NONE', #198225, #75570 ) ;
#22=CARTESIAN_POINT ( 'NONE',  ( 21.05000000000000071, 11.75000000001116263, -93.48519422934610645 ) ) ;
#43=TOROIDAL_SURFACE ( 'NONE', #87521, 0.2000000000000000111, 0.1000000000000000056 ) ;
#59=CARTESIAN_POINT ( 'NONE',  ( 21.05000000000000071, -0.08559286335111461475, -60.58633726513042461 ) ) ;
#84=EDGE_CURVE ( 'NONE', #177357, #123054, #144663, .T. ) ;
#96=EDGE_LOOP ( 'NONE', ( #150504, #184348, #87694, #206446 ) ) ;
#110=EDGE_CURVE ( 'NONE', #147343, #202762, #12898, .T. ) ;
#143=AXIS2_PLACEMENT_3D ( 'NONE', #77919, #25665, #21818 ) ;
#197=EDGE_CURVE ( 'NONE', #86923, #12856, #126876, .T. ) ;
#230=DIRECTION ( 'NONE',  ( 0.000000000000000000, 0.000000000000000000, -1.000000000000000000 ) ) ;
#246=CARTESIAN_POINT ( 'NONE',  ( 22.39999999999999503, -0.09999999998884338825, -55.35042919245524473 ) ) ;
#275=EDGE_LOOP ( 'NONE', ( #125788, #98661, #200671, #130469 ) ) ;
#312=ADVANCED_FACE ( 'NONE', ( #35040 ), #74164, .F. ) ;
#341=AXIS2_PLACEMENT_3D ( 'NONE', #63201, #44950, #142741 ) ;
#357=AXIS2_PLACEMENT_3D ( 'NONE', #213494, #19149, #34902 ) ;
#366=DIRECTION ( 'NONE',  ( 0.000000000000000000, 0.000000000000000000, -1.000000000000000000 ) ) ;
#374=VERTEX_POINT ( 'NONE', #183498 ) ;
#376=ORIENTED_EDGE ( 'NONE', *, *, #193695, .T. ) ;
#394=CYLINDRICAL_SURFACE ( 'NONE', #26043, 0.09999999999999939493 ) ;
#399=CARTESIAN_POINT ( 'NONE',  ( 21.05000000000000071, -11.74999999998883560, -97.40000000000004832 ) ) ;
#441=LINE ( 'NONE', #175283, #227247 ) ;
#449=VECTOR ( 'NONE', #150397, 1000.000000000000000 ) ;
#458=EDGE_CURVE ( 'NONE', #4905, #253894, #120982, .T. ) ;
#475=AXIS2_PLACEMENT_3D ( 'NONE', #177956, #81371, #38431 ) ;
#480=ORIENTED_EDGE ( 'NONE', *, *, #233587, .T. ) ;
#481=EDGE_CURVE ( 'NONE', #3545, #139104, #71272, .T. ) ;
#492=DIRECTION ( 'NONE',  ( 0.000000000000000000, -1.000000000000000000, -2.891205793294679805E-16 ) ) ;
#502=CARTESIAN_POINT ( 'NONE',  ( 22.39999999999999503, 11.75000000001115552, -67.00000000000004263 ) ) ;
#575=ORIENTED_EDGE ( 'NONE', *, *, #24922, .T. ) ;
#623=CARTESIAN_POINT ( 'NONE',  ( 21.06490991615909181, 10.72489134759826790, -79.20371135353316561 ) ) ;
#630=CARTESIAN_POINT ( 'NONE',  ( -18.59999999999999787, 1.115600667400684642E-11, -67.00000000000004263 ) ) ;
#698=DIRECTION ( 'NONE',  ( -1.000000000000000000, 0.000000000000000000, 0.000000000000000000 ) ) ;
#716=ORIENTED_EDGE ( 'NONE', *, *, #78279, .T. ) ;
#728=DIRECTION ( 'NONE',  ( 0.000000000000000000, 0.9908441862701600211, -0.1350103645451876666 ) ) ;
#872=CARTESIAN_POINT ( 'NONE',  ( 23.15000000000000213, -12.41227409413852811, -97.50000000000004263 ) ) ;
#905=CARTESIAN_POINT ( 'NONE',  ( -23.15000000000000213, 1.925233644870972816, -79.73024353312617052 ) ) ;
#909=CARTESIAN_POINT ( 'NONE',  ( -23.15000000000000213, 4.250000000011156409, -88.25000000000005684 ) ) ;
#924=CARTESIAN_POINT ( 'NONE',  ( -22.49510344025093644, 0.06712767820541534758, -55.35002989488578606 ) ) ;
#927=EDGE_LOOP ( 'NONE', ( #85776, #236101, #50558, #161418 ) ) ;
#941=UNCERTAINTY_MEASURE_WITH_UNIT (LENGTH_MEASURE( 1.000000000000000082E-05 ), #199056, 'distance_accuracy_value', 'NONE');
#981=CARTESIAN_POINT ( 'NONE',  ( 20.94999999999999929, 1.115600667400684642E-11, -100.5000000000000426 ) ) ;
#983=CARTESIAN_POINT ( 'NONE',  ( -23.25000000000000000, 2.000000000011154189, -87.87537807723795424 ) ) ;
#999=CARTESIAN_POINT ( 'NONE',  ( -20.94999999999999929, 1.115600667400684642E-11, -100.5000000000000426 ) ) ;
#1015=CIRCLE ( 'NONE', #130218, 0.09999999999999907574 ) ;
#1023=DIRECTION ( 'NONE',  ( 0.000000000000000000, 0.000000000000000000, 1.000000000000000000 ) ) ;
#1088=ORIENTED_EDGE ( 'NONE', *, *, #35954, .T. ) ;
#1092=CARTESIAN_POINT ( 'NONE',  ( 20.94999999999999929, -8.730841121484166578, -90.90192528101570701 ) ) ;
#1110=FACE_OUTER_BOUND ( 'NONE', #233161, .T. ) ;
#1138=ORIENTED_EDGE ( 'NONE', *, *, #55559, .F. ) ;
#1169=EDGE_CURVE ( 'NONE', #149634, #78058, #175861, .T. ) ;
#1183=AXIS2_PLACEMENT_3D ( 'NONE', #208111, #209369, #67292 ) ;
#1219=DIRECTION ( 'NONE',  ( 1.000000000000000000, -0.000000000000000000, -0.000000000000000000 ) ) ;
#1222=VECTOR ( 'NONE', #70005, 1000.000000000000000 ) ;
#1250=CIRCLE ( 'NONE', #209554, 0.2000000000000057288 ) ;
#1253=ADVANCED_FACE ( 'NONE', ( #12943 ), #10365, .F. ) ;
#1271=ORIENTED_EDGE ( 'NONE', *, *, #247386, .F. ) ;
#1272=EDGE_CURVE ( 'NONE', #91651, #218145, #55012, .T. ) ;
#1321=LINE ( 'NONE', #118740, #239105 ) ;
#1389=TOROIDAL_SURFACE ( 'NONE', #39030, 0.2000000000000000111, 0.1000000000000000056 ) ;
#1399=( LENGTH_UNIT ( ) NAMED_UNIT ( * ) SI_UNIT ( .MILLI., .METRE. ) );
#1420=CARTESIAN_POINT ( 'NONE',  ( -18.59999999999999787, 11.65000000001115232, -74.01480577065404987 ) ) ;
#1428=ADVANCED_FACE ( 'NONE', ( #156308 ), #251014, .T. ) ;
#1460=VECTOR ( 'NONE', #174331, 1000.000000000000000 ) ;
#1469=CYLINDRICAL_SURFACE ( 'NONE', #111460, 0.1000000000000028644 ) ;
#1487=DIRECTION ( 'NONE',  ( 1.000000000000000000, 0.000000000000000000, 0.000000000000000000 ) ) ;
#1499=CARTESIAN_POINT ( 'NONE',  ( -20.94999999999999929, 1.115600667400684642E-11, -96.40000000000003411 ) ) ;
#1501=EDGE_LOOP ( 'NONE', ( #80472, #68584, #253815, #52085 ) ) ;
#1549=CYLINDRICAL_SURFACE ( 'NONE', #157506, 0.09999999999999939493 ) ;
#1559=CARTESIAN_POINT ( 'NONE',  ( 23.14999999999999858, 2.000000000011158630, -100.5000000000000426 ) ) ;
#1624=DIRECTION ( 'NONE',  ( 0.000000000000000000, 0.000000000000000000, -1.000000000000000000 ) ) ;
#1649=CARTESIAN_POINT ( 'NONE',  ( -18.59999999999999787, 9.350000000011156942, -88.25000000000005684 ) ) ;
#1688=ORIENTED_EDGE ( 'NONE', *, *, #170645, .T. ) ;
#1692=CARTESIAN_POINT ( 'NONE',  ( -20.64999999999999858, 2.000000000011154189, -87.27537807723794572 ) ) ;
#1709=AXIS2_PLACEMENT_3D ( 'NONE', #219039, #76967, #142072 ) ;
#1728=AXIS2_PLACEMENT_3D ( 'NONE', #100004, #115753, #236991 ) ;
#1761=AXIS2_PLACEMENT_3D ( 'NONE', #217075, #1877, #162281 ) ;
#1774=LINE ( 'NONE', #179174, #234436 ) ;
#1787=CARTESIAN_POINT ( 'NONE',  ( 23.14999999999999858, 1.115600667400684642E-11, -100.5000000000000426 ) ) ;
#1797=CIRCLE ( 'NONE', #243412, 0.1000000000000002554 ) ;
#1813=DIRECTION ( 'NONE',  ( 0.000000000000000000, 0.000000000000000000, -1.000000000000000000 ) ) ;
#1864=CARTESIAN_POINT ( 'NONE',  ( -18.59999999999999787, -1.249999999988843369, -75.00000000000004263 ) ) ;
#1868=CIRCLE ( 'NONE', #135143, 3.899999999999999467 ) ;
#1877=DIRECTION ( 'NONE',  ( -1.000000000000000000, -0.000000000000000000, 0.000000000000000000 ) ) ;
#1891=ORIENTED_EDGE ( 'NONE', *, *, #139422, .T. ) ;
#1913=ORIENTED_EDGE ( 'NONE', *, *, #102055, .F. ) ;
#1945=CIRCLE ( 'NONE', #113834, 0.9750000000000036415 ) ;
#1964=EDGE_CURVE ( 'NONE', #195562, #196915, #50122, .T. ) ;
#1970=EDGE_CURVE ( 'NONE', #257729, #70270, #134489, .T. ) ;
#1984=DIRECTION ( 'NONE',  ( 0.000000000000000000, 0.000000000000000000, -1.000000000000000000 ) ) ;
#2019=ORIENTED_EDGE ( 'NONE', *, *, #17909, .T. ) ;
#2058=ORIENTED_EDGE ( 'NONE', *, *, #174890, .F. ) ;
#2061=AXIS2_PLACEMENT_3D ( 'NONE', #88179, #246008, #206879 ) ;
#2068=ADVANCED_FACE ( 'NONE', ( #53983 ), #194808, .T. ) ;
#2110=EDGE_CURVE ( 'NONE', #153327, #225893, #171407, .T. ) ;
#2158=DIRECTION ( 'NONE',  ( -1.000000000000000000, -0.000000000000000000, -0.000000000000000000 ) ) ;
#2161=ORIENTED_EDGE ( 'NONE', *, *, #100078, .F. ) ;
#2173=DIRECTION ( 'NONE',  ( 0.000000000000000000, 0.000000000000000000, -1.000000000000000000 ) ) ;
#2183=CARTESIAN_POINT ( 'NONE',  ( 18.49999999999999289, 6.450000000011156587, -77.01702717044007329 ) ) ;
#2221=CIRCLE ( 'NONE', #214611, 0.5000000000000004441 ) ;
#2248=CARTESIAN_POINT ( 'NONE',  ( -21.65000000000000213, 7.708578643773852157, -88.15000000000004832 ) ) ;
#2255=LINE ( 'NONE', #41426, #216030 ) ;
#2274=ORIENTED_EDGE ( 'NONE', *, *, #41752, .T. ) ;
#2276=ORIENTED_EDGE ( 'NONE', *, *, #136399, .F. ) ;
#2303=AXIS2_PLACEMENT_3D ( 'NONE', #215291, #116217, #17118 ) ;
#2322=VERTEX_POINT ( 'NONE', #164653 ) ;
#2371=EDGE_LOOP ( 'NONE', ( #248798, #144734, #105475 ) ) ;
#2381=LINE ( 'NONE', #20704, #57114 ) ;
#2387=CARTESIAN_POINT ( 'NONE',  ( 23.24999999999999289, 11.75000000001116263, -55.25000000000004974 ) ) ;
#2389=CARTESIAN_POINT ( 'NONE',  ( -20.94999999999999929, 11.65000000001115232, -93.71613433702194129 ) ) ;
#2419=CARTESIAN_POINT ( 'NONE',  ( 22.42196299218230493, 0.002441673998456600492, -55.35038829735057675 ) ) ;
#2425=AXIS2_PLACEMENT_3D ( 'NONE', #153513, #135160, #16531 ) ;
#2450=DIRECTION ( 'NONE',  ( 1.000000000000000000, 0.000000000000000000, 0.000000000000000000 ) ) ;
#2463=DIRECTION ( 'NONE',  ( 1.000000000000000000, -0.000000000000000000, -0.000000000000000000 ) ) ;
#2480=CIRCLE ( 'NONE', #98309, 11.80000000000000426 ) ;
#2504=EDGE_CURVE ( 'NONE', #75643, #187772, #112330, .T. ) ;
#2529=DIRECTION ( 'NONE',  ( 1.000000000000000000, -0.000000000000000000, -0.000000000000000000 ) ) ;
#2544=ORIENTED_EDGE ( 'NONE', *, *, #30633, .F. ) ;
#2566=FACE_OUTER_BOUND ( 'NONE', #144052, .T. ) ;
#2581=ADVANCED_FACE ( 'NONE', ( #59942 ), #102922, .T. ) ;
#2649=VECTOR ( 'NONE', #232974, 1000.000000000000000 ) ;
#2660=ORIENTED_EDGE ( 'NONE', *, *, #171683, .T. ) ;
#2672=LINE ( 'NONE', #84747, #218888 ) ;
#2681=CARTESIAN_POINT ( 'NONE',  ( -23.15000000000000213, -8.999999999988844479, -91.10603087734760663 ) ) ;
#2685=EDGE_LOOP ( 'NONE', ( #83981, #123688, #240456, #190334 ) ) ;
#2700=AXIS2_PLACEMENT_3D ( 'NONE', #38627, #98548, #19057 ) ;
#2727=CARTESIAN_POINT ( 'NONE',  ( 18.59999999999999432, -1.299733671219632791, -57.02812952286944892 ) ) ;
#2747=DIRECTION ( 'NONE',  ( 1.000000000000000000, 0.000000000000000000, 0.000000000000000000 ) ) ;
#2750=CARTESIAN_POINT ( 'NONE',  ( -20.93302460841142931, 10.31565961587945424, -106.0364194119178620 ) ) ;
#2760=CARTESIAN_POINT ( 'NONE',  ( 21.05000000000000071, -8.999999999988842703, -91.10603087734760663 ) ) ;
#2769=CARTESIAN_POINT ( 'NONE',  ( -21.05000000000000071, -0.01771943329742826576, -60.55891531152861518 ) ) ;
#2796=ORIENTED_EDGE ( 'NONE', *, *, #159102, .F. ) ;
#2797=LINE ( 'NONE', #40703, #158002 ) ;
#2831=CARTESIAN_POINT ( 'NONE',  ( 18.44444291854882678, -9.490101180932068559, -107.1289039648910233 ) ) ;
#2839=CARTESIAN_POINT ( 'NONE',  ( -18.59999999999999787, 11.75000000001115552, -88.25000000000005684 ) ) ;
#2840=EDGE_CURVE ( 'NONE', #128673, #153546, #241988, .T. ) ;
#2851=ORIENTED_EDGE ( 'NONE', *, *, #53293, .F. ) ;
#2872=CARTESIAN_POINT ( 'NONE',  ( 21.05000000000000071, -1.360870587180885716, -75.07299792709100927 ) ) ;
#2889=CARTESIAN_POINT ( 'NONE',  ( -21.05000000000000071, 1.835341550235569663, -78.55515129256303908 ) ) ;
#2935=EDGE_CURVE ( 'NONE', #77148, #24665, #143437, .T. ) ;
#2940=LINE ( 'NONE', #201153, #143563 ) ;
#2967=CARTESIAN_POINT ( 'NONE',  ( -20.85000000000000142, 7.021664781911246322, -104.3335654018973315 ) ) ;
#2996=ORIENTED_EDGE ( 'NONE', *, *, #173000, .F. ) ;
#3057=ORIENTED_EDGE ( 'NONE', *, *, #241751, .T. ) ;
#3080=DIRECTION ( 'NONE',  ( 0.000000000000000000, 1.000000000000000000, -6.308085367188393199E-16 ) ) ;
#3104=ADVANCED_FACE ( 'NONE', ( #191034 ), #175327, .F. ) ;
#3109=EDGE_CURVE ( 'NONE', #17147, #94857, #235029, .T. ) ;
#3117=CARTESIAN_POINT ( 'NONE',  ( 21.05000000000000071, 6.413978881499641460, -67.08579911627448666 ) ) ;
#3141=DIRECTION ( 'NONE',  ( 0.000000000000000000, 0.000000000000000000, 1.000000000000000000 ) ) ;
#3186=CARTESIAN_POINT ( 'NONE',  ( -21.05000000000000071, -12.41227409413852811, -97.60000000000005116 ) ) ;
#3192=VERTEX_POINT ( 'NONE', #252248 ) ;
#3245=EDGE_CURVE ( 'NONE', #236296, #187409, #215683, .T. ) ;
#3247=ORIENTED_EDGE ( 'NONE', *, *, #121550, .T. ) ;
#3250=EDGE_CURVE ( 'NONE', #251583, #12856, #116604, .T. ) ;
#3254=CIRCLE ( 'NONE', #215646, 12.87499999999999822 ) ;
#3255=CARTESIAN_POINT ( 'NONE',  ( 20.94999999999999574, 1.162701749949165642, -75.10000000000003695 ) ) ;
#3342=DIRECTION ( 'NONE',  ( 0.000000000000000000, 0.000000000000000000, 1.000000000000000000 ) ) ;
#3371=DIRECTION ( 'NONE',  ( 0.000000000000000000, 0.000000000000000000, -1.000000000000000000 ) ) ;
#3373=VERTEX_POINT ( 'NONE', #245552 ) ;
#3384=ORIENTED_EDGE ( 'NONE', *, *, #68692, .T. ) ;
#3392=AXIS2_PLACEMENT_3D ( 'NONE', #227620, #89393, #26895 ) ;
#3397=FILL_AREA_STYLE ('',( #140345 ) ) ;
#3435=FACE_OUTER_BOUND ( 'NONE', #49851, .T. ) ;
#3446=AXIS2_PLACEMENT_3D ( 'NONE', #8011, #107086, #130501 ) ;
#3464=CARTESIAN_POINT ( 'NONE',  ( 18.49999999999999645, -1.164121893230052995, -108.4148480855716485 ) ) ;
#3482=SPHERICAL_SURFACE ( 'NONE', #72528, 0.1000000000000000056 ) ;
#3492=DIRECTION ( 'NONE',  ( 0.000000000000000000, -0.5000000000000078826, -0.8660254037844340447 ) ) ;
#3511=ORIENTED_EDGE ( 'NONE', *, *, #221935, .T. ) ;
#3517=CARTESIAN_POINT ( 'NONE',  ( -22.49756042579671700, 0.07804633702833754794, -55.35013503889771869 ) ) ;
#3524=DIRECTION ( 'NONE',  ( 0.000000000000000000, -1.000000000000000000, 0.000000000000000000 ) ) ;
#3545=VERTEX_POINT ( 'NONE', #55023 ) ;
#3547=DIRECTION ( 'NONE',  ( -1.000000000000000000, 0.000000000000000000, -0.000000000000000000 ) ) ;
#3554=CIRCLE ( 'NONE', #82636, 0.1000000000000028644 ) ;
#3575=CARTESIAN_POINT ( 'NONE',  ( 20.85000000000000142, -1.835859311432481045, -112.0044391687985694 ) ) ;
#3578=CARTESIAN_POINT ( 'NONE',  ( -20.64999999999999858, 7.150000000011155876, -88.15000000000004832 ) ) ;
#3585=AXIS2_PLACEMENT_3D ( 'NONE', #15020, #95797, #72430 ) ;
#3606=CARTESIAN_POINT ( 'NONE',  ( -18.43569575749026512, -9.519327731081288491, -73.97297637655937308 ) ) ;
#3611=DIRECTION ( 'NONE',  ( 0.000000000000000000, 1.000000000000000000, 0.000000000000000000 ) ) ;
#3680=CARTESIAN_POINT ( 'NONE',  ( 18.50000000000000355, -9.399999999988846611, -107.3820418481727188 ) ) ;
#3695=ORIENTED_EDGE ( 'NONE', *, *, #142615, .F. ) ;
#3714=CIRCLE ( 'NONE', #170360, 0.1000000000000028644 ) ;
#3725=AXIS2_PLACEMENT_3D ( 'NONE', #91067, #12837, #192749 ) ;
#3744=ORIENTED_EDGE ( 'NONE', *, *, #115559, .F. ) ;
#3759=DIRECTION ( 'NONE',  ( 0.000000000000000000, -0.000000000000000000, 1.000000000000000000 ) ) ;
#3783=FACE_OUTER_BOUND ( 'NONE', #172469, .T. ) ;
#3795=DIRECTION ( 'NONE',  ( 0.000000000000000000, -1.000000000000000000, 0.000000000000000000 ) ) ;
#3803=DIRECTION ( 'NONE',  ( 1.000000000000000000, 0.000000000000000000, 0.000000000000000000 ) ) ;
#3892=CIRCLE ( 'NONE', #237121, 0.2000000000000057288 ) ;
#3934=EDGE_LOOP ( 'NONE', ( #188992, #180900, #27949, #5598 ) ) ;
#3946=VECTOR ( 'NONE', #228098, 1000.000000000000000 ) ;
#4032=ORIENTED_EDGE ( 'NONE', *, *, #186651, .F. ) ;
#4062=DIRECTION ( 'NONE',  ( 0.000000000000000000, -0.9908441862701596881, -0.1350103645451904977 ) ) ;
#4064=VERTEX_POINT ( 'NONE', #19141 ) ;
#4071=DIRECTION ( 'NONE',  ( 0.000000000000000000, 0.000000000000000000, -1.000000000000000000 ) ) ;
#4102=CARTESIAN_POINT ( 'NONE',  ( -20.94999999999999929, 1.115600667400684642E-11, -96.50000000000004263 ) ) ;
#4107=EDGE_CURVE ( 'NONE', #13417, #257729, #243935, .T. ) ;
#4119=TOROIDAL_SURFACE ( 'NONE', #116560, 0.2000000000000000111, 0.1000000000000000056 ) ;
#4120=CARTESIAN_POINT ( 'NONE',  ( -23.25000000000000000, -11.64999999998884483, -55.25000000000004974 ) ) ;
#4153=AXIS2_PLACEMENT_3D ( 'NONE', #240403, #61755, #224670 ) ;
#4161=LINE ( 'NONE', #6736, #145171 ) ;
#4176=CARTESIAN_POINT ( 'NONE',  ( -23.25000000000000000, 1.115651490242849210E-11, -62.85000000000004405 ) ) ;
#4184=CARTESIAN_POINT ( 'NONE',  ( -21.05000000000000071, 1.115650877919449575E-11, -104.6000000000000512 ) ) ;
#4211=DIRECTION ( 'NONE',  ( -1.000000000000000000, 0.000000000000000000, 0.000000000000000000 ) ) ;
#4212=VERTEX_POINT ( 'NONE', #125929 ) ;
#4223=DIRECTION ( 'NONE',  ( -0.000000000000000000, -1.000000000000000000, 6.308085367188393199E-16 ) ) ;
#4235=CIRCLE ( 'NONE', #137327, 0.09999999999999892308 ) ;
#4239=ORIENTED_EDGE ( 'NONE', *, *, #103625, .F. ) ;
#4255=VERTEX_POINT ( 'NONE', #251002 ) ;
#4278=VECTOR ( 'NONE', #28057, 1000.000000000000000 ) ;
#4337=DIRECTION ( 'NONE',  ( -1.000000000000000000, -1.836970198721029934E-16, 0.000000000000000000 ) ) ;
#4349=DIRECTION ( 'NONE',  ( 0.000000000000000000, 0.000000000000000000, 1.000000000000000000 ) ) ;
#4359=LINE ( 'NONE', #147745, #220275 ) ;
#4391=LINE ( 'NONE', #223436, #145725 ) ;
#4402=DIRECTION ( 'NONE',  ( 1.000000000000000000, 0.000000000000000000, 0.000000000000000000 ) ) ;
#4417=EDGE_LOOP ( 'NONE', ( #70885, #113290, #59142, #181456 ) ) ;
#4426=DIRECTION ( 'NONE',  ( 1.000000000000000000, -0.000000000000000000, -0.000000000000000000 ) ) ;
#4485=EDGE_CURVE ( 'NONE', #37535, #192064, #104897, .T. ) ;
#4499=EDGE_CURVE ( 'NONE', #202644, #229956, #208991, .T. ) ;
#4523=DIRECTION ( 'NONE',  ( 0.000000000000000000, 0.000000000000000000, 1.000000000000000000 ) ) ;
#4531=CARTESIAN_POINT ( 'NONE',  ( 22.50000000000000000, 11.64957080755595520, -66.90000000000004832 ) ) ;
#4553=VECTOR ( 'NONE', #242409, 1000.000000000000000 ) ;
#4554=DIRECTION ( 'NONE',  ( 0.000000000000000000, -0.000000000000000000, 1.000000000000000000 ) ) ;
#4562=EDGE_CURVE ( 'NONE', #242093, #38707, #242304, .T. ) ;
#4586=CARTESIAN_POINT ( 'NONE',  ( -18.59999999999999787, 1.115600667400684642E-11, -100.5000000000000426 ) ) ;
#4588=EDGE_CURVE ( 'NONE', #89932, #39964, #221625, .T. ) ;
#4590=AXIS2_PLACEMENT_3D ( 'NONE', #176333, #219279, #15986 ) ;
#4603=ORIENTED_EDGE ( 'NONE', *, *, #233075, .F. ) ;
#4627=DIRECTION ( 'NONE',  ( 4.239556034732056743E-17, -0.1298341882520022972, -0.9915357197604853789 ) ) ;
#4659=DIRECTION ( 'NONE',  ( -1.000000000000000000, 0.000000000000000000, 0.000000000000000000 ) ) ;
#4670=ORIENTED_EDGE ( 'NONE', *, *, #143665, .F. ) ;
#4672=DIRECTION ( 'NONE',  ( 0.000000000000000000, 0.000000000000000000, 1.000000000000000000 ) ) ;
#4688=DIRECTION ( 'NONE',  ( 0.5000000000001141309, 0.000000000000000000, -0.8660254037843729824 ) ) ;
#4698=CARTESIAN_POINT ( 'NONE',  ( 20.95462737510932882, 10.55678195165489441, -74.56995005656234810 ) ) ;
#4722=EDGE_CURVE ( 'NONE', #151819, #250043, #105082, .T. ) ;
#4746=AXIS2_PLACEMENT_3D ( 'NONE', #20853, #156523, #174815 ) ;
#4762=FACE_OUTER_BOUND ( 'NONE', #199336, .T. ) ;
#4767=CARTESIAN_POINT ( 'NONE',  ( -18.52328366898031931, -9.642321089030096104, -107.2148193375700913 ) ) ;
#4780=CARTESIAN_POINT ( 'NONE',  ( 18.59999999999999432, 1.162701749949165642, -75.10000000000003695 ) ) ;
#4788=EDGE_LOOP ( 'NONE', ( #164385, #234012, #149234 ) ) ;
#4797=ORIENTED_EDGE ( 'NONE', *, *, #236602, .F. ) ;
#4854=CARTESIAN_POINT ( 'NONE',  ( 20.85000000000000142, 1.115600667400684642E-11, -100.5000000000000426 ) ) ;
#4871=CARTESIAN_POINT ( 'NONE',  ( -20.64999999999999858, 7.150000000011155876, -79.35000000000005116 ) ) ;
#4885=FACE_OUTER_BOUND ( 'NONE', #96604, .T. ) ;
#4905=VERTEX_POINT ( 'NONE', #173509 ) ;
#4915=ORIENTED_EDGE ( 'NONE', *, *, #74996, .F. ) ;
#4916=ORIENTED_EDGE ( 'NONE', *, *, #135592, .T. ) ;
#4930=VERTEX_POINT ( 'NONE', #210023 ) ;
#4935=ORIENTED_EDGE ( 'NONE', *, *, #77415, .T. ) ;
#4961=ORIENTED_EDGE ( 'NONE', *, *, #41112, .F. ) ;
#5063=ORIENTED_EDGE ( 'NONE', *, *, #101790, .T. ) ;
#5075=CARTESIAN_POINT ( 'NONE',  ( -18.44362607810620958, -9.490496158073669974, -74.05795386684718551 ) ) ;
#5084=FACE_OUTER_BOUND ( 'NONE', #29685, .T. ) ;
#5093=EDGE_CURVE ( 'NONE', #256646, #6741, #42763, .T. ) ;
#5099=DIRECTION ( 'NONE',  ( -0.000000000000000000, -0.000000000000000000, 1.000000000000000000 ) ) ;
#5110=DIRECTION ( 'NONE',  ( -1.000000000000000000, 0.000000000000000000, 0.000000000000000000 ) ) ;
#5111=DIRECTION ( 'NONE',  ( -1.000000000000000000, -0.000000000000000000, -0.000000000000000000 ) ) ;
#5123=CARTESIAN_POINT ( 'NONE',  ( 20.04142135623731136, 11.75000000001116085, -91.76715728752543555 ) ) ;
#5132=FACE_OUTER_BOUND ( 'NONE', #10293, .T. ) ;
#5138=AXIS2_PLACEMENT_3D ( 'NONE', #54235, #206906, #28304 ) ;
#5162=CARTESIAN_POINT ( 'NONE',  ( -23.15000000000000213, 1.115600667400684642E-11, -100.5000000000000426 ) ) ;
#5166=ORIENTED_EDGE ( 'NONE', *, *, #236314, .F. ) ;
#5169=CARTESIAN_POINT ( 'NONE',  ( -21.05000000000000071, 14.05000000001115623, -72.51369507076104526 ) ) ;
#5228=VECTOR ( 'NONE', #257686, 1000.000000000000000 ) ;
#5252=DIRECTION ( 'NONE',  ( -1.000000000000000000, -3.265361837132813093E-16, 0.000000000000000000 ) ) ;
#5254=CARTESIAN_POINT ( 'NONE',  ( -20.94999999999999929, 1.115600667400684642E-11, -100.5000000000000426 ) ) ;
#5274=DIRECTION ( 'NONE',  ( 0.000000000000000000, 1.000000000000000000, 0.000000000000000000 ) ) ;
#5278=DIRECTION ( 'NONE',  ( 1.000000000000000000, 0.000000000000000000, 0.000000000000000000 ) ) ;
#5354=DIRECTION ( 'NONE',  ( 0.000000000000000000, 0.000000000000000000, -1.000000000000000000 ) ) ;
#5389=AXIS2_PLACEMENT_3D ( 'NONE', #48719, #30468, #109974 ) ;
#5435=DIRECTION ( 'NONE',  ( -1.000000000000000000, 0.000000000000000000, 0.000000000000000000 ) ) ;
#5439=DIRECTION ( 'NONE',  ( 0.000000000000000000, -1.000000000000000000, 0.000000000000000000 ) ) ;
#5440=CARTESIAN_POINT ( 'NONE',  ( -20.64999999999999858, -9.399999999988850163, -76.89396912265249284 ) ) ;
#5451=AXIS2_PLACEMENT_3D ( 'NONE', #235450, #77650, #257532 ) ;
#5459=DIRECTION ( 'NONE',  ( 0.000000000000000000, 1.000000000000000000, 1.626303258728238113E-15 ) ) ;
#5467=CIRCLE ( 'NONE', #184545, 0.5999999999999998668 ) ;
#5495=VECTOR ( 'NONE', #36429, 999.9999999999998863 ) ;
#5531=VERTEX_POINT ( 'NONE', #42296 ) ;
#5542=DIRECTION ( 'NONE',  ( -1.000000000000000000, 0.000000000000000000, 0.000000000000000000 ) ) ;
#5598=ORIENTED_EDGE ( 'NONE', *, *, #204717, .F. ) ;
#5617=CIRCLE ( 'NONE', #234605, 3.999999999999999112 ) ;
#5652=CARTESIAN_POINT ( 'NONE',  ( -20.64999999999999858, 4.350000000011156054, -79.35000000000005116 ) ) ;
#5677=CARTESIAN_POINT ( 'NONE',  ( 21.05000000000000071, 6.540656951712401579, -67.10000000000005116 ) ) ;
#5723=ORIENTED_EDGE ( 'NONE', *, *, #51650, .F. ) ;
#5741=AXIS2_PLACEMENT_3D ( 'NONE', #203374, #102964, #142102 ) ;
#5760=AXIS2_PLACEMENT_3D ( 'NONE', #10284, #7718, #128943 ) ;
#5766=ORIENTED_EDGE ( 'NONE', *, *, #104102, .T. ) ;
#5772=B_SPLINE_CURVE_WITH_KNOTS ( 'NONE', 3,
 ( #142272, #80999, #103132, #39355, #238817, #182709, #24923, #198400, #2750, #121465, #240104, #200967, #161869, #164419, #22356, #138394, #19782, #61459, #99279 ),
 .UNSPECIFIED., .F., .F.,
 ( 4, 3, 3, 3, 3, 3, 4 ),
 ( -2.000416914658901521E-06, 0.000000000000000000, 4.714008503744565809E-05, 9.979203887777271477E-05, 0.0001372215519229478891, 0.0001635031576220937453, 0.0001900083748504128364 ),
 .UNSPECIFIED. ) ;
#5779=AXIS2_PLACEMENT_3D ( 'NONE', #226845, #9087, #49499 ) ;
#5786=CARTESIAN_POINT ( 'NONE',  ( 20.95512820512820440, 10.62384868372303615, -88.25000000000005684 ) ) ;
#5794=AXIS2_PLACEMENT_3D ( 'NONE', #133231, #58478, #216281 ) ;
#5800=ORIENTED_EDGE ( 'NONE', *, *, #205657, .F. ) ;
#5803=CIRCLE ( 'NONE', #172468, 4.100000000000006750 ) ;
#5807=CARTESIAN_POINT ( 'NONE',  ( 22.49999999999999645, 11.64976291804307884, -66.91119002361310208 ) ) ;
#5829=DIRECTION ( 'NONE',  ( 0.000000000000000000, 0.000000000000000000, -1.000000000000000000 ) ) ;
#5845=ORIENTED_EDGE ( 'NONE', *, *, #247835, .T. ) ;
#5868=DIRECTION ( 'NONE',  ( 0.000000000000000000, 0.000000000000000000, 1.000000000000000000 ) ) ;
#5888=CARTESIAN_POINT ( 'NONE',  ( -20.94999999999999929, 14.05000000001115623, -72.51369507076104526 ) ) ;
#5891=FACE_OUTER_BOUND ( 'NONE', #211353, .T. ) ;
#5893=EDGE_LOOP ( 'NONE', ( #147012, #187117, #127902, #186541 ) ) ;
#5921=FACE_OUTER_BOUND ( 'NONE', #110133, .T. ) ;
#5934=ORIENTED_EDGE ( 'NONE', *, *, #123495, .T. ) ;
#5936=LINE ( 'NONE', #162487, #220593 ) ;
#5937=CARTESIAN_POINT ( 'NONE',  ( 18.58143601961936042, 10.43572941510541519, -91.75000000000005684 ) ) ;
#5952=ADVANCED_FACE ( 'NONE', ( #234602 ), #190161, .T. ) ;
#5959=SURFACE_STYLE_USAGE ( .BOTH. , #82919 ) ;
#5967=EDGE_CURVE ( 'NONE', #85621, #150821, #244297, .T. ) ;
#5993=CARTESIAN_POINT ( 'NONE',  ( -20.15000000000000568, 9.291421356248463326, -88.15000000000004832 ) ) ;
#6002=DIRECTION ( 'NONE',  ( 1.000000000000000000, -0.000000000000000000, -0.000000000000000000 ) ) ;
#6005=ORIENTED_EDGE ( 'NONE', *, *, #14562, .F. ) ;
#6011=DIRECTION ( 'NONE',  ( -1.000000000000000000, 0.000000000000000000, 0.000000000000000000 ) ) ;
#6017=EDGE_CURVE ( 'NONE', #51884, #83940, #56090, .T. ) ;
#6024=CARTESIAN_POINT ( 'NONE',  ( -20.64999999999999858, 1.115600667400684642E-11, -67.00000000000004263 ) ) ;
#6058=ORIENTED_EDGE ( 'NONE', *, *, #149060, .F. ) ;
#6069=AXIS2_PLACEMENT_3D ( 'NONE', #214392, #77426, #59133 ) ;
#6072=FACE_OUTER_BOUND ( 'NONE', #149636, .T. ) ;
#6073=VECTOR ( 'NONE', #209597, 1000.000000000000000 ) ;
#6127=AXIS2_PLACEMENT_3D ( 'NONE', #129289, #229674, #227086 ) ;
#6186=ORIENTED_EDGE ( 'NONE', *, *, #117485, .F. ) ;
#6248=ORIENTED_EDGE ( 'NONE', *, *, #21439, .T. ) ;
#6263=LINE ( 'NONE', #29732, #167808 ) ;
#6273=CARTESIAN_POINT ( 'NONE',  ( -21.14999999999999858, -0.09999999998884338825, -55.35042919245524473 ) ) ;
#6302=CARTESIAN_POINT ( 'NONE',  ( 18.49999999999999645, -1.866714910046153308, -78.75267524628205251 ) ) ;
#6319=CARTESIAN_POINT ( 'NONE',  ( 20.85000000000000142, -11.64999999998883595, -97.60000000000005116 ) ) ;
#6389=CARTESIAN_POINT ( 'NONE',  ( -18.50000000000000000, -9.399999999988850163, -74.29725975966333351 ) ) ;
#6415=ORIENTED_EDGE ( 'NONE', *, *, #149911, .F. ) ;
#6450=CARTESIAN_POINT ( 'NONE',  ( -21.05000000000000071, -11.64999999998884306, -97.60000000000005116 ) ) ;
#6452=EDGE_LOOP ( 'NONE', ( #162533, #85119, #184964, #206073 ) ) ;
#6459=LINE ( 'NONE', #165554, #167683 ) ;
#6488=ADVANCED_FACE ( 'NONE', ( #40313 ), #144484, .T. ) ;
#6494=VECTOR ( 'NONE', #41657, 999.9999999999998863 ) ;
#6498=VERTEX_POINT ( 'NONE', #220205 ) ;
#6506=EDGE_LOOP ( 'NONE', ( #55695, #98187, #155795, #189013 ) ) ;
#6526=CARTESIAN_POINT ( 'NONE',  ( -18.47130263965434338, -9.471155585952871547, -107.1834047654770501 ) ) ;
#6527=EDGE_LOOP ( 'NONE', ( #140506, #171485, #186288, #118148, #94080, #23167, #138620, #134191 ) ) ;
#6538=CARTESIAN_POINT ( 'NONE',  ( -20.64999999999999858, 4.350000000011156054, -88.15000000000004832 ) ) ;
#6632=CARTESIAN_POINT ( 'NONE',  ( -23.15000000000000213, 11.75000000001115552, -55.25000000000004974 ) ) ;
#6713=CYLINDRICAL_SURFACE ( 'NONE', #167884, 0.09999999999999939493 ) ;
#6736=CARTESIAN_POINT ( 'NONE',  ( -20.54999999999999716, 4.350000000011156054, -83.75000000000004263 ) ) ;
#6741=VERTEX_POINT ( 'NONE', #96069 ) ;
#6749=FACE_OUTER_BOUND ( 'NONE', #109431, .T. ) ;
#6802=ORIENTED_EDGE ( 'NONE', *, *, #216266, .F. ) ;
#6856=DIRECTION ( 'NONE',  ( 0.000000000000000000, 0.000000000000000000, -1.000000000000000000 ) ) ;
#6865=VERTEX_POINT ( 'NONE', #183017 ) ;
#6867=VERTEX_POINT ( 'NONE', #145140 ) ;
#6877=TOROIDAL_SURFACE ( 'NONE', #244190, 0.6000000000000009770, 0.1000000000000000056 ) ;
#6885=DIRECTION ( 'NONE',  ( 0.000000000000000000, 0.000000000000000000, -1.000000000000000000 ) ) ;
#6911=ADVANCED_FACE ( 'NONE', ( #103439 ), #206873, .T. ) ;
#6924=CARTESIAN_POINT ( 'NONE',  ( 21.05000000000000071, -11.64999999998883595, -97.60000000000005116 ) ) ;
#6959=CARTESIAN_POINT ( 'NONE',  ( -18.50000000000000000, 1.340746217944851715, -56.72713749457886223 ) ) ;
#6979=ORIENTED_EDGE ( 'NONE', *, *, #159504, .T. ) ;
#6983=EDGE_CURVE ( 'NONE', #38016, #178965, #106004, .T. ) ;
#7049=DIRECTION ( 'NONE',  ( -1.000000000000000000, 0.000000000000000000, 0.000000000000000000 ) ) ;
#7093=CARTESIAN_POINT ( 'NONE',  ( -23.25000000000000000, 1.115626384983466744E-11, -98.40000000000004832 ) ) ;
#7100=ORIENTED_EDGE ( 'NONE', *, *, #23377, .F. ) ;
#7121=DIRECTION ( 'NONE',  ( 0.000000000000000000, 0.000000000000000000, -1.000000000000000000 ) ) ;
#7124=AXIS2_PLACEMENT_3D ( 'NONE', #87440, #247813, #50866 ) ;
#7134=AXIS2_PLACEMENT_3D ( 'NONE', #195495, #155089, #216299 ) ;
#7140=DIRECTION ( 'NONE',  ( 1.000000000000000000, -0.000000000000000000, -0.000000000000000000 ) ) ;
#7149=DIRECTION ( 'NONE',  ( -0.1538461538461510236, 0.9880948137434718559, 0.000000000000000000 ) ) ;
#7179=CARTESIAN_POINT ( 'NONE',  ( 20.04142135623730070, 11.75000000001115907, -55.25000000000004974 ) ) ;
#7192=VECTOR ( 'NONE', #13538, 1000.000000000000000 ) ;
#7210=CARTESIAN_POINT ( 'NONE',  ( 20.94999999999999929, -12.41227409413852811, -97.50000000000004263 ) ) ;
#7230=CARTESIAN_POINT ( 'NONE',  ( 23.14999999999999503, 6.450000000011156587, -88.15000000000004832 ) ) ;
#7254=ORIENTED_EDGE ( 'NONE', *, *, #146256, .T. ) ;
#7279=CARTESIAN_POINT ( 'NONE',  ( -20.85000000000000142, -11.64999999998884483, -100.5000000000000426 ) ) ;
#7302=AXIS2_PLACEMENT_3D ( 'NONE', #162830, #44157, #140674 ) ;
#7307=CIRCLE ( 'NONE', #248938, 0.09999999999999967248 ) ;
#7311=EDGE_CURVE ( 'NONE', #210821, #188126, #102796, .T. ) ;
#7331=CIRCLE ( 'NONE', #128147, 0.09999999999999939493 ) ;
#7403=CARTESIAN_POINT ( 'NONE',  ( 23.14999999999999858, 1.115600667400684642E-11, -100.5000000000000426 ) ) ;
#7406=CARTESIAN_POINT ( 'NONE',  ( 21.14999999999999503, 1.115600667400684642E-11, -60.75000000000004974 ) ) ;
#7408=VECTOR ( 'NONE', #60561, 1000.000000000000114 ) ;
#7436=LINE ( 'NONE', #12607, #73274 ) ;
#7448=AXIS2_PLACEMENT_3D ( 'NONE', #13607, #74890, #211811 ) ;
#7449=EDGE_LOOP ( 'NONE', ( #81686, #132579, #171907, #9699 ) ) ;
#7461=CARTESIAN_POINT ( 'NONE',  ( -23.15000000000000213, -11.64999999998884483, -97.40000000000004832 ) ) ;
#7490=CIRCLE ( 'NONE', #136662, 0.1000000000000028644 ) ;
#7494=VERTEX_POINT ( 'NONE', #251663 ) ;
#7547=ADVANCED_FACE ( 'NONE', ( #226966 ), #198678, .T. ) ;
#7579=VECTOR ( 'NONE', #185692, 1000.000000000000000 ) ;
#7619=DIRECTION ( 'NONE',  ( 2.827886303505249259E-16, -0.8660254037844411501, -0.4999999999999956701 ) ) ;
#7622=DIRECTION ( 'NONE',  ( 0.000000000000000000, 0.000000000000000000, -1.000000000000000000 ) ) ;
#7655=VECTOR ( 'NONE', #218555, 1000.000000000000000 ) ;
#7678=VECTOR ( 'NONE', #194343, 1000.000000000000000 ) ;
#7697=CARTESIAN_POINT ( 'NONE',  ( -20.94999999999999929, 1.115650877919449575E-11, -104.6000000000000512 ) ) ;
#7703=CARTESIAN_POINT ( 'NONE',  ( 18.59999999999999787, 1.115600667400684642E-11, -67.00000000000004263 ) ) ;
#7718=DIRECTION ( 'NONE',  ( 3.616040088954497272E-32, -1.224646799147352961E-16, 1.000000000000000000 ) ) ;
#7773=DIRECTION ( 'NONE',  ( 0.000000000000000000, 0.1495327102803586661, -0.9887567792719350601 ) ) ;
#7788=EDGE_CURVE ( 'NONE', #221912, #251583, #61502, .T. ) ;
#7809=ORIENTED_EDGE ( 'NONE', *, *, #170687, .F. ) ;
#7834=FACE_OUTER_BOUND ( 'NONE', #70502, .T. ) ;
#7848=CARTESIAN_POINT ( 'NONE',  ( 20.94999999999999929, 5.400000000011154988, -79.40526601891313874 ) ) ;
#7866=ORIENTED_EDGE ( 'NONE', *, *, #229019, .F. ) ;
#7871=CYLINDRICAL_SURFACE ( 'NONE', #200973, 0.1000000000000028644 ) ;
#7918=DIRECTION ( 'NONE',  ( -1.000000000000000000, 0.000000000000000000, 0.000000000000000000 ) ) ;
#7937=CARTESIAN_POINT ( 'NONE',  ( -21.05000000000000071, -0.09999999998884474828, -60.45934304829881256 ) ) ;
#7960=TOROIDAL_SURFACE ( 'NONE', #107716, 0.2000000000000000111, 0.1000000000000000056 ) ;
#7996=DIRECTION ( 'NONE',  ( 0.000000000000000000, 0.000000000000000000, 1.000000000000000000 ) ) ;
#8011=CARTESIAN_POINT ( 'NONE',  ( 21.05000000000000071, 1.115600667400684642E-11, -100.5000000000000426 ) ) ;
#8026=ORIENTED_EDGE ( 'NONE', *, *, #141615, .T. ) ;
#8037=CARTESIAN_POINT ( 'NONE',  ( -1.739115166359751170E-14, 11.65000000001114699, -79.25000000000004263 ) ) ;
#8066=DIRECTION ( 'NONE',  ( 0.000000000000000000, 0.000000000000000000, -1.000000000000000000 ) ) ;
#8112=EDGE_CURVE ( 'NONE', #57960, #184752, #249141, .T. ) ;
#8127=CARTESIAN_POINT ( 'NONE',  ( -20.94999999999999929, 11.75000000001115197, -74.01480577065406408 ) ) ;
#8139=ORIENTED_EDGE ( 'NONE', *, *, #216232, .F. ) ;
#8151=CARTESIAN_POINT ( 'NONE',  ( -23.25000000000000000, 1.115600667400684642E-11, -67.00000000000004263 ) ) ;
#8169=VERTEX_POINT ( 'NONE', #21742 ) ;
#8177=ORIENTED_EDGE ( 'NONE', *, *, #231117, .F. ) ;
#8213=AXIS2_PLACEMENT_3D ( 'NONE', #31010, #132648, #133914 ) ;
#8229=ORIENTED_EDGE ( 'NONE', *, *, #28288, .F. ) ;
#8267=EDGE_CURVE ( 'NONE', #74473, #120817, #70075, .T. ) ;
#8269=DIRECTION ( 'NONE',  ( 0.000000000000000000, -1.000000000000000000, 0.000000000000000000 ) ) ;
#8271=CARTESIAN_POINT ( 'NONE',  ( 22.39999999999999858, 7.790779598384538929, -66.90000000000004832 ) ) ;
#8301=AXIS2_PLACEMENT_3D ( 'NONE', #253372, #119016, #96834 ) ;
#8310=CARTESIAN_POINT ( 'NONE',  ( -20.94999999999999929, 1.835341550235569663, -78.55515129256302487 ) ) ;
#8319=DIRECTION ( 'NONE',  ( 0.000000000000000000, -0.9915357197604792727, 0.1298341882520475943 ) ) ;
#8320=CYLINDRICAL_SURFACE ( 'NONE', #196109, 4.049999999999998046 ) ;
#8323=VERTEX_POINT ( 'NONE', #209344 ) ;
#8326=DIRECTION ( 'NONE',  ( 0.000000000000000000, 0.000000000000000000, -1.000000000000000000 ) ) ;
#8341=DIRECTION ( 'NONE',  ( 0.000000000000000000, 0.000000000000000000, -1.000000000000000000 ) ) ;
#8353=DIRECTION ( 'NONE',  ( 1.000000000000000000, -0.000000000000000000, -0.000000000000000000 ) ) ;
#8356=CARTESIAN_POINT ( 'NONE',  ( 23.15000000000000213, -8.596261682231828516, -91.04987248284976431 ) ) ;
#8360=DIRECTION ( 'NONE',  ( 0.7071067811865388020, -0.7071067811865561215, 0.000000000000000000 ) ) ;
#8366=LINE ( 'NONE', #226086, #256594 ) ;
#8375=CIRCLE ( 'NONE', #25130, 7.800000000000001599 ) ;
#8403=FACE_OUTER_BOUND ( 'NONE', #73943, .T. ) ;
#8421=DIRECTION ( 'NONE',  ( 0.000000000000000000, 0.000000000000000000, 1.000000000000000000 ) ) ;
#8440=VECTOR ( 'NONE', #57588, 1000.000000000000114 ) ;
#8448=EDGE_CURVE ( 'NONE', #91478, #194502, #116047, .T. ) ;
#8459=B_SPLINE_CURVE_WITH_KNOTS ( 'NONE', 3,
 ( #92915, #9529, #168669, #48657, #169948, #52500, #210322 ),
 .UNSPECIFIED., .F., .F.,
 ( 4, 3, 4 ),
 ( 0.000000000000000000, 0.0009834301579439998740, 0.001767853679402675614 ),
 .UNSPECIFIED. ) ;
#8467=DIRECTION ( 'NONE',  ( 0.000000000000000000, 0.000000000000000000, 1.000000000000000000 ) ) ;
#8485=EDGE_CURVE ( 'NONE', #134186, #96293, #140991, .T. ) ;
#8513=B_SPLINE_CURVE_WITH_KNOTS ( 'NONE', 3,
 ( #115197, #194760, #112634, #31838, #16123, #91782, #192184, #111348, #136015, #73533, #95622, #231311, #76063, #175220, #254662, #52641, #30545, #59033, #21263 ),
 .UNSPECIFIED., .F., .F.,
 ( 4, 3, 3, 3, 3, 3, 4 ),
 ( 0.000000000000000000, 7.110282409889913185E-05, 0.0001508797727291429644, 0.0002027344179858502646, 0.0002343294522349018692, 0.0002454816334821173789, 0.0002619873080085545719 ),
 .UNSPECIFIED. ) ;
#8523=ORIENTED_EDGE ( 'NONE', *, *, #162197, .F. ) ;
#8527=ORIENTED_EDGE ( 'NONE', *, *, #195927, .F. ) ;
#8534=CARTESIAN_POINT ( 'NONE',  ( 18.49999999999999289, 10.25000000263022848, -91.68717194963235784 ) ) ;
#8535=VECTOR ( 'NONE', #201725, 1000.000000000000000 ) ;
#8538=CYLINDRICAL_SURFACE ( 'NONE', #134965, 0.1000000000000028644 ) ;
#8571=CARTESIAN_POINT ( 'NONE',  ( -20.94999999999999929, 7.120270961708750512, -104.1595630418393768 ) ) ;
#8572=CARTESIAN_POINT ( 'NONE',  ( 23.14999999999998792, 11.65000000001115588, -67.00000000000004263 ) ) ;
#8574=CARTESIAN_POINT ( 'NONE',  ( 20.12481660106788084, 9.526343992285099205, -75.22614166909309574 ) ) ;
#8581=ORIENTED_EDGE ( 'NONE', *, *, #11194, .F. ) ;
#8631=AXIS2_PLACEMENT_3D ( 'NONE', #113043, #149624, #213409 ) ;
#8649=LINE ( 'NONE', #88149, #118513 ) ;
#8703=CARTESIAN_POINT ( 'NONE',  ( -23.15000000000000213, -11.48912529306489994, -97.40000000000004832 ) ) ;
#8718=EDGE_LOOP ( 'NONE', ( #194100, #65864, #83870 ) ) ;
#8741=ORIENTED_EDGE ( 'NONE', *, *, #121649, .T. ) ;
#8765=DIRECTION ( 'NONE',  ( 1.000000000000000000, -0.000000000000000000, -0.000000000000000000 ) ) ;
#8778=CYLINDRICAL_SURFACE ( 'NONE', #94073, 0.09999999999999939493 ) ;
#8817=EDGE_CURVE ( 'NONE', #165054, #170816, #207830, .T. ) ;
#8915=ORIENTED_EDGE ( 'NONE', *, *, #88006, .F. ) ;
#8916=AXIS2_PLACEMENT_3D ( 'NONE', #208122, #183733, #110271 ) ;
#8921=DIRECTION ( 'NONE',  ( 2.715809747126116508E-16, -1.000000000000000000, 0.000000000000000000 ) ) ;
#8936=ORIENTED_EDGE ( 'NONE', *, *, #227286, .F. ) ;
#8940=DIRECTION ( 'NONE',  ( 1.000000000000000000, 0.000000000000000000, -0.000000000000000000 ) ) ;
#8942=ADVANCED_FACE ( 'NONE', ( #61208 ), #41667, .F. ) ;
#8996=EDGE_CURVE ( 'NONE', #207164, #190222, #245224, .T. ) ;
#8998=EDGE_CURVE ( 'NONE', #195562, #121203, #16278, .T. ) ;
#9017=CARTESIAN_POINT ( 'NONE',  ( -20.85000000000000497, 11.75000000001115019, -93.58085275404135928 ) ) ;
#9053=FACE_OUTER_BOUND ( 'NONE', #183730, .T. ) ;
#9062=CARTESIAN_POINT ( 'NONE',  ( 21.05000000000000071, 11.60000000001116049, -93.57179676972454274 ) ) ;
#9082=CIRCLE ( 'NONE', #242301, 0.6000000000000033085 ) ;
#9087=DIRECTION ( 'NONE',  ( 1.000000000000000000, 0.000000000000000000, 0.000000000000000000 ) ) ;
#9106=CARTESIAN_POINT ( 'NONE',  ( -18.54260524012581612, -9.624219390062492607, -107.2407730457710073 ) ) ;
#9157=ORIENTED_EDGE ( 'NONE', *, *, #174249, .T. ) ;
#9158=DIRECTION ( 'NONE',  ( 1.000000000000000000, -0.000000000000000000, -0.000000000000000000 ) ) ;
#9176=ORIENTED_EDGE ( 'NONE', *, *, #116042, .T. ) ;
#9182=FACE_OUTER_BOUND ( 'NONE', #128838, .T. ) ;
#9199=CYLINDRICAL_SURFACE ( 'NONE', #52014, 0.09999999999999939493 ) ;
#9209=CARTESIAN_POINT ( 'NONE',  ( -18.39999999999999858, -9.599999999988849453, -107.1001893912220879 ) ) ;
#9230=ORIENTED_EDGE ( 'NONE', *, *, #227136, .F. ) ;
#9249=LINE ( 'NONE', #105754, #104322 ) ;
#9260=AXIS2_PLACEMENT_3D ( 'NONE', #216723, #117629, #237584 ) ;
#9277=DIRECTION ( 'NONE',  ( 1.000000000000000000, -0.000000000000000000, -0.000000000000000000 ) ) ;
#9289=CARTESIAN_POINT ( 'NONE',  ( 23.14999999999999858, 4.813084112160684214, -88.55848224347622022 ) ) ;
#9310=CIRCLE ( 'NONE', #213306, 0.1000000000000004774 ) ;
#9315=ORIENTED_EDGE ( 'NONE', *, *, #234714, .T. ) ;
#9353=ORIENTED_EDGE ( 'NONE', *, *, #11897, .T. ) ;
#9383=ORIENTED_EDGE ( 'NONE', *, *, #75208, .F. ) ;
#9393=B_SPLINE_CURVE_WITH_KNOTS ( 'NONE', 3,
 ( #141478, #123206, #166219, #22847, #121930, #43673 ),
 .UNSPECIFIED., .F., .F.,
 ( 4, 2, 4 ),
 ( 1.138412281109779656E-18, 0.0001569047307838638975, 0.0003138094615677266023 ),
 .UNSPECIFIED. ) ;
#9405=EDGE_CURVE ( 'NONE', #211645, #150463, #16638, .T. ) ;
#9412=ORIENTED_EDGE ( 'NONE', *, *, #53208, .T. ) ;
#9448=ORIENTED_EDGE ( 'NONE', *, *, #23057, .F. ) ;
#9456=DIRECTION ( 'NONE',  ( 0.000000000000000000, -1.000000000000000000, -0.000000000000000000 ) ) ;
#9459=CARTESIAN_POINT ( 'NONE',  ( 20.85000000000000142, -11.74999999998883560, -97.60000000000005116 ) ) ;
#9469=EDGE_LOOP ( 'NONE', ( #147585, #148990, #257070, #106515 ) ) ;
#9495=LINE ( 'NONE', #89028, #183353 ) ;
#9521=CARTESIAN_POINT ( 'NONE',  ( -21.59142135623730852, 7.850000000011158718, -79.25000000000004263 ) ) ;
#9523=AXIS2_PLACEMENT_3D ( 'NONE', #250194, #31188, #88524 ) ;
#9529=CARTESIAN_POINT ( 'NONE',  ( -22.16821283564876666, 7.558973340791935058, -67.00000000000004263 ) ) ;
#9535=CARTESIAN_POINT ( 'NONE',  ( 21.06277459767431992, 8.872862438279401687, -79.20399919235673281 ) ) ;
#9544=CIRCLE ( 'NONE', #196983, 0.1000000000000028644 ) ;
#9560=CIRCLE ( 'NONE', #126072, 0.3999999999999975797 ) ;
#9568=DIRECTION ( 'NONE',  ( 0.000000000000000000, 0.000000000000000000, -1.000000000000000000 ) ) ;
#9582=CARTESIAN_POINT ( 'NONE',  ( -21.05000000000000071, 1.360870587203197646, -75.07299792709100927 ) ) ;
#9597=FACE_OUTER_BOUND ( 'NONE', #178134, .T. ) ;
#9614=CARTESIAN_POINT ( 'NONE',  ( 20.94983749550516450, 10.29766095125292402, -105.9743663933276139 ) ) ;
#9651=CARTESIAN_POINT ( 'NONE',  ( -20.54999999999999716, -11.74999999998884448, -83.75000000000004263 ) ) ;
#9676=CIRCLE ( 'NONE', #226127, 0.09999999999999892308 ) ;
#9677=FACE_OUTER_BOUND ( 'NONE', #96, .T. ) ;
#9685=EDGE_LOOP ( 'NONE', ( #49606, #141905, #236382, #237881 ) ) ;
#9692=DIRECTION ( 'NONE',  ( 0.000000000000000000, 0.1350103645451904977, -0.9908441862701596881 ) ) ;
#9696=VERTEX_POINT ( 'NONE', #142670 ) ;
#9699=ORIENTED_EDGE ( 'NONE', *, *, #47874, .T. ) ;
#9715=DIRECTION ( 'NONE',  ( 0.000000000000000000, -0.1568667991644863147, 0.9876197685951252359 ) ) ;
#9719=DIRECTION ( 'NONE',  ( 0.000000000000000000, 1.000000000000000000, 2.891205793294679805E-16 ) ) ;
#9727=CARTESIAN_POINT ( 'NONE',  ( 18.59999999999996945, 10.33248238083634440, -106.0948465439131922 ) ) ;
#9734=ORIENTED_EDGE ( 'NONE', *, *, #47147, .T. ) ;
#9746=ADVANCED_FACE ( 'NONE', ( #189542 ), #10903, .T. ) ;
#9756=DIRECTION ( 'NONE',  ( 0.000000000000000000, 0.000000000000000000, -1.000000000000000000 ) ) ;
#9778=TOROIDAL_SURFACE ( 'NONE', #34762, 4.149999999999999467, 0.1000000000000000056 ) ;
#9789=PRODUCT_DEFINITION_SHAPE ( 'NONE', 'NONE',  #160032 ) ;
#9806=DIRECTION ( 'NONE',  ( 1.000000000000000000, 0.000000000000000000, 0.000000000000000000 ) ) ;
#9834=ORIENTED_EDGE ( 'NONE', *, *, #1964, .T. ) ;
#9872=ADVANCED_FACE ( 'NONE', ( #87833 ), #43, .F. ) ;
#9887=EDGE_CURVE ( 'NONE', #36999, #102833, #212447, .T. ) ;
#9910=AXIS2_PLACEMENT_3D ( 'NONE', #40254, #231072, #198002 ) ;
#9914=CARTESIAN_POINT ( 'NONE',  ( -18.59999999999999787, 1.115600667400684642E-11, -100.5000000000000426 ) ) ;
#9930=VECTOR ( 'NONE', #169731, 1000.000000000000000 ) ;
#9947=ORIENTED_EDGE ( 'NONE', *, *, #139030, .T. ) ;
#9961=ORIENTED_EDGE ( 'NONE', *, *, #227998, .T. ) ;
#9969=DIRECTION ( 'NONE',  ( 0.000000000000000000, 1.000000000000000000, 0.000000000000000000 ) ) ;
#10014=CARTESIAN_POINT ( 'NONE',  ( -2.995603634470829482E-16, -11.74999999998884448, -79.25000000000004263 ) ) ;
#10059=VECTOR ( 'NONE', #242137, 1000.000000000000000 ) ;
#10061=AXIS2_PLACEMENT_3D ( 'NONE', #44480, #180139, #198403 ) ;
#10085=VERTEX_POINT ( 'NONE', #44497 ) ;
#10107=ORIENTED_EDGE ( 'NONE', *, *, #25772, .T. ) ;
#10115=DIRECTION ( 'NONE',  ( 1.000000000000000000, -0.000000000000000000, -0.000000000000000000 ) ) ;
#10134=SPHERICAL_SURFACE ( 'NONE', #230862, 0.1000000000000000056 ) ;
#10137=CARTESIAN_POINT ( 'NONE',  ( -20.64999999999999858, 1.115600667400684642E-11, -79.87500000000004263 ) ) ;
#10162=CARTESIAN_POINT ( 'NONE',  ( 18.49999999999998934, 19.85039924724470950, -69.28030305780140452 ) ) ;
#10196=DIRECTION ( 'NONE',  ( -0.000000000000000000, 0.000000000000000000, 1.000000000000000000 ) ) ;
#10232=CARTESIAN_POINT ( 'NONE',  ( 18.49999999999999289, 10.20857864377385127, -91.65000000000004832 ) ) ;
#10238=CARTESIAN_POINT ( 'NONE',  ( 23.15000000000000213, -12.41227409413852811, -97.40000000000004832 ) ) ;
#10263=VERTEX_POINT ( 'NONE', #26220 ) ;
#10284=CARTESIAN_POINT ( 'NONE',  ( 23.14999999999999147, 4.150000000011154988, -67.00000000000004263 ) ) ;
#10293=EDGE_LOOP ( 'NONE', ( #212810, #38345, #235393, #94777 ) ) ;
#10350=CARTESIAN_POINT ( 'NONE',  ( -23.25000000000000000, 4.250000000011156409, -88.15000000000004832 ) ) ;
#10362=CARTESIAN_POINT ( 'NONE',  ( -23.25000000000000000, -1.249999999988843369, -108.3004807544151191 ) ) ;
#10365=CYLINDRICAL_SURFACE ( 'NONE', #167494, 4.049999999999998046 ) ;
#10381=DIRECTION ( 'NONE',  ( 3.469446951953635015E-14, -0.000000000000000000, 1.000000000000000000 ) ) ;
#10383=ORIENTED_EDGE ( 'NONE', *, *, #242915, .T. ) ;
#10388=ORIENTED_EDGE ( 'NONE', *, *, #110095, .T. ) ;
#10396=ORIENTED_EDGE ( 'NONE', *, *, #181239, .T. ) ;
#10401=FACE_OUTER_BOUND ( 'NONE', #93182, .T. ) ;
#10420=CARTESIAN_POINT ( 'NONE',  ( 23.14999999999999858, 11.65000000001116298, -93.48519422934610645 ) ) ;
#10458=CARTESIAN_POINT ( 'NONE',  ( -20.64999999999999858, 2.500000000011154633, -87.27537807723794572 ) ) ;
#10465=AXIS2_PLACEMENT_3D ( 'NONE', #85688, #165266, #145689 ) ;
#10486=DIRECTION ( 'NONE',  ( 0.000000000000000000, 1.000000000000000000, 0.000000000000000000 ) ) ;
#10499=CARTESIAN_POINT ( 'NONE',  ( -21.14999999999999858, -0.09999999998884338825, -60.75000000000004974 ) ) ;
#10540=DIRECTION ( 'NONE',  ( -0.000000000000000000, 0.000000000000000000, 1.000000000000000000 ) ) ;
#10568=ORIENTED_EDGE ( 'NONE', *, *, #116948, .F. ) ;
#10570=EDGE_CURVE ( 'NONE', #120408, #214743, #197125, .T. ) ;
#10611=CIRCLE ( 'NONE', #252014, 11.65000000000000036 ) ;
#10623=EDGE_CURVE ( 'NONE', #118177, #66589, #162983, .T. ) ;
#10654=ORIENTED_EDGE ( 'NONE', *, *, #169233, .T. ) ;
#10680=EDGE_CURVE ( 'NONE', #237092, #170195, #221597, .T. ) ;
#10684=ORIENTED_EDGE ( 'NONE', *, *, #9405, .T. ) ;
#10687=EDGE_CURVE ( 'NONE', #31646, #120408, #204860, .T. ) ;
#10688=LINE ( 'NONE', #249310, #242045 ) ;
#10709=FACE_OUTER_BOUND ( 'NONE', #214046, .T. ) ;
#10719=DIRECTION ( 'NONE',  ( 2.952720810173289112E-16, -1.000000000000000000, 0.000000000000000000 ) ) ;
#10727=ORIENTED_EDGE ( 'NONE', *, *, #5967, .T. ) ;
#10793=DIRECTION ( 'NONE',  ( 0.000000000000000000, 0.000000000000000000, -1.000000000000000000 ) ) ;
#10806=CARTESIAN_POINT ( 'NONE',  ( -18.50000000000000000, 11.75000000001115197, -55.25000000000004974 ) ) ;
#10811=VECTOR ( 'NONE', #230408, 1000.000000000000000 ) ;
#10864=EDGE_CURVE ( 'NONE', #124815, #143703, #188488, .T. ) ;
#10869=FACE_OUTER_BOUND ( 'NONE', #206312, .T. ) ;
#10887=CARTESIAN_POINT ( 'NONE',  ( 22.59066674512258643, 11.75000000001115552, -66.96949587636957801 ) ) ;
#10892=VERTEX_POINT ( 'NONE', #120868 ) ;
#10903=CYLINDRICAL_SURFACE ( 'NONE', #37668, 12.87499999999999822 ) ;
#10920=EDGE_LOOP ( 'NONE', ( #101886, #176267, #81248, #194910 ) ) ;
#10951=CARTESIAN_POINT ( 'NONE',  ( 23.24999999999999645, 5.600000000011153389, -55.25000000000004974 ) ) ;
#10966=DIRECTION ( 'NONE',  ( 0.000000000000000000, 1.000000000000000000, 0.000000000000000000 ) ) ;
#10975=SPHERICAL_SURFACE ( 'NONE', #110747, 0.1000000000000000056 ) ;
#11006=DIRECTION ( 'NONE',  ( 2.978066053179067751E-16, -1.000000000000000000, 0.000000000000000000 ) ) ;
#11035=CARTESIAN_POINT ( 'NONE',  ( 18.59999999999999076, 1.835341550235567887, -78.55515129256302487 ) ) ;
#11039=CARTESIAN_POINT ( 'NONE',  ( -20.94999999999999929, -1.835341550213255957, -78.55515129256302487 ) ) ;
#11060=CARTESIAN_POINT ( 'NONE',  ( -20.94999999999999929, -11.39257802169451672, -70.07394957983198935 ) ) ;
#11066=EDGE_LOOP ( 'NONE', ( #5934, #146113, #81108 ) ) ;
#11084=EDGE_CURVE ( 'NONE', #202894, #71736, #130209, .T. ) ;
#11086=DIRECTION ( 'NONE',  ( 0.000000000000000000, 0.000000000000000000, 1.000000000000000000 ) ) ;
#11092=CARTESIAN_POINT ( 'NONE',  ( -2.995603634470829482E-16, 6.650000000011155876, -88.15000000000004832 ) ) ;
#11116=CARTESIAN_POINT ( 'NONE',  ( 20.94999999999999574, 10.47338541492405994, -74.57865446424858646 ) ) ;
#11117=VERTEX_POINT ( 'NONE', #131098 ) ;
#11118=DIRECTION ( 'NONE',  ( -0.000000000000000000, 1.000000000000000000, 0.000000000000000000 ) ) ;
#11120=ADVANCED_FACE ( 'NONE', ( #249768 ), #21905, .F. ) ;
#11134=CYLINDRICAL_SURFACE ( 'NONE', #239886, 0.09999999999999939493 ) ;
#11140=CARTESIAN_POINT ( 'NONE',  ( 20.97438252431638972, 8.925423506087151182, -75.47237068901085877 ) ) ;
#11168=AXIS2_PLACEMENT_3D ( 'NONE', #240381, #121731, #43459 ) ;
#11181=ORIENTED_EDGE ( 'NONE', *, *, #105509, .T. ) ;
#11183=CARTESIAN_POINT ( 'NONE',  ( 18.59999999999999076, 1.835341550235567887, -78.55515129256302487 ) ) ;
#11194=EDGE_CURVE ( 'NONE', #203901, #201185, #57959, .T. ) ;
#11210=EDGE_CURVE ( 'NONE', #2322, #221912, #105234, .T. ) ;
#11218=CARTESIAN_POINT ( 'NONE',  ( 21.07964655665547937, 8.774889614989714204, -79.22191658296409855 ) ) ;
#11252=CARTESIAN_POINT ( 'NONE',  ( 20.95512820512820440, 10.62384868372303615, -79.15000000000004832 ) ) ;
#11297=VERTEX_POINT ( 'NONE', #215755 ) ;
#11300=ADVANCED_FACE ( 'NONE', ( #144886 ), #137497, .T. ) ;
#11314=EDGE_LOOP ( 'NONE', ( #165044, #47569, #149053, #3511 ) ) ;
#11364=DIRECTION ( 'NONE',  ( 1.000000000000000000, 3.265361837132813093E-16, -0.000000000000000000 ) ) ;
#11387=EDGE_CURVE ( 'NONE', #167725, #242093, #247854, .T. ) ;
#11392=EDGE_CURVE ( 'NONE', #242599, #20178, #76231, .T. ) ;
#11404=DIRECTION ( 'NONE',  ( 0.000000000000000000, 1.000000000000000000, 0.000000000000000000 ) ) ;
#11414=FACE_OUTER_BOUND ( 'NONE', #129602, .T. ) ;
#11435=ORIENTED_EDGE ( 'NONE', *, *, #100356, .T. ) ;
#11446=ORIENTED_EDGE ( 'NONE', *, *, #143150, .F. ) ;
#11489=EDGE_CURVE ( 'NONE', #73311, #238735, #133058, .T. ) ;
#11506=CARTESIAN_POINT ( 'NONE',  ( 20.02499999999999858, 9.750000000011153745, -88.25000000000005684 ) ) ;
#11541=SPHERICAL_SURFACE ( 'NONE', #32995, 0.1000000000000000056 ) ;
#11543=EDGE_CURVE ( 'NONE', #117385, #194152, #151282, .T. ) ;
#11544=CARTESIAN_POINT ( 'NONE',  ( -18.59999999999999787, 11.75000000001115197, -55.25000000000004974 ) ) ;
#11567=EDGE_LOOP ( 'NONE', ( #240657, #216875, #83798, #192037 ) ) ;
#11592=DIRECTION ( 'NONE',  ( 0.000000000000000000, 1.000000000000000000, 0.000000000000000000 ) ) ;
#11619=FACE_BOUND ( 'NONE', #36314, .T. ) ;
#11645=DIRECTION ( 'NONE',  ( 0.000000000000000000, 0.7397360091702755991, -0.6728971962616832059 ) ) ;
#11653=CARTESIAN_POINT ( 'NONE',  ( 21.05315837424256031, 11.75000000154545177, -93.65835600266693461 ) ) ;
#11673=CARTESIAN_POINT ( 'NONE',  ( 20.85000000000000142, -1.149570369564537842, -108.3159124845020074 ) ) ;
#11695=ORIENTED_EDGE ( 'NONE', *, *, #239344, .F. ) ;
#11729=ADVANCED_FACE ( 'NONE', ( #229282 ), #145869, .T. ) ;
#11750=EDGE_CURVE ( 'NONE', #12745, #187441, #50613, .T. ) ;
#11771=CIRCLE ( 'NONE', #157524, 0.09999999999999939493 ) ;
#11780=CARTESIAN_POINT ( 'NONE',  ( 23.24999999999999645, 4.775700934590591196, -88.65123189595408348 ) ) ;
#11809=DIRECTION ( 'NONE',  ( 0.000000000000000000, -0.9915357197604882655, 0.1298341882519793711 ) ) ;
#11843=CIRCLE ( 'NONE', #53327, 0.5000000000000004441 ) ;
#11845=CARTESIAN_POINT ( 'NONE',  ( 21.30000000000002558, 1.115600667400684642E-11, -71.05000000000003979 ) ) ;
#11862=CIRCLE ( 'NONE', #3446, 2.000000000000001776 ) ;
#11893=CARTESIAN_POINT ( 'NONE',  ( 18.52928932188133970, 10.27928932189250411, -91.65000000000004832 ) ) ;
#11897=EDGE_CURVE ( 'NONE', #181640, #179663, #47186, .T. ) ;
#11934=DIRECTION ( 'NONE',  ( 0.000000000000000000, 0.000000000000000000, -1.000000000000000000 ) ) ;
#11940=ADVANCED_FACE ( 'NONE', ( #255189 ), #9778, .T. ) ;
#11960=ADVANCED_FACE ( 'NONE', ( #156180 ), #55723, .F. ) ;
#11990=VERTEX_POINT ( 'NONE', #196552 ) ;
#11994=EDGE_LOOP ( 'NONE', ( #32153, #171502, #64550, #256901 ) ) ;
#12007=DIRECTION ( 'NONE',  ( 1.000000000000000000, -0.000000000000000000, -0.000000000000000000 ) ) ;
#12011=DIRECTION ( 'NONE',  ( -1.836970198721029934E-16, 1.000000000000000000, 0.000000000000000000 ) ) ;
#12120=ADVANCED_FACE ( 'NONE', ( #221238 ), #3482, .F. ) ;
#12129=CARTESIAN_POINT ( 'NONE',  ( 21.53551880898956838, 6.784797761427480367, -66.90103026542837483 ) ) ;
#12162=CIRCLE ( 'NONE', #212061, 0.09999999999999939493 ) ;
#12186=CARTESIAN_POINT ( 'NONE',  ( -20.07928932188135107, 9.220710678129810489, -88.15000000000004832 ) ) ;
#12187=CARTESIAN_POINT ( 'NONE',  ( 22.49544290803770608, 11.74987023786810880, -66.93468804074250045 ) ) ;
#12210=VECTOR ( 'NONE', #29880, 1000.000000000000114 ) ;
#12242=ORIENTED_EDGE ( 'NONE', *, *, #145880, .F. ) ;
#12249=AXIS2_PLACEMENT_3D ( 'NONE', #215857, #39841, #195057 ) ;
#12268=LINE ( 'NONE', #70969, #7192 ) ;
#12271=VECTOR ( 'NONE', #165517, 1000.000000000000000 ) ;
#12291=ADVANCED_FACE ( 'NONE', ( #171585 ), #143244, .T. ) ;
#12312=AXIS2_PLACEMENT_3D ( 'NONE', #51592, #148155, #49053 ) ;
#12325=DIRECTION ( 'NONE',  ( 0.000000000000000000, 0.000000000000000000, -1.000000000000000000 ) ) ;
#12341=ADVANCED_FACE ( 'NONE', ( #95846 ), #33371, .F. ) ;
#12400=CARTESIAN_POINT ( 'NONE',  ( 23.15000000000000213, -11.74999999998883737, -88.35000000000003695 ) ) ;
#12424=ORIENTED_EDGE ( 'NONE', *, *, #13202, .F. ) ;
#12442=CARTESIAN_POINT ( 'NONE',  ( 20.59588692710267921, 10.36872342117990975, -74.63908109451070061 ) ) ;
#12460=VECTOR ( 'NONE', #238326, 1000.000000000000000 ) ;
#12463=EDGE_CURVE ( 'NONE', #166675, #233701, #35145, .T. ) ;
#12483=FACE_OUTER_BOUND ( 'NONE', #67885, .T. ) ;
#12485=EDGE_CURVE ( 'NONE', #230941, #203487, #180551, .T. ) ;
#12487=DIRECTION ( 'NONE',  ( 0.000000000000000000, -0.9908441862701596881, -0.1350103645451904977 ) ) ;
#12500=EDGE_CURVE ( 'NONE', #61933, #187354, #147531, .T. ) ;
#12509=CARTESIAN_POINT ( 'NONE',  ( -20.85000000000000142, -1.851617760457748618, -112.1031897196037050 ) ) ;
#12519=FACE_OUTER_BOUND ( 'NONE', #1501, .T. ) ;
#12531=DIRECTION ( 'NONE',  ( 0.000000000000000000, 0.9915357197604794948, -0.1298341882520470392 ) ) ;
#12549=ADVANCED_FACE ( 'NONE', ( #9597 ), #247487, .T. ) ;
#12557=EDGE_CURVE ( 'NONE', #61933, #45948, #55920, .T. ) ;
#12571=CARTESIAN_POINT ( 'NONE',  ( 23.14999999999999858, 1.115600667400684642E-11, -100.5000000000000426 ) ) ;
#12607=CARTESIAN_POINT ( 'NONE',  ( 20.94999999999999929, 1.115625160336667635E-11, -98.50000000000004263 ) ) ;
#12639=VECTOR ( 'NONE', #183048, 1000.000000000000114 ) ;
#12640=DIRECTION ( 'NONE',  ( 0.000000000000000000, -0.8660254037844411501, -0.4999999999999956146 ) ) ;
#12683=DIRECTION ( 'NONE',  ( 0.000000000000000000, -0.1350103645451876666, -0.9908441862701600211 ) ) ;
#12719=VERTEX_POINT ( 'NONE', #51268 ) ;
#12724=AXIS2_PLACEMENT_3D ( 'NONE', #226654, #12780, #247518 ) ;
#12745=VERTEX_POINT ( 'NONE', #50016 ) ;
#12747=CARTESIAN_POINT ( 'NONE',  ( 21.05000000000000071, -1.162701749926853712, -75.10000000000003695 ) ) ;
#12780=DIRECTION ( 'NONE',  ( 0.000000000000000000, 0.000000000000000000, 1.000000000000000000 ) ) ;
#12826=ORIENTED_EDGE ( 'NONE', *, *, #2935, .T. ) ;
#12833=DIRECTION ( 'NONE',  ( 1.000000000000000000, 0.000000000000000000, 0.000000000000000000 ) ) ;
#12837=DIRECTION ( 'NONE',  ( 1.000000000000000000, 0.000000000000000000, -0.000000000000000000 ) ) ;
#12856=VERTEX_POINT ( 'NONE', #254614 ) ;
#12898=LINE ( 'NONE', #151105, #91054 ) ;
#12900=CIRCLE ( 'NONE', #46181, 0.09999999999999939493 ) ;
#12908=AXIS2_PLACEMENT_3D ( 'NONE', #149264, #13596, #12325 ) ;
#12921=EDGE_CURVE ( 'NONE', #140349, #205600, #226207, .T. ) ;
#12928=ORIENTED_EDGE ( 'NONE', *, *, #87763, .F. ) ;
#12929=CIRCLE ( 'NONE', #62965, 0.3999999999999975797 ) ;
#12943=FACE_OUTER_BOUND ( 'NONE', #81070, .T. ) ;
#12947=DIRECTION ( 'NONE',  ( 0.000000000000000000, 1.000000000000000000, 0.000000000000000000 ) ) ;
#12963=AXIS2_PLACEMENT_3D ( 'NONE', #230542, #251372, #212270 ) ;
#13016=VERTEX_POINT ( 'NONE', #62852 ) ;
#13039=DIRECTION ( 'NONE',  ( 1.000000000000000000, 0.000000000000000000, 0.000000000000000000 ) ) ;
#13140=VERTEX_POINT ( 'NONE', #228357 ) ;
#13174=ORIENTED_EDGE ( 'NONE', *, *, #169537, .T. ) ;
#13197=DIRECTION ( 'NONE',  ( 0.000000000000000000, 1.000000000000000000, -1.224646799147353207E-16 ) ) ;
#13202=EDGE_CURVE ( 'NONE', #89853, #18191, #174513, .T. ) ;
#13227=VERTEX_POINT ( 'NONE', #163897 ) ;
#13228=CIRCLE ( 'NONE', #100658, 0.6000000000000015321 ) ;
#13250=CARTESIAN_POINT ( 'NONE',  ( -18.44448725179913851, -9.490081715472175716, -107.1289602940625372 ) ) ;
#13279=ORIENTED_EDGE ( 'NONE', *, *, #60657, .T. ) ;
#13293=DIRECTION ( 'NONE',  ( -0.000000000000000000, -0.8660254037844459241, -0.4999999999999873990 ) ) ;
#13313=VERTEX_POINT ( 'NONE', #165172 ) ;
#13329=DIRECTION ( 'NONE',  ( -2.952720810173289112E-16, 1.000000000000000000, 0.000000000000000000 ) ) ;
#13338=ORIENTED_EDGE ( 'NONE', *, *, #22075, .T. ) ;
#13391=EDGE_CURVE ( 'NONE', #123588, #123054, #113993, .T. ) ;
#13398=CIRCLE ( 'NONE', #42421, 0.09999999999999939493 ) ;
#13407=DIRECTION ( 'NONE',  ( 6.938893903907030216E-14, 0.000000000000000000, 1.000000000000000000 ) ) ;
#13417=VERTEX_POINT ( 'NONE', #133739 ) ;
#13418=DIRECTION ( 'NONE',  ( 0.000000000000000000, 0.000000000000000000, -1.000000000000000000 ) ) ;
#13457=EDGE_LOOP ( 'NONE', ( #142674, #89468, #92268, #136773 ) ) ;
#13460=ADVANCED_FACE ( 'NONE', ( #73803 ), #135003, .F. ) ;
#13479=EDGE_CURVE ( 'NONE', #157348, #70815, #168218, .T. ) ;
#13501=AXIS2_PLACEMENT_3D ( 'NONE', #52864, #252349, #133696 ) ;
#13519=CIRCLE ( 'NONE', #76045, 11.65000000000000746 ) ;
#13529=CARTESIAN_POINT ( 'NONE',  ( -20.54999999999999716, 2.000000000011154189, -87.27537807723794572 ) ) ;
#13538=DIRECTION ( 'NONE',  ( 1.000000000000000000, -0.000000000000000000, -0.000000000000000000 ) ) ;
#13550=CYLINDRICAL_SURFACE ( 'NONE', #58078, 0.09999999999999939493 ) ;
#13553=CARTESIAN_POINT ( 'NONE',  ( -20.54999999999999716, -9.399999999988848387, -76.89396912265249284 ) ) ;
#13568=DIRECTION ( 'NONE',  ( 1.000000000000000000, -0.000000000000000000, 0.000000000000000000 ) ) ;
#13596=DIRECTION ( 'NONE',  ( -1.000000000000000000, -0.000000000000000000, 0.000000000000000000 ) ) ;
#13607=CARTESIAN_POINT ( 'NONE',  ( 23.14999999999999858, 1.115600667400684642E-11, -100.5000000000000426 ) ) ;
#13614=EDGE_CURVE ( 'NONE', #2322, #80091, #60007, .T. ) ;
#13620=ADVANCED_FACE ( 'NONE', ( #152907 ), #92885, .T. ) ;
#13637=VECTOR ( 'NONE', #96737, 1000.000000000000000 ) ;
#13674=ORIENTED_EDGE ( 'NONE', *, *, #139438, .T. ) ;
#13683=ORIENTED_EDGE ( 'NONE', *, *, #12463, .F. ) ;
#13728=VECTOR ( 'NONE', #116842, 1000.000000000000000 ) ;
#13736=TOROIDAL_SURFACE ( 'NONE', #105276, 0.2000000000000000111, 0.1000000000000000056 ) ;
#13751=DIRECTION ( 'NONE',  ( 0.000000000000000000, 0.000000000000000000, 1.000000000000000000 ) ) ;
#13810=ADVANCED_FACE ( 'NONE', ( #190544 ), #14478, .T. ) ;
#13859=CARTESIAN_POINT ( 'NONE',  ( -23.15000000000000213, -11.74999999998884448, -67.00000000000004263 ) ) ;
#13886=LINE ( 'NONE', #157269, #234977 ) ;
#13976=DIRECTION ( 'NONE',  ( 0.000000000000000000, -1.000000000000000000, 0.000000000000000000 ) ) ;
#13980=ORIENTED_EDGE ( 'NONE', *, *, #65709, .T. ) ;
#13993=VERTEX_POINT ( 'NONE', #205917 ) ;
#13999=ORIENTED_EDGE ( 'NONE', *, *, #107347, .T. ) ;
#14001=EDGE_LOOP ( 'NONE', ( #201575, #62425, #67462 ) ) ;
#14002=CARTESIAN_POINT ( 'NONE',  ( -22.60000000000094289, 0.1008583691096561347, -55.25043287651063650 ) ) ;
#14006=CIRCLE ( 'NONE', #72460, 11.90000000000000036 ) ;
#14014=AXIS2_PLACEMENT_3D ( 'NONE', #139716, #161895, #4071 ) ;
#14027=ORIENTED_EDGE ( 'NONE', *, *, #233482, .F. ) ;
#14039=CIRCLE ( 'NONE', #197167, 0.09999999999999939493 ) ;
#14119=DIRECTION ( 'NONE',  ( -1.000000000000000000, 0.000000000000000000, 0.000000000000000000 ) ) ;
#14144=DIRECTION ( 'NONE',  ( -0.000000000000000000, 0.1350103645451876666, 0.9908441862701600211 ) ) ;
#14147=ADVANCED_FACE ( 'NONE', ( #128964 ), #147229, .T. ) ;
#14188=CARTESIAN_POINT ( 'NONE',  ( 20.94999999999999929, 6.550000000011156231, -79.25000000000004263 ) ) ;
#14191=ORIENTED_EDGE ( 'NONE', *, *, #107034, .T. ) ;
#14195=CIRCLE ( 'NONE', #26661, 0.2000000000000057288 ) ;
#14196=FACE_BOUND ( 'NONE', #164128, .T. ) ;
#14230=CARTESIAN_POINT ( 'NONE',  ( 18.39999999999999858, -9.519327731081279609, -73.97297637655938729 ) ) ;
#14231=CARTESIAN_POINT ( 'NONE',  ( -23.15000000000000213, 1.115600667400684642E-11, -100.5000000000000426 ) ) ;
#14247=ORIENTED_EDGE ( 'NONE', *, *, #129134, .T. ) ;
#14254=EDGE_CURVE ( 'NONE', #20178, #33168, #247651, .T. ) ;
#14264=DIRECTION ( 'NONE',  ( 0.000000000000000000, 0.000000000000000000, 1.000000000000000000 ) ) ;
#14276=EDGE_LOOP ( 'NONE', ( #26876, #245073, #195279, #202181, #216253, #153486, #480, #82340 ) ) ;
#14279=ORIENTED_EDGE ( 'NONE', *, *, #116769, .T. ) ;
#14300=CARTESIAN_POINT ( 'NONE',  ( 20.94999999999999929, 1.115600667400684642E-11, -108.3000000000000540 ) ) ;
#14305=DIRECTION ( 'NONE',  ( 0.000000000000000000, 0.000000000000000000, 1.000000000000000000 ) ) ;
#14316=CIRCLE ( 'NONE', #214205, 7.800000000000000711 ) ;
#14326=CARTESIAN_POINT ( 'NONE',  ( 20.94999999999999929, 10.72371710471868056, -79.15000000000004832 ) ) ;
#14352=EDGE_LOOP ( 'NONE', ( #125740, #113749, #143247, #142152, #42841 ) ) ;
#14353=CARTESIAN_POINT ( 'NONE',  ( 20.12500000000000355, 10.24195072709382970, -74.86020372708617288 ) ) ;
#14359=CARTESIAN_POINT ( 'NONE',  ( 18.59999999999999076, -1.835859311432481045, -112.0044391687985694 ) ) ;
#14386=VECTOR ( 'NONE', #14144, 1000.000000000000000 ) ;
#14390=EDGE_CURVE ( 'NONE', #212939, #128108, #135387, .T. ) ;
#14420=DIRECTION ( 'NONE',  ( -1.000000000000000000, -0.000000000000000000, -0.000000000000000000 ) ) ;
#14442=CARTESIAN_POINT ( 'NONE',  ( 22.39999999999999503, -0.1008583690875579364, -55.25043287651065782 ) ) ;
#14453=ORIENTED_EDGE ( 'NONE', *, *, #107012, .T. ) ;
#14454=AXIS2_PLACEMENT_3D ( 'NONE', #208513, #11592, #130222 ) ;
#14455=AXIS2_PLACEMENT_3D ( 'NONE', #160458, #239975, #61330 ) ;
#14463=VERTEX_POINT ( 'NONE', #101321 ) ;
#14468=DIRECTION ( 'NONE',  ( 0.000000000000000000, -1.000000000000000000, 0.000000000000000000 ) ) ;
#14469=CARTESIAN_POINT ( 'NONE',  ( 21.00000000000000000, 9.750000000011153745, -88.25000000000005684 ) ) ;
#14471=EDGE_CURVE ( 'NONE', #119208, #214056, #139489, .T. ) ;
#14478=PLANE ( 'NONE',  #155907 ) ;
#14480=DIRECTION ( 'NONE',  ( 0.000000000000000000, 0.000000000000000000, -1.000000000000000000 ) ) ;
#14482=AXIS2_PLACEMENT_3D ( 'NONE', #28638, #208523, #108124 ) ;
#14491=CARTESIAN_POINT ( 'NONE',  ( 21.05000000000000071, 1.115600667400684642E-11, -67.00000000000004263 ) ) ;
#14515=FACE_OUTER_BOUND ( 'NONE', #36131, .T. ) ;
#14562=EDGE_CURVE ( 'NONE', #151973, #8323, #52186, .T. ) ;
#14566=ADVANCED_FACE ( 'NONE', ( #229039 ), #56281, .F. ) ;
#14574=ORIENTED_EDGE ( 'NONE', *, *, #233913, .T. ) ;
#14581=EDGE_CURVE ( 'NONE', #156376, #247484, #127031, .T. ) ;
#14603=VERTEX_POINT ( 'NONE', #157224 ) ;
#14607=FACE_OUTER_BOUND ( 'NONE', #207161, .T. ) ;
#14608=AXIS2_PLACEMENT_3D ( 'NONE', #96612, #217849, #39269 ) ;
#14633=CARTESIAN_POINT ( 'NONE',  ( 18.43565242384934422, -9.519327731081284938, -73.97297637655937308 ) ) ;
#14660=AXIS2_PLACEMENT_3D ( 'NONE', #235754, #19286, #57100 ) ;
#14745=EDGE_LOOP ( 'NONE', ( #41555, #192487, #233042, #230766 ) ) ;
#14753=DIRECTION ( 'NONE',  ( 0.000000000000000000, -1.000000000000000000, 0.000000000000000000 ) ) ;
#14787=ORIENTED_EDGE ( 'NONE', *, *, #45292, .T. ) ;
#14797=CARTESIAN_POINT ( 'NONE',  ( -23.25000000000000000, 2.000000000011154189, -80.22462192276213955 ) ) ;
#14857=AXIS2_PLACEMENT_3D ( 'NONE', #109700, #245387, #47148 ) ;
#14865=DIRECTION ( 'NONE',  ( 6.938893903907030216E-14, 0.000000000000000000, 1.000000000000000000 ) ) ;
#14887=CARTESIAN_POINT ( 'NONE',  ( -18.60000000000000142, -9.321008403350123928, -74.23593824907794669 ) ) ;
#14920=FACE_OUTER_BOUND ( 'NONE', #206615, .T. ) ;
#14936=AXIS2_PLACEMENT_3D ( 'NONE', #67706, #209792, #66428 ) ;
#14986=ORIENTED_EDGE ( 'NONE', *, *, #176207, .F. ) ;
#15020=CARTESIAN_POINT ( 'NONE',  ( 23.24999999999999645, 1.115600667400684642E-11, -67.00000000000004263 ) ) ;
#15023=DIRECTION ( 'NONE',  ( 0.000000000000000000, 0.000000000000000000, 1.000000000000000000 ) ) ;
#15036=DIRECTION ( 'NONE',  ( 0.000000000000000000, 0.000000000000000000, 1.000000000000000000 ) ) ;
#15049=DIRECTION ( 'NONE',  ( 0.000000000000000000, -0.1350103645451904977, 0.9908441862701596881 ) ) ;
#15077=ADVANCED_FACE ( 'NONE', ( #126423 ), #204664, .T. ) ;
#15084=AXIS2_PLACEMENT_3D ( 'NONE', #21161, #201048, #107075 ) ;
#15121=ORIENTED_EDGE ( 'NONE', *, *, #206515, .F. ) ;
#15125=CARTESIAN_POINT ( 'NONE',  ( 21.05000000000000071, 8.815201804578357780, -75.42053749668541229 ) ) ;
#15154=EDGE_CURVE ( 'NONE', #58451, #50622, #2480, .T. ) ;
#15168=CARTESIAN_POINT ( 'NONE',  ( 23.24999999999999645, 1.115600667400684642E-11, -100.5000000000000426 ) ) ;
#15184=CARTESIAN_POINT ( 'NONE',  ( -21.10320863425827298, 0.02502225123826237740, -60.59972261354081269 ) ) ;
#15199=FACE_OUTER_BOUND ( 'NONE', #20014, .T. ) ;
#15201=EDGE_CURVE ( 'NONE', #115244, #225971, #185830, .T. ) ;
#15221=FACE_OUTER_BOUND ( 'NONE', #239408, .T. ) ;
#15238=CYLINDRICAL_SURFACE ( 'NONE', #112498, 0.1000000000000000472 ) ;
#15258=FACE_OUTER_BOUND ( 'NONE', #101382, .T. ) ;
#15270=FACE_OUTER_BOUND ( 'NONE', #22279, .T. ) ;
#15271=AXIS2_PLACEMENT_3D ( 'NONE', #99626, #160934, #200051 ) ;
#15304=ORIENTED_EDGE ( 'NONE', *, *, #41430, .F. ) ;
#15306=AXIS2_PLACEMENT_3D ( 'NONE', #12400, #250970, #9806 ) ;
#15328=VECTOR ( 'NONE', #196117, 1000.000000000000000 ) ;
#15344=EDGE_LOOP ( 'NONE', ( #6058, #33021, #206710, #76244 ) ) ;
#15350=EDGE_CURVE ( 'NONE', #140891, #62297, #127396, .T. ) ;
#15376=ORIENTED_EDGE ( 'NONE', *, *, #199509, .F. ) ;
#15394=DIRECTION ( 'NONE',  ( -1.000000000000000000, -3.265361837132813093E-16, 0.000000000000000000 ) ) ;
#15406=AXIS2_PLACEMENT_3D ( 'NONE', #125475, #139875, #21265 ) ;
#15420=FACE_OUTER_BOUND ( 'NONE', #75635, .T. ) ;
#15459=AXIS2_PLACEMENT_3D ( 'NONE', #250790, #214244, #33083 ) ;
#15472=DIRECTION ( 'NONE',  ( 0.000000000000000000, 0.000000000000000000, -1.000000000000000000 ) ) ;
#15478=ORIENTED_EDGE ( 'NONE', *, *, #121372, .T. ) ;
#15488=DIRECTION ( 'NONE',  ( 0.000000000000000000, 0.000000000000000000, -1.000000000000000000 ) ) ;
#15518=CARTESIAN_POINT ( 'NONE',  ( 20.94999999999999929, -11.64999999998883595, -97.60000000000005116 ) ) ;
#15521=SPHERICAL_SURFACE ( 'NONE', #114017, 0.1000000000000000056 ) ;
#15527=CARTESIAN_POINT ( 'NONE',  ( 21.05000000000000071, 11.75000000001116263, -93.48519422934610645 ) ) ;
#15582=CARTESIAN_POINT ( 'NONE',  ( 18.59999999999999432, -1.835859311432484375, -112.0044391687985694 ) ) ;
#15590=CARTESIAN_POINT ( 'NONE',  ( 18.41356215285961895, -9.499999999988869348, -74.03206939669966857 ) ) ;
#15594=VERTEX_POINT ( 'NONE', #111682 ) ;
#15596=DIRECTION ( 'NONE',  ( 0.000000000000000000, -0.3738317757009718689, 0.9274965247785342815 ) ) ;
#15607=DIRECTION ( 'NONE',  ( -1.000000000000000000, -0.000000000000000000, 0.000000000000000000 ) ) ;
#15624=AXIS2_PLACEMENT_3D ( 'NONE', #85899, #42965, #63808 ) ;
#15631=ORIENTED_EDGE ( 'NONE', *, *, #176735, .F. ) ;
#15647=DIRECTION ( 'NONE',  ( 0.000000000000000000, -1.000000000000000000, 0.000000000000000000 ) ) ;
#15684=DIRECTION ( 'NONE',  ( -1.000000000000000000, -0.000000000000000000, -0.000000000000000000 ) ) ;
#15687=LINE ( 'NONE', #74385, #119633 ) ;
#15696=CARTESIAN_POINT ( 'NONE',  ( 18.59999999999999432, 1.162701749949165642, -75.10000000000003695 ) ) ;
#15700=DIRECTION ( 'NONE',  ( 0.000000000000000000, -1.000000000000000000, 0.000000000000000000 ) ) ;
#15729=DIRECTION ( 'NONE',  ( 1.000000000000000000, 3.265361837132813093E-16, -0.000000000000000000 ) ) ;
#15734=LINE ( 'NONE', #73143, #201803 ) ;
#15755=ADVANCED_FACE ( 'NONE', ( #176812 ), #94678, .F. ) ;
#15756=LINE ( 'NONE', #254310, #112038 ) ;
#15768=ORIENTED_EDGE ( 'NONE', *, *, #27877, .T. ) ;
#15797=DIRECTION ( 'NONE',  ( 0.000000000000000000, -1.000000000000000000, 0.000000000000000000 ) ) ;
#15803=FACE_OUTER_BOUND ( 'NONE', #95074, .T. ) ;
#15804=EDGE_LOOP ( 'NONE', ( #169491, #181668, #123083 ) ) ;
#15815=CARTESIAN_POINT ( 'NONE',  ( 21.05000000000000071, 1.115600667400684642E-11, -100.5000000000000426 ) ) ;
#15846=ADVANCED_FACE ( 'NONE', ( #82780 ), #162382, .T. ) ;
#15860=DIRECTION ( 'NONE',  ( -1.000000000000000000, -0.000000000000000000, 0.000000000000000000 ) ) ;
#15861=ORIENTED_EDGE ( 'NONE', *, *, #8996, .F. ) ;
#15894=EDGE_LOOP ( 'NONE', ( #90887, #23496, #189905, #175031 ) ) ;
#15902=CARTESIAN_POINT ( 'NONE',  ( 23.15000000000000213, -11.48912529306489994, -97.40000000000004832 ) ) ;
#15918=CARTESIAN_POINT ( 'NONE',  ( -21.05000000000000071, -11.64999999998884306, -97.60000000000005116 ) ) ;
#15986=DIRECTION ( 'NONE',  ( 0.000000000000000000, 0.000000000000000000, -1.000000000000000000 ) ) ;
#15999=CARTESIAN_POINT ( 'NONE',  ( 23.14999999999999858, 11.65000000001116298, -93.48519422934610645 ) ) ;
#16002=VERTEX_POINT ( 'NONE', #132230 ) ;
#16019=FACE_OUTER_BOUND ( 'NONE', #134501, .T. ) ;
#16032=CARTESIAN_POINT ( 'NONE',  ( -18.59999999999999787, -1.149570369564537842, -108.3159124845020074 ) ) ;
#16076=ORIENTED_EDGE ( 'NONE', *, *, #104411, .F. ) ;
#16077=CARTESIAN_POINT ( 'NONE',  ( 22.00411653889209873, 0.09903810579706272266, -59.74655713235965493 ) ) ;
#16123=CARTESIAN_POINT ( 'NONE',  ( 21.11927991906888025, 6.448493118502572230, -66.99091632052613932 ) ) ;
#16134=CARTESIAN_POINT ( 'NONE',  ( -18.39999999999999858, -9.499999999988849808, -107.1001893912220879 ) ) ;
#16175=CARTESIAN_POINT ( 'NONE',  ( -18.49999999999997158, -9.321008403350138138, -74.23593824907793248 ) ) ;
#16222=FACE_OUTER_BOUND ( 'NONE', #60796, .T. ) ;
#16228=EDGE_CURVE ( 'NONE', #59145, #40125, #223788, .T. ) ;
#16256=FACE_OUTER_BOUND ( 'NONE', #186281, .T. ) ;
#16271=FACE_OUTER_BOUND ( 'NONE', #82687, .T. ) ;
#16276=ORIENTED_EDGE ( 'NONE', *, *, #33190, .F. ) ;
#16278=CIRCLE ( 'NONE', #20366, 0.2000000000000057288 ) ;
#16299=FACE_OUTER_BOUND ( 'NONE', #8718, .T. ) ;
#16304=DIRECTION ( 'NONE',  ( 0.000000000000000000, 0.4999999999999949485, -0.8660254037844415942 ) ) ;
#16307=ORIENTED_EDGE ( 'NONE', *, *, #24830, .F. ) ;
#16313=ORIENTED_EDGE ( 'NONE', *, *, #144072, .F. ) ;
#16336=EDGE_LOOP ( 'NONE', ( #102908, #54971, #189783, #108592 ) ) ;
#16357=CARTESIAN_POINT ( 'NONE',  ( 21.14999999999999858, 11.65000000001115943, -79.15000000000004832 ) ) ;
#16360=ORIENTED_EDGE ( 'NONE', *, *, #252200, .F. ) ;
#16363=ORIENTED_EDGE ( 'NONE', *, *, #176559, .F. ) ;
#16388=DIRECTION ( 'NONE',  ( 1.000000000000000000, -0.000000000000000000, -0.000000000000000000 ) ) ;
#16396=ORIENTED_EDGE ( 'NONE', *, *, #102032, .F. ) ;
#16425=CARTESIAN_POINT ( 'NONE',  ( -18.59999999999999787, 10.33248238083634440, -106.0948465439131922 ) ) ;
#16466=CIRCLE ( 'NONE', #162031, 0.09999999999999939493 ) ;
#16472=CARTESIAN_POINT ( 'NONE',  ( 20.94999999999999929, 6.650000000011155876, -79.15000000000004832 ) ) ;
#16476=CARTESIAN_POINT ( 'NONE',  ( -21.07933241753356413, 0.09337959043042065588, -60.67135405162031248 ) ) ;
#16482=DIRECTION ( 'NONE',  ( 0.000000000000000000, 1.000000000000000000, 0.000000000000000000 ) ) ;
#16505=CIRCLE ( 'NONE', #253793, 7.900000000000003908 ) ;
#16531=DIRECTION ( 'NONE',  ( 1.000000000000000000, 0.000000000000000000, 0.000000000000000000 ) ) ;
#16576=EDGE_CURVE ( 'NONE', #39159, #100102, #174148, .T. ) ;
#16581=ADVANCED_FACE ( 'NONE', ( #25777 ), #141860, .F. ) ;
#16604=VERTEX_POINT ( 'NONE', #126139 ) ;
#16638=CIRCLE ( 'NONE', #54025, 0.09999999999999824307 ) ;
#16681=CIRCLE ( 'NONE', #108255, 0.1000000000000000472 ) ;
#16753=DIRECTION ( 'NONE',  ( -1.000000000000000000, -1.836970198721029934E-16, -3.186635328391151676E-31 ) ) ;
#16760=PLANE ( 'NONE',  #237657 ) ;
#16776=AXIS2_PLACEMENT_3D ( 'NONE', #178690, #116125, #4 ) ;
#16777=AXIS2_PLACEMENT_3D ( 'NONE', #250391, #90022, #228274 ) ;
#16792=CARTESIAN_POINT ( 'NONE',  ( 18.52165635395191501, -9.481150711270952769, -74.02483758286261661 ) ) ;
#16803=DIRECTION ( 'NONE',  ( 1.000000000000000000, 0.000000000000000000, 0.000000000000000000 ) ) ;
#16807=PLANE ( 'NONE',  #77483 ) ;
#16811=ORIENTED_EDGE ( 'NONE', *, *, #68904, .F. ) ;
#16829=CARTESIAN_POINT ( 'NONE',  ( 20.94999999999999574, -1.162701749926853712, -75.10000000000003695 ) ) ;
#16860=DIRECTION ( 'NONE',  ( -1.000000000000000000, -0.000000000000000000, -0.000000000000000000 ) ) ;
#16864=CARTESIAN_POINT ( 'NONE',  ( 21.97500000000000497, 9.750000000011153745, -79.25000000000004263 ) ) ;
#16869=AXIS2_PLACEMENT_3D ( 'NONE', #52814, #256095, #97042 ) ;
#16889=DIRECTION ( 'NONE',  ( 2.952720810173288619E-16, -1.000000000000000000, 0.000000000000000000 ) ) ;
#16916=LINE ( 'NONE', #96417, #254908 ) ;
#16938=DIRECTION ( 'NONE',  ( 1.000000000000000000, 0.000000000000000000, 0.000000000000000000 ) ) ;
#16950=DIRECTION ( 'NONE',  ( 1.000000000000000000, 0.000000000000000000, 0.000000000000000000 ) ) ;
#16985=DIRECTION ( 'NONE',  ( 0.000000000000000000, 0.000000000000000000, 1.000000000000000000 ) ) ;
#16997=CARTESIAN_POINT ( 'NONE',  ( -23.25000000000000000, -11.74999999998884448, -67.00000000000004263 ) ) ;
#17036=ORIENTED_EDGE ( 'NONE', *, *, #78120, .F. ) ;
#17054=EDGE_CURVE ( 'NONE', #72480, #10263, #25056, .T. ) ;
#17063=DIRECTION ( 'NONE',  ( -1.000000000000000000, -3.265361837132813093E-16, 0.000000000000000000 ) ) ;
#17118=DIRECTION ( 'NONE',  ( 0.000000000000000000, 0.5000000000000078826, 0.8660254037844340447 ) ) ;
#17134=CYLINDRICAL_SURFACE ( 'NONE', #14608, 0.1000000000000028644 ) ;
#17147=VERTEX_POINT ( 'NONE', #182998 ) ;
#17165=VERTEX_POINT ( 'NONE', #42197 ) ;
#17193=DIRECTION ( 'NONE',  ( -0.000000000000000000, -0.000000000000000000, 1.000000000000000000 ) ) ;
#17229=DIRECTION ( 'NONE',  ( 0.000000000000000000, 0.000000000000000000, 1.000000000000000000 ) ) ;
#17256=CARTESIAN_POINT ( 'NONE',  ( 21.05000000000000071, 11.65000000001116298, -93.48519422934610645 ) ) ;
#17299=FACE_OUTER_BOUND ( 'NONE', #84154, .T. ) ;
#17343=DIRECTION ( 'NONE',  ( -2.840903330521631775E-16, 0.8700118002898321601, -0.4930308989875230030 ) ) ;
#17348=DIRECTION ( 'NONE',  ( 0.000000000000000000, 1.000000000000000000, -6.308085367188393199E-16 ) ) ;
#17366=CIRCLE ( 'NONE', #200516, 0.1000000000000028644 ) ;
#17374=SPHERICAL_SURFACE ( 'NONE', #72859, 0.1000000000000000056 ) ;
#17405=ORIENTED_EDGE ( 'NONE', *, *, #132700, .F. ) ;
#17426=ORIENTED_EDGE ( 'NONE', *, *, #226224, .F. ) ;
#17440=CIRCLE ( 'NONE', #204687, 0.1000000000000028644 ) ;
#17467=CARTESIAN_POINT ( 'NONE',  ( -22.49231231312463208, 11.64998490368843953, -66.93894711239866524 ) ) ;
#17476=CIRCLE ( 'NONE', #138269, 0.1000000000000028644 ) ;
#17504=EDGE_CURVE ( 'NONE', #12856, #81812, #221775, .T. ) ;
#17514=ORIENTED_EDGE ( 'NONE', *, *, #123126, .T. ) ;
#17531=FACE_OUTER_BOUND ( 'NONE', #185700, .T. ) ;
#17538=EDGE_CURVE ( 'NONE', #27504, #4255, #102969, .T. ) ;
#17544=EDGE_CURVE ( 'NONE', #29887, #138550, #99271, .T. ) ;
#17550=ORIENTED_EDGE ( 'NONE', *, *, #225634, .T. ) ;
#17569=ORIENTED_EDGE ( 'NONE', *, *, #4588, .T. ) ;
#17667=CARTESIAN_POINT ( 'NONE',  ( 20.95429402530545815, 8.876194151113343977, -75.52308669793789875 ) ) ;
#17670=ADVANCED_FACE ( 'NONE', ( #225627 ), #109545, .T. ) ;
#17713=CARTESIAN_POINT ( 'NONE',  ( -21.08884785362073089, 0.04978309507788075683, -60.64280663257443393 ) ) ;
#17780=ORIENTED_EDGE ( 'NONE', *, *, #185928, .F. ) ;
#17804=DIRECTION ( 'NONE',  ( 0.000000000000000000, 0.1350103645451876666, -0.9908441862701600211 ) ) ;
#17882=ADVANCED_FACE ( 'NONE', ( #83240 ), #257233, .F. ) ;
#17885=DIRECTION ( 'NONE',  ( 1.000000000000000000, 0.000000000000000000, 0.000000000000000000 ) ) ;
#17904=AXIS2_PLACEMENT_3D ( 'NONE', #42544, #202907, #23022 ) ;
#17909=EDGE_CURVE ( 'NONE', #253099, #60368, #107258, .T. ) ;
#17991=AXIS2_PLACEMENT_3D ( 'NONE', #43228, #65346, #122781 ) ;
#18018=CARTESIAN_POINT ( 'NONE',  ( -22.50000000000000000, 1.115600667400684642E-11, -60.75000000000004974 ) ) ;
#18023=CARTESIAN_POINT ( 'NONE',  ( 18.59999999999999787, -1.263275465206102233, -108.4018646667464481 ) ) ;
#18077=CARTESIAN_POINT ( 'NONE',  ( 20.94999999999999929, 1.115600667400684642E-11, -100.5000000000000426 ) ) ;
#18124=CARTESIAN_POINT ( 'NONE',  ( -23.25000000000000000, 11.65000000001115588, -55.25000000000004974 ) ) ;
#18130=CIRCLE ( 'NONE', #43083, 0.09999999999999939493 ) ;
#18178=CARTESIAN_POINT ( 'NONE',  ( 21.87500000000000355, 9.750000000011153745, -88.15000000000004832 ) ) ;
#18191=VERTEX_POINT ( 'NONE', #120837 ) ;
#18217=ADVANCED_FACE ( 'NONE', ( #176959 ), #149169, .F. ) ;
#18239=DIRECTION ( 'NONE',  ( 1.000000000000000000, -0.000000000000000000, -0.000000000000000000 ) ) ;
#18315=FACE_OUTER_BOUND ( 'NONE', #4788, .T. ) ;
#18349=AXIS2_PLACEMENT_3D ( 'NONE', #26056, #143417, #160447 ) ;
#18356=CARTESIAN_POINT ( 'NONE',  ( -22.39999999999999858, 11.65000000001115588, -66.90000000000004832 ) ) ;
#18377=CARTESIAN_POINT ( 'NONE',  ( -20.94999999999999929, 11.60000000001115161, -73.92820323027559937 ) ) ;
#18387=ORIENTED_EDGE ( 'NONE', *, *, #225931, .T. ) ;
#18407=CARTESIAN_POINT ( 'NONE',  ( -20.64999999999999858, -8.730841121484170131, -90.90192528101572123 ) ) ;
#18413=FACE_OUTER_BOUND ( 'NONE', #210123, .T. ) ;
#18424=ORIENTED_EDGE ( 'NONE', *, *, #197196, .F. ) ;
#18473=ORIENTED_EDGE ( 'NONE', *, *, #20834, .F. ) ;
#18493=VECTOR ( 'NONE', #20634, 1000.000000000000000 ) ;
#18527=DIRECTION ( 'NONE',  ( -3.469446951953604722E-14, -0.9999176327611370985, -0.01283462868040260302 ) ) ;
#18572=ORIENTED_EDGE ( 'NONE', *, *, #145528, .T. ) ;
#18580=CARTESIAN_POINT ( 'NONE',  ( 20.85000000000000142, 1.115600667400684642E-11, -100.5000000000000426 ) ) ;
#18615=VERTEX_POINT ( 'NONE', #56630 ) ;
#18651=ORIENTED_EDGE ( 'NONE', *, *, #103497, .F. ) ;
#18652=FACE_OUTER_BOUND ( 'NONE', #54582, .T. ) ;
#18689=DIRECTION ( 'NONE',  ( 0.000000000000000000, 0.000000000000000000, -1.000000000000000000 ) ) ;
#18749=DIRECTION ( 'NONE',  ( 6.484947573744954877E-15, 0.9274965247785529332, -0.3738317757009255171 ) ) ;
#18798=EDGE_LOOP ( 'NONE', ( #131641, #211155, #99168 ) ) ;
#18800=ADVANCED_FACE ( 'NONE', ( #211280 ), #93889, .T. ) ;
#18801=CYLINDRICAL_SURFACE ( 'NONE', #134618, 0.1000000000000028644 ) ;
#18815=CIRCLE ( 'NONE', #56412, 11.65000000000000746 ) ;
#18833=AXIS2_PLACEMENT_3D ( 'NONE', #233825, #17348, #218083 ) ;
#18835=DIRECTION ( 'NONE',  ( 0.000000000000000000, 0.000000000000000000, -1.000000000000000000 ) ) ;
#18858=DIRECTION ( 'NONE',  ( -0.8660254037844653530, 0.000000000000000000, 0.4999999999999539257 ) ) ;
#18864=LINE ( 'NONE', #21463, #79560 ) ;
#18880=CIRCLE ( 'NONE', #243744, 11.80000000000000426 ) ;
#18908=TOROIDAL_SURFACE ( 'NONE', #123162, 0.6000000000000004219, 0.1000000000000000056 ) ;
#18909=EDGE_LOOP ( 'NONE', ( #206407, #165913, #107249, #170297 ) ) ;
#18912=DIRECTION ( 'NONE',  ( -1.000000000000000000, -0.000000000000000000, -0.000000000000000000 ) ) ;
#18927=EDGE_CURVE ( 'NONE', #114500, #142483, #62031, .T. ) ;
#18959=AXIS2_PLACEMENT_3D ( 'NONE', #11039, #72314, #153158 ) ;
#18995=VERTEX_POINT ( 'NONE', #40382 ) ;
#18998=CIRCLE ( 'NONE', #60682, 0.09999999999999967248 ) ;
#19051=ORIENTED_EDGE ( 'NONE', *, *, #119051, .T. ) ;
#19057=DIRECTION ( 'NONE',  ( 0.000000000000000000, 0.000000000000000000, 1.000000000000000000 ) ) ;
#19109=AXIS2_PLACEMENT_3D ( 'NONE', #59823, #79396, #117264 ) ;
#19123=EDGE_LOOP ( 'NONE', ( #56240, #244718, #204206, #231578, #231698 ) ) ;
#19141=CARTESIAN_POINT ( 'NONE',  ( -20.94999999999999929, 1.261786168576181755, -75.08649896354552311 ) ) ;
#19149=DIRECTION ( 'NONE',  ( 0.000000000000000000, 0.000000000000000000, 1.000000000000000000 ) ) ;
#19230=EDGE_CURVE ( 'NONE', #202644, #217587, #116214, .T. ) ;
#19252=VECTOR ( 'NONE', #53962, 1000.000000000000000 ) ;
#19254=VECTOR ( 'NONE', #106567, 1000.000000000000000 ) ;
#19265=DIRECTION ( 'NONE',  ( 0.000000000000000000, -1.000000000000000000, 0.000000000000000000 ) ) ;
#19286=DIRECTION ( 'NONE',  ( -0.000000000000000000, 0.000000000000000000, 1.000000000000000000 ) ) ;
#19314=VECTOR ( 'NONE', #211259, 1000.000000000000000 ) ;
#19346=DIRECTION ( 'NONE',  ( 0.000000000000000000, 1.000000000000000000, -6.938893903907240999E-14 ) ) ;
#19347=DIRECTION ( 'NONE',  ( 1.000000000000000000, 0.000000000000000000, 0.000000000000000000 ) ) ;
#19349=EDGE_LOOP ( 'NONE', ( #121429, #178057, #1138, #127045, #137642, #198313, #69430, #29722, #257127, #164834, #1088, #122217, #57490, #131488, #73272, #201159 ) ) ;
#19375=DIRECTION ( 'NONE',  ( 1.000000000000000000, -0.000000000000000000, -0.000000000000000000 ) ) ;
#19394=ORIENTED_EDGE ( 'NONE', *, *, #185638, .T. ) ;
#19432=ORIENTED_EDGE ( 'NONE', *, *, #180719, .F. ) ;
#19452=ORIENTED_EDGE ( 'NONE', *, *, #247386, .T. ) ;
#19455=EDGE_CURVE ( 'NONE', #133216, #134711, #54478, .T. ) ;
#19456=LINE ( 'NONE', #22031, #213164 ) ;
#19472=LINE ( 'NONE', #141968, #64420 ) ;
#19513=EDGE_CURVE ( 'NONE', #12745, #96642, #83665, .T. ) ;
#19540=CARTESIAN_POINT ( 'NONE',  ( -21.05000000000000071, 5.900000000011102586, -77.21909976465646253 ) ) ;
#19542=VERTEX_POINT ( 'NONE', #254848 ) ;
#19576=VECTOR ( 'NONE', #155229, 1000.000000000000000 ) ;
#19579=VECTOR ( 'NONE', #194596, 1000.000000000000000 ) ;
#19586=CIRCLE ( 'NONE', #198632, 0.5000000000000004441 ) ;
#19589=LINE ( 'NONE', #42999, #249967 ) ;
#19664=EDGE_CURVE ( 'NONE', #70270, #6867, #97076, .T. ) ;
#19670=EDGE_CURVE ( 'NONE', #71510, #29887, #21370, .T. ) ;
#19673=ADVANCED_FACE ( 'NONE', ( #42290 ), #192065, .F. ) ;
#19677=CIRCLE ( 'NONE', #15406, 0.09999999999999939493 ) ;
#19694=ORIENTED_EDGE ( 'NONE', *, *, #70088, .T. ) ;
#19726=ORIENTED_EDGE ( 'NONE', *, *, #229683, .F. ) ;
#19727=DIRECTION ( 'NONE',  ( 0.000000000000000000, 0.000000000000000000, -1.000000000000000000 ) ) ;
#19776=DIRECTION ( 'NONE',  ( 1.000000000000000000, -0.000000000000000000, -0.000000000000000000 ) ) ;
#19782=CARTESIAN_POINT ( 'NONE',  ( -20.86777300164945004, 10.33200063080771969, -106.0931674956643320 ) ) ;
#19788=AXIS2_PLACEMENT_3D ( 'NONE', #236329, #137228, #60250 ) ;
#19812=DIRECTION ( 'NONE',  ( 0.000000000000000000, 2.891205793294679805E-16, -1.000000000000000000 ) ) ;
#19827=PLANE ( 'NONE',  #4590 ) ;
#19842=VERTEX_POINT ( 'NONE', #172561 ) ;
#19929=DIRECTION ( 'NONE',  ( 0.000000000000000000, -1.224646799142015331E-16, 1.000000000000000000 ) ) ;
#19976=ORIENTED_EDGE ( 'NONE', *, *, #217389, .F. ) ;
#20014=EDGE_LOOP ( 'NONE', ( #197304, #193207, #199949, #249919, #30284, #198304 ) ) ;
#20052=DIRECTION ( 'NONE',  ( 0.000000000000000000, -0.1350103645451876944, -0.9908441862701601321 ) ) ;
#20060=DIRECTION ( 'NONE',  ( 0.000000000000000000, 0.000000000000000000, -1.000000000000000000 ) ) ;
#20088=ORIENTED_EDGE ( 'NONE', *, *, #97769, .F. ) ;
#20092=DIRECTION ( 'NONE',  ( 0.000000000000000000, -1.000000000000000000, 6.308085367188393199E-16 ) ) ;
#20097=LINE ( 'NONE', #502, #69874 ) ;
#20098=ADVANCED_FACE ( 'NONE', ( #17299 ), #211311, .T. ) ;
#20111=DIRECTION ( 'NONE',  ( 1.000000000000000000, 0.000000000000000000, 0.000000000000000000 ) ) ;
#20131=DIRECTION ( 'NONE',  ( 0.000000000000000000, 0.1350103645451876666, 0.9908441862701600211 ) ) ;
#20140=CARTESIAN_POINT ( 'NONE',  ( 23.14999999999999503, 6.450000000011156587, -79.35000000000005116 ) ) ;
#20153=CARTESIAN_POINT ( 'NONE',  ( -18.50000000000000000, 9.350000000011156942, -79.35000000000005116 ) ) ;
#20160=DIRECTION ( 'NONE',  ( 0.000000000000000000, 0.000000000000000000, -1.000000000000000000 ) ) ;
#20161=AXIS2_PLACEMENT_3D ( 'NONE', #49687, #249186, #247886 ) ;
#20165=DIRECTION ( 'NONE',  ( -1.000000000000000000, -0.000000000000000000, -0.000000000000000000 ) ) ;
#20175=DIRECTION ( 'NONE',  ( -1.000000000000000000, 0.000000000000000000, 0.000000000000000000 ) ) ;
#20178=VERTEX_POINT ( 'NONE', #27595 ) ;
#20217=LINE ( 'NONE', #75072, #34646 ) ;
#20240=CIRCLE ( 'NONE', #249379, 0.1000000000000000472 ) ;
#20278=EDGE_LOOP ( 'NONE', ( #43849, #118825, #247847, #43837 ) ) ;
#20327=CYLINDRICAL_SURFACE ( 'NONE', #51113, 0.09999999999999939493 ) ;
#20331=CIRCLE ( 'NONE', #228623, 4.049999999999998046 ) ;
#20366=AXIS2_PLACEMENT_3D ( 'NONE', #82017, #161620, #202006 ) ;
#20399=CARTESIAN_POINT ( 'NONE',  ( -21.53551880898957904, 0.09896973458281840830, -60.21520223858371423 ) ) ;
#20400=VERTEX_POINT ( 'NONE', #87051 ) ;
#20404=DIRECTION ( 'NONE',  ( 1.000000000000000000, -0.000000000000000000, -0.000000000000000000 ) ) ;
#20417=ORIENTED_EDGE ( 'NONE', *, *, #72059, .F. ) ;
#20443=ADVANCED_FACE ( 'NONE', ( #15258 ), #233028, .T. ) ;
#20444=DIRECTION ( 'NONE',  ( -0.8660254037843878594, 0.000000000000000000, -0.5000000000000880407 ) ) ;
#20486=FACE_OUTER_BOUND ( 'NONE', #188413, .T. ) ;
#20519=CARTESIAN_POINT ( 'NONE',  ( -20.54999999999999716, 7.250000000011155521, -88.15000000000004832 ) ) ;
#20542=AXIS2_PLACEMENT_3D ( 'NONE', #94473, #171492, #93194 ) ;
#20546=DIRECTION ( 'NONE',  ( 0.000000000000000000, 0.000000000000000000, -1.000000000000000000 ) ) ;
#20598=VECTOR ( 'NONE', #32322, 1000.000000000000000 ) ;
#20603=EDGE_CURVE ( 'NONE', #194521, #252230, #240702, .T. ) ;
#20634=DIRECTION ( 'NONE',  ( 1.000000000000000000, -0.000000000000000000, -0.000000000000000000 ) ) ;
#20663=FACE_OUTER_BOUND ( 'NONE', #183629, .T. ) ;
#20685=ORIENTED_EDGE ( 'NONE', *, *, #92253, .T. ) ;
#20704=CARTESIAN_POINT ( 'NONE',  ( -23.25000000000000000, 4.350000000011156054, -79.25000000000004263 ) ) ;
#20712=CARTESIAN_POINT ( 'NONE',  ( -20.54999999999999716, 4.350000000011156054, -79.35000000000005116 ) ) ;
#20736=CARTESIAN_POINT ( 'NONE',  ( -20.54999999999999716, 2.000000000011154189, -80.22462192276213955 ) ) ;
#20800=CARTESIAN_POINT ( 'NONE',  ( 21.05000000000000071, 11.60000000001116227, -93.57179676972454274 ) ) ;
#20828=ADVANCED_FACE ( 'NONE', ( #74218 ), #57054, .T. ) ;
#20834=EDGE_CURVE ( 'NONE', #177357, #210178, #116016, .T. ) ;
#20837=EDGE_CURVE ( 'NONE', #232467, #258086, #45066, .T. ) ;
#20851=DIRECTION ( 'NONE',  ( -1.000000000000000000, -0.000000000000000000, -0.000000000000000000 ) ) ;
#20853=CARTESIAN_POINT ( 'NONE',  ( -22.39999999999999858, 0.1000000000111554016, -67.00000000000004263 ) ) ;
#20863=EDGE_CURVE ( 'NONE', #48905, #236070, #3554, .T. ) ;
#20871=AXIS2_PLACEMENT_3D ( 'NONE', #188822, #209675, #205817 ) ;
#20885=FACE_OUTER_BOUND ( 'NONE', #64900, .T. ) ;
#20894=DIRECTION ( 'NONE',  ( 0.000000000000000000, -0.8700118002898322711, 0.4930308989875231140 ) ) ;
#20903=CARTESIAN_POINT ( 'NONE',  ( -23.15000000000000213, 11.75000000001115552, -67.00000000000004263 ) ) ;
#20907=DIRECTION ( 'NONE',  ( 0.000000000000000000, 0.000000000000000000, 1.000000000000000000 ) ) ;
#20913=EDGE_CURVE ( 'NONE', #210178, #204053, #61835, .T. ) ;
#20919=CARTESIAN_POINT ( 'NONE',  ( 20.94999999999999574, 6.550000000011159784, -76.84382208968318650 ) ) ;
#20922=CARTESIAN_POINT ( 'NONE',  ( 18.59999999999999076, 1.835341550235567887, -78.55515129256302487 ) ) ;
#20934=DIRECTION ( 'NONE',  ( -0.7071067811865475727, -0.7071067811865475727, 0.000000000000000000 ) ) ;
#20935=DIRECTION ( 'NONE',  ( -1.000000000000000000, 0.000000000000000000, 0.000000000000000000 ) ) ;
#20949=DIRECTION ( 'NONE',  ( 0.000000000000000000, 0.000000000000000000, -1.000000000000000000 ) ) ;
#20964=CARTESIAN_POINT ( 'NONE',  ( -22.47071067811865319, 0.09909245471376171288, -59.27992525550198621 ) ) ;
#20974=CARTESIAN_POINT ( 'NONE',  ( 20.94999999999999929, -8.663551401858002876, -76.52410111806734960 ) ) ;
#21011=CARTESIAN_POINT ( 'NONE',  ( 21.05000000000000071, 1.115600667400684642E-11, -100.5000000000000426 ) ) ;
#21016=CARTESIAN_POINT ( 'NONE',  ( 22.39999999999999503, 0.1000000000111554016, -60.75000000000004974 ) ) ;
#21078=ORIENTED_EDGE ( 'NONE', *, *, #99950, .F. ) ;
#21088=EDGE_CURVE ( 'NONE', #230047, #18995, #20331, .T. ) ;
#21090=EDGE_CURVE ( 'NONE', #33168, #100804, #152144, .T. ) ;
#21093=CARTESIAN_POINT ( 'NONE',  ( 21.14999999999999858, 1.115600667400684642E-11, -67.00000000000004263 ) ) ;
#21102=TOROIDAL_SURFACE ( 'NONE', #41943, 1.900000000000002576, 0.1000000000000000056 ) ;
#21107=VERTEX_POINT ( 'NONE', #214646 ) ;
#21149=ADVANCED_FACE ( 'NONE', ( #137662 ), #101070, .T. ) ;
#21161=CARTESIAN_POINT ( 'NONE',  ( 20.94999999999999574, -11.64999999998883595, -70.10000000000005116 ) ) ;
#21177=FACE_OUTER_BOUND ( 'NONE', #11994, .T. ) ;
#21263=CARTESIAN_POINT ( 'NONE',  ( 21.07928932188134397, 6.328516656404459262, -66.90110485434564680 ) ) ;
#21265=DIRECTION ( 'NONE',  ( 1.000000000000000000, 0.000000000000000000, 0.000000000000000000 ) ) ;
#21266=EDGE_LOOP ( 'NONE', ( #175609, #50782, #102086, #71222, #47235 ) ) ;
#21268=DIRECTION ( 'NONE',  ( 1.000000000000000000, -0.000000000000000000, -0.000000000000000000 ) ) ;
#21290=ORIENTED_EDGE ( 'NONE', *, *, #193182, .T. ) ;
#21301=DIRECTION ( 'NONE',  ( 0.000000000000000000, -8.673617379883787770E-15, 1.000000000000000000 ) ) ;
#21307=CIRCLE ( 'NONE', #167059, 0.09999999999999917288 ) ;
#21360=ORIENTED_EDGE ( 'NONE', *, *, #227454, .F. ) ;
#21370=CIRCLE ( 'NONE', #250299, 0.1000000000000028644 ) ;
#21372=CYLINDRICAL_SURFACE ( 'NONE', #4153, 4.000000000000003553 ) ;
#21379=DIRECTION ( 'NONE',  ( -1.000000000000000000, -2.952720810173289112E-16, 0.000000000000000000 ) ) ;
#21391=VECTOR ( 'NONE', #81291, 1000.000000000000000 ) ;
#21392=DIRECTION ( 'NONE',  ( 0.000000000000000000, -1.000000000000000000, 0.000000000000000000 ) ) ;
#21393=CARTESIAN_POINT ( 'NONE',  ( 20.95512820512820440, 10.62384868372303615, -74.66491356908764487 ) ) ;
#21413=AXIS2_PLACEMENT_3D ( 'NONE', #137595, #217127, #218416 ) ;
#21416=TOROIDAL_SURFACE ( 'NONE', #175539, 0.2000000000000000111, 0.1000000000000000056 ) ;
#21439=EDGE_CURVE ( 'NONE', #146445, #163852, #95680, .T. ) ;
#21446=CARTESIAN_POINT ( 'NONE',  ( 21.11833042828145324, 6.445644693866474206, -66.99289949094061569 ) ) ;
#21463=CARTESIAN_POINT ( 'NONE',  ( -20.94999999999999929, 11.60000000001115517, -93.57179676972454274 ) ) ;
#21471=LINE ( 'NONE', #239211, #7408 ) ;
#21484=DIRECTION ( 'NONE',  ( 0.000000000000000000, 0.000000000000000000, -1.000000000000000000 ) ) ;
#21494=CARTESIAN_POINT ( 'NONE',  ( -22.39999999999999858, 11.75000000001115552, -67.10000000000005116 ) ) ;
#21536=ORIENTED_EDGE ( 'NONE', *, *, #166842, .F. ) ;
#21607=AXIS2_PLACEMENT_3D ( 'NONE', #115009, #170218, #55009 ) ;
#21641=DIRECTION ( 'NONE',  ( 0.000000000000000000, 0.9999631594459056361, -0.008583690987128059571 ) ) ;
#21642=EDGE_CURVE ( 'NONE', #141973, #251583, #188072, .T. ) ;
#21660=ORIENTED_EDGE ( 'NONE', *, *, #257521, .T. ) ;
#21719=CARTESIAN_POINT ( 'NONE',  ( -18.59999999999999787, 11.65000000001115232, -74.01480577065404987 ) ) ;
#21730=CYLINDRICAL_SURFACE ( 'NONE', #83142, 0.09999999999999939493 ) ;
#21742=CARTESIAN_POINT ( 'NONE',  ( -18.50000000000000000, -9.399999999988850163, -107.3820418481727046 ) ) ;
#21764=DIRECTION ( 'NONE',  ( 1.000000000000000000, 0.000000000000000000, -0.000000000000000000 ) ) ;
#21803=CARTESIAN_POINT ( 'NONE',  ( -20.54999999999999716, 4.350000000011156054, -88.15000000000004832 ) ) ;
#21810=CARTESIAN_POINT ( 'NONE',  ( -22.50000000000000000, 11.65000000001115588, -67.00000000000004263 ) ) ;
#21812=MANIFOLD_SOLID_BREP ( 'Stock-MAS-200-1', #178192 ) ;
#21818=DIRECTION ( 'NONE',  ( 0.000000000000000000, 0.000000000000000000, -1.000000000000000000 ) ) ;
#21821=CARTESIAN_POINT ( 'NONE',  ( -22.46246831459151494, 0.02191216695058596786, -55.35013543879008324 ) ) ;
#21827=ADVANCED_FACE ( 'NONE', ( #254430 ), #215726, .F. ) ;
#21844=FACE_BOUND ( 'NONE', #176956, .T. ) ;
#21847=ORIENTED_EDGE ( 'NONE', *, *, #177706, .T. ) ;
#21854=CARTESIAN_POINT ( 'NONE',  ( -23.25000000000000000, -11.64999999998884483, -97.50000000000004263 ) ) ;
#21864=CARTESIAN_POINT ( 'NONE',  ( -21.06715728752538652, 11.75000000001115197, -74.01480577065406408 ) ) ;
#21884=ORIENTED_EDGE ( 'NONE', *, *, #22990, .T. ) ;
#21890=CARTESIAN_POINT ( 'NONE',  ( 21.05000000000000071, 6.477067021135910707, -67.10000000000005116 ) ) ;
#21898=ADVANCED_FACE ( 'NONE', ( #18413 ), #96632, .T. ) ;
#21905=TOROIDAL_SURFACE ( 'NONE', #184385, 0.2000000000000000111, 0.1000000000000000056 ) ;
#21913=DIRECTION ( 'NONE',  ( 0.000000000000000000, -0.000000000000000000, 1.000000000000000000 ) ) ;
#21940=ORIENTED_EDGE ( 'NONE', *, *, #184442, .T. ) ;
#21952=FACE_OUTER_BOUND ( 'NONE', #55157, .T. ) ;
#21975=ORIENTED_EDGE ( 'NONE', *, *, #173000, .T. ) ;
#21992=DIRECTION ( 'NONE',  ( 1.000000000000000000, -0.000000000000000000, 0.000000000000000000 ) ) ;
#21996=VERTEX_POINT ( 'NONE', #13553 ) ;
#21999=CARTESIAN_POINT ( 'NONE',  ( -21.05000000000000071, 0.09779029131994770863, -60.74218538952393232 ) ) ;
#22031=CARTESIAN_POINT ( 'NONE',  ( -21.05000000000000071, 1.115600667400684642E-11, -71.29999999999999716 ) ) ;
#22075=EDGE_CURVE ( 'NONE', #214743, #18615, #203278, .T. ) ;
#22080=CARTESIAN_POINT ( 'NONE',  ( 21.05000000000000071, -11.29603075032412640, -97.45210084033617193 ) ) ;
#22138=CARTESIAN_POINT ( 'NONE',  ( 23.14999999999999858, 5.000000000011153745, -79.40526601891313874 ) ) ;
#22143=TOROIDAL_SURFACE ( 'NONE', #238599, 11.65000000000000036, 0.1000000000000000056 ) ;
#22152=ORIENTED_EDGE ( 'NONE', *, *, #255960, .F. ) ;
#22156=CIRCLE ( 'NONE', #67919, 0.1000000000000028644 ) ;
#22159=EDGE_LOOP ( 'NONE', ( #66489, #31347, #49256, #250097 ) ) ;
#22178=CARTESIAN_POINT ( 'NONE',  ( 21.05000000000000071, 1.115600667400684642E-11, -102.5000000000000426 ) ) ;
#22181=AXIS2_PLACEMENT_3D ( 'NONE', #22803, #123165, #25367 ) ;
#22191=ORIENTED_EDGE ( 'NONE', *, *, #256332, .T. ) ;
#22192=CARTESIAN_POINT ( 'NONE',  ( -23.25000000000000000, -8.999999999988844479, -91.20603087734760095 ) ) ;
#22235=EDGE_LOOP ( 'NONE', ( #36136, #254132, #82146, #177422 ) ) ;
#22245=ORIENTED_EDGE ( 'NONE', *, *, #239861, .F. ) ;
#22255=ORIENTED_EDGE ( 'NONE', *, *, #56623, .T. ) ;
#22279=EDGE_LOOP ( 'NONE', ( #31031, #100730, #42538, #15121 ) ) ;
#22280=EDGE_CURVE ( 'NONE', #83831, #252613, #78556, .T. ) ;
#22310=CARTESIAN_POINT ( 'NONE',  ( -20.94999999999999929, 10.29270135741298731, -105.9573618871519756 ) ) ;
#22347=ORIENTED_EDGE ( 'NONE', *, *, #216363, .F. ) ;
#22356=CARTESIAN_POINT ( 'NONE',  ( -20.88420186297724257, 10.33025634372637391, -106.0870929282639281 ) ) ;
#22365=EDGE_LOOP ( 'NONE', ( #54090, #90351, #62931, #182255 ) ) ;
#22428=CIRCLE ( 'NONE', #122186, 0.09999999999999971412 ) ;
#22458=CARTESIAN_POINT ( 'NONE',  ( 20.94999999999999929, 1.115600667400684642E-11, -100.5000000000000426 ) ) ;
#22466=VECTOR ( 'NONE', #196610, 1000.000000000000000 ) ;
#22472=EDGE_LOOP ( 'NONE', ( #237729, #178792 ) ) ;
#22489=ORIENTED_EDGE ( 'NONE', *, *, #228719, .T. ) ;
#22498=DIRECTION ( 'NONE',  ( 0.000000000000000000, -1.000000000000000000, 0.000000000000000000 ) ) ;
#22506=TOROIDAL_SURFACE ( 'NONE', #247320, 1.900000000000002576, 0.1000000000000000056 ) ;
#22540=CARTESIAN_POINT ( 'NONE',  ( 21.05000000000000071, 1.115600667400684642E-11, -97.60000000000005116 ) ) ;
#22549=CIRCLE ( 'NONE', #93435, 0.1000000000000028644 ) ;
#22580=ORIENTED_EDGE ( 'NONE', *, *, #188559, .T. ) ;
#22592=CIRCLE ( 'NONE', #168374, 0.1000000000000028644 ) ;
#22612=CIRCLE ( 'NONE', #251534, 0.1000000000000028644 ) ;
#22635=DIRECTION ( 'NONE',  ( 0.000000000000000000, 0.000000000000000000, -1.000000000000000000 ) ) ;
#22642=ORIENTED_EDGE ( 'NONE', *, *, #117083, .T. ) ;
#22643=VECTOR ( 'NONE', #99135, 999.9999999999998863 ) ;
#22666=FACE_OUTER_BOUND ( 'NONE', #151256, .T. ) ;
#22695=EDGE_CURVE ( 'NONE', #4930, #205409, #71765, .T. ) ;
#22702=CARTESIAN_POINT ( 'NONE',  ( 18.59999999999999076, 7.120270961708750512, -104.1595630418393768 ) ) ;
#22705=EDGE_CURVE ( 'NONE', #151216, #91092, #187093, .T. ) ;
#22719=CYLINDRICAL_SURFACE ( 'NONE', #15271, 0.5000000000000004441 ) ;
#22730=CARTESIAN_POINT ( 'NONE',  ( -21.05000000000000071, -9.519327731081284938, -73.97297637655937308 ) ) ;
#22735=ADVANCED_FACE ( 'NONE', ( #92343 ), #182827, .F. ) ;
#22751=FACE_OUTER_BOUND ( 'NONE', #231729, .T. ) ;
#22766=EDGE_CURVE ( 'NONE', #39792, #134077, #170367, .T. ) ;
#22781=TOROIDAL_SURFACE ( 'NONE', #43420, 4.099999999999999645, 0.1000000000000000056 ) ;
#22803=CARTESIAN_POINT ( 'NONE',  ( -18.59999999999999787, -1.835341550213255957, -78.55515129256302487 ) ) ;
#22809=DIRECTION ( 'NONE',  ( 1.000000000000000000, 0.000000000000000000, 0.000000000000000000 ) ) ;
#22817=DIRECTION ( 'NONE',  ( 1.000000000000000000, 1.836970198721029934E-16, 0.000000000000000000 ) ) ;
#22818=EDGE_CURVE ( 'NONE', #175744, #238381, #236964, .T. ) ;
#22834=ORIENTED_EDGE ( 'NONE', *, *, #126242, .T. ) ;
#22847=CARTESIAN_POINT ( 'NONE',  ( 22.50497660315937409, -0.07871793021434789206, -55.25020449510461162 ) ) ;
#22919=DIRECTION ( 'NONE',  ( 0.000000000000000000, 0.000000000000000000, -1.000000000000000000 ) ) ;
#22936=ORIENTED_EDGE ( 'NONE', *, *, #237325, .T. ) ;
#22968=VERTEX_POINT ( 'NONE', #196573 ) ;
#22990=EDGE_CURVE ( 'NONE', #142483, #83831, #37523, .T. ) ;
#23003=ORIENTED_EDGE ( 'NONE', *, *, #243872, .T. ) ;
#23004=CARTESIAN_POINT ( 'NONE',  ( 18.52928932188133970, 10.27928932189250411, -91.65000000000004832 ) ) ;
#23007=AXIS2_PLACEMENT_3D ( 'NONE', #135080, #229082, #251178 ) ;
#23022=DIRECTION ( 'NONE',  ( 2.952720810173289112E-16, -1.000000000000000000, 0.000000000000000000 ) ) ;
#23041=EDGE_LOOP ( 'NONE', ( #211208, #133668, #95370, #39099 ) ) ;
#23057=EDGE_CURVE ( 'NONE', #189831, #140297, #29080, .T. ) ;
#23084=ORIENTED_EDGE ( 'NONE', *, *, #14254, .T. ) ;
#23093=ORIENTED_EDGE ( 'NONE', *, *, #165346, .T. ) ;
#23121=ADVANCED_FACE ( 'NONE', ( #124754 ), #90097, .F. ) ;
#23167=ORIENTED_EDGE ( 'NONE', *, *, #92751, .T. ) ;
#23179=ORIENTED_EDGE ( 'NONE', *, *, #245256, .T. ) ;
#23220=EDGE_CURVE ( 'NONE', #71443, #248210, #124722, .T. ) ;
#23221=EDGE_CURVE ( 'NONE', #150237, #56745, #208156, .T. ) ;
#23238=VECTOR ( 'NONE', #96845, 1000.000000000000227 ) ;
#23243=VERTEX_POINT ( 'NONE', #232855 ) ;
#23283=ORIENTED_EDGE ( 'NONE', *, *, #250888, .T. ) ;
#23291=CARTESIAN_POINT ( 'NONE',  ( -21.12642695952773764, 6.375659922046319927, -66.90109671681068448 ) ) ;
#23319=DIRECTION ( 'NONE',  ( 0.000000000000000000, -0.9915357197604792727, 0.1298341882520475943 ) ) ;
#23332=DIRECTION ( 'NONE',  ( -0.000000000000000000, 1.000000000000000000, -0.000000000000000000 ) ) ;
#23342=CARTESIAN_POINT ( 'NONE',  ( -22.50000000000000000, 11.64987090377452184, -66.91748010912704103 ) ) ;
#23361=LINE ( 'NONE', #117297, #212679 ) ;
#23377=EDGE_CURVE ( 'NONE', #80091, #77103, #157177, .T. ) ;
#23412=ORIENTED_EDGE ( 'NONE', *, *, #121748, .F. ) ;
#23415=CARTESIAN_POINT ( 'NONE',  ( 21.05000000000000071, 10.47338541492405639, -74.57865446424858646 ) ) ;
#23452=CARTESIAN_POINT ( 'NONE',  ( -23.15000000000000213, 4.150000000011156764, -88.15000000000004832 ) ) ;
#23496=ORIENTED_EDGE ( 'NONE', *, *, #121789, .F. ) ;
#23512=SPHERICAL_SURFACE ( 'NONE', #89243, 0.1000000000000000056 ) ;
#23517=EDGE_LOOP ( 'NONE', ( #115143, #118785, #241302, #113242 ) ) ;
#23605=CIRCLE ( 'NONE', #65254, 0.09999999999999892308 ) ;
#23606=DIRECTION ( 'NONE',  ( 1.000000000000000000, -0.000000000000000000, -0.000000000000000000 ) ) ;
#23619=TOROIDAL_SURFACE ( 'NONE', #219383, 4.099999999999999645, 0.1000000000000000056 ) ;
#23621=DIRECTION ( 'NONE',  ( 1.000000000000000000, -0.000000000000000000, 0.000000000000000000 ) ) ;
#23625=ADVANCED_FACE ( 'NONE', ( #135657 ), #129189, .T. ) ;
#23631=LINE ( 'NONE', #86097, #73773 ) ;
#23647=CARTESIAN_POINT ( 'NONE',  ( -18.59999999999999787, -1.164121893230052995, -108.3148480855716542 ) ) ;
#23652=CARTESIAN_POINT ( 'NONE',  ( -23.25000000000000000, 4.350000000011156054, -79.15000000000004832 ) ) ;
#23670=CARTESIAN_POINT ( 'NONE',  ( -21.04999999999999716, 0.05132743235275089716, -60.69981666373099216 ) ) ;
#23696=ADVANCED_FACE ( 'NONE', ( #2566 ), #234777, .T. ) ;
#23734=CARTESIAN_POINT ( 'NONE',  ( 18.47688499308726406, -9.464855950272974994, -107.2013477531374406 ) ) ;
#23745=CARTESIAN_POINT ( 'NONE',  ( -23.25000000000000000, -0.09999999998884338825, -55.35042919245524473 ) ) ;
#23792=DIRECTION ( 'NONE',  ( -1.000000000000000000, -7.304098846218134667E-16, 0.000000000000000000 ) ) ;
#23828=CARTESIAN_POINT ( 'NONE',  ( -18.59999999999999787, -9.399999999988787991, -74.29725975966333351 ) ) ;
#23868=VERTEX_POINT ( 'NONE', #150383 ) ;
#23883=ORIENTED_EDGE ( 'NONE', *, *, #6983, .T. ) ;
#23884=CIRCLE ( 'NONE', #57143, 0.09999999999999939493 ) ;
#23959=DIRECTION ( 'NONE',  ( 1.000000000000000000, 2.952720810173289112E-16, -0.000000000000000000 ) ) ;
#23978=ORIENTED_EDGE ( 'NONE', *, *, #158782, .F. ) ;
#23989=CARTESIAN_POINT ( 'NONE',  ( -23.25000000000000000, 11.65000000001115588, -55.25000000000004974 ) ) ;
#23998=CARTESIAN_POINT ( 'NONE',  ( 21.05000000000000071, -11.39257802169451139, -97.42605042016811012 ) ) ;
#24008=ORIENTED_EDGE ( 'NONE', *, *, #151227, .T. ) ;
#24010=CARTESIAN_POINT ( 'NONE',  ( 21.04999999999999716, 6.300183336278585955, -66.94867256765833474 ) ) ;
#24014=EDGE_LOOP ( 'NONE', ( #29055, #86739, #158169, #6802 ) ) ;
#24050=EDGE_CURVE ( 'NONE', #144670, #11990, #64201, .T. ) ;
#24055=EDGE_CURVE ( 'NONE', #190429, #27504, #65471, .T. ) ;
#24059=CIRCLE ( 'NONE', #98823, 0.09999999999999939493 ) ;
#24078=ORIENTED_EDGE ( 'NONE', *, *, #185552, .F. ) ;
#24085=ORIENTED_EDGE ( 'NONE', *, *, #144499, .F. ) ;
#24097=ORIENTED_EDGE ( 'NONE', *, *, #167061, .F. ) ;
#24104=CYLINDRICAL_SURFACE ( 'NONE', #175728, 0.09999999999999939493 ) ;
#24119=DIRECTION ( 'NONE',  ( 0.000000000000000000, 0.000000000000000000, 1.000000000000000000 ) ) ;
#24185=CARTESIAN_POINT ( 'NONE',  ( -21.14999999999999858, -0.09999999998884338825, -55.35042919245524473 ) ) ;
#24196=EDGE_CURVE ( 'NONE', #214744, #161687, #187833, .T. ) ;
#24224=DIRECTION ( 'NONE',  ( 0.000000000000000000, -8.881784197001832136E-16, -1.000000000000000000 ) ) ;
#24232=CYLINDRICAL_SURFACE ( 'NONE', #231162, 0.09999999999999954758 ) ;
#24247=CYLINDRICAL_SURFACE ( 'NONE', #201012, 0.1000000000000028644 ) ;
#24250=CARTESIAN_POINT ( 'NONE',  ( -23.15000000000000213, 4.250000000011156409, -79.35000000000005116 ) ) ;
#24269=DIRECTION ( 'NONE',  ( -0.000000000000000000, -0.000000000000000000, 1.000000000000000000 ) ) ;
#24273=ORIENTED_EDGE ( 'NONE', *, *, #56675, .F. ) ;
#24289=ORIENTED_EDGE ( 'NONE', *, *, #210086, .F. ) ;
#24300=DIRECTION ( 'NONE',  ( 1.000000000000000000, 0.000000000000000000, -0.000000000000000000 ) ) ;
#24316=EDGE_LOOP ( 'NONE', ( #9412, #192261, #31789, #5166 ) ) ;
#24320=CARTESIAN_POINT ( 'NONE',  ( 21.07016717456946253, 6.320940838111409832, -67.00000000000004263 ) ) ;
#24380=CARTESIAN_POINT ( 'NONE',  ( -22.50000000000000000, 1.115600667400684642E-11, -67.00000000000004263 ) ) ;
#24401=CARTESIAN_POINT ( 'NONE',  ( -22.50000000000000000, 0.1000000000111554016, -55.35042919245524473 ) ) ;
#24409=FACE_OUTER_BOUND ( 'NONE', #154435, .T. ) ;
#24433=ORIENTED_EDGE ( 'NONE', *, *, #31493, .F. ) ;
#24436=DIRECTION ( 'NONE',  ( 0.000000000000000000, 1.000000000000000000, 0.000000000000000000 ) ) ;
#24440=DIRECTION ( 'NONE',  ( 1.000000000000000000, 2.952720810173289112E-16, -0.000000000000000000 ) ) ;
#24463=CARTESIAN_POINT ( 'NONE',  ( 19.97071067811864609, 11.72071067812981404, -88.35000000000003695 ) ) ;
#24482=ORIENTED_EDGE ( 'NONE', *, *, #194135, .F. ) ;
#24491=ORIENTED_EDGE ( 'NONE', *, *, #89995, .F. ) ;
#24503=PLANE ( 'NONE',  #106695 ) ;
#24516=CARTESIAN_POINT ( 'NONE',  ( -23.15000000000000213, 1.115600667400684642E-11, -67.00000000000004263 ) ) ;
#24536=CARTESIAN_POINT ( 'NONE',  ( 23.15000000000000213, -8.663551401858002876, -76.52410111806734960 ) ) ;
#24598=CARTESIAN_POINT ( 'NONE',  ( 22.49999999999999645, 0.08880997639808872746, -55.35023708196812464 ) ) ;
#24603=AXIS2_PLACEMENT_3D ( 'NONE', #130207, #209768, #32447 ) ;
#24624=VERTEX_POINT ( 'NONE', #212404 ) ;
#24643=EDGE_CURVE ( 'NONE', #224755, #102331, #175541, .T. ) ;
#24647=CARTESIAN_POINT ( 'NONE',  ( 21.93642651522410603, 7.327166239336949438, -67.00000000000004263 ) ) ;
#24665=VERTEX_POINT ( 'NONE', #214951 ) ;
#24677=ORIENTED_EDGE ( 'NONE', *, *, #33221, .T. ) ;
#24695=CARTESIAN_POINT ( 'NONE',  ( 21.05000000000000071, 10.72371681401022592, -74.59439923588408305 ) ) ;
#24712=ORIENTED_EDGE ( 'NONE', *, *, #177706, .F. ) ;
#24749=CARTESIAN_POINT ( 'NONE',  ( -20.54999999999999716, 2.400000000011155432, -87.27537807723794572 ) ) ;
#24774=EDGE_CURVE ( 'NONE', #47997, #124622, #185945, .T. ) ;
#24793=DIRECTION ( 'NONE',  ( -1.000000000000000000, 0.000000000000000000, 0.000000000000000000 ) ) ;
#24808=DIRECTION ( 'NONE',  ( 0.000000000000000000, -0.1298341882520022694, -0.9915357197604853789 ) ) ;
#24809=VECTOR ( 'NONE', #17193, 1000.000000000000000 ) ;
#24830=EDGE_CURVE ( 'NONE', #51736, #176751, #244750, .T. ) ;
#24853=AXIS2_PLACEMENT_3D ( 'NONE', #98272, #218236, #80001 ) ;
#24856=ORIENTED_EDGE ( 'NONE', *, *, #110927, .T. ) ;
#24864=VERTEX_POINT ( 'NONE', #210788 ) ;
#24879=FACE_OUTER_BOUND ( 'NONE', #2685, .T. ) ;
#24885=EDGE_LOOP ( 'NONE', ( #94883, #113306, #39417, #158944 ) ) ;
#24899=VERTEX_POINT ( 'NONE', #46561 ) ;
#24922=EDGE_CURVE ( 'NONE', #187354, #206992, #22156, .T. ) ;
#24923=CARTESIAN_POINT ( 'NONE',  ( -20.94403535211772294, 10.30632246271647467, -106.0041836778896283 ) ) ;
#24943=VERTEX_POINT ( 'NONE', #127408 ) ;
#24946=CARTESIAN_POINT ( 'NONE',  ( -21.05000000000000071, -0.02110330804785563383, -60.69548367073601725 ) ) ;
#24989=EDGE_CURVE ( 'NONE', #150875, #150463, #126366, .T. ) ;
#24995=ORIENTED_EDGE ( 'NONE', *, *, #33509, .T. ) ;
#25039=EDGE_CURVE ( 'NONE', #94857, #238735, #51318, .T. ) ;
#25056=LINE ( 'NONE', #62868, #86777 ) ;
#25072=ADVANCED_FACE ( 'NONE', ( #218465 ), #159814, .T. ) ;
#25092=CARTESIAN_POINT ( 'NONE',  ( -20.64999999999999858, -8.999999999988846255, -76.39396912265249284 ) ) ;
#25104=CARTESIAN_POINT ( 'NONE',  ( 20.94999999999999574, -11.41227409413852989, -69.90000000000004832 ) ) ;
#25108=CARTESIAN_POINT ( 'NONE',  ( -18.59999999999999787, 1.115600667400684642E-11, -67.00000000000004263 ) ) ;
#25121=DIRECTION ( 'NONE',  ( 1.000000000000000000, 0.000000000000000000, -0.000000000000000000 ) ) ;
#25130=AXIS2_PLACEMENT_3D ( 'NONE', #141355, #4402, #163491 ) ;
#25174=ORIENTED_EDGE ( 'NONE', *, *, #229030, .T. ) ;
#25225=CARTESIAN_POINT ( 'NONE',  ( 22.39999999999999503, 1.115600667400684642E-11, -59.25000000000003553 ) ) ;
#25240=CIRCLE ( 'NONE', #225106, 1.899999999999999023 ) ;
#25244=AXIS2_PLACEMENT_3D ( 'NONE', #41000, #141351, #241735 ) ;
#25246=B_SPLINE_CURVE_WITH_KNOTS ( 'NONE', 3,
 ( #156723, #237519, #138381, #193257, #212821, #217919, #14633, #92851 ),
 .UNSPECIFIED., .F., .F.,
 ( 4, 2, 2, 4 ),
 ( 0.000000000000000000, 0.0002114466876442108679, 0.0003171700314663126563, 0.0004228933752884144175 ),
 .UNSPECIFIED. ) ;
#25269=CARTESIAN_POINT ( 'NONE',  ( -22.50000000000000000, 1.115600667400684642E-11, -60.75000000000004974 ) ) ;
#25289=DIRECTION ( 'NONE',  ( -1.000000000000000000, 0.000000000000000000, 0.000000000000000000 ) ) ;
#25291=AXIS2_PLACEMENT_3D ( 'NONE', #114408, #192669, #193955 ) ;
#25309=EDGE_CURVE ( 'NONE', #193140, #68295, #134720, .T. ) ;
#25317=FACE_OUTER_BOUND ( 'NONE', #191524, .T. ) ;
#25341=DIRECTION ( 'NONE',  ( 1.000000000000000000, -0.000000000000000000, -0.000000000000000000 ) ) ;
#25359=FACE_OUTER_BOUND ( 'NONE', #234333, .T. ) ;
#25365=EDGE_CURVE ( 'NONE', #10892, #77390, #205638, .T. ) ;
#25367=DIRECTION ( 'NONE',  ( 0.000000000000000000, 0.000000000000000000, 1.000000000000000000 ) ) ;
#25376=AXIS2_PLACEMENT_3D ( 'NONE', #33192, #31892, #9719 ) ;
#25389=CIRCLE ( 'NONE', #112861, 0.1000000000000028644 ) ;
#25461=DIRECTION ( 'NONE',  ( 0.000000000000000000, -1.000000000000000000, 0.000000000000000000 ) ) ;
#25478=ORIENTED_EDGE ( 'NONE', *, *, #79344, .T. ) ;
#25488=CARTESIAN_POINT ( 'NONE',  ( -21.13614978966382196, 6.499104701844945708, -67.00000000000004263 ) ) ;
#25505=EDGE_CURVE ( 'NONE', #240643, #61134, #68300, .T. ) ;
#25527=DIRECTION ( 'NONE',  ( 0.000000000000000000, 0.9915357197604792727, -0.1298341882520475943 ) ) ;
#25558=ADVANCED_FACE ( 'NONE', ( #172951 ), #153369, .F. ) ;
#25581=CARTESIAN_POINT ( 'NONE',  ( 20.95561247346651967, 10.59500736521470721, -74.59378276698168975 ) ) ;
#25644=EDGE_CURVE ( 'NONE', #237434, #173330, #176778, .T. ) ;
#25652=CARTESIAN_POINT ( 'NONE',  ( -21.07016717456946608, 6.320940838111406279, -67.00000000000004263 ) ) ;
#25657=ADVANCED_FACE ( 'NONE', ( #82639 ), #63444, .T. ) ;
#25665=DIRECTION ( 'NONE',  ( 0.000000000000000000, -1.000000000000000000, 0.000000000000000000 ) ) ;
#25666=ADVANCED_FACE ( 'NONE', ( #124383 ), #13736, .F. ) ;
#25679=VECTOR ( 'NONE', #47756, 999.9999999999998863 ) ;
#25700=DIRECTION ( 'NONE',  ( 0.000000000000000000, -1.000000000000000000, 0.000000000000000000 ) ) ;
#25710=EDGE_LOOP ( 'NONE', ( #239487, #229734, #102080 ) ) ;
#25712=CARTESIAN_POINT ( 'NONE',  ( -20.15000000000000568, 9.291421356248463326, -88.25000000000005684 ) ) ;
#25720=DIRECTION ( 'NONE',  ( 1.000000000000000000, 0.000000000000000000, 0.000000000000000000 ) ) ;
#25741=ORIENTED_EDGE ( 'NONE', *, *, #137292, .T. ) ;
#25772=EDGE_CURVE ( 'NONE', #192398, #8323, #245609, .T. ) ;
#25777=FACE_OUTER_BOUND ( 'NONE', #154684, .T. ) ;
#25785=ORIENTED_EDGE ( 'NONE', *, *, #251746, .T. ) ;
#25817=ADVANCED_FACE ( 'NONE', ( #246876 ), #255286, .F. ) ;
#25822=DIRECTION ( 'NONE',  ( 0.000000000000000000, 0.000000000000000000, 1.000000000000000000 ) ) ;
#25833=DIRECTION ( 'NONE',  ( 7.304098846218134667E-16, -1.000000000000000000, 0.000000000000000000 ) ) ;
#25866=TOROIDAL_SURFACE ( 'NONE', #59123, 0.2000000000000000111, 0.1000000000000000056 ) ;
#25895=ORIENTED_EDGE ( 'NONE', *, *, #201300, .F. ) ;
#25906=CYLINDRICAL_SURFACE ( 'NONE', #202998, 0.1000000000000028644 ) ;
#25921=ADVANCED_FACE ( 'NONE', ( #212901 ), #22143, .T. ) ;
#25923=EDGE_CURVE ( 'NONE', #133253, #219149, #1250, .T. ) ;
#25937=EDGE_LOOP ( 'NONE', ( #207143, #140432, #202548, #152228 ) ) ;
#25943=DIRECTION ( 'NONE',  ( -1.000000000000000000, -0.000000000000000000, -0.000000000000000000 ) ) ;
#25945=EDGE_LOOP ( 'NONE', ( #53007, #211515, #94727, #39584 ) ) ;
#25974=DIRECTION ( 'NONE',  ( 0.000000000000000000, 0.000000000000000000, 1.000000000000000000 ) ) ;
#25992=DIRECTION ( 'NONE',  ( 0.000000000000000000, 0.000000000000000000, 1.000000000000000000 ) ) ;
#25998=AXIS2_PLACEMENT_3D ( 'NONE', #100808, #20052, #81265 ) ;
#26005=DIRECTION ( 'NONE',  ( 0.000000000000000000, 0.000000000000000000, -1.000000000000000000 ) ) ;
#26041=ORIENTED_EDGE ( 'NONE', *, *, #231747, .F. ) ;
#26043=AXIS2_PLACEMENT_3D ( 'NONE', #145047, #159502, #99482 ) ;
#26056=CARTESIAN_POINT ( 'NONE',  ( -23.25000000000000000, 1.115600667400684642E-11, -67.00000000000004263 ) ) ;
#26075=CARTESIAN_POINT ( 'NONE',  ( -21.05000000000000071, -11.48912529306489994, -97.40000000000004832 ) ) ;
#26111=CARTESIAN_POINT ( 'NONE',  ( -18.36527282682037310, -9.500000599987968641, -107.4221489644983905 ) ) ;
#26112=CIRCLE ( 'NONE', #151190, 0.1000000000000000472 ) ;
#26114=DIRECTION ( 'NONE',  ( 0.000000000000000000, 0.000000000000000000, -1.000000000000000000 ) ) ;
#26131=CIRCLE ( 'NONE', #213549, 12.97499999999999964 ) ;
#26155=AXIS2_PLACEMENT_3D ( 'NONE', #76258, #193659, #15036 ) ;
#26176=FACE_OUTER_BOUND ( 'NONE', #136874, .T. ) ;
#26204=ORIENTED_EDGE ( 'NONE', *, *, #104628, .F. ) ;
#26207=CARTESIAN_POINT ( 'NONE',  ( 20.94999999999999574, 1.115600667400684642E-11, -67.00000000000004263 ) ) ;
#26220=CARTESIAN_POINT ( 'NONE',  ( 21.05000000000000071, 6.650000000011155876, -77.01702717044007329 ) ) ;
#26226=VECTOR ( 'NONE', #87955, 1000.000000000000000 ) ;
#26273=CARTESIAN_POINT ( 'NONE',  ( 20.94999999999999929, -9.499999999988844479, -90.60603087734760663 ) ) ;
#26282=CARTESIAN_POINT ( 'NONE',  ( -22.57320508075687115, 11.75000000001115552, -67.00000000000004263 ) ) ;
#26313=CIRCLE ( 'NONE', #59583, 3.899999999999999467 ) ;
#26328=CARTESIAN_POINT ( 'NONE',  ( -20.85000000000000142, 11.75000000001115552, -100.5000000000000426 ) ) ;
#26336=ORIENTED_EDGE ( 'NONE', *, *, #237175, .F. ) ;
#26378=VERTEX_POINT ( 'NONE', #225078 ) ;
#26417=CARTESIAN_POINT ( 'NONE',  ( -21.00448002041592943, 11.75000000001115552, -73.84834086231086303 ) ) ;
#26476=CARTESIAN_POINT ( 'NONE',  ( -21.05000000000000426, -0.09999999998884340213, -60.52293297887530343 ) ) ;
#26487=AXIS2_PLACEMENT_3D ( 'NONE', #42762, #141851, #102704 ) ;
#26503=EDGE_LOOP ( 'NONE', ( #117513, #185381, #61329, #222043 ) ) ;
#26549=DIRECTION ( 'NONE',  ( 0.000000000000000000, 0.008583690987124697677, -0.9999631594459055250 ) ) ;
#26565=CARTESIAN_POINT ( 'NONE',  ( 22.50000000000000000, 0.1000000000111554016, -55.25000000000004974 ) ) ;
#26581=ORIENTED_EDGE ( 'NONE', *, *, #196586, .F. ) ;
#26594=CIRCLE ( 'NONE', #97259, 0.2000000000000057288 ) ;
#26649=DIRECTION ( 'NONE',  ( 0.000000000000000000, 0.000000000000000000, 1.000000000000000000 ) ) ;
#26657=DIRECTION ( 'NONE',  ( 0.000000000000000000, -1.000000000000000000, 0.000000000000000000 ) ) ;
#26661=AXIS2_PLACEMENT_3D ( 'NONE', #250371, #146127, #144832 ) ;
#26682=ORIENTED_EDGE ( 'NONE', *, *, #196042, .F. ) ;
#26687=DIRECTION ( 'NONE',  ( -1.000000000000000000, -0.000000000000000000, 0.000000000000000000 ) ) ;
#26691=ADVANCED_FACE ( 'NONE', ( #180547 ), #222202, .T. ) ;
#26718=CARTESIAN_POINT ( 'NONE',  ( -21.04999999999999716, 6.497017786443340270, -67.01454569057010247 ) ) ;
#26743=AXIS2_PLACEMENT_3D ( 'NONE', #54164, #172888, #112867 ) ;
#26754=AXIS2_PLACEMENT_3D ( 'NONE', #137753, #156090, #159928 ) ;
#26767=CARTESIAN_POINT ( 'NONE',  ( -22.50000000000000000, 11.75000000001115552, -67.00000000000004263 ) ) ;
#26769=ORIENTED_EDGE ( 'NONE', *, *, #202223, .F. ) ;
#26799=CARTESIAN_POINT ( 'NONE',  ( 23.24999999999999289, 11.65000000001116298, -93.48519422934610645 ) ) ;
#26834=DIRECTION ( 'NONE',  ( 1.000000000000000000, 2.952720810173289112E-16, -0.000000000000000000 ) ) ;
#26848=EDGE_LOOP ( 'NONE', ( #53504, #108058, #104179, #253478 ) ) ;
#26876=ORIENTED_EDGE ( 'NONE', *, *, #77921, .T. ) ;
#26877=CARTESIAN_POINT ( 'NONE',  ( -18.59999999999999787, -1.835859311432481045, -112.1044391687985780 ) ) ;
#26881=CARTESIAN_POINT ( 'NONE',  ( 20.95512820512820440, 10.62384868372303615, -74.66491356908764487 ) ) ;
#26888=CYLINDRICAL_SURFACE ( 'NONE', #257530, 0.1000000000000028644 ) ;
#26895=DIRECTION ( 'NONE',  ( 0.000000000000000000, 0.1568667991644863147, -0.9876197685951252359 ) ) ;
#26922=ORIENTED_EDGE ( 'NONE', *, *, #128599, .F. ) ;
#26965=DIRECTION ( 'NONE',  ( 0.000000000000000000, 0.000000000000000000, -1.000000000000000000 ) ) ;
#26998=CARTESIAN_POINT ( 'NONE',  ( -18.59999999999999787, 11.65000000001115232, -88.35000000000003695 ) ) ;
#27039=EDGE_CURVE ( 'NONE', #236288, #13140, #1797, .T. ) ;
#27043=DIRECTION ( 'NONE',  ( 0.000000000000000000, -0.000000000000000000, 1.000000000000000000 ) ) ;
#27053=DIRECTION ( 'NONE',  ( 0.000000000000000000, 8.881784197000696176E-16, -1.000000000000000000 ) ) ;
#27070=EDGE_LOOP ( 'NONE', ( #9176, #229075, #195769, #120195 ) ) ;
#27072=VERTEX_POINT ( 'NONE', #55117 ) ;
#27101=ORIENTED_EDGE ( 'NONE', *, *, #235263, .T. ) ;
#27137=FACE_OUTER_BOUND ( 'NONE', #37114, .T. ) ;
#27165=ORIENTED_EDGE ( 'NONE', *, *, #254563, .F. ) ;
#27209=ORIENTED_EDGE ( 'NONE', *, *, #3250, .F. ) ;
#27210=CARTESIAN_POINT ( 'NONE',  ( -20.94999999999999929, -11.64999999998884483, -97.50000000000004263 ) ) ;
#27226=VECTOR ( 'NONE', #184322, 1000.000000000000000 ) ;
#27233=DIRECTION ( 'NONE',  ( -3.265361837132813093E-16, 1.000000000000000000, 0.000000000000000000 ) ) ;
#27259=VECTOR ( 'NONE', #23792, 1000.000000000000000 ) ;
#27274=CIRCLE ( 'NONE', #106312, 0.2000000000000057288 ) ;
#27323=LINE ( 'NONE', #162961, #91561 ) ;
#27332=ORIENTED_EDGE ( 'NONE', *, *, #42473, .T. ) ;
#27341=CARTESIAN_POINT ( 'NONE',  ( 23.14999999999999858, 1.115600667400684642E-11, -100.5000000000000426 ) ) ;
#27370=DIRECTION ( 'NONE',  ( 1.000000000000000000, 0.000000000000000000, 0.000000000000000000 ) ) ;
#27389=CARTESIAN_POINT ( 'NONE',  ( 20.94999999999999574, 11.75000000001115552, -93.71613433702195550 ) ) ;
#27405=CARTESIAN_POINT ( 'NONE',  ( -18.59999999999999787, 5.950000000011100632, -77.30570230503489881 ) ) ;
#27410=CIRCLE ( 'NONE', #43933, 0.1000000000000028644 ) ;
#27423=CARTESIAN_POINT ( 'NONE',  ( -18.43459694179558639, -9.494210124986880217, -107.1170052026610051 ) ) ;
#27434=ORIENTED_EDGE ( 'NONE', *, *, #34328, .T. ) ;
#27463=ORIENTED_EDGE ( 'NONE', *, *, #110077, .F. ) ;
#27477=EDGE_LOOP ( 'NONE', ( #95132, #244587, #150772, #49746 ) ) ;
#27487=DIRECTION ( 'NONE',  ( 0.000000000000000000, 0.9654727137038715545, 0.2605042016806676242 ) ) ;
#27493=FACE_OUTER_BOUND ( 'NONE', #119415, .T. ) ;
#27503=TOROIDAL_SURFACE ( 'NONE', #156666, 2.100000000000002309, 0.1000000000000000056 ) ;
#27504=VERTEX_POINT ( 'NONE', #112895 ) ;
#27530=EDGE_LOOP ( 'NONE', ( #119336, #179787, #255377 ) ) ;
#27532=DIRECTION ( 'NONE',  ( 0.000000000000000000, 0.000000000000000000, -1.000000000000000000 ) ) ;
#27550=VECTOR ( 'NONE', #64053, 1000.000000000000000 ) ;
#27564=EDGE_CURVE ( 'NONE', #11990, #219131, #235226, .T. ) ;
#27590=DIRECTION ( 'NONE',  ( 0.000000000000000000, -1.000000000000000000, 0.000000000000000000 ) ) ;
#27595=CARTESIAN_POINT ( 'NONE',  ( 21.14999999999999858, 11.65000000001116298, -79.25000000000004263 ) ) ;
#27629=PLANE ( 'NONE',  #62341 ) ;
#27672=AXIS2_PLACEMENT_3D ( 'NONE', #172682, #73565, #14865 ) ;
#27675=LINE ( 'NONE', #186722, #109907 ) ;
#27712=EDGE_CURVE ( 'NONE', #95067, #22968, #93753, .T. ) ;
#27713=AXIS2_PLACEMENT_3D ( 'NONE', #96543, #176132, #97819 ) ;
#27733=CARTESIAN_POINT ( 'NONE',  ( -18.50000000000000000, 6.846123162363745074, -104.2377262668499043 ) ) ;
#27764=ORIENTED_EDGE ( 'NONE', *, *, #9405, .F. ) ;
#27800=AXIS2_PLACEMENT_3D ( 'NONE', #167500, #87907, #84029 ) ;
#27820=CARTESIAN_POINT ( 'NONE',  ( -18.59999999999999787, 7.021664781911246322, -104.2335654018973372 ) ) ;
#27823=DIRECTION ( 'NONE',  ( -2.915501640297153790E-16, 1.000000000000000000, 0.000000000000000000 ) ) ;
#27838=PLANE ( 'NONE',  #94404 ) ;
#27854=DIRECTION ( 'NONE',  ( -1.000000000000000000, -0.000000000000000000, -0.000000000000000000 ) ) ;
#27877=EDGE_CURVE ( 'NONE', #189461, #88741, #256184, .T. ) ;
#27880=ADVANCED_FACE ( 'NONE', ( #226087 ), #127021, .T. ) ;
#27893=DIRECTION ( 'NONE',  ( 1.000000000000000000, 0.000000000000000000, 0.000000000000000000 ) ) ;
#27905=CARTESIAN_POINT ( 'NONE',  ( 21.13461538461538325, 10.61458296203669249, -79.35000000000005116 ) ) ;
#27919=DIRECTION ( 'NONE',  ( 0.000000000000000000, 0.000000000000000000, -1.000000000000000000 ) ) ;
#27932=CARTESIAN_POINT ( 'NONE',  ( 20.94999999999999929, -11.64999999998883595, -100.5000000000000426 ) ) ;
#27942=DIRECTION ( 'NONE',  ( 0.000000000000000000, 0.000000000000000000, -1.000000000000000000 ) ) ;
#27949=ORIENTED_EDGE ( 'NONE', *, *, #29199, .F. ) ;
#27984=DIRECTION ( 'NONE',  ( 0.000000000000000000, 1.000000000000000000, 0.000000000000000000 ) ) ;
#27988=EDGE_CURVE ( 'NONE', #104152, #163525, #172618, .T. ) ;
#27993=DIRECTION ( 'NONE',  ( -0.000000000000000000, 1.000000000000000000, 0.000000000000000000 ) ) ;
#28046=CARTESIAN_POINT ( 'NONE',  ( 18.59117750673696179, 10.33248238083634796, -106.0948465439131922 ) ) ;
#28057=DIRECTION ( 'NONE',  ( 0.000000000000000000, -1.000000000000000000, -0.000000000000000000 ) ) ;
#28079=DIRECTION ( 'NONE',  ( -0.7071067811865475727, -0.7071067811865475727, 0.000000000000000000 ) ) ;
#28080=DIRECTION ( 'NONE',  ( 1.000000000000000000, 0.000000000000000000, 0.000000000000000000 ) ) ;
#28088=CARTESIAN_POINT ( 'NONE',  ( 20.94999999999999929, 1.115600667400684642E-11, -67.00000000000004263 ) ) ;
#28125=LINE ( 'NONE', #64651, #63647 ) ;
#28163=CARTESIAN_POINT ( 'NONE',  ( 20.53930447207976684, 8.977148687535432714, -75.44250714157833215 ) ) ;
#28184=CARTESIAN_POINT ( 'NONE',  ( 21.30000000000002558, 1.115650265596050101E-11, -62.95000000000004547 ) ) ;
#28189=EDGE_CURVE ( 'NONE', #110538, #183134, #177373, .T. ) ;
#28200=DIRECTION ( 'NONE',  ( 1.000000000000000000, 0.000000000000000000, 0.000000000000000000 ) ) ;
#28241=LINE ( 'NONE', #128596, #37034 ) ;
#28250=ADVANCED_FACE ( 'NONE', ( #224522 ), #127265, .T. ) ;
#28251=CARTESIAN_POINT ( 'NONE',  ( -21.05000000000000071, 1.115600667400684642E-11, -67.00000000000004263 ) ) ;
#28260=EDGE_CURVE ( 'NONE', #242599, #6865, #66745, .T. ) ;
#28267=DIRECTION ( 'NONE',  ( 1.000000000000000000, 6.938893903907222067E-15, 0.000000000000000000 ) ) ;
#28268=DIRECTION ( 'NONE',  ( 1.000000000000000000, -0.000000000000000000, -0.000000000000000000 ) ) ;
#28288=EDGE_CURVE ( 'NONE', #71547, #224195, #206559, .T. ) ;
#28296=CARTESIAN_POINT ( 'NONE',  ( -20.64999999999999858, 1.115600667400684642E-11, -67.00000000000004263 ) ) ;
#28304=DIRECTION ( 'NONE',  ( 0.000000000000000000, 0.000000000000000000, -1.000000000000000000 ) ) ;
#28308=DIRECTION ( 'NONE',  ( -0.000000000000000000, -1.000000000000000000, -1.734723475976807292E-15 ) ) ;
#28317=ORIENTED_EDGE ( 'NONE', *, *, #137570, .F. ) ;
#28342=ADVANCED_FACE ( 'NONE', ( #18315 ), #191853, .T. ) ;
#28364=ORIENTED_EDGE ( 'NONE', *, *, #78214, .F. ) ;
#28432=FACE_OUTER_BOUND ( 'NONE', #134836, .T. ) ;
#28433=CARTESIAN_POINT ( 'NONE',  ( -20.94999999999999929, 7.070967871809997973, -104.2465642218683541 ) ) ;
#28448=TOROIDAL_SURFACE ( 'NONE', #232442, 12.97499999999999787, 0.1000000000000000056 ) ;
#28461=CARTESIAN_POINT ( 'NONE',  ( -22.50000000000088463, 0.04536165659888222873, -55.34949116579123540 ) ) ;
#28471=EDGE_CURVE ( 'NONE', #116664, #244409, #127444, .T. ) ;
#28487=ORIENTED_EDGE ( 'NONE', *, *, #95490, .F. ) ;
#28488=CARTESIAN_POINT ( 'NONE',  ( 20.94999999999999929, -1.835341550213257733, -78.55515129256303908 ) ) ;
#28526=CIRCLE ( 'NONE', #103281, 0.1000000000000028644 ) ;
#28580=CARTESIAN_POINT ( 'NONE',  ( -20.64999999999999858, -9.399999999988846611, -90.60603087734760663 ) ) ;
#28588=ORIENTED_EDGE ( 'NONE', *, *, #88215, .T. ) ;
#28606=ORIENTED_EDGE ( 'NONE', *, *, #53815, .F. ) ;
#28638=CARTESIAN_POINT ( 'NONE',  ( -18.59999999999999787, 9.150000000011157653, -88.15000000000004832 ) ) ;
#28666=DIRECTION ( 'NONE',  ( -0.000000000000000000, -0.000000000000000000, 1.000000000000000000 ) ) ;
#28686=VECTOR ( 'NONE', #118503, 1000.000000000000000 ) ;
#28695=EDGE_CURVE ( 'NONE', #85481, #87673, #156891, .T. ) ;
#28711=CIRCLE ( 'NONE', #224474, 0.8750000000000007772 ) ;
#28712=ADVANCED_FACE ( 'NONE', ( #185092 ), #135990, .F. ) ;
#28715=CARTESIAN_POINT ( 'NONE',  ( -18.48179518609225624, -9.518325300483391871, -107.3897055767624522 ) ) ;
#28756=CARTESIAN_POINT ( 'NONE',  ( 21.05000000000000071, 4.813084112160684214, -88.55848224347622022 ) ) ;
#28812=DIRECTION ( 'NONE',  ( 0.000000000000000000, 0.000000000000000000, -1.000000000000000000 ) ) ;
#28834=VECTOR ( 'NONE', #200417, 1000.000000000000000 ) ;
#28836=EDGE_CURVE ( 'NONE', #238735, #250167, #190189, .T. ) ;
#28839=ADVANCED_FACE ( 'NONE', ( #81468 ), #23619, .F. ) ;
#28866=ORIENTED_EDGE ( 'NONE', *, *, #49932, .T. ) ;
#28875=CARTESIAN_POINT ( 'NONE',  ( 21.05000000000000071, -11.29603075032412995, -70.04789915966391334 ) ) ;
#28887=CARTESIAN_POINT ( 'NONE',  ( -21.05000000000000071, 5.900000000011162093, -90.28090023534366537 ) ) ;
#28912=AXIS2_PLACEMENT_3D ( 'NONE', #88383, #123697, #183672 ) ;
#28962=CARTESIAN_POINT ( 'NONE',  ( 23.24999999999999645, 1.115600667400684642E-11, -100.5000000000000426 ) ) ;
#28970=ORIENTED_EDGE ( 'NONE', *, *, #64343, .T. ) ;
#29001=EDGE_LOOP ( 'NONE', ( #249948, #253133, #170357, #248624 ) ) ;
#29016=ADVANCED_FACE ( 'NONE', ( #8403 ), #167491, .T. ) ;
#29036=ORIENTED_EDGE ( 'NONE', *, *, #38810, .F. ) ;
#29055=ORIENTED_EDGE ( 'NONE', *, *, #232480, .T. ) ;
#29056=ORIENTED_EDGE ( 'NONE', *, *, #123062, .F. ) ;
#29063=DIRECTION ( 'NONE',  ( -2.940209281316621509E-16, 1.000000000000000000, 2.352167425053297207E-15 ) ) ;
#29071=DIRECTION ( 'NONE',  ( -1.000000000000000000, -0.000000000000000000, -0.000000000000000000 ) ) ;
#29075=CARTESIAN_POINT ( 'NONE',  ( 23.15000000000000213, -8.999999999988844479, -76.89396912265249284 ) ) ;
#29080=CIRCLE ( 'NONE', #212219, 0.09999999999999693856 ) ;
#29085=ORIENTED_EDGE ( 'NONE', *, *, #110953, .T. ) ;
#29109=FACE_OUTER_BOUND ( 'NONE', #71549, .T. ) ;
#29129=DIRECTION ( 'NONE',  ( -0.7071067811865388020, 0.7071067811865561215, 0.000000000000000000 ) ) ;
#29199=EDGE_CURVE ( 'NONE', #83997, #16604, #19677, .T. ) ;
#29210=CIRCLE ( 'NONE', #41652, 0.09999999999999939493 ) ;
#29232=VERTEX_POINT ( 'NONE', #1649 ) ;
#29279=ORIENTED_EDGE ( 'NONE', *, *, #251746, .F. ) ;
#29297=FACE_OUTER_BOUND ( 'NONE', #80336, .T. ) ;
#29309=AXIS2_PLACEMENT_3D ( 'NONE', #244351, #47430, #27919 ) ;
#29310=CARTESIAN_POINT ( 'NONE',  ( 20.84999999999999432, 7.021664781911246322, -104.3335654018973315 ) ) ;
#29368=CARTESIAN_POINT ( 'NONE',  ( 21.05000000000000071, -8.999999999988842703, -90.60603087734760663 ) ) ;
#29383=DIRECTION ( 'NONE',  ( -1.000000000000000000, -0.000000000000000000, -0.000000000000000000 ) ) ;
#29402=ADVANCED_FACE ( 'NONE', ( #246687 ), #70662, .F. ) ;
#29461=CARTESIAN_POINT ( 'NONE',  ( 20.95556889135987788, 10.62194358774625336, -74.64239422185755757 ) ) ;
#29509=CIRCLE ( 'NONE', #145989, 0.1000000000000028644 ) ;
#29519=EDGE_LOOP ( 'NONE', ( #250829, #163724, #119639, #77360 ) ) ;
#29526=FACE_OUTER_BOUND ( 'NONE', #75161, .T. ) ;
#29551=EDGE_LOOP ( 'NONE', ( #231261, #16396, #245054, #41011 ) ) ;
#29634=ORIENTED_EDGE ( 'NONE', *, *, #181241, .T. ) ;
#29635=DIRECTION ( 'NONE',  ( -0.000000000000000000, 1.000000000000000000, 0.000000000000000000 ) ) ;
#29677=DIRECTION ( 'NONE',  ( 1.000000000000000000, 1.836970198721029934E-16, 0.000000000000000000 ) ) ;
#29685=EDGE_LOOP ( 'NONE', ( #111827, #24273, #2019, #217885, #223715 ) ) ;
#29722=ORIENTED_EDGE ( 'NONE', *, *, #256149, .T. ) ;
#29732=CARTESIAN_POINT ( 'NONE',  ( -23.25000000000000000, -1.835859311432481045, -112.1044391687985780 ) ) ;
#29759=EDGE_CURVE ( 'NONE', #254405, #9696, #246398, .T. ) ;
#29762=CARTESIAN_POINT ( 'NONE',  ( 18.52928932188133970, 10.27928932189250411, -91.75000000000005684 ) ) ;
#29779=VERTEX_POINT ( 'NONE', #190288 ) ;
#29791=SPHERICAL_SURFACE ( 'NONE', #20871, 0.1000000000000000056 ) ;
#29793=DIRECTION ( 'NONE',  ( 0.000000000000000000, 0.000000000000000000, -1.000000000000000000 ) ) ;
#29821=CARTESIAN_POINT ( 'NONE',  ( 18.49999999999999289, 10.20857864377384239, -91.76715728752546397 ) ) ;
#29847=CARTESIAN_POINT ( 'NONE',  ( -21.05315837397170142, 11.75000000001115019, -93.65835600089312152 ) ) ;
#29854=ADVANCED_FACE ( 'NONE', ( #70357 ), #253556, .T. ) ;
#29861=CARTESIAN_POINT ( 'NONE',  ( 22.39999999999999858, 1.115600667400684642E-11, -67.00000000000004263 ) ) ;
#29880=DIRECTION ( 'NONE',  ( 0.000000000000000000, -0.8660254037844383745, 0.5000000000000003331 ) ) ;
#29887=VERTEX_POINT ( 'NONE', #192848 ) ;
#29892=DIRECTION ( 'NONE',  ( -1.000000000000000000, -1.836970198721029934E-16, -0.000000000000000000 ) ) ;
#29895=DIRECTION ( 'NONE',  ( 1.000000000000000000, 2.952720810173289112E-16, -0.000000000000000000 ) ) ;
#29908=EDGE_CURVE ( 'NONE', #80974, #214401, #156310, .T. ) ;
#29915=DIRECTION ( 'NONE',  ( 0.000000000000000000, 1.776356839400254803E-15, 1.000000000000000000 ) ) ;
#29928=DIRECTION ( 'NONE',  ( 0.000000000000000000, 0.4999999999999956701, -0.8660254037844411501 ) ) ;
#29970=ORIENTED_EDGE ( 'NONE', *, *, #158161, .T. ) ;
#29977=ORIENTED_EDGE ( 'NONE', *, *, #152703, .F. ) ;
#29978=CARTESIAN_POINT ( 'NONE',  ( -18.40904629823846150, -9.499999999988851584, -107.1001895624817024 ) ) ;
#30058=DIRECTION ( 'NONE',  ( 0.000000000000000000, -0.9908441862701596881, -0.1350103645451904977 ) ) ;
#30070=CARTESIAN_POINT ( 'NONE',  ( -21.05000000000000071, 1.115653327213047955E-11, -62.70000000000008811 ) ) ;
#30093=EDGE_CURVE ( 'NONE', #173330, #68843, #237948, .T. ) ;
#30101=CARTESIAN_POINT ( 'NONE',  ( 18.59999999999998721, 19.85039924724470950, -69.28030305780140452 ) ) ;
#30187=ORIENTED_EDGE ( 'NONE', *, *, #214466, .F. ) ;
#30194=ORIENTED_EDGE ( 'NONE', *, *, #15154, .F. ) ;
#30207=CARTESIAN_POINT ( 'NONE',  ( -23.15000000000000213, -8.596261682231830292, -91.04987248284976431 ) ) ;
#30249=CARTESIAN_POINT ( 'NONE',  ( -23.15000000000000213, 11.75000000001115552, -88.35000000000003695 ) ) ;
#30251=CARTESIAN_POINT ( 'NONE',  ( -23.15000000000000213, 11.65000000001115588, -79.25000000000004263 ) ) ;
#30265=DIRECTION ( 'NONE',  ( 0.000000000000000000, -0.5907332058517320572, 0.8068669527896995541 ) ) ;
#30274=ORIENTED_EDGE ( 'NONE', *, *, #110927, .F. ) ;
#30280=AXIS2_PLACEMENT_3D ( 'NONE', #245813, #145411, #9756 ) ;
#30284=ORIENTED_EDGE ( 'NONE', *, *, #232480, .F. ) ;
#30291=AXIS2_PLACEMENT_3D ( 'NONE', #252791, #33806, #233276 ) ;
#30312=EDGE_CURVE ( 'NONE', #29779, #237818, #215912, .T. ) ;
#30330=DIRECTION ( 'NONE',  ( 0.000000000000000000, -1.000000000000000000, 0.000000000000000000 ) ) ;
#30331=LINE ( 'NONE', #105972, #157918 ) ;
#30337=ORIENTED_EDGE ( 'NONE', *, *, #8267, .T. ) ;
#30350=ORIENTED_EDGE ( 'NONE', *, *, #139916, .F. ) ;
#30366=ORIENTED_EDGE ( 'NONE', *, *, #237160, .T. ) ;
#30378=DIRECTION ( 'NONE',  ( 0.000000000000000000, 0.000000000000000000, -1.000000000000000000 ) ) ;
#30383=DIRECTION ( 'NONE',  ( 1.000000000000000000, -7.304098846218134667E-16, 0.000000000000000000 ) ) ;
#30403=AXIS2_PLACEMENT_3D ( 'NONE', #43845, #4688, #20444 ) ;
#30414=CARTESIAN_POINT ( 'NONE',  ( 21.04999999999999361, 0.03486800302426068532, -60.72991413631088875 ) ) ;
#30419=DIRECTION ( 'NONE',  ( 0.000000000000000000, 0.000000000000000000, -1.000000000000000000 ) ) ;
#30422=DIRECTION ( 'NONE',  ( 0.000000000000000000, 0.000000000000000000, -1.000000000000000000 ) ) ;
#30458=FACE_OUTER_BOUND ( 'NONE', #61380, .T. ) ;
#30465=AXIS2_PLACEMENT_3D ( 'NONE', #158334, #102139, #139992 ) ;
#30468=DIRECTION ( 'NONE',  ( 1.000000000000000000, 0.000000000000000000, 0.000000000000000000 ) ) ;
#30488=CARTESIAN_POINT ( 'NONE',  ( 20.93302460841142931, 10.31565961587945424, -106.0364194119178620 ) ) ;
#30539=DIRECTION ( 'NONE',  ( 1.000000000000000000, 0.000000000000000000, 0.000000000000000000 ) ) ;
#30544=DIRECTION ( 'NONE',  ( 0.000000000000000000, 0.000000000000000000, 1.000000000000000000 ) ) ;
#30545=CARTESIAN_POINT ( 'NONE',  ( 21.07971444708685738, 6.329792081637702239, -66.91217656368215216 ) ) ;
#30556=DIRECTION ( 'NONE',  ( 0.000000000000000000, 0.000000000000000000, -1.000000000000000000 ) ) ;
#30571=CARTESIAN_POINT ( 'NONE',  ( -21.04999999999999716, 6.344723404101464403, -66.98528214347604148 ) ) ;
#30574=CARTESIAN_POINT ( 'NONE',  ( -23.15000000000000213, 1.115600667400684642E-11, -100.5000000000000426 ) ) ;
#30593=CARTESIAN_POINT ( 'NONE',  ( -21.05000000000000071, 0.2561057921033771945, -66.96510355832775474 ) ) ;
#30633=EDGE_CURVE ( 'NONE', #230995, #77584, #218561, .T. ) ;
#30636=CYLINDRICAL_SURFACE ( 'NONE', #180128, 0.09999999999999939493 ) ;
#30647=VECTOR ( 'NONE', #199717, 1000.000000000000000 ) ;
#30665=CARTESIAN_POINT ( 'NONE',  ( -20.94999999999999929, 11.60000000001115161, -73.92820323027559937 ) ) ;
#30674=FACE_OUTER_BOUND ( 'NONE', #46260, .T. ) ;
#30699=EDGE_CURVE ( 'NONE', #58722, #11117, #122924, .T. ) ;
#30715=AXIS2_PLACEMENT_3D ( 'NONE', #135077, #157261, #137644 ) ;
#30723=FACE_OUTER_BOUND ( 'NONE', #23041, .T. ) ;
#30724=ADVANCED_FACE ( 'NONE', ( #256950 ), #17134, .T. ) ;
#30730=CARTESIAN_POINT ( 'NONE',  ( 20.22894356738450838, 9.278498222849625776, -75.26852290624343311 ) ) ;
#30777=DIRECTION ( 'NONE',  ( 0.000000000000000000, 0.000000000000000000, -1.000000000000000000 ) ) ;
#30808=CARTESIAN_POINT ( 'NONE',  ( -20.94999999999999929, -1.360870587180885716, -75.07299792709100927 ) ) ;
#30809=EDGE_LOOP ( 'NONE', ( #254340, #38309, #144350, #67569 ) ) ;
#30832=AXIS2_PLACEMENT_3D ( 'NONE', #111019, #34089, #70644 ) ;
#30836=ORIENTED_EDGE ( 'NONE', *, *, #132898, .T. ) ;
#30837=CARTESIAN_POINT ( 'NONE',  ( 20.97224591636398827, 10.62515341617478271, -79.24992590466362685 ) ) ;
#30851=DIRECTION ( 'NONE',  ( 1.000000000000000000, 0.000000000000000000, 0.000000000000000000 ) ) ;
#30854=EDGE_LOOP ( 'NONE', ( #170981, #63870, #44340, #16307, #147062, #202055, #221544, #75135, #249329, #215671, #210553, #213010, #19394, #155768, #62365, #241898, #120615, #70168, #204558, #238720, #213556, #76588, #50501, #110358, #172926, #109124, #107908 ) ) ;
#30885=AXIS2_PLACEMENT_3D ( 'NONE', #254741, #76142, #155724 ) ;
#30902=DIRECTION ( 'NONE',  ( 0.000000000000000000, 1.776356839400303713E-15, 1.000000000000000000 ) ) ;
#30947=CIRCLE ( 'NONE', #10061, 11.74999999999999645 ) ;
#30971=CARTESIAN_POINT ( 'NONE',  ( -23.15000000000000213, -8.999999999988844479, -91.20603087734760095 ) ) ;
#31008=EDGE_LOOP ( 'NONE', ( #91186, #140275, #43018, #17405 ) ) ;
#31010=CARTESIAN_POINT ( 'NONE',  ( -20.54999999999999716, -8.999999999988844479, -90.60603087734760663 ) ) ;
#31011=DIRECTION ( 'NONE',  ( -1.000000000000000000, 0.000000000000000000, 0.000000000000000000 ) ) ;
#31018=VERTEX_POINT ( 'NONE', #105137 ) ;
#31031=ORIENTED_EDGE ( 'NONE', *, *, #161379, .T. ) ;
#31042=ADVANCED_FACE ( 'NONE', ( #6072 ), #165164, .T. ) ;
#31077=CIRCLE ( 'NONE', #6069, 0.1000000000000028644 ) ;
#31102=ORIENTED_EDGE ( 'NONE', *, *, #24643, .T. ) ;
#31107=AXIS2_PLACEMENT_3D ( 'NONE', #184050, #240192, #164507 ) ;
#31134=DIRECTION ( 'NONE',  ( 1.000000000000000000, 0.000000000000000000, 0.000000000000000000 ) ) ;
#31146=DIRECTION ( 'NONE',  ( 1.000000000000000000, -0.000000000000000000, -0.000000000000000000 ) ) ;
#31172=AXIS2_PLACEMENT_3D ( 'NONE', #250176, #110656, #33739 ) ;
#31188=DIRECTION ( 'NONE',  ( -1.000000000000000000, -0.000000000000000000, -0.000000000000000000 ) ) ;
#31244=CARTESIAN_POINT ( 'NONE',  ( 21.05000000000000071, 11.75000000001116085, -93.65839931010300745 ) ) ;
#31248=DIRECTION ( 'NONE',  ( 0.000000000000000000, 0.000000000000000000, -1.000000000000000000 ) ) ;
#31256=ORIENTED_EDGE ( 'NONE', *, *, #56199, .T. ) ;
#31293=VERTEX_POINT ( 'NONE', #57377 ) ;
#31297=DIRECTION ( 'NONE',  ( -3.469446951953635015E-14, 1.000000000000000000, 0.000000000000000000 ) ) ;
#31338=CARTESIAN_POINT ( 'NONE',  ( 19.99999999738043144, 11.75000000001115907, -91.68717194963230099 ) ) ;
#31347=ORIENTED_EDGE ( 'NONE', *, *, #45170, .T. ) ;
#31351=DIRECTION ( 'NONE',  ( 0.000000000000000000, 0.000000000000000000, -1.000000000000000000 ) ) ;
#31361=AXIS2_PLACEMENT_3D ( 'NONE', #110130, #189674, #231380 ) ;
#31399=CYLINDRICAL_SURFACE ( 'NONE', #225351, 0.09999999999999693856 ) ;
#31481=CYLINDRICAL_SURFACE ( 'NONE', #231587, 0.1000000000000028644 ) ;
#31493=EDGE_CURVE ( 'NONE', #102331, #56430, #248880, .T. ) ;
#31538=TOROIDAL_SURFACE ( 'NONE', #152333, 11.65000000000000036, 0.1000000000000000056 ) ;
#31553=CARTESIAN_POINT ( 'NONE',  ( -18.45140287520618116, -9.486077739518409047, -107.1405231266861620 ) ) ;
#31559=CARTESIAN_POINT ( 'NONE',  ( -20.85000000000000142, -0.3238857010591806307, -100.4575895893140256 ) ) ;
#31560=EDGE_CURVE ( 'NONE', #173700, #154701, #51928, .T. ) ;
#31574=EDGE_LOOP ( 'NONE', ( #167597, #3384, #152882, #226446 ) ) ;
#31584=ORIENTED_EDGE ( 'NONE', *, *, #141221, .F. ) ;
#31588=CYLINDRICAL_SURFACE ( 'NONE', #92247, 0.5000000000000004441 ) ;
#31603=VERTEX_POINT ( 'NONE', #171945 ) ;
#31609=CIRCLE ( 'NONE', #64878, 0.1000000000000008937 ) ;
#31643=AXIS2_PLACEMENT_3D ( 'NONE', #58329, #239568, #123468 ) ;
#31646=VERTEX_POINT ( 'NONE', #91081 ) ;
#31674=EDGE_CURVE ( 'NONE', #144670, #23868, #126990, .T. ) ;
#31695=ORIENTED_EDGE ( 'NONE', *, *, #132319, .F. ) ;
#31789=ORIENTED_EDGE ( 'NONE', *, *, #60657, .F. ) ;
#31790=CARTESIAN_POINT ( 'NONE',  ( 20.84999999999998721, 10.33248238083634440, -106.0948465439131922 ) ) ;
#31838=CARTESIAN_POINT ( 'NONE',  ( 21.12757541349815682, 6.473380571262609351, -66.99483878419029281 ) ) ;
#31852=TOROIDAL_SURFACE ( 'NONE', #52840, 11.65000000000000036, 0.1000000000000000056 ) ;
#31877=ORIENTED_EDGE ( 'NONE', *, *, #247308, .F. ) ;
#31892=DIRECTION ( 'NONE',  ( 0.000000000000000000, 2.891205793294679805E-16, -1.000000000000000000 ) ) ;
#31895=DIRECTION ( 'NONE',  ( 0.000000000000000000, 0.000000000000000000, -1.000000000000000000 ) ) ;
#31914=EDGE_CURVE ( 'NONE', #13227, #177719, #56047, .T. ) ;
#31955=PLANE ( 'NONE',  #50953 ) ;
#31958=CIRCLE ( 'NONE', #2700, 0.1000000000000028644 ) ;
#31967=FACE_OUTER_BOUND ( 'NONE', #124423, .T. ) ;
#32001=CARTESIAN_POINT ( 'NONE',  ( -20.64999999999999858, -8.730841121484171907, -76.59807471898437825 ) ) ;
#32006=CARTESIAN_POINT ( 'NONE',  ( 20.13684514580102913, 9.495855392761558988, -75.14303168568623903 ) ) ;
#32010=ADVANCED_FACE ( 'NONE', ( #138538 ), #195993, .T. ) ;
#32026=CARTESIAN_POINT ( 'NONE',  ( 21.05000000000000071, -11.48912529306490349, -70.10000000000005116 ) ) ;
#32084=CARTESIAN_POINT ( 'NONE',  ( 21.09706851349342216, 8.775842513484549912, -79.23556621639968967 ) ) ;
#32089=VERTEX_POINT ( 'NONE', #224518 ) ;
#32094=AXIS2_PLACEMENT_3D ( 'NONE', #150577, #148005, #112730 ) ;
#32100=EDGE_CURVE ( 'NONE', #52066, #33168, #141146, .T. ) ;
#32131=DIRECTION ( 'NONE',  ( 0.000000000000000000, 0.000000000000000000, -1.000000000000000000 ) ) ;
#32149=EDGE_CURVE ( 'NONE', #118177, #51736, #93852, .T. ) ;
#32153=ORIENTED_EDGE ( 'NONE', *, *, #73807, .T. ) ;
#32163=DIRECTION ( 'NONE',  ( 0.000000000000000000, 0.000000000000000000, -1.000000000000000000 ) ) ;
#32171=ADVANCED_FACE ( 'NONE', ( #49735 ), #114705, .T. ) ;
#32186=ORIENTED_EDGE ( 'NONE', *, *, #246647, .F. ) ;
#32301=VECTOR ( 'NONE', #92801, 1000.000000000000000 ) ;
#32305=ORIENTED_EDGE ( 'NONE', *, *, #116944, .F. ) ;
#32312=ADVANCED_FACE ( 'NONE', ( #230969 ), #31538, .T. ) ;
#32322=DIRECTION ( 'NONE',  ( 0.000000000000000000, 0.000000000000000000, 1.000000000000000000 ) ) ;
#32333=CARTESIAN_POINT ( 'NONE',  ( -21.59142135623730852, 7.850000000011158718, -88.25000000000005684 ) ) ;
#32341=ORIENTED_EDGE ( 'NONE', *, *, #158330, .F. ) ;
#32347=ADVANCED_FACE ( 'NONE', ( #133130 ), #214833, .F. ) ;
#32359=ADVANCED_FACE ( 'NONE', ( #195696 ), #243871, .F. ) ;
#32367=CARTESIAN_POINT ( 'NONE',  ( 23.24999999999999289, 6.650000000011155876, -88.35000000000003695 ) ) ;
#32385=DIRECTION ( 'NONE',  ( 0.000000000000000000, 0.000000000000000000, -1.000000000000000000 ) ) ;
#32391=DIRECTION ( 'NONE',  ( 1.000000000000000000, 0.000000000000000000, -0.000000000000000000 ) ) ;
#32399=EDGE_LOOP ( 'NONE', ( #243949, #194115, #252622 ) ) ;
#32415=CARTESIAN_POINT ( 'NONE',  ( -21.14999999999999858, -0.09999999998884338825, -55.35042919245523763 ) ) ;
#32424=FACE_OUTER_BOUND ( 'NONE', #207726, .T. ) ;
#32430=ADVANCED_FACE ( 'NONE', ( #5132 ), #200805, .F. ) ;
#32437=DIRECTION ( 'NONE',  ( 0.000000000000000000, 0.9908441862701596881, 0.1350103645451904977 ) ) ;
#32447=DIRECTION ( 'NONE',  ( 0.000000000000000000, 0.000000000000000000, 1.000000000000000000 ) ) ;
#32451=CARTESIAN_POINT ( 'NONE',  ( -21.07094088545368749, 0.09889370256337755294, -60.67983277808291120 ) ) ;
#32477=FACE_OUTER_BOUND ( 'NONE', #226522, .T. ) ;
#32488=DIRECTION ( 'NONE',  ( 1.000000000000000000, 0.000000000000000000, 0.000000000000000000 ) ) ;
#32502=EDGE_CURVE ( 'NONE', #240985, #256256, #108405, .T. ) ;
#32537=AXIS2_PLACEMENT_3D ( 'NONE', #108387, #9277, #88790 ) ;
#32540=AXIS2_PLACEMENT_3D ( 'NONE', #34929, #114428, #174452 ) ;
#32546=DIRECTION ( 'NONE',  ( -1.000000000000000000, 0.000000000000000000, 0.000000000000000000 ) ) ;
#32562=DIRECTION ( 'NONE',  ( 1.000000000000000000, 0.000000000000000000, 0.000000000000000000 ) ) ;
#32574=ADVANCED_FACE ( 'NONE', ( #89821 ), #239799, .T. ) ;
#32593=ORIENTED_EDGE ( 'NONE', *, *, #251993, .T. ) ;
#32629=ORIENTED_EDGE ( 'NONE', *, *, #176643, .F. ) ;
#32632=ORIENTED_EDGE ( 'NONE', *, *, #215464, .T. ) ;
#32634=( GEOMETRIC_REPRESENTATION_CONTEXT ( 3 ) GLOBAL_UNCERTAINTY_ASSIGNED_CONTEXT ( ( #197955 ) ) GLOBAL_UNIT_ASSIGNED_CONTEXT ( ( #1399, #138334, #174974 ) ) REPRESENTATION_CONTEXT ( 'NONE', 'WORKASPACE' ) );
#32680=CARTESIAN_POINT ( 'NONE',  ( 23.15000000000000213, -11.64999999998883595, -97.40000000000004832 ) ) ;
#32682=EDGE_CURVE ( 'NONE', #93742, #374, #126676, .T. ) ;
#32770=AXIS2_PLACEMENT_3D ( 'NONE', #6538, #148641, #206034 ) ;
#32784=CARTESIAN_POINT ( 'NONE',  ( 18.59999999999999076, 11.65000000001115943, -91.85000000000003695 ) ) ;
#32805=AXIS2_PLACEMENT_3D ( 'NONE', #224180, #83366, #165518 ) ;
#32821=AXIS2_PLACEMENT_3D ( 'NONE', #15902, #135798, #116268 ) ;
#32882=ORIENTED_EDGE ( 'NONE', *, *, #134713, .F. ) ;
#32897=ORIENTED_EDGE ( 'NONE', *, *, #63569, .T. ) ;
#32905=CARTESIAN_POINT ( 'NONE',  ( 20.94999999999999574, -1.162701749926853712, -75.00000000000004263 ) ) ;
#32912=AXIS2_PLACEMENT_3D ( 'NONE', #15918, #234942, #35484 ) ;
#32945=CARTESIAN_POINT ( 'NONE',  ( -21.37071067811865532, 8.070710678129811910, -79.25000000000004263 ) ) ;
#32948=ORIENTED_EDGE ( 'NONE', *, *, #116767, .T. ) ;
#32965=TOROIDAL_SURFACE ( 'NONE', #245310, 11.90000000000000391, 0.1000000000000000056 ) ;
#32995=AXIS2_PLACEMENT_3D ( 'NONE', #34983, #91063, #250141 ) ;
#33003=AXIS2_PLACEMENT_3D ( 'NONE', #231884, #71529, #187619 ) ;
#33015=VECTOR ( 'NONE', #100525, 1000.000000000000000 ) ;
#33021=ORIENTED_EDGE ( 'NONE', *, *, #13202, .T. ) ;
#33052=LINE ( 'NONE', #49993, #449 ) ;
#33060=PLANE ( 'NONE',  #146986 ) ;
#33065=ORIENTED_EDGE ( 'NONE', *, *, #163812, .T. ) ;
#33082=AXIS2_PLACEMENT_3D ( 'NONE', #235739, #57083, #146892 ) ;
#33083=DIRECTION ( 'NONE',  ( 2.952720810173289112E-16, -1.000000000000000000, 0.000000000000000000 ) ) ;
#33090=CARTESIAN_POINT ( 'NONE',  ( 22.47071067811864964, 0.09909245471376176839, -59.27992525550201464 ) ) ;
#33104=AXIS2_PLACEMENT_3D ( 'NONE', #69162, #5278, #44454 ) ;
#33168=VERTEX_POINT ( 'NONE', #252433 ) ;
#33177=VECTOR ( 'NONE', #236579, 1000.000000000000000 ) ;
#33190=EDGE_CURVE ( 'NONE', #68442, #188971, #36161, .T. ) ;
#33192=CARTESIAN_POINT ( 'NONE',  ( -20.00857864376270001, 9.150000000011157653, -79.35000000000005116 ) ) ;
#33199=CARTESIAN_POINT ( 'NONE',  ( 20.85000000000000142, 1.115600667400684642E-11, -100.5000000000000426 ) ) ;
#33208=CARTESIAN_POINT ( 'NONE',  ( -20.54999999999999716, -11.74999999998884448, -88.15000000000004832 ) ) ;
#33211=CYLINDRICAL_SURFACE ( 'NONE', #31361, 0.09999999999999939493 ) ;
#33221=EDGE_CURVE ( 'NONE', #6867, #150875, #123211, .T. ) ;
#33227=FACE_BOUND ( 'NONE', #250776, .T. ) ;
#33231=CARTESIAN_POINT ( 'NONE',  ( -18.59999999999999787, 11.75000000001115197, -88.35000000000003695 ) ) ;
#33280=ADVANCED_FACE ( 'NONE', ( #43679 ), #121936, .F. ) ;
#33289=VECTOR ( 'NONE', #24793, 1000.000000000000000 ) ;
#33294=ADVANCED_FACE ( 'NONE', ( #98464 ), #44351, .T. ) ;
#33296=DIRECTION ( 'NONE',  ( -0.000000000000000000, -1.000000000000000000, -5.421010862427649374E-16 ) ) ;
#33343=VECTOR ( 'NONE', #217024, 1000.000000000000000 ) ;
#33364=EDGE_LOOP ( 'NONE', ( #126087, #130292 ) ) ;
#33371=CYLINDRICAL_SURFACE ( 'NONE', #26743, 0.5000000000000004441 ) ;
#33381=CARTESIAN_POINT ( 'NONE',  ( 21.04999999999908411, 8.776282895301829257, -79.15790900265254493 ) ) ;
#33415=EDGE_CURVE ( 'NONE', #208514, #138090, #134013, .T. ) ;
#33425=ADVANCED_FACE ( 'NONE', ( #9677 ), #152699, .F. ) ;
#33467=VERTEX_POINT ( 'NONE', #106193 ) ;
#33509=EDGE_CURVE ( 'NONE', #238381, #239916, #23884, .T. ) ;
#33515=DIRECTION ( 'NONE',  ( -1.000000000000000000, 0.000000000000000000, 0.000000000000000000 ) ) ;
#33567=EDGE_LOOP ( 'NONE', ( #173696, #74858, #157161, #66577 ) ) ;
#33636=CARTESIAN_POINT ( 'NONE',  ( 20.95224633520496127, 8.900522166568386240, -75.49327644792130343 ) ) ;
#33659=ADVANCED_FACE ( 'NONE', ( #140877 ), #222961, .F. ) ;
#33667=EDGE_CURVE ( 'NONE', #239872, #128673, #123633, .T. ) ;
#33672=CARTESIAN_POINT ( 'NONE',  ( 20.04142135623730070, 11.65000000001115943, -88.25000000000005684 ) ) ;
#33695=AXIS2_PLACEMENT_3D ( 'NONE', #82446, #4211, #83720 ) ;
#33717=CARTESIAN_POINT ( 'NONE',  ( 21.13461538461538680, 10.61458296203669427, -79.25000000000005684 ) ) ;
#33718=DIRECTION ( 'NONE',  ( 0.000000000000000000, 1.000000000000000000, 0.000000000000000000 ) ) ;
#33739=DIRECTION ( 'NONE',  ( 0.000000000000000000, 0.000000000000000000, -1.000000000000000000 ) ) ;
#33773=CIRCLE ( 'NONE', #196044, 0.1000000000000028644 ) ;
#33779=DIRECTION ( 'NONE',  ( 0.000000000000000000, 0.000000000000000000, -1.000000000000000000 ) ) ;
#33792=ORIENTED_EDGE ( 'NONE', *, *, #8998, .F. ) ;
#33795=EDGE_LOOP ( 'NONE', ( #244366, #94069, #104533, #233535 ) ) ;
#33806=DIRECTION ( 'NONE',  ( -1.000000000000000000, 0.000000000000000000, 0.000000000000000000 ) ) ;
#33813=SPHERICAL_SURFACE ( 'NONE', #245000, 0.1000000000000000056 ) ;
#33818=ORIENTED_EDGE ( 'NONE', *, *, #237325, .F. ) ;
#33845=EDGE_CURVE ( 'NONE', #253894, #152504, #49473, .T. ) ;
#33878=CIRCLE ( 'NONE', #150370, 0.09999999999999939493 ) ;
#33884=FACE_OUTER_BOUND ( 'NONE', #217868, .T. ) ;
#33889=FACE_OUTER_BOUND ( 'NONE', #58647, .T. ) ;
#33896=LINE ( 'NONE', #113386, #143354 ) ;
#33944=DIRECTION ( 'NONE',  ( 0.000000000000000000, 0.000000000000000000, -1.000000000000000000 ) ) ;
#33951=CARTESIAN_POINT ( 'NONE',  ( 23.24999999999997513, 11.65000000001116298, -93.48519422934610645 ) ) ;
#33963=EDGE_CURVE ( 'NONE', #82676, #236070, #24059, .T. ) ;
#33970=AXIS2_PLACEMENT_3D ( 'NONE', #82612, #117911, #100881 ) ;
#34012=FACE_OUTER_BOUND ( 'NONE', #15344, .T. ) ;
#34044=CARTESIAN_POINT ( 'NONE',  ( 21.05000000000000071, 1.115600667400684642E-11, -102.4000000000000483 ) ) ;
#34061=AXIS2_PLACEMENT_3D ( 'NONE', #175727, #216097, #79146 ) ;
#34075=DIRECTION ( 'NONE',  ( -1.000000000000000000, -0.000000000000000000, -0.000000000000000000 ) ) ;
#34082=DIRECTION ( 'NONE',  ( -0.000000000000000000, -0.000000000000000000, 1.000000000000000000 ) ) ;
#34089=DIRECTION ( 'NONE',  ( 1.000000000000000000, 0.000000000000000000, -0.000000000000000000 ) ) ;
#34125=DIRECTION ( 'NONE',  ( 0.000000000000000000, -1.000000000000000000, 0.000000000000000000 ) ) ;
#34170=SPHERICAL_SURFACE ( 'NONE', #90155, 0.1000000000000000056 ) ;
#34181=VERTEX_POINT ( 'NONE', #90835 ) ;
#34182=CIRCLE ( 'NONE', #175815, 0.1000000000000000472 ) ;
#34230=AXIS2_PLACEMENT_3D ( 'NONE', #202005, #3803, #156494 ) ;
#34235=ORIENTED_EDGE ( 'NONE', *, *, #154194, .F. ) ;
#34264=EDGE_LOOP ( 'NONE', ( #44604, #131622, #170745, #131993 ) ) ;
#34276=CARTESIAN_POINT ( 'NONE',  ( 18.59999999999999787, -1.851028230129704522, -78.65391326942254580 ) ) ;
#34293=DIRECTION ( 'NONE',  ( 1.000000000000000000, -0.000000000000000000, -0.000000000000000000 ) ) ;
#34298=CARTESIAN_POINT ( 'NONE',  ( 20.94999999999999574, -1.835341550213255957, -78.65515129256301918 ) ) ;
#34328=EDGE_CURVE ( 'NONE', #224594, #217530, #207402, .T. ) ;
#34356=CARTESIAN_POINT ( 'NONE',  ( 21.05000000000000071, 1.360870587203197646, -75.07299792709100927 ) ) ;
#34363=DIRECTION ( 'NONE',  ( -0.7071067811865475727, -0.7071067811865475727, 0.000000000000000000 ) ) ;
#34365=EDGE_LOOP ( 'NONE', ( #92202, #203183, #47895, #212596, #79781 ) ) ;
#34374=ORIENTED_EDGE ( 'NONE', *, *, #151870, .F. ) ;
#34381=ADVANCED_FACE ( 'NONE', ( #137650 ), #240624, .T. ) ;
#34391=DIRECTION ( 'NONE',  ( -1.000000000000000000, 0.000000000000000000, 0.000000000000000000 ) ) ;
#34431=CIRCLE ( 'NONE', #67533, 0.1000000000000000472 ) ;
#34441=ORIENTED_EDGE ( 'NONE', *, *, #256246, .F. ) ;
#34444=ORIENTED_EDGE ( 'NONE', *, *, #33509, .F. ) ;
#34454=TOROIDAL_SURFACE ( 'NONE', #96743, 1.900000000000002576, 0.1000000000000000056 ) ;
#34463=CARTESIAN_POINT ( 'NONE',  ( -18.52186455168988743, -9.481018481431364719, -74.02501647791453365 ) ) ;
#34466=ORIENTED_EDGE ( 'NONE', *, *, #113330, .F. ) ;
#34470=CIRCLE ( 'NONE', #51153, 0.1000000000000028644 ) ;
#34478=FACE_OUTER_BOUND ( 'NONE', #165635, .T. ) ;
#34481=ORIENTED_EDGE ( 'NONE', *, *, #121575, .T. ) ;
#34494=CARTESIAN_POINT ( 'NONE',  ( 23.25000000000000000, -11.74999999998883560, -55.25000000000004974 ) ) ;
#34608=FACE_OUTER_BOUND ( 'NONE', #170563, .T. ) ;
#34612=ORIENTED_EDGE ( 'NONE', *, *, #85058, .F. ) ;
#34646=VECTOR ( 'NONE', #217093, 1000.000000000000000 ) ;
#34663=CARTESIAN_POINT ( 'NONE',  ( 18.59999999999998366, 7.021664781911246322, -104.3335654018973315 ) ) ;
#34700=AXIS2_PLACEMENT_3D ( 'NONE', #106135, #185702, #219672 ) ;
#34722=ORIENTED_EDGE ( 'NONE', *, *, #111768, .F. ) ;
#34734=ORIENTED_EDGE ( 'NONE', *, *, #243629, .T. ) ;
#34757=DIRECTION ( 'NONE',  ( -0.000000000000000000, 0.000000000000000000, 1.000000000000000000 ) ) ;
#34762=AXIS2_PLACEMENT_3D ( 'NONE', #235675, #32391, #230565 ) ;
#34775=DIRECTION ( 'NONE',  ( -1.000000000000000000, 0.000000000000000000, 0.000000000000000000 ) ) ;
#34784=AXIS2_PLACEMENT_3D ( 'NONE', #38103, #53797, #133344 ) ;
#34805=CARTESIAN_POINT ( 'NONE',  ( 18.59999999999999076, 6.650000000011155876, -88.15000000000004832 ) ) ;
#34838=CARTESIAN_POINT ( 'NONE',  ( 20.94999999999999929, 6.650000000011155876, -77.01702717044007329 ) ) ;
#34881=TOROIDAL_SURFACE ( 'NONE', #5779, 0.2000000000000000111, 0.1000000000000000056 ) ;
#34897=ORIENTED_EDGE ( 'NONE', *, *, #71221, .T. ) ;
#34901=AXIS2_PLACEMENT_3D ( 'NONE', #70134, #47958, #68835 ) ;
#34902=DIRECTION ( 'NONE',  ( 1.000000000000000000, 0.000000000000000000, 0.000000000000000000 ) ) ;
#34904=CARTESIAN_POINT ( 'NONE',  ( 20.95346350065193519, 8.887177249185651107, -75.51173194703542890 ) ) ;
#34905=AXIS2_PLACEMENT_3D ( 'NONE', #120329, #160731, #240247 ) ;
#34929=CARTESIAN_POINT ( 'NONE',  ( 20.94999999999999574, 1.835341550235567887, -78.55515129256303908 ) ) ;
#34983=CARTESIAN_POINT ( 'NONE',  ( -18.59999999999999787, 11.65000000001115232, -79.15000000000003411 ) ) ;
#34995=CARTESIAN_POINT ( 'NONE',  ( -20.64999999999999858, -8.663551401858004652, -76.52410111806734960 ) ) ;
#35003=DIRECTION ( 'NONE',  ( -1.000000000000000000, 0.000000000000000000, 0.000000000000000000 ) ) ;
#35031=CARTESIAN_POINT ( 'NONE',  ( 23.14999999999999503, 6.550000000011156231, -88.25000000000005684 ) ) ;
#35040=FACE_OUTER_BOUND ( 'NONE', #29519, .T. ) ;
#35046=ADVANCED_FACE ( 'NONE', ( #174028 ), #111908, .T. ) ;
#35058=CARTESIAN_POINT ( 'NONE',  ( -20.64999999999999858, -8.999999999988844479, -91.00603087734759811 ) ) ;
#35078=ADVANCED_FACE ( 'NONE', ( #98251 ), #100815, .T. ) ;
#35140=DIRECTION ( 'NONE',  ( 0.000000000000000000, 1.000000000000000000, 0.000000000000000000 ) ) ;
#35145=CIRCLE ( 'NONE', #180859, 0.1999999999999996503 ) ;
#35159=CARTESIAN_POINT ( 'NONE',  ( 18.33683296300512922, -9.511149971121900748, -107.4057074127093756 ) ) ;
#35161=DIRECTION ( 'NONE',  ( -1.000000000000000000, 0.000000000000000000, 0.000000000000000000 ) ) ;
#35166=CARTESIAN_POINT ( 'NONE',  ( 18.45068634130097607, -9.486506073331600675, -74.06877843116815541 ) ) ;
#35205=EDGE_CURVE ( 'NONE', #165054, #4905, #30331, .T. ) ;
#35214=FACE_OUTER_BOUND ( 'NONE', #252007, .T. ) ;
#35237=ORIENTED_EDGE ( 'NONE', *, *, #158386, .F. ) ;
#35267=ORIENTED_EDGE ( 'NONE', *, *, #25644, .F. ) ;
#35284=CIRCLE ( 'NONE', #85083, 0.1000000000000028644 ) ;
#35291=CARTESIAN_POINT ( 'NONE',  ( 20.94999999999999929, 10.72371710471867701, -88.25000000000005684 ) ) ;
#35319=CIRCLE ( 'NONE', #181032, 0.09999999999999867328 ) ;
#35332=CARTESIAN_POINT ( 'NONE',  ( 20.94999999999999574, 1.162701749949165642, -75.00000000000004263 ) ) ;
#35347=ORIENTED_EDGE ( 'NONE', *, *, #66719, .T. ) ;
#35354=EDGE_CURVE ( 'NONE', #136961, #51884, #152871, .T. ) ;
#35363=AXIS2_PLACEMENT_3D ( 'NONE', #230260, #247250, #12531 ) ;
#35463=ORIENTED_EDGE ( 'NONE', *, *, #197, .T. ) ;
#35484=DIRECTION ( 'NONE',  ( -1.000000000000000000, 0.000000000000000000, 0.000000000000000000 ) ) ;
#35490=FACE_OUTER_BOUND ( 'NONE', #33364, .T. ) ;
#35501=AXIS2_PLACEMENT_3D ( 'NONE', #199416, #140699, #122433 ) ;
#35531=LINE ( 'NONE', #78456, #19579 ) ;
#35582=EDGE_CURVE ( 'NONE', #233528, #195076, #79695, .T. ) ;
#35603=CARTESIAN_POINT ( 'NONE',  ( -18.39999999999999858, -9.682403433465239573, -107.1568433774128408 ) ) ;
#35622=DIRECTION ( 'NONE',  ( -1.000000000000000000, -0.000000000000000000, -0.000000000000000000 ) ) ;
#35633=VECTOR ( 'NONE', #34082, 1000.000000000000000 ) ;
#35674=CIRCLE ( 'NONE', #68985, 0.9750000000000036415 ) ;
#35687=AXIS2_PLACEMENT_3D ( 'NONE', #90265, #30330, #173733 ) ;
#35720=ADVANCED_FACE ( 'NONE', ( #213454 ), #128801, .F. ) ;
#35745=DIRECTION ( 'NONE',  ( 0.000000000000000000, 0.008583690987128220901, 0.9999631594459055250 ) ) ;
#35758=ORIENTED_EDGE ( 'NONE', *, *, #10864, .F. ) ;
#35766=AXIS2_PLACEMENT_3D ( 'NONE', #89910, #131612, #130321 ) ;
#35775=CARTESIAN_POINT ( 'NONE',  ( -22.48660254037843487, 11.65000000001115588, -66.95000000000005969 ) ) ;
#35833=EDGE_CURVE ( 'NONE', #61020, #134077, #83172, .T. ) ;
#35874=DIRECTION ( 'NONE',  ( 0.000000000000000000, -1.000000000000000000, 0.000000000000000000 ) ) ;
#35935=DIRECTION ( 'NONE',  ( 0.000000000000000000, -1.000000000000000000, -0.000000000000000000 ) ) ;
#35954=EDGE_CURVE ( 'NONE', #143795, #242995, #5936, .T. ) ;
#35982=CARTESIAN_POINT ( 'NONE',  ( -18.50000000000000000, 10.29270135741298375, -105.9573618871519898 ) ) ;
#36041=CARTESIAN_POINT ( 'NONE',  ( 18.39999999999999858, -9.519327731081283162, -73.97297637655937308 ) ) ;
#36046=CARTESIAN_POINT ( 'NONE',  ( -23.25000000000000000, -1.164121893230052995, -108.4148480855716485 ) ) ;
#36058=AXIS2_PLACEMENT_3D ( 'NONE', #186921, #8269, #70828 ) ;
#36116=CARTESIAN_POINT ( 'NONE',  ( 21.56666275994539461, 1.115600667400684642E-11, -60.04263159310671938 ) ) ;
#36120=CARTESIAN_POINT ( 'NONE',  ( 20.00000000000000355, 11.75000000001116263, -91.65000000000004832 ) ) ;
#36131=EDGE_LOOP ( 'NONE', ( #205393, #224989, #169139, #130114 ) ) ;
#36136=ORIENTED_EDGE ( 'NONE', *, *, #49027, .T. ) ;
#36148=CIRCLE ( 'NONE', #185973, 0.1000000000000000472 ) ;
#36149=ORIENTED_EDGE ( 'NONE', *, *, #75013, .T. ) ;
#36161=CIRCLE ( 'NONE', #185981, 0.1000000000000002554 ) ;
#36170=DIRECTION ( 'NONE',  ( 1.000000000000000000, 0.000000000000000000, 0.000000000000000000 ) ) ;
#36266=EDGE_CURVE ( 'NONE', #22968, #205612, #70390, .T. ) ;
#36286=CARTESIAN_POINT ( 'NONE',  ( -21.45000000000000284, 7.708578643773852157, -88.15000000000004832 ) ) ;
#36291=DIRECTION ( 'NONE',  ( 0.000000000000000000, 0.000000000000000000, -1.000000000000000000 ) ) ;
#36314=EDGE_LOOP ( 'NONE', ( #246517, #82333 ) ) ;
#36325=DIRECTION ( 'NONE',  ( 1.000000000000000000, 0.000000000000000000, 0.000000000000000000 ) ) ;
#36337=FACE_OUTER_BOUND ( 'NONE', #254668, .T. ) ;
#36349=CARTESIAN_POINT ( 'NONE',  ( -20.64999999999999858, 7.150000000011155876, -79.35000000000005116 ) ) ;
#36385=EDGE_LOOP ( 'NONE', ( #225780, #159660, #118741 ) ) ;
#36401=DIRECTION ( 'NONE',  ( -1.000000000000000000, 0.000000000000000000, 0.000000000000000000 ) ) ;
#36418=VERTEX_POINT ( 'NONE', #69508 ) ;
#36429=DIRECTION ( 'NONE',  ( 0.000000000000000000, -0.8660254037844411501, -0.4999999999999956701 ) ) ;
#36446=CYLINDRICAL_SURFACE ( 'NONE', #48935, 11.80000000000000426 ) ;
#36447=AXIS2_PLACEMENT_3D ( 'NONE', #247974, #229708, #148895 ) ;
#36471=ORIENTED_EDGE ( 'NONE', *, *, #107347, .F. ) ;
#36555=DIRECTION ( 'NONE',  ( -2.952720810173289112E-16, 1.000000000000000000, 0.000000000000000000 ) ) ;
#36575=ADVANCED_FACE ( 'NONE', ( #55035 ), #195877, .F. ) ;
#36605=ORIENTED_EDGE ( 'NONE', *, *, #11194, .T. ) ;
#36606=CARTESIAN_POINT ( 'NONE',  ( 20.94999999999999929, 7.021664781911246322, -104.3335654018973315 ) ) ;
#36611=DIRECTION ( 'NONE',  ( -0.000000000000000000, 0.000000000000000000, -1.000000000000000000 ) ) ;
#36645=CARTESIAN_POINT ( 'NONE',  ( 23.14999999999999858, 5.000000000011153745, -79.40526601891313874 ) ) ;
#36681=CARTESIAN_POINT ( 'NONE',  ( -20.05000000000000426, 9.250000000011157297, -88.15000000000004832 ) ) ;
#36779=DIRECTION ( 'NONE',  ( 0.000000000000000000, 0.4999999999999956701, -0.8660254037844411501 ) ) ;
#36794=CARTESIAN_POINT ( 'NONE',  ( 22.59999999999999787, 11.64957080755595520, -66.90000000000004832 ) ) ;
#36834=LINE ( 'NONE', #257072, #159402 ) ;
#36867=ORIENTED_EDGE ( 'NONE', *, *, #200392, .T. ) ;
#36870=ADVANCED_FACE ( 'NONE', ( #126592 ), #67900, .T. ) ;
#36999=VERTEX_POINT ( 'NONE', #73079 ) ;
#37018=CARTESIAN_POINT ( 'NONE',  ( -23.15000000000000213, 4.150000000011156764, -55.25000000000004974 ) ) ;
#37020=ORIENTED_EDGE ( 'NONE', *, *, #215104, .F. ) ;
#37023=CARTESIAN_POINT ( 'NONE',  ( -18.54159361262942696, -9.463132135481979290, -74.04912221629291480 ) ) ;
#37034=VECTOR ( 'NONE', #111599, 1000.000000000000000 ) ;
#37052=AXIS2_PLACEMENT_3D ( 'NONE', #63266, #45000, #123250 ) ;
#37063=SPHERICAL_SURFACE ( 'NONE', #76653, 0.1000000000000000056 ) ;
#37069=LINE ( 'NONE', #236511, #240137 ) ;
#37070=DIRECTION ( 'NONE',  ( 0.000000000000000000, 0.000000000000000000, -1.000000000000000000 ) ) ;
#37071=CARTESIAN_POINT ( 'NONE',  ( 23.14999999999999147, 1.115600667400684642E-11, -67.00000000000004263 ) ) ;
#37102=CYLINDRICAL_SURFACE ( 'NONE', #108257, 0.09999999999999939493 ) ;
#37114=EDGE_LOOP ( 'NONE', ( #110959, #129865, #162740, #24491 ) ) ;
#37124=ORIENTED_EDGE ( 'NONE', *, *, #170655, .T. ) ;
#37125=AXIS2_PLACEMENT_3D ( 'NONE', #66829, #146344, #47238 ) ;
#37129=EDGE_LOOP ( 'NONE', ( #22834, #48780, #129313, #102775 ) ) ;
#37141=DIRECTION ( 'NONE',  ( -2.915501640297154283E-16, 1.000000000000000000, 0.000000000000000000 ) ) ;
#37157=ORIENTED_EDGE ( 'NONE', *, *, #13479, .F. ) ;
#37164=CIRCLE ( 'NONE', #216193, 0.09999999999999971412 ) ;
#37218=EDGE_LOOP ( 'NONE', ( #9315, #195986, #21360, #80851 ) ) ;
#37225=EDGE_CURVE ( 'NONE', #44645, #129552, #204525, .T. ) ;
#37268=CARTESIAN_POINT ( 'NONE',  ( 21.05000000000000071, 8.776282895303630482, -75.55862899514100661 ) ) ;
#37274=ADVANCED_FACE ( 'NONE', ( #130125 ), #29791, .T. ) ;
#37294=EDGE_LOOP ( 'NONE', ( #130349, #95382, #198127, #151376 ) ) ;
#37296=ORIENTED_EDGE ( 'NONE', *, *, #57199, .T. ) ;
#37328=ORIENTED_EDGE ( 'NONE', *, *, #152678, .T. ) ;
#37353=DIRECTION ( 'NONE',  ( 0.000000000000000000, 0.9908441862701596881, 0.1350103645451904977 ) ) ;
#37355=CARTESIAN_POINT ( 'NONE',  ( 20.94999999999999929, 5.850000000011160495, -90.36750277572211587 ) ) ;
#37439=CARTESIAN_POINT ( 'NONE',  ( -20.94999999999999929, -1.835341550213257733, -78.55515129256303908 ) ) ;
#37523=LINE ( 'NONE', #909, #95663 ) ;
#37530=LINE ( 'NONE', #55754, #169748 ) ;
#37535=VERTEX_POINT ( 'NONE', #42270 ) ;
#37552=ORIENTED_EDGE ( 'NONE', *, *, #75278, .T. ) ;
#37559=UNCERTAINTY_MEASURE_WITH_UNIT (LENGTH_MEASURE( 1.000000000000000082E-05 ), #240756, 'distance_accuracy_value', 'NONE');
#37569=ORIENTED_EDGE ( 'NONE', *, *, #54750, .T. ) ;
#37583=ADVANCED_FACE ( 'NONE', ( #51215 ), #149084, .F. ) ;
#37592=ORIENTED_EDGE ( 'NONE', *, *, #99960, .F. ) ;
#37598=AXIS2_PLACEMENT_3D ( 'NONE', #20140, #123090, #60517 ) ;
#37601=ADVANCED_FACE ( 'NONE', ( #189484 ), #92930, .T. ) ;
#37651=AXIS2_PLACEMENT_3D ( 'NONE', #31559, #94051, #172365 ) ;
#37665=CARTESIAN_POINT ( 'NONE',  ( -20.00857864376270001, 9.350000000011156942, -88.15000000000004832 ) ) ;
#37668=AXIS2_PLACEMENT_3D ( 'NONE', #186988, #128280, #106110 ) ;
#37694=DIRECTION ( 'NONE',  ( -1.000000000000000000, 0.000000000000000000, 0.000000000000000000 ) ) ;
#37704=ORIENTED_EDGE ( 'NONE', *, *, #119658, .T. ) ;
#37710=DIRECTION ( 'NONE',  ( 0.000000000000000000, 0.9915357197604973694, -0.1298341882519105928 ) ) ;
#37716=CARTESIAN_POINT ( 'NONE',  ( -23.25000000000000000, -11.74999999998884448, -67.00000000000004263 ) ) ;
#37717=DIRECTION ( 'NONE',  ( -1.000000000000000000, 0.000000000000000000, 0.000000000000000000 ) ) ;
#37739=ORIENTED_EDGE ( 'NONE', *, *, #53736, .F. ) ;
#37742=CARTESIAN_POINT ( 'NONE',  ( 20.94999999999999574, 1.736257131608553550, -78.56865232901755292 ) ) ;
#37754=DIRECTION ( 'NONE',  ( 0.000000000000000000, 0.000000000000000000, -1.000000000000000000 ) ) ;
#37761=CARTESIAN_POINT ( 'NONE',  ( 20.12500000000000000, 9.750000000011153745, -75.11177128211431864 ) ) ;
#37763=ORIENTED_EDGE ( 'NONE', *, *, #153591, .F. ) ;
#37810=CIRCLE ( 'NONE', #162896, 0.09999999999999939493 ) ;
#37814=TOROIDAL_SURFACE ( 'NONE', #191940, 0.6000000000000009770, 0.1000000000000000056 ) ;
#37936=CARTESIAN_POINT ( 'NONE',  ( 21.05000000000000071, 0.03201369319893290072, -60.74115727646245233 ) ) ;
#37963=LINE ( 'NONE', #20974, #191783 ) ;
#37971=ORIENTED_EDGE ( 'NONE', *, *, #158669, .T. ) ;
#37977=ORIENTED_EDGE ( 'NONE', *, *, #17909, .F. ) ;
#38016=VERTEX_POINT ( 'NONE', #11845 ) ;
#38051=CARTESIAN_POINT ( 'NONE',  ( -21.05000000000000071, -11.48912529306489994, -97.60000000000005116 ) ) ;
#38067=CARTESIAN_POINT ( 'NONE',  ( 18.49999999999998934, 10.25000000001115552, -91.65000000000004832 ) ) ;
#38092=VERTEX_POINT ( 'NONE', #222685 ) ;
#38103=CARTESIAN_POINT ( 'NONE',  ( -20.85000000000000142, 7.120270961708750512, -104.1595630418393768 ) ) ;
#38126=ORIENTED_EDGE ( 'NONE', *, *, #222057, .F. ) ;
#38133=ORIENTED_EDGE ( 'NONE', *, *, #20837, .T. ) ;
#38174=ADVANCED_FACE ( 'NONE', ( #46613 ), #150406, .F. ) ;
#38196=ORIENTED_EDGE ( 'NONE', *, *, #183299, .F. ) ;
#38199=CARTESIAN_POINT ( 'NONE',  ( -21.14999999999999858, -11.64999999998884483, -69.90000000000004832 ) ) ;
#38220=EDGE_CURVE ( 'NONE', #82481, #48218, #237691, .T. ) ;
#38230=CARTESIAN_POINT ( 'NONE',  ( -21.56666275994539816, 1.115600667400684642E-11, -60.04263159310671938 ) ) ;
#38270=ORIENTED_EDGE ( 'NONE', *, *, #230460, .F. ) ;
#38306=AXIS2_PLACEMENT_3D ( 'NONE', #250109, #71493, #191454 ) ;
#38309=ORIENTED_EDGE ( 'NONE', *, *, #38822, .T. ) ;
#38321=AXIS2_PLACEMENT_3D ( 'NONE', #121010, #89536, #127400 ) ;
#38324=TOROIDAL_SURFACE ( 'NONE', #117435, 0.4000000000000003553, 0.1000000000000000056 ) ;
#38345=ORIENTED_EDGE ( 'NONE', *, *, #102652, .T. ) ;
#38381=FACE_OUTER_BOUND ( 'NONE', #171746, .T. ) ;
#38427=VECTOR ( 'NONE', #152992, 1000.000000000000000 ) ;
#38431=DIRECTION ( 'NONE',  ( 0.000000000000000000, 0.000000000000000000, -1.000000000000000000 ) ) ;
#38465=AXIS2_PLACEMENT_3D ( 'NONE', #6319, #247514, #48017 ) ;
#38467=AXIS2_PLACEMENT_3D ( 'NONE', #152453, #190286, #87301 ) ;
#38478=AXIS2_PLACEMENT_3D ( 'NONE', #3575, #139219, #217478 ) ;
#38539=CARTESIAN_POINT ( 'NONE',  ( -18.54148534481894117, 10.32532329027886320, -106.0699343018360139 ) ) ;
#38543=CIRCLE ( 'NONE', #146842, 4.049999999999998046 ) ;
#38589=EDGE_CURVE ( 'NONE', #109372, #93529, #238522, .T. ) ;
#38609=VECTOR ( 'NONE', #43291, 1000.000000000000000 ) ;
#38627=CARTESIAN_POINT ( 'NONE',  ( -20.64999999999999858, 7.150000000011155876, -79.35000000000005116 ) ) ;
#38637=VERTEX_POINT ( 'NONE', #80080 ) ;
#38644=AXIS2_PLACEMENT_3D ( 'NONE', #257303, #237803, #82540 ) ;
#38682=DIRECTION ( 'NONE',  ( 0.000000000000000000, -0.8660254037844383745, 0.5000000000000003331 ) ) ;
#38686=AXIS2_PLACEMENT_3D ( 'NONE', #55399, #39758, #20175 ) ;
#38705=CIRCLE ( 'NONE', #67920, 0.1000000000000013933 ) ;
#38707=VERTEX_POINT ( 'NONE', #219621 ) ;
#38723=ORIENTED_EDGE ( 'NONE', *, *, #88006, .T. ) ;
#38747=ADVANCED_FACE ( 'NONE', ( #43572 ), #218323, .T. ) ;
#38780=ADVANCED_FACE ( 'NONE', ( #10869 ), #66978, .F. ) ;
#38787=EDGE_CURVE ( 'NONE', #177157, #178346, #168705, .T. ) ;
#38803=CARTESIAN_POINT ( 'NONE',  ( -18.60000000000000142, -9.523954320741632174, -107.3820170568273795 ) ) ;
#38807=DIRECTION ( 'NONE',  ( 1.000000000000000000, 0.000000000000000000, 0.000000000000000000 ) ) ;
#38809=EDGE_CURVE ( 'NONE', #220045, #75643, #230314, .T. ) ;
#38810=EDGE_CURVE ( 'NONE', #256646, #113878, #76183, .T. ) ;
#38822=EDGE_CURVE ( 'NONE', #70992, #172403, #47143, .T. ) ;
#38878=AXIS2_PLACEMENT_3D ( 'NONE', #37665, #95044, #195460 ) ;
#38911=DIRECTION ( 'NONE',  ( 0.000000000000000000, 0.000000000000000000, -1.000000000000000000 ) ) ;
#38978=ORIENTED_EDGE ( 'NONE', *, *, #90164, .T. ) ;
#39030=AXIS2_PLACEMENT_3D ( 'NONE', #63997, #50825, #73027 ) ;
#39042=ORIENTED_EDGE ( 'NONE', *, *, #60726, .T. ) ;
#39046=FACE_OUTER_BOUND ( 'NONE', #207361, .T. ) ;
#39053=ORIENTED_EDGE ( 'NONE', *, *, #231761, .F. ) ;
#39099=ORIENTED_EDGE ( 'NONE', *, *, #3245, .F. ) ;
#39111=EDGE_CURVE ( 'NONE', #136961, #13313, #209426, .T. ) ;
#39121=DIRECTION ( 'NONE',  ( 1.000000000000000000, 0.000000000000000000, 0.000000000000000000 ) ) ;
#39133=CIRCLE ( 'NONE', #130677, 0.1000000000000000472 ) ;
#39137=CIRCLE ( 'NONE', #159933, 0.1000000000000028644 ) ;
#39159=VERTEX_POINT ( 'NONE', #28887 ) ;
#39165=CIRCLE ( 'NONE', #9910, 11.80000000000000426 ) ;
#39201=ORIENTED_EDGE ( 'NONE', *, *, #212387, .F. ) ;
#39214=ORIENTED_EDGE ( 'NONE', *, *, #11750, .T. ) ;
#39223=FACE_OUTER_BOUND ( 'NONE', #248037, .T. ) ;
#39248=DIRECTION ( 'NONE',  ( 0.000000000000000000, 0.000000000000000000, 1.000000000000000000 ) ) ;
#39251=CYLINDRICAL_SURFACE ( 'NONE', #112647, 0.5000000000000004441 ) ;
#39269=DIRECTION ( 'NONE',  ( 0.000000000000000000, 0.000000000000000000, -1.000000000000000000 ) ) ;
#39287=EDGE_CURVE ( 'NONE', #140297, #179663, #213890, .T. ) ;
#39305=DIRECTION ( 'NONE',  ( -0.000000000000000000, -0.1350103645451876666, 0.9908441862701600211 ) ) ;
#39312=AXIS2_PLACEMENT_3D ( 'NONE', #134144, #194155, #257898 ) ;
#39319=ORIENTED_EDGE ( 'NONE', *, *, #201924, .T. ) ;
#39342=EDGE_LOOP ( 'NONE', ( #252368, #91867, #54968 ) ) ;
#39355=CARTESIAN_POINT ( 'NONE',  ( -20.94999027547553894, 10.29326151435327219, -105.9592822510415431 ) ) ;
#39365=LINE ( 'NONE', #121471, #30647 ) ;
#39367=CIRCLE ( 'NONE', #218371, 0.5000000000000004441 ) ;
#39372=EDGE_CURVE ( 'NONE', #187441, #248700, #5617, .T. ) ;
#39402=FACE_OUTER_BOUND ( 'NONE', #165975, .T. ) ;
#39408=CARTESIAN_POINT ( 'NONE',  ( -23.25000000000000000, 2.600000000011156054, -80.22462192276213955 ) ) ;
#39417=ORIENTED_EDGE ( 'NONE', *, *, #42636, .F. ) ;
#39429=EDGE_CURVE ( 'NONE', #72835, #189461, #22428, .T. ) ;
#39440=EDGE_CURVE ( 'NONE', #55413, #196163, #161648, .T. ) ;
#39445=CARTESIAN_POINT ( 'NONE',  ( 18.45139536634707511, -9.486081720270043149, -107.1405116178107164 ) ) ;
#39485=EDGE_CURVE ( 'NONE', #24624, #257729, #237314, .T. ) ;
#39515=VERTEX_POINT ( 'NONE', #205874 ) ;
#39516=AXIS2_PLACEMENT_3D ( 'NONE', #212683, #34075, #8066 ) ;
#39555=VERTEX_POINT ( 'NONE', #144605 ) ;
#39570=ORIENTED_EDGE ( 'NONE', *, *, #155723, .T. ) ;
#39578=ADVANCED_FACE ( 'NONE', ( #65084 ), #190576, .T. ) ;
#39584=ORIENTED_EDGE ( 'NONE', *, *, #182222, .F. ) ;
#39590=ORIENTED_EDGE ( 'NONE', *, *, #43194, .T. ) ;
#39592=EDGE_CURVE ( 'NONE', #29887, #151973, #248835, .T. ) ;
#39617=ORIENTED_EDGE ( 'NONE', *, *, #216232, .T. ) ;
#39636=DIRECTION ( 'NONE',  ( 0.000000000000000000, 1.000000000000000000, 0.000000000000000000 ) ) ;
#39642=CARTESIAN_POINT ( 'NONE',  ( -20.94999999999999929, -11.48912529306489994, -97.60000000000005116 ) ) ;
#39650=EDGE_LOOP ( 'NONE', ( #14279, #155882, #148205, #197748 ) ) ;
#39668=CARTESIAN_POINT ( 'NONE',  ( -21.55000000000000071, 7.350000000011155166, -79.25000000000004263 ) ) ;
#39674=DIRECTION ( 'NONE',  ( 0.000000000000000000, 0.000000000000000000, -1.000000000000000000 ) ) ;
#39695=VERTEX_POINT ( 'NONE', #128924 ) ;
#39747=DIRECTION ( 'NONE',  ( 0.000000000000000000, 0.000000000000000000, -1.000000000000000000 ) ) ;
#39758=DIRECTION ( 'NONE',  ( -0.000000000000000000, -0.000000000000000000, 1.000000000000000000 ) ) ;
#39771=EDGE_CURVE ( 'NONE', #31018, #116760, #94677, .T. ) ;
#39792=VERTEX_POINT ( 'NONE', #102255 ) ;
#39841=DIRECTION ( 'NONE',  ( 0.000000000000000000, 0.8660254037844352659, -0.5000000000000058842 ) ) ;
#39855=EDGE_CURVE ( 'NONE', #17165, #237745, #37530, .T. ) ;
#39895=AXIS2_PLACEMENT_3D ( 'NONE', #30207, #191866, #75748 ) ;
#39901=DIRECTION ( 'NONE',  ( 0.000000000000000000, 0.000000000000000000, -1.000000000000000000 ) ) ;
#39947=EDGE_CURVE ( 'NONE', #39515, #125649, #210404, .T. ) ;
#39964=VERTEX_POINT ( 'NONE', #246932 ) ;
#39968=DIRECTION ( 'NONE',  ( 0.000000000000000000, 0.000000000000000000, -1.000000000000000000 ) ) ;
#39976=VERTEX_POINT ( 'NONE', #27932 ) ;
#39985=FACE_OUTER_BOUND ( 'NONE', #187477, .T. ) ;
#39990=ADVANCED_FACE ( 'NONE', ( #207851 ), #209099, .F. ) ;
#39991=EDGE_CURVE ( 'NONE', #51884, #241599, #253081, .T. ) ;
#39993=AXIS2_PLACEMENT_3D ( 'NONE', #129786, #188475, #226298 ) ;
#39996=CIRCLE ( 'NONE', #19109, 0.1000000000000008937 ) ;
#40014=CIRCLE ( 'NONE', #135826, 0.1000000000000028644 ) ;
#40125=VERTEX_POINT ( 'NONE', #257160 ) ;
#40133=AXIS2_PLACEMENT_3D ( 'NONE', #29310, #248316, #5829 ) ;
#40142=PRODUCT_DEFINITION_CONTEXT ( 'detailed design', #232514, 'design' ) ;
#40165=PLANE ( 'NONE',  #44674 ) ;
#40213=DIRECTION ( 'NONE',  ( 0.000000000000000000, 0.9999631594459053030, 0.008583690987162899758 ) ) ;
#40254=CARTESIAN_POINT ( 'NONE',  ( 20.94999999999999574, 1.115600667400684642E-11, -67.00000000000004263 ) ) ;
#40286=TOROIDAL_SURFACE ( 'NONE', #223571, 4.099999999999999645, 0.1000000000000000056 ) ;
#40296=DIRECTION ( 'NONE',  ( -0.000000000000000000, 1.000000000000000000, -0.000000000000000000 ) ) ;
#40313=FACE_OUTER_BOUND ( 'NONE', #242037, .T. ) ;
#40318=FACE_OUTER_BOUND ( 'NONE', #93998, .T. ) ;
#40323=CARTESIAN_POINT ( 'NONE',  ( 22.45301702632625762, 0.01521087972134078925, -55.35020777573965489 ) ) ;
#40339=DIRECTION ( 'NONE',  ( -1.000000000000000000, -0.000000000000000000, -0.000000000000000000 ) ) ;
#40376=VECTOR ( 'NONE', #57920, 1000.000000000000000 ) ;
#40382=CARTESIAN_POINT ( 'NONE',  ( -21.29999999999995808, 1.115650265596050101E-11, -62.95000000000004547 ) ) ;
#40386=DIRECTION ( 'NONE',  ( 0.000000000000000000, 0.2605042016806715099, 0.9654727137038706664 ) ) ;
#40423=ADVANCED_FACE ( 'NONE', ( #194395 ), #92691, .F. ) ;
#40432=EDGE_LOOP ( 'NONE', ( #107881, #120484, #158109, #224988 ) ) ;
#40445=CARTESIAN_POINT ( 'NONE',  ( 22.57320508075687115, 11.75000000001115552, -67.00000000000004263 ) ) ;
#40457=DIRECTION ( 'NONE',  ( -7.304098846218134667E-16, -1.000000000000000000, 0.000000000000000000 ) ) ;
#40499=AXIS2_PLACEMENT_3D ( 'NONE', #235531, #171753, #114310 ) ;
#40512=CARTESIAN_POINT ( 'NONE',  ( -23.15000000000000213, 11.65000000001115588, -55.25000000000004974 ) ) ;
#40523=DIRECTION ( 'NONE',  ( -3.265361837132813093E-16, 1.000000000000000000, 0.000000000000000000 ) ) ;
#40526=ORIENTED_EDGE ( 'NONE', *, *, #247156, .T. ) ;
#40539=VECTOR ( 'NONE', #8353, 1000.000000000000000 ) ;
#40542=LINE ( 'NONE', #217826, #131062 ) ;
#40662=ORIENTED_EDGE ( 'NONE', *, *, #1169, .T. ) ;
#40671=LINE ( 'NONE', #101855, #110898 ) ;
#40688=ORIENTED_EDGE ( 'NONE', *, *, #67321, .T. ) ;
#40703=CARTESIAN_POINT ( 'NONE',  ( 20.94999999999999929, -9.499999999988848032, -76.89396912265249284 ) ) ;
#40794=CIRCLE ( 'NONE', #244739, 4.000000000000003553 ) ;
#40836=DIRECTION ( 'NONE',  ( 0.000000000000000000, 0.000000000000000000, -1.000000000000000000 ) ) ;
#40841=CARTESIAN_POINT ( 'NONE',  ( -20.94999999999999929, -0.2561057920810652089, -66.96510355832775474 ) ) ;
#40843=AXIS2_PLACEMENT_3D ( 'NONE', #231769, #99591, #137446 ) ;
#40852=ORIENTED_EDGE ( 'NONE', *, *, #184710, .T. ) ;
#40867=CARTESIAN_POINT ( 'NONE',  ( -18.59999999999999787, 1.835341550235567887, -78.55515129256302487 ) ) ;
#40883=ADVANCED_FACE ( 'NONE', ( #251460 ), #229352, .T. ) ;
#40884=ORIENTED_EDGE ( 'NONE', *, *, #92717, .T. ) ;
#40896=ORIENTED_EDGE ( 'NONE', *, *, #103625, .T. ) ;
#40907=TOROIDAL_SURFACE ( 'NONE', #232440, 7.800000000000000711, 0.1000000000000000056 ) ;
#40925=FACE_OUTER_BOUND ( 'NONE', #97657, .T. ) ;
#40951=DIRECTION ( 'NONE',  ( -1.836970198721029934E-16, 1.000000000000000000, 0.000000000000000000 ) ) ;
#40959=CARTESIAN_POINT ( 'NONE',  ( 23.24999999999999645, 1.115600667400684642E-11, -100.5000000000000426 ) ) ;
#40974=EDGE_CURVE ( 'NONE', #208826, #88741, #2255, .T. ) ;
#40990=AXIS2_PLACEMENT_3D ( 'NONE', #38051, #117558, #232398 ) ;
#41000=CARTESIAN_POINT ( 'NONE',  ( -20.85000000000000142, 7.021664781911246322, -104.1335654018973287 ) ) ;
#41011=ORIENTED_EDGE ( 'NONE', *, *, #105237, .F. ) ;
#41014=CARTESIAN_POINT ( 'NONE',  ( -20.94999999999999929, 1.115600667400684642E-11, -88.80000000000003979 ) ) ;
#41018=CARTESIAN_POINT ( 'NONE',  ( -23.25000000000000000, -11.74999999998884448, -100.5000000000000426 ) ) ;
#41067=ORIENTED_EDGE ( 'NONE', *, *, #3109, .F. ) ;
#41085=CARTESIAN_POINT ( 'NONE',  ( 23.14999999999999858, 1.115600667400684642E-11, -100.5000000000000426 ) ) ;
#41112=EDGE_CURVE ( 'NONE', #238489, #51379, #166376, .T. ) ;
#41128=CARTESIAN_POINT ( 'NONE',  ( -18.56579813702276027, 10.33025634372637569, -106.0870929282639423 ) ) ;
#41158=CARTESIAN_POINT ( 'NONE',  ( 21.00000000000000000, 9.750000000011153745, -79.25000000000004263 ) ) ;
#41184=CARTESIAN_POINT ( 'NONE',  ( 18.49999999999999289, 10.29270135741298731, -105.9573618871519756 ) ) ;
#41225=DIRECTION ( 'NONE',  ( 1.000000000000000000, 0.000000000000000000, 0.000000000000000000 ) ) ;
#41242=EDGE_CURVE ( 'NONE', #211645, #135773, #220526, .T. ) ;
#41263=CARTESIAN_POINT ( 'NONE',  ( -23.15000000000000213, 11.65000000001115588, -79.15000000000004832 ) ) ;
#41270=CIRCLE ( 'NONE', #124630, 0.1000000000000028644 ) ;
#41299=DIRECTION ( 'NONE',  ( 0.000000000000000000, 0.000000000000000000, 1.000000000000000000 ) ) ;
#41314=CARTESIAN_POINT ( 'NONE',  ( -20.54999999999999716, 1.115600667400684642E-11, -100.5000000000000426 ) ) ;
#41362=EDGE_CURVE ( 'NONE', #129546, #169137, #149613, .T. ) ;
#41377=ORIENTED_EDGE ( 'NONE', *, *, #24989, .T. ) ;
#41397=CARTESIAN_POINT ( 'NONE',  ( -22.49917693094574389, 0.08522996423282767908, -55.35020421546937541 ) ) ;
#41401=ORIENTED_EDGE ( 'NONE', *, *, #92717, .F. ) ;
#41414=EDGE_CURVE ( 'NONE', #104099, #95314, #9393, .T. ) ;
#41426=CARTESIAN_POINT ( 'NONE',  ( -21.05000000000000071, 1.116121084443477685E-11, -69.90000000000003411 ) ) ;
#41430=EDGE_CURVE ( 'NONE', #151973, #121203, #221003, .T. ) ;
#41439=CARTESIAN_POINT ( 'NONE',  ( -20.64999999999999858, 4.350000000011156054, -79.35000000000005116 ) ) ;
#41484=CARTESIAN_POINT ( 'NONE',  ( -23.15000000000000213, 2.000000000011154189, -80.22462192276213955 ) ) ;
#41486=CARTESIAN_POINT ( 'NONE',  ( 18.59999999999999787, -1.835341550213255957, -78.55515129256302487 ) ) ;
#41555=ORIENTED_EDGE ( 'NONE', *, *, #148810, .F. ) ;
#41574=CARTESIAN_POINT ( 'NONE',  ( 18.59999999999999787, -1.835341550213255957, -78.65515129256301918 ) ) ;
#41576=TOROIDAL_SURFACE ( 'NONE', #58083, 0.2000000000000000111, 0.1000000000000000056 ) ;
#41595=CARTESIAN_POINT ( 'NONE',  ( 22.49436431346199683, 0.06690352973341695542, -55.35004905234658423 ) ) ;
#41605=CARTESIAN_POINT ( 'NONE',  ( -20.64999999999999858, 1.940186915899004161, -87.67088078894671810 ) ) ;
#41625=EDGE_LOOP ( 'NONE', ( #220450, #24008, #129517 ) ) ;
#41652=AXIS2_PLACEMENT_3D ( 'NONE', #103816, #187250, #167695 ) ;
#41657=DIRECTION ( 'NONE',  ( -0.000000000000000000, 0.1298341882520022694, 0.9915357197604853789 ) ) ;
#41663=CARTESIAN_POINT ( 'NONE',  ( 20.85000000000000142, -1.135018845899022466, -108.2169768834323662 ) ) ;
#41667=CYLINDRICAL_SURFACE ( 'NONE', #157778, 2.000000000000001776 ) ;
#41686=ADVANCED_FACE ( 'NONE', ( #239967 ), #62611, .F. ) ;
#41710=ORIENTED_EDGE ( 'NONE', *, *, #78112, .F. ) ;
#41730=CARTESIAN_POINT ( 'NONE',  ( -20.64999999999999858, 2.000000000011154189, -87.77537807723795993 ) ) ;
#41738=EDGE_LOOP ( 'NONE', ( #113672, #199204, #224684 ) ) ;
#41749=DIRECTION ( 'NONE',  ( -1.000000000000000000, 0.000000000000000000, 0.000000000000000000 ) ) ;
#41752=EDGE_CURVE ( 'NONE', #145626, #23243, #247659, .T. ) ;
#41780=FACE_OUTER_BOUND ( 'NONE', #6527, .T. ) ;
#41796=EDGE_CURVE ( 'NONE', #16604, #76466, #129005, .T. ) ;
#41826=ORIENTED_EDGE ( 'NONE', *, *, #39111, .T. ) ;
#41841=ORIENTED_EDGE ( 'NONE', *, *, #204225, .F. ) ;
#41853=ORIENTED_EDGE ( 'NONE', *, *, #85058, .T. ) ;
#41899=CARTESIAN_POINT ( 'NONE',  ( -21.05000000000000071, 6.258316057343178862, -66.93429838967794865 ) ) ;
#41904=EDGE_CURVE ( 'NONE', #168456, #163852, #95769, .T. ) ;
#41922=DIRECTION ( 'NONE',  ( 1.000000000000000000, 0.000000000000000000, 0.000000000000000000 ) ) ;
#41924=DIRECTION ( 'NONE',  ( 0.000000000000000000, 0.1568667991644863147, -0.9876197685951252359 ) ) ;
#41943=AXIS2_PLACEMENT_3D ( 'NONE', #122315, #61042, #181016 ) ;
#42017=DIRECTION ( 'NONE',  ( 1.000000000000000000, -0.000000000000000000, -0.000000000000000000 ) ) ;
#42031=DIRECTION ( 'NONE',  ( -1.000000000000000000, -0.000000000000000000, -0.000000000000000000 ) ) ;
#42038=ADVANCED_BREP_SHAPE_REPRESENTATION ( '', ( #21812, #2425 ), #94000 ) ;
#42073=EDGE_CURVE ( 'NONE', #134077, #248044, #130671, .T. ) ;
#42088=VECTOR ( 'NONE', #133653, 1000.000000000000114 ) ;
#42139=DIRECTION ( 'NONE',  ( 0.000000000000000000, 0.000000000000000000, -1.000000000000000000 ) ) ;
#42180=FACE_OUTER_BOUND ( 'NONE', #216843, .T. ) ;
#42191=LINE ( 'NONE', #104679, #114426 ) ;
#42197=CARTESIAN_POINT ( 'NONE',  ( -18.50000000000000000, 1.637172712981535883, -78.58215336547205254 ) ) ;
#42220=DIRECTION ( 'NONE',  ( 0.000000000000000000, -0.1455152366551522025, -0.9893560106964505163 ) ) ;
#42238=LINE ( 'NONE', #124344, #173586 ) ;
#42243=EDGE_CURVE ( 'NONE', #78058, #39695, #37164, .T. ) ;
#42247=CARTESIAN_POINT ( 'NONE',  ( 20.94999999999999574, 8.926614585098251453, -75.47168301922316402 ) ) ;
#42252=DIRECTION ( 'NONE',  ( -1.000000000000000000, -0.000000000000000000, -0.000000000000000000 ) ) ;
#42263=CARTESIAN_POINT ( 'NONE',  ( 18.49999999999999645, 1.115600667400684642E-11, -67.00000000000004263 ) ) ;
#42270=CARTESIAN_POINT ( 'NONE',  ( -20.64999999999999858, 1.115600667400684642E-11, -98.50000000000004263 ) ) ;
#42274=CARTESIAN_POINT ( 'NONE',  ( 21.14999999999999858, 6.650000000011155876, -79.15000000000004832 ) ) ;
#42288=CARTESIAN_POINT ( 'NONE',  ( 20.94999999999999929, 1.115600667400684642E-11, -67.00000000000004263 ) ) ;
#42289=CIRCLE ( 'NONE', #196395, 12.87499999999999822 ) ;
#42290=FACE_OUTER_BOUND ( 'NONE', #34264, .T. ) ;
#42296=CARTESIAN_POINT ( 'NONE',  ( 22.39999999999999503, 11.65000000001116298, -67.00000000000004263 ) ) ;
#42326=CARTESIAN_POINT ( 'NONE',  ( 18.59999999999999076, 6.450000000011156587, -88.15000000000004832 ) ) ;
#42328=CARTESIAN_POINT ( 'NONE',  ( -20.85000000000000142, -11.64999999998884483, -97.60000000000005116 ) ) ;
#42329=ORIENTED_EDGE ( 'NONE', *, *, #224395, .F. ) ;
#42376=CARTESIAN_POINT ( 'NONE',  ( 20.94999999999999574, -11.74999999998883560, -70.10000000000005116 ) ) ;
#42421=AXIS2_PLACEMENT_3D ( 'NONE', #123449, #42620, #243382 ) ;
#42432=CARTESIAN_POINT ( 'NONE',  ( -23.25000000000000000, 1.115600667400684642E-11, -79.77500000000003411 ) ) ;
#42434=DIRECTION ( 'NONE',  ( 0.000000000000000000, 0.000000000000000000, 1.000000000000000000 ) ) ;
#42464=ORIENTED_EDGE ( 'NONE', *, *, #139361, .F. ) ;
#42473=EDGE_CURVE ( 'NONE', #215522, #224607, #207873, .T. ) ;
#42477=ORIENTED_EDGE ( 'NONE', *, *, #209871, .F. ) ;
#42480=ORIENTED_EDGE ( 'NONE', *, *, #112968, .T. ) ;
#42482=ORIENTED_EDGE ( 'NONE', *, *, #249228, .F. ) ;
#42501=ORIENTED_EDGE ( 'NONE', *, *, #65877, .F. ) ;
#42527=CARTESIAN_POINT ( 'NONE',  ( 18.52928932188133970, 10.27928932189249878, -91.70857864376273483 ) ) ;
#42538=ORIENTED_EDGE ( 'NONE', *, *, #8267, .F. ) ;
#42544=CARTESIAN_POINT ( 'NONE',  ( 23.14999999999999858, 1.115600667400684642E-11, -100.5000000000000426 ) ) ;
#42572=ORIENTED_EDGE ( 'NONE', *, *, #141615, .F. ) ;
#42573=CARTESIAN_POINT ( 'NONE',  ( 21.93340585971920120, 7.324147022865871826, -67.00000000000004263 ) ) ;
#42576=CARTESIAN_POINT ( 'NONE',  ( 20.94999999999999929, 5.000000000011153745, -79.40526601891313874 ) ) ;
#42591=( BOUNDED_CURVE ( )  B_SPLINE_CURVE ( 3, ( #23004, #42527, #204159, #65953 ),
 .UNSPECIFIED., .F., .F. ) 
 B_SPLINE_CURVE_WITH_KNOTS ( ( 4, 4 ),
 ( 3.141592653589793116, 4.712388980384689674 ),
 .UNSPECIFIED. ) 
 CURVE ( )  GEOMETRIC_REPRESENTATION_ITEM ( )  RATIONAL_B_SPLINE_CURVE ( ( 1.000000000000000000, 0.8047378541243649375, 0.8047378541243649375, 1.000000000000000000 ) ) 
 REPRESENTATION_ITEM ( '' )  );
#42608=DIRECTION ( 'NONE',  ( 1.000000000000000000, 0.000000000000000000, 0.000000000000000000 ) ) ;
#42620=DIRECTION ( 'NONE',  ( -0.000000000000000000, -0.000000000000000000, 1.000000000000000000 ) ) ;
#42636=EDGE_CURVE ( 'NONE', #111464, #49762, #220506, .T. ) ;
#42639=CARTESIAN_POINT ( 'NONE',  ( -22.00411653962179415, 7.253442868381127617, -66.90096189419944039 ) ) ;
#42659=CIRCLE ( 'NONE', #242568, 11.70000000000000284 ) ;
#42671=DIRECTION ( 'NONE',  ( -1.000000000000000000, 0.000000000000000000, 0.000000000000000000 ) ) ;
#42690=CARTESIAN_POINT ( 'NONE',  ( 23.14999999999999858, 5.000000000011153745, -88.09473398108696074 ) ) ;
#42697=FACE_OUTER_BOUND ( 'NONE', #50899, .T. ) ;
#42762=CARTESIAN_POINT ( 'NONE',  ( -22.39999999999999858, -0.09999999998884338825, -55.35042919245524473 ) ) ;
#42763=CIRCLE ( 'NONE', #213446, 0.1000000000000017958 ) ;
#42766=ORIENTED_EDGE ( 'NONE', *, *, #147035, .F. ) ;
#42787=CARTESIAN_POINT ( 'NONE',  ( -20.64999999999999858, 1.115600667400684642E-11, -100.5000000000000426 ) ) ;
#42800=CARTESIAN_POINT ( 'NONE',  ( -18.50000000000000000, 11.65000000001115232, -79.15000000000003411 ) ) ;
#42803=ORIENTED_EDGE ( 'NONE', *, *, #20863, .T. ) ;
#42841=ORIENTED_EDGE ( 'NONE', *, *, #190632, .F. ) ;
#42859=ORIENTED_EDGE ( 'NONE', *, *, #79042, .F. ) ;
#42866=DIRECTION ( 'NONE',  ( 0.000000000000000000, 0.000000000000000000, -1.000000000000000000 ) ) ;
#42908=EDGE_CURVE ( 'NONE', #237980, #100973, #246210, .T. ) ;
#42917=ORIENTED_EDGE ( 'NONE', *, *, #155150, .T. ) ;
#42934=CARTESIAN_POINT ( 'NONE',  ( -23.25000000000000000, 1.115600667400684642E-11, -100.5000000000000426 ) ) ;
#42941=ORIENTED_EDGE ( 'NONE', *, *, #224877, .T. ) ;
#42965=DIRECTION ( 'NONE',  ( 1.000000000000000000, 0.000000000000000000, -0.000000000000000000 ) ) ;
#42973=CIRCLE ( 'NONE', #155427, 0.2000000000000005107 ) ;
#42985=DIRECTION ( 'NONE',  ( -0.000000000000000000, -1.000000000000000000, -0.000000000000000000 ) ) ;
#42999=CARTESIAN_POINT ( 'NONE',  ( 21.14999999999999858, -11.74999999998884448, -79.25000000000004263 ) ) ;
#43018=ORIENTED_EDGE ( 'NONE', *, *, #121153, .F. ) ;
#43056=AXIS2_PLACEMENT_3D ( 'NONE', #211133, #16803, #131591 ) ;
#43083=AXIS2_PLACEMENT_3D ( 'NONE', #56453, #134703, #96848 ) ;
#43130=ORIENTED_EDGE ( 'NONE', *, *, #118147, .F. ) ;
#43138=DIRECTION ( 'NONE',  ( 1.000000000000000000, 1.836970198721029934E-16, 3.186635328391151676E-31 ) ) ;
#43151=AXIS2_PLACEMENT_3D ( 'NONE', #201535, #97262, #60725 ) ;
#43180=EDGE_CURVE ( 'NONE', #70992, #59145, #122106, .T. ) ;
#43194=EDGE_CURVE ( 'NONE', #192087, #151216, #100021, .T. ) ;
#43201=DIRECTION ( 'NONE',  ( 0.000000000000000000, -0.1350103645451876666, 0.9908441862701600211 ) ) ;
#43228=CARTESIAN_POINT ( 'NONE',  ( -23.15000000000000213, 1.115600667400684642E-11, -100.5000000000000426 ) ) ;
#43237=CARTESIAN_POINT ( 'NONE',  ( 20.94999999999999574, -1.835341550213255957, -78.55515129256302487 ) ) ;
#43291=DIRECTION ( 'NONE',  ( 0.000000000000000000, -1.000000000000000000, 0.000000000000000000 ) ) ;
#43295=VERTEX_POINT ( 'NONE', #230178 ) ;
#43328=DIRECTION ( 'NONE',  ( 0.000000000000000000, -0.8660254037844411501, -0.4999999999999956146 ) ) ;
#43345=DIRECTION ( 'NONE',  ( 4.239556034732056743E-17, -0.1298341882520022694, -0.9915357197604852679 ) ) ;
#43393=ORIENTED_EDGE ( 'NONE', *, *, #99886, .F. ) ;
#43401=ORIENTED_EDGE ( 'NONE', *, *, #184762, .T. ) ;
#43419=CARTESIAN_POINT ( 'NONE',  ( -20.64999999999999858, 1.115600667400684642E-11, -102.4000000000000483 ) ) ;
#43420=AXIS2_PLACEMENT_3D ( 'NONE', #183032, #245571, #83868 ) ;
#43431=ORIENTED_EDGE ( 'NONE', *, *, #102538, .T. ) ;
#43459=DIRECTION ( 'NONE',  ( 0.000000000000000000, 8.881784197000778021E-16, -1.000000000000000000 ) ) ;
#43492=ADVANCED_FACE ( 'NONE', ( #16299 ), #137479, .T. ) ;
#43524=EDGE_CURVE ( 'NONE', #59101, #38092, #195935, .T. ) ;
#43527=EDGE_LOOP ( 'NONE', ( #81345, #161335, #29279 ) ) ;
#43541=PLANE ( 'NONE',  #156888 ) ;
#43552=CARTESIAN_POINT ( 'NONE',  ( -23.15000000000000213, 2.000000000011154189, -87.27537807723794572 ) ) ;
#43572=FACE_OUTER_BOUND ( 'NONE', #59838, .T. ) ;
#43578=DIRECTION ( 'NONE',  ( -6.938893903907222856E-15, 1.000000000000000000, 0.000000000000000000 ) ) ;
#43645=EDGE_CURVE ( 'NONE', #209971, #56894, #171030, .T. ) ;
#43653=ORIENTED_EDGE ( 'NONE', *, *, #200155, .T. ) ;
#43664=FACE_OUTER_BOUND ( 'NONE', #256558, .T. ) ;
#43673=CARTESIAN_POINT ( 'NONE',  ( 22.39999999999999503, -0.1008583690875579364, -55.25043287651065782 ) ) ;
#43679=FACE_OUTER_BOUND ( 'NONE', #166664, .T. ) ;
#43692=DIRECTION ( 'NONE',  ( 1.000000000000000000, -0.000000000000000000, -0.000000000000000000 ) ) ;
#43700=ADVANCED_FACE ( 'NONE', ( #109916 ), #180457, .F. ) ;
#43730=CIRCLE ( 'NONE', #156188, 0.1000000000000028644 ) ;
#43758=DIRECTION ( 'NONE',  ( 0.000000000000000000, 0.000000000000000000, 1.000000000000000000 ) ) ;
#43776=AXIS2_PLACEMENT_3D ( 'NONE', #201106, #22498, #101976 ) ;
#43789=EDGE_CURVE ( 'NONE', #78058, #58451, #192057, .T. ) ;
#43800=CARTESIAN_POINT ( 'NONE',  ( -21.07928932188134041, 0.09889514566555068775, -60.67148334360675221 ) ) ;
#43808=CARTESIAN_POINT ( 'NONE',  ( 21.05000000000000426, 10.72371710471867878, -74.59441739161313478 ) ) ;
#43823=LINE ( 'NONE', #142890, #247477 ) ;
#43837=ORIENTED_EDGE ( 'NONE', *, *, #80950, .F. ) ;
#43845=CARTESIAN_POINT ( 'NONE',  ( -22.57320508075687115, 11.65000000001115588, -67.00000000000007105 ) ) ;
#43849=ORIENTED_EDGE ( 'NONE', *, *, #28189, .F. ) ;
#43873=DIRECTION ( 'NONE',  ( -1.000000000000000000, 0.000000000000000000, 0.000000000000000000 ) ) ;
#43880=AXIS2_PLACEMENT_3D ( 'NONE', #51301, #248253, #245684 ) ;
#43890=CARTESIAN_POINT ( 'NONE',  ( -20.64999999999999858, 1.115600667400684642E-11, -100.5000000000000426 ) ) ;
#43910=CIRCLE ( 'NONE', #256223, 0.09999999999999939493 ) ;
#43923=CARTESIAN_POINT ( 'NONE',  ( -21.53699400380687834, 6.787711793201953725, -67.00000000000004263 ) ) ;
#43933=AXIS2_PLACEMENT_3D ( 'NONE', #223002, #204720, #26114 ) ;
#43938=CARTESIAN_POINT ( 'NONE',  ( -22.47120815636973745, 0.02890382191504723905, -55.35006801124654885 ) ) ;
#43950=DIRECTION ( 'NONE',  ( 1.000000000000000000, 3.265361837132813093E-16, -0.000000000000000000 ) ) ;
#43964=DIRECTION ( 'NONE',  ( 0.000000000000000000, 0.000000000000000000, -1.000000000000000000 ) ) ;
#44064=EDGE_CURVE ( 'NONE', #152197, #53634, #125371, .T. ) ;
#44076=DIRECTION ( 'NONE',  ( 0.000000000000000000, 1.000000000000000000, 0.000000000000000000 ) ) ;
#44104=CARTESIAN_POINT ( 'NONE',  ( 18.48413544395651442, -9.664304033616561540, -107.1831049930384125 ) ) ;
#44109=CARTESIAN_POINT ( 'NONE',  ( 21.09610168723073187, 0.03358950690265036926, -60.62104428477527307 ) ) ;
#44111=ORIENTED_EDGE ( 'NONE', *, *, #224031, .T. ) ;
#44133=DIRECTION ( 'NONE',  ( 1.000000000000000000, -0.000000000000000000, -0.000000000000000000 ) ) ;
#44149=CIRCLE ( 'NONE', #77266, 0.09999999999999939493 ) ;
#44153=AXIS2_PLACEMENT_3D ( 'NONE', #123539, #25720, #64833 ) ;
#44154=ORIENTED_EDGE ( 'NONE', *, *, #85818, .F. ) ;
#44157=DIRECTION ( 'NONE',  ( 1.000000000000000000, -0.000000000000000000, -0.000000000000000000 ) ) ;
#44169=CARTESIAN_POINT ( 'NONE',  ( -22.49999999999999645, 11.74956712350054744, -66.89914163090132604 ) ) ;
#44170=CIRCLE ( 'NONE', #161048, 0.09999999999999939493 ) ;
#44220=ORIENTED_EDGE ( 'NONE', *, *, #206958, .T. ) ;
#44226=CARTESIAN_POINT ( 'NONE',  ( -20.64999999999999858, 1.115600667400684642E-11, -79.97500000000005116 ) ) ;
#44227=CIRCLE ( 'NONE', #98328, 0.1000000000000028644 ) ;
#44244=LINE ( 'NONE', #88466, #228589 ) ;
#44263=FACE_OUTER_BOUND ( 'NONE', #241364, .T. ) ;
#44284=LINE ( 'NONE', #125108, #66420 ) ;
#44307=DIRECTION ( 'NONE',  ( 0.000000000000000000, 0.000000000000000000, 1.000000000000000000 ) ) ;
#44308=CARTESIAN_POINT ( 'NONE',  ( 20.84999999999999787, 11.75000000001116085, -93.58085275404134507 ) ) ;
#44340=ORIENTED_EDGE ( 'NONE', *, *, #173932, .T. ) ;
#44351=TOROIDAL_SURFACE ( 'NONE', #210932, 12.77499999999999858, 0.1000000000000000056 ) ;
#44373=AXIS2_PLACEMENT_3D ( 'NONE', #247367, #144399, #67451 ) ;
#44375=CARTESIAN_POINT ( 'NONE',  ( -20.54999999999999361, 11.65000000001115232, -88.35000000000003695 ) ) ;
#44418=EDGE_LOOP ( 'NONE', ( #244373, #105267, #123980, #77305 ) ) ;
#44425=CARTESIAN_POINT ( 'NONE',  ( -23.25000000000000000, -1.851617760457748618, -112.1031897196037050 ) ) ;
#44454=DIRECTION ( 'NONE',  ( 0.000000000000000000, 0.000000000000000000, -1.000000000000000000 ) ) ;
#44480=CARTESIAN_POINT ( 'NONE',  ( -22.59999999999999787, 1.115600667400684642E-11, -67.00000000000004263 ) ) ;
#44489=DIRECTION ( 'NONE',  ( 0.000000000000000000, 0.000000000000000000, 1.000000000000000000 ) ) ;
#44497=CARTESIAN_POINT ( 'NONE',  ( -18.50000000000000000, 5.950000000011100632, -77.30570230503489881 ) ) ;
#44498=DIRECTION ( 'NONE',  ( 1.000000000000000000, 0.000000000000000000, 0.000000000000000000 ) ) ;
#44526=DIRECTION ( 'NONE',  ( 0.000000000000000000, -0.3738317757009345654, 0.9274965247785492695 ) ) ;
#44532=DIRECTION ( 'NONE',  ( 1.000000000000000000, -0.000000000000000000, -0.000000000000000000 ) ) ;
#44553=CARTESIAN_POINT ( 'NONE',  ( 23.14999999999999858, 5.600000000011153389, -88.09473398108696074 ) ) ;
#44604=ORIENTED_EDGE ( 'NONE', *, *, #231747, .T. ) ;
#44630=CIRCLE ( 'NONE', #202292, 0.1000000000000028644 ) ;
#44633=DIRECTION ( 'NONE',  ( -3.265361837132813093E-16, 1.000000000000000000, -0.000000000000000000 ) ) ;
#44638=EDGE_CURVE ( 'NONE', #12719, #203190, #214501, .T. ) ;
#44645=VERTEX_POINT ( 'NONE', #217054 ) ;
#44654=VERTEX_POINT ( 'NONE', #73743 ) ;
#44674=AXIS2_PLACEMENT_3D ( 'NONE', #60969, #140498, #220055 ) ;
#44682=CIRCLE ( 'NONE', #73926, 0.1999999999999987899 ) ;
#44695=ORIENTED_EDGE ( 'NONE', *, *, #116042, .F. ) ;
#44703=AXIS2_PLACEMENT_3D ( 'NONE', #143507, #126522, #87373 ) ;
#44731=CARTESIAN_POINT ( 'NONE',  ( -23.25000000000000000, 1.115600667400684642E-11, -67.00000000000004263 ) ) ;
#44733=VECTOR ( 'NONE', #121460, 1000.000000000000000 ) ;
#44743=ORIENTED_EDGE ( 'NONE', *, *, #30093, .T. ) ;
#44768=CARTESIAN_POINT ( 'NONE',  ( 23.14999999999999858, 5.500000000011153745, -88.09473398108696074 ) ) ;
#44776=ORIENTED_EDGE ( 'NONE', *, *, #38220, .T. ) ;
#44798=B_SPLINE_CURVE_WITH_KNOTS ( 'NONE', 3,
 ( #192600, #148336, #49229, #252553 ),
 .UNSPECIFIED., .F., .F.,
 ( 4, 4 ),
 ( 0.000000000000000000, 0.0002118541922231923684 ),
 .UNSPECIFIED. ) ;
#44803=FACE_OUTER_BOUND ( 'NONE', #29001, .T. ) ;
#44811=ORIENTED_EDGE ( 'NONE', *, *, #137489, .F. ) ;
#44822=CARTESIAN_POINT ( 'NONE',  ( 21.97500000000000497, 9.750000000011153745, -88.15000000000004832 ) ) ;
#44845=CARTESIAN_POINT ( 'NONE',  ( -20.64999999999999858, -8.999999999988844479, -91.10603087734760663 ) ) ;
#44851=DIRECTION ( 'NONE',  ( -1.000000000000000000, -7.304098846218134667E-16, 0.000000000000000000 ) ) ;
#44856=ORIENTED_EDGE ( 'NONE', *, *, #170723, .T. ) ;
#44919=CARTESIAN_POINT ( 'NONE',  ( 20.94999999999999574, -11.41227409413852989, -70.00000000000004263 ) ) ;
#44922=EDGE_CURVE ( 'NONE', #57960, #31018, #257134, .T. ) ;
#44923=ORIENTED_EDGE ( 'NONE', *, *, #102055, .T. ) ;
#44924=CIRCLE ( 'NONE', #65762, 0.1999999999999987899 ) ;
#44950=DIRECTION ( 'NONE',  ( 0.000000000000000000, -1.000000000000000000, 0.000000000000000000 ) ) ;
#44967=ORIENTED_EDGE ( 'NONE', *, *, #237688, .F. ) ;
#45000=DIRECTION ( 'NONE',  ( -1.000000000000000000, -3.265361837132813093E-16, 0.000000000000000000 ) ) ;
#45007=CARTESIAN_POINT ( 'NONE',  ( -18.59999999999999787, -1.362429037182155023, -108.3888812479212476 ) ) ;
#45021=DIRECTION ( 'NONE',  ( 0.000000000000000000, -1.000000000000000000, 0.000000000000000000 ) ) ;
#45066=CIRCLE ( 'NONE', #170027, 0.09999999999999939493 ) ;
#45116=ORIENTED_EDGE ( 'NONE', *, *, #232934, .T. ) ;
#45166=ORIENTED_EDGE ( 'NONE', *, *, #251354, .T. ) ;
#45170=EDGE_CURVE ( 'NONE', #203104, #71443, #67648, .T. ) ;
#45175=VECTOR ( 'NONE', #13976, 1000.000000000000000 ) ;
#45178=CARTESIAN_POINT ( 'NONE',  ( 21.05000000000000071, 1.115600667400684642E-11, -79.87500000000004263 ) ) ;
#45218=DIRECTION ( 'NONE',  ( 1.000000000000000000, 0.000000000000000000, 0.000000000000000000 ) ) ;
#45234=AXIS2_PLACEMENT_3D ( 'NONE', #150812, #191252, #30902 ) ;
#45259=AXIS2_PLACEMENT_3D ( 'NONE', #193044, #134319, #173523 ) ;
#45261=EDGE_CURVE ( 'NONE', #155361, #26378, #9560, .T. ) ;
#45292=EDGE_CURVE ( 'NONE', #242521, #39555, #123657, .T. ) ;
#45318=VERTEX_POINT ( 'NONE', #144466 ) ;
#45319=CARTESIAN_POINT ( 'NONE',  ( -23.25000000000000000, -9.599999999988845900, -90.60603087734760663 ) ) ;
#45329=ORIENTED_EDGE ( 'NONE', *, *, #20913, .T. ) ;
#45337=EDGE_CURVE ( 'NONE', #151819, #39792, #70122, .T. ) ;
#45339=DIRECTION ( 'NONE',  ( 1.000000000000000000, 0.000000000000000000, -0.000000000000000000 ) ) ;
#45353=DIRECTION ( 'NONE',  ( 0.000000000000000000, 0.000000000000000000, -1.000000000000000000 ) ) ;
#45384=CIRCLE ( 'NONE', #95455, 2.100000000000004530 ) ;
#45419=EDGE_CURVE ( 'NONE', #196915, #94787, #142814, .T. ) ;
#45427=AXIS2_PLACEMENT_3D ( 'NONE', #50813, #148672, #74291 ) ;
#45439=ORIENTED_EDGE ( 'NONE', *, *, #242937, .F. ) ;
#45448=ORIENTED_EDGE ( 'NONE', *, *, #69036, .T. ) ;
#45479=DIRECTION ( 'NONE',  ( -1.000000000000000000, 0.000000000000000000, 0.000000000000000000 ) ) ;
#45487=AXIS2_PLACEMENT_3D ( 'NONE', #25104, #82448, #366 ) ;
#45499=EDGE_CURVE ( 'NONE', #100973, #137777, #229173, .T. ) ;
#45511=CARTESIAN_POINT ( 'NONE',  ( 21.05000000000000071, 10.56271494673974232, -74.45680210564449908 ) ) ;
#45531=DIRECTION ( 'NONE',  ( 0.000000000000000000, 0.000000000000000000, 1.000000000000000000 ) ) ;
#45534=CIRCLE ( 'NONE', #62104, 0.1000000000000028644 ) ;
#45582=ADVANCED_FACE ( 'NONE', ( #226343 ), #51544, .T. ) ;
#45605=CIRCLE ( 'NONE', #133094, 0.1000000000000028644 ) ;
#45649=AXIS2_PLACEMENT_3D ( 'NONE', #3578, #205624, #200508 ) ;
#45659=ORIENTED_EDGE ( 'NONE', *, *, #150387, .T. ) ;
#45694=CARTESIAN_POINT ( 'NONE',  ( -23.15000000000000213, 1.115600667400684642E-11, -96.50000000000004263 ) ) ;
#45699=ORIENTED_EDGE ( 'NONE', *, *, #24196, .F. ) ;
#45704=AXIS2_PLACEMENT_3D ( 'NONE', #209097, #253355, #113848 ) ;
#45758=DIRECTION ( 'NONE',  ( 0.000000000000000000, 0.000000000000000000, -1.000000000000000000 ) ) ;
#45810=DIRECTION ( 'NONE',  ( 2.952720810173289112E-16, -1.000000000000000000, 0.000000000000000000 ) ) ;
#45815=ORIENTED_EDGE ( 'NONE', *, *, #35205, .T. ) ;
#45819=LINE ( 'NONE', #4120, #102731 ) ;
#45908=DIRECTION ( 'NONE',  ( 0.000000000000000000, 0.000000000000000000, -1.000000000000000000 ) ) ;
#45948=VERTEX_POINT ( 'NONE', #206500 ) ;
#45958=AXIS2_PLACEMENT_3D ( 'NONE', #34044, #14468, #122543 ) ;
#45959=CARTESIAN_POINT ( 'NONE',  ( -21.03571358705762506, 11.75000000001115197, -73.82510682205845853 ) ) ;
#45978=ORIENTED_EDGE ( 'NONE', *, *, #101790, .F. ) ;
#45981=ORIENTED_EDGE ( 'NONE', *, *, #125377, .F. ) ;
#45983=AXIS2_PLACEMENT_3D ( 'NONE', #126498, #127796, #120441 ) ;
#46009=ORIENTED_EDGE ( 'NONE', *, *, #197227, .T. ) ;
#46045=CARTESIAN_POINT ( 'NONE',  ( 20.85000000000000142, 1.115600667400684642E-11, -100.5000000000000426 ) ) ;
#46073=DIRECTION ( 'NONE',  ( 1.000000000000000000, 0.000000000000000000, 0.000000000000000000 ) ) ;
#46091=CARTESIAN_POINT ( 'NONE',  ( 21.05000000000000071, 8.776282895303626930, -79.15000000000004832 ) ) ;
#46093=VECTOR ( 'NONE', #140094, 1000.000000000000000 ) ;
#46144=LINE ( 'NONE', #166137, #211437 ) ;
#46149=CARTESIAN_POINT ( 'NONE',  ( -21.05000000000000071, 1.750000000011155743, -78.66951155790169992 ) ) ;
#46181=AXIS2_PLACEMENT_3D ( 'NONE', #71638, #10381, #49494 ) ;
#46199=CARTESIAN_POINT ( 'NONE',  ( -2.995603634470829482E-16, 6.650000000011155876, -88.25000000000005684 ) ) ;
#46234=EDGE_LOOP ( 'NONE', ( #96665, #179359, #112381, #17514 ) ) ;
#46246=CARTESIAN_POINT ( 'NONE',  ( -21.05000000000000071, 6.304961112695920633, -67.02138556593754970 ) ) ;
#46248=ADVANCED_FACE ( 'NONE', ( #85887 ), #117249, .F. ) ;
#46258=ORIENTED_EDGE ( 'NONE', *, *, #149898, .F. ) ;
#46260=EDGE_LOOP ( 'NONE', ( #177541, #106750, #251323, #184961 ) ) ;
#46310=EDGE_CURVE ( 'NONE', #194502, #91478, #109878, .T. ) ;
#46357=DIRECTION ( 'NONE',  ( -0.7071067811865475727, -0.7071067811865475727, -0.000000000000000000 ) ) ;
#46392=CARTESIAN_POINT ( 'NONE',  ( 20.87631937322879594, 10.47149503677605509, -74.57974587458122073 ) ) ;
#46425=CARTESIAN_POINT ( 'NONE',  ( 18.60000000000000142, -9.321008403350125704, -74.23593824907794669 ) ) ;
#46470=VECTOR ( 'NONE', #167310, 1000.000000000000000 ) ;
#46474=EDGE_CURVE ( 'NONE', #11297, #52066, #55879, .T. ) ;
#46493=LINE ( 'NONE', #107764, #193115 ) ;
#46496=CARTESIAN_POINT ( 'NONE',  ( 18.59999999999999432, 1.162701749949165642, -75.10000000000003695 ) ) ;
#46521=ORIENTED_EDGE ( 'NONE', *, *, #81626, .F. ) ;
#46557=CIRCLE ( 'NONE', #250580, 0.09999999999999939493 ) ;
#46561=CARTESIAN_POINT ( 'NONE',  ( -23.25000000000000000, -8.596261682231835621, -76.45012751715033517 ) ) ;
#46576=ORIENTED_EDGE ( 'NONE', *, *, #45337, .T. ) ;
#46589=CIRCLE ( 'NONE', #183993, 0.1000000000000028644 ) ;
#46598=ORIENTED_EDGE ( 'NONE', *, *, #171673, .T. ) ;
#46610=DIRECTION ( 'NONE',  ( -1.000000000000000000, -0.000000000000000000, -0.000000000000000000 ) ) ;
#46613=FACE_OUTER_BOUND ( 'NONE', #130348, .T. ) ;
#46628=ORIENTED_EDGE ( 'NONE', *, *, #101064, .T. ) ;
#46647=CARTESIAN_POINT ( 'NONE',  ( -23.15000000000000213, 5.950000000011163692, -90.19429769496522908 ) ) ;
#46685=ORIENTED_EDGE ( 'NONE', *, *, #190632, .T. ) ;
#46695=EDGE_CURVE ( 'NONE', #192087, #250224, #251537, .T. ) ;
#46714=CARTESIAN_POINT ( 'NONE',  ( -23.15000000000000213, 11.65000000001115588, -93.48519422934609224 ) ) ;
#46715=CIRCLE ( 'NONE', #200854, 0.1000000000000028644 ) ;
#46776=DIRECTION ( 'NONE',  ( 1.000000000000000000, 0.000000000000000000, 0.000000000000000000 ) ) ;
#46812=TOROIDAL_SURFACE ( 'NONE', #30280, 0.6000000000000015321, 0.1000000000000000056 ) ;
#46816=CARTESIAN_POINT ( 'NONE',  ( -23.15000000000000213, -8.999999999988846255, -76.89396912265249284 ) ) ;
#46861=ADVANCED_FACE ( 'NONE', ( #195005 ), #179301, .F. ) ;
#46864=FACE_OUTER_BOUND ( 'NONE', #79477, .T. ) ;
#46874=CARTESIAN_POINT ( 'NONE',  ( 23.25000000000000000, -9.599999999988842347, -90.60603087734760663 ) ) ;
#46914=EDGE_LOOP ( 'NONE', ( #25785, #142589, #192617, #19726 ) ) ;
#46921=CARTESIAN_POINT ( 'NONE',  ( -18.52309608778539385, -9.642476320044121252, -107.2145963411695675 ) ) ;
#46931=AXIS2_PLACEMENT_3D ( 'NONE', #163799, #244595, #184627 ) ;
#46947=CARTESIAN_POINT ( 'NONE',  ( 22.50000000000000000, 0.1000000000111554016, -59.20922040162665922 ) ) ;
#46962=FACE_OUTER_BOUND ( 'NONE', #89533, .T. ) ;
#47009=ADVANCED_FACE ( 'NONE', ( #125715 ), #47125, .T. ) ;
#47010=AXIS2_PLACEMENT_3D ( 'NONE', #247424, #227870, #148334 ) ;
#47075=FACE_OUTER_BOUND ( 'NONE', #161163, .T. ) ;
#47085=DIRECTION ( 'NONE',  ( 1.000000000000000000, 0.000000000000000000, 0.000000000000000000 ) ) ;
#47087=CARTESIAN_POINT ( 'NONE',  ( -22.50000000000000000, 1.115600667400684642E-11, -55.35042919245524473 ) ) ;
#47125=TOROIDAL_SURFACE ( 'NONE', #34700, 11.65000000000000036, 0.1000000000000000056 ) ;
#47137=DIRECTION ( 'NONE',  ( 0.000000000000000000, 0.000000000000000000, 1.000000000000000000 ) ) ;
#47141=CARTESIAN_POINT ( 'NONE',  ( -18.59999999999999787, 11.60000000001115872, -73.92820323027559937 ) ) ;
#47143=CIRCLE ( 'NONE', #151237, 0.1000000000000028644 ) ;
#47147=EDGE_CURVE ( 'NONE', #13016, #256646, #234585, .T. ) ;
#47148=DIRECTION ( 'NONE',  ( 2.952720810173289112E-16, -1.000000000000000000, 0.000000000000000000 ) ) ;
#47159=EDGE_CURVE ( 'NONE', #238735, #24864, #55672, .T. ) ;
#47166=EDGE_CURVE ( 'NONE', #197693, #131787, #255378, .T. ) ;
#47176=CARTESIAN_POINT ( 'NONE',  ( 23.24999999999999289, 6.450000000011156587, -55.25000000000004974 ) ) ;
#47186=CIRCLE ( 'NONE', #218057, 0.09999999999999693856 ) ;
#47204=CARTESIAN_POINT ( 'NONE',  ( 22.57320508075687115, 11.75000000001115552, -67.00000000000004263 ) ) ;
#47205=EDGE_CURVE ( 'NONE', #150331, #222218, #14039, .T. ) ;
#47222=CARTESIAN_POINT ( 'NONE',  ( 23.14999999999999858, 5.600000000011153389, -79.40526601891313874 ) ) ;
#47225=CARTESIAN_POINT ( 'NONE',  ( -21.05000000000000071, 11.65000000001115055, -73.78386566297820082 ) ) ;
#47232=EDGE_CURVE ( 'NONE', #208826, #80974, #230511, .T. ) ;
#47235=ORIENTED_EDGE ( 'NONE', *, *, #186030, .F. ) ;
#47237=VERTEX_POINT ( 'NONE', #34356 ) ;
#47238=DIRECTION ( 'NONE',  ( 0.000000000000000000, 0.000000000000000000, -1.000000000000000000 ) ) ;
#47273=EDGE_CURVE ( 'NONE', #68442, #203190, #195989, .T. ) ;
#47293=CARTESIAN_POINT ( 'NONE',  ( 20.94999999999999929, 5.000000000011153745, -88.49473398108695221 ) ) ;
#47341=EDGE_CURVE ( 'NONE', #15594, #95642, #147292, .T. ) ;
#47353=DIRECTION ( 'NONE',  ( 0.000000000000000000, 1.000000000000000000, 0.000000000000000000 ) ) ;
#47354=EDGE_CURVE ( 'NONE', #132550, #21996, #247231, .T. ) ;
#47374=CARTESIAN_POINT ( 'NONE',  ( 21.05000000000000071, 0.09779029131994770863, -60.74218538952391810 ) ) ;
#47390=ORIENTED_EDGE ( 'NONE', *, *, #204225, .T. ) ;
#47395=DIRECTION ( 'NONE',  ( 1.000000000000000000, 3.265361837132813093E-16, -0.000000000000000000 ) ) ;
#47398=CARTESIAN_POINT ( 'NONE',  ( 22.39999999999999503, 11.75000000001116263, -66.90000000000004832 ) ) ;
#47430=DIRECTION ( 'NONE',  ( 1.000000000000000000, 0.000000000000000000, 0.000000000000000000 ) ) ;
#47440=CARTESIAN_POINT ( 'NONE',  ( 20.93975676684922504, 10.31104185824063180, -106.0204516983106231 ) ) ;
#47459=DIRECTION ( 'NONE',  ( 0.000000000000000000, 0.000000000000000000, -1.000000000000000000 ) ) ;
#47471=EDGE_CURVE ( 'NONE', #187409, #150205, #22592, .T. ) ;
#47475=AXIS2_PLACEMENT_3D ( 'NONE', #73008, #250323, #174694 ) ;
#47491=DIRECTION ( 'NONE',  ( -3.469446951953660258E-14, 0.5000000000000209832, 0.8660254037844264952 ) ) ;
#47568=PLANE ( 'NONE',  #90640 ) ;
#47569=ORIENTED_EDGE ( 'NONE', *, *, #155694, .T. ) ;
#47579=VECTOR ( 'NONE', #43138, 1000.000000000000000 ) ;
#47612=EDGE_LOOP ( 'NONE', ( #141636, #93805, #173722, #213466, #48127, #98284, #42501 ) ) ;
#47616=CYLINDRICAL_SURFACE ( 'NONE', #141339, 0.09999999999999939493 ) ;
#47630=CARTESIAN_POINT ( 'NONE',  ( 18.59999999999999076, 10.49142135624846617, -91.75000000000005684 ) ) ;
#47654=ORIENTED_EDGE ( 'NONE', *, *, #57314, .T. ) ;
#47672=CARTESIAN_POINT ( 'NONE',  ( 20.97217846901852312, 8.875441724720827708, -75.50122768393727313 ) ) ;
#47695=CARTESIAN_POINT ( 'NONE',  ( 22.47007471830798053, 7.720710651937614522, -67.00000000000004263 ) ) ;
#47720=CARTESIAN_POINT ( 'NONE',  ( 23.14999999999999503, 14.05000000001115623, -94.98630492923912527 ) ) ;
#47756=DIRECTION ( 'NONE',  ( -0.000000000000000000, 0.8660254037844411501, 0.4999999999999956701 ) ) ;
#47789=DIRECTION ( 'NONE',  ( 0.000000000000000000, 0.1495327102803586661, -0.9887567792719350601 ) ) ;
#47799=CARTESIAN_POINT ( 'NONE',  ( 21.00000000000000000, 9.750000000011153745, -79.35000000000005116 ) ) ;
#47815=DIRECTION ( 'NONE',  ( -0.000000000000000000, 1.000000000000000000, -0.000000000000000000 ) ) ;
#47834=ORIENTED_EDGE ( 'NONE', *, *, #196709, .T. ) ;
#47837=DIRECTION ( 'NONE',  ( 0.000000000000000000, -0.8660254037844412611, -0.4999999999999956701 ) ) ;
#47851=( BOUNDED_CURVE ( )  B_SPLINE_CURVE ( 3, ( #18377, #77059, #255657, #180034 ),
 .UNSPECIFIED., .F., .F. ) 
 B_SPLINE_CURVE_WITH_KNOTS ( ( 4, 4 ),
 ( 3.141592653589793116, 4.712388980384689674 ),
 .UNSPECIFIED. ) 
 CURVE ( )  GEOMETRIC_REPRESENTATION_ITEM ( )  RATIONAL_B_SPLINE_CURVE ( ( 1.000000000000000000, 0.8047378541243649375, 0.8047378541243649375, 1.000000000000000000 ) ) 
 REPRESENTATION_ITEM ( '' )  );
#47874=EDGE_CURVE ( 'NONE', #179033, #185550, #202843, .T. ) ;
#47881=EDGE_CURVE ( 'NONE', #113090, #153266, #255764, .T. ) ;
#47895=ORIENTED_EDGE ( 'NONE', *, *, #155300, .F. ) ;
#47902=DIRECTION ( 'NONE',  ( 1.000000000000000000, 0.000000000000000000, 0.000000000000000000 ) ) ;
#47910=DIRECTION ( 'NONE',  ( -1.000000000000000000, 0.000000000000000000, 0.000000000000000000 ) ) ;
#47958=DIRECTION ( 'NONE',  ( 1.000000000000000000, 0.000000000000000000, 0.000000000000000000 ) ) ;
#47979=EDGE_CURVE ( 'NONE', #246766, #146445, #175476, .T. ) ;
#47997=VERTEX_POINT ( 'NONE', #76332 ) ;
#48017=DIRECTION ( 'NONE',  ( 1.000000000000000000, 0.000000000000000000, 0.000000000000000000 ) ) ;
#48028=CARTESIAN_POINT ( 'NONE',  ( 21.05000000000000071, 1.115600667400684642E-11, -67.00000000000004263 ) ) ;
#48082=DIRECTION ( 'NONE',  ( 0.000000000000000000, 0.000000000000000000, -1.000000000000000000 ) ) ;
#48085=DIRECTION ( 'NONE',  ( 0.000000000000000000, 4.440892098500570153E-15, -1.000000000000000000 ) ) ;
#48090=CARTESIAN_POINT ( 'NONE',  ( 20.85000000000000142, 11.65000000001115943, -100.5000000000000426 ) ) ;
#48116=FACE_OUTER_BOUND ( 'NONE', #11567, .T. ) ;
#48127=ORIENTED_EDGE ( 'NONE', *, *, #47874, .F. ) ;
#48150=CARTESIAN_POINT ( 'NONE',  ( -18.50000000000000000, -1.164121893230052995, -108.2148480855716457 ) ) ;
#48174=EDGE_CURVE ( 'NONE', #38637, #196915, #214306, .T. ) ;
#48185=CARTESIAN_POINT ( 'NONE',  ( 20.87155475150661132, 11.75000000001115907, -93.59558652915731614 ) ) ;
#48217=ORIENTED_EDGE ( 'NONE', *, *, #100480, .T. ) ;
#48218=VERTEX_POINT ( 'NONE', #129615 ) ;
#48222=ORIENTED_EDGE ( 'NONE', *, *, #175193, .F. ) ;
#48224=CARTESIAN_POINT ( 'NONE',  ( -18.31331870001056217, -9.536294719169665868, -107.3685786909854727 ) ) ;
#48274=ADVANCED_FACE ( 'NONE', ( #18652 ), #17374, .F. ) ;
#48292=AXIS2_PLACEMENT_3D ( 'NONE', #66455, #185120, #205962 ) ;
#48325=FACE_OUTER_BOUND ( 'NONE', #213160, .T. ) ;
#48331=CARTESIAN_POINT ( 'NONE',  ( -21.05000000000000071, 1.261786168576181755, -75.08649896354552311 ) ) ;
#48373=DIRECTION ( 'NONE',  ( 0.7071067811865475727, -0.7071067811865475727, 0.000000000000000000 ) ) ;
#48374=VECTOR ( 'NONE', #49553, 1000.000000000000000 ) ;
#48380=CARTESIAN_POINT ( 'NONE',  ( -20.94999999999999929, -12.41227409413852811, -97.50000000000004263 ) ) ;
#48392=ORIENTED_EDGE ( 'NONE', *, *, #120704, .T. ) ;
#48411=VECTOR ( 'NONE', #223197, 1000.000000000000000 ) ;
#48454=DIRECTION ( 'NONE',  ( 0.000000000000000000, 1.224646799142015331E-16, 1.000000000000000000 ) ) ;
#48455=ORIENTED_EDGE ( 'NONE', *, *, #99886, .T. ) ;
#48458=CARTESIAN_POINT ( 'NONE',  ( -20.94999999999999929, -11.48912529306490349, -69.90000000000004832 ) ) ;
#48484=EDGE_LOOP ( 'NONE', ( #95656, #198161, #122664 ) ) ;
#48524=CARTESIAN_POINT ( 'NONE',  ( -21.12844524849339223, 11.75000000001115197, -73.90441347084285439 ) ) ;
#48525=EDGE_LOOP ( 'NONE', ( #118592, #160817, #74484, #230094 ) ) ;
#48593=AXIS2_PLACEMENT_3D ( 'NONE', #192208, #57791, #233883 ) ;
#48641=EDGE_CURVE ( 'NONE', #166675, #118383, #211418, .T. ) ;
#48657=CARTESIAN_POINT ( 'NONE',  ( -21.70464131381649509, 7.095358018979010417, -67.00000000000004263 ) ) ;
#48669=CARTESIAN_POINT ( 'NONE',  ( 21.05000000000000071, -0.09999999998884338825, -60.45934304829879835 ) ) ;
#48688=FACE_OUTER_BOUND ( 'NONE', #249032, .T. ) ;
#48719=CARTESIAN_POINT ( 'NONE',  ( -20.94999999999999929, -1.835341550213255957, -78.55515129256303908 ) ) ;
#48723=DIRECTION ( 'NONE',  ( 0.000000000000000000, 1.000000000000000000, 2.891205793294679805E-16 ) ) ;
#48727=ADVANCED_FACE ( 'NONE', ( #74519 ), #248451, .T. ) ;
#48762=VECTOR ( 'NONE', #128970, 1000.000000000000000 ) ;
#48780=ORIENTED_EDGE ( 'NONE', *, *, #60325, .T. ) ;
#48793=FACE_OUTER_BOUND ( 'NONE', #49462, .T. ) ;
#48820=CARTESIAN_POINT ( 'NONE',  ( -21.11825140030079240, 6.445407565431027663, -66.99279637936723475 ) ) ;
#48854=CARTESIAN_POINT ( 'NONE',  ( 21.05000000000000071, 1.115600667400684642E-11, -100.5000000000000426 ) ) ;
#48856=CARTESIAN_POINT ( 'NONE',  ( 22.45380639572154990, 1.426823211110743220E-07, -55.24956710889318146 ) ) ;
#48868=DIRECTION ( 'NONE',  ( -3.265361837132813093E-16, 1.000000000000000000, 0.000000000000000000 ) ) ;
#48905=VERTEX_POINT ( 'NONE', #181296 ) ;
#48922=DIRECTION ( 'NONE',  ( -1.000000000000000000, 0.000000000000000000, 0.000000000000000000 ) ) ;
#48935=AXIS2_PLACEMENT_3D ( 'NONE', #95107, #174699, #254162 ) ;
#48941=ORIENTED_EDGE ( 'NONE', *, *, #106331, .T. ) ;
#48945=CARTESIAN_POINT ( 'NONE',  ( 21.05000000000000071, -11.48912529306489994, -97.60000000000005116 ) ) ;
#48952=EDGE_LOOP ( 'NONE', ( #127912, #58749, #159541, #183712 ) ) ;
#48958=CARTESIAN_POINT ( 'NONE',  ( -20.54999999999999716, -9.399999999988846611, -90.60603087734760663 ) ) ;
#48971=CARTESIAN_POINT ( 'NONE',  ( 20.97107704358301916, 8.875478152032441059, -75.55897322938929506 ) ) ;
#48976=CARTESIAN_POINT ( 'NONE',  ( 20.95035502843362707, 10.47763832678762164, -74.57629970873641412 ) ) ;
#49027=EDGE_CURVE ( 'NONE', #109568, #240894, #86289, .T. ) ;
#49036=AXIS2_PLACEMENT_3D ( 'NONE', #92027, #132444, #208150 ) ;
#49053=DIRECTION ( 'NONE',  ( -1.000000000000000000, 0.000000000000000000, 0.000000000000000000 ) ) ;
#49081=DIRECTION ( 'NONE',  ( -0.000000000000000000, 0.8660254037844383745, -0.5000000000000003331 ) ) ;
#49109=EDGE_CURVE ( 'NONE', #124485, #196062, #73691, .T. ) ;
#49151=EDGE_CURVE ( 'NONE', #250043, #191668, #161155, .T. ) ;
#49164=AXIS2_PLACEMENT_3D ( 'NONE', #241575, #25121, #107192 ) ;
#49169=DIRECTION ( 'NONE',  ( 0.000000000000000000, 0.5000000000000144329, 0.8660254037844302699 ) ) ;
#49186=TOROIDAL_SURFACE ( 'NONE', #140783, 0.6000000000000009770, 0.1000000000000000056 ) ;
#49211=ORIENTED_EDGE ( 'NONE', *, *, #39372, .F. ) ;
#49224=DIRECTION ( 'NONE',  ( 0.000000000000000000, 1.000000000000000000, 2.891205793294679805E-16 ) ) ;
#49229=CARTESIAN_POINT ( 'NONE',  ( 21.05000000000000071, 8.815452279208699338, -75.42039255261430242 ) ) ;
#49230=DIRECTION ( 'NONE',  ( 0.000000000000000000, -0.5000000000000275335, -0.8660254037844228314 ) ) ;
#49256=ORIENTED_EDGE ( 'NONE', *, *, #97630, .T. ) ;
#49260=CARTESIAN_POINT ( 'NONE',  ( -22.50875500270928598, -0.1008579137641426871, -55.25043287260216118 ) ) ;
#49306=FACE_BOUND ( 'NONE', #75797, .T. ) ;
#49312=ADVANCED_FACE ( 'NONE', ( #57663 ), #240273, .F. ) ;
#49335=CIRCLE ( 'NONE', #224115, 0.09999999999999939493 ) ;
#49359=AXIS2_PLACEMENT_3D ( 'NONE', #222647, #80559, #3611 ) ;
#49376=DIRECTION ( 'NONE',  ( 0.000000000000000000, 0.000000000000000000, -1.000000000000000000 ) ) ;
#49422=EDGE_LOOP ( 'NONE', ( #195189, #60233, #14027, #174332 ) ) ;
#49462=EDGE_LOOP ( 'NONE', ( #86598, #87138, #52229, #114977 ) ) ;
#49473=LINE ( 'NONE', #191583, #236417 ) ;
#49492=ORIENTED_EDGE ( 'NONE', *, *, #216147, .T. ) ;
#49494=DIRECTION ( 'NONE',  ( -1.000000000000000000, 0.000000000000000000, 0.000000000000000000 ) ) ;
#49499=DIRECTION ( 'NONE',  ( 0.000000000000000000, 0.000000000000000000, -1.000000000000000000 ) ) ;
#49518=CARTESIAN_POINT ( 'NONE',  ( -18.46154800491018477, -9.480206274230813079, -107.1574508383815214 ) ) ;
#49528=CARTESIAN_POINT ( 'NONE',  ( -21.14999999999999858, 0.09779029131994770863, -60.74218538952393232 ) ) ;
#49535=ORIENTED_EDGE ( 'NONE', *, *, #144792, .T. ) ;
#49543=ORIENTED_EDGE ( 'NONE', *, *, #191094, .T. ) ;
#49548=CARTESIAN_POINT ( 'NONE',  ( 20.85000000000000142, -1.749999999988843813, -112.1189500386223017 ) ) ;
#49553=DIRECTION ( 'NONE',  ( 0.000000000000000000, -0.1350103645451876666, -0.9908441862701600211 ) ) ;
#49565=DIRECTION ( 'NONE',  ( 0.000000000000000000, 0.000000000000000000, -1.000000000000000000 ) ) ;
#49574=ORIENTED_EDGE ( 'NONE', *, *, #162849, .F. ) ;
#49578=CARTESIAN_POINT ( 'NONE',  ( -21.05000000000000426, 6.270085863700299633, -66.96513199698695473 ) ) ;
#49606=ORIENTED_EDGE ( 'NONE', *, *, #231117, .T. ) ;
#49610=CARTESIAN_POINT ( 'NONE',  ( -23.15000000000000213, 11.65000000001115588, -93.48519422934610645 ) ) ;
#49622=CARTESIAN_POINT ( 'NONE',  ( 23.14999999999999503, 11.75000000001116263, -55.25000000000004974 ) ) ;
#49640=DIRECTION ( 'NONE',  ( 0.000000000000000000, -0.000000000000000000, 1.000000000000000000 ) ) ;
#49653=DIRECTION ( 'NONE',  ( 0.000000000000000000, 0.000000000000000000, -1.000000000000000000 ) ) ;
#49661=CARTESIAN_POINT ( 'NONE',  ( 18.59999999999999076, 6.450000000011156587, -77.01702717044007329 ) ) ;
#49687=CARTESIAN_POINT ( 'NONE',  ( -20.85000000000000142, -1.164121893230052995, -108.4148480855716485 ) ) ;
#49692=CARTESIAN_POINT ( 'NONE',  ( -23.25000000000000000, -1.736705739456431807, -112.0174225876237699 ) ) ;
#49729=CARTESIAN_POINT ( 'NONE',  ( -21.14999999999999858, 11.65000000001115232, -67.00000000000004263 ) ) ;
#49735=FACE_OUTER_BOUND ( 'NONE', #248586, .T. ) ;
#49746=ORIENTED_EDGE ( 'NONE', *, *, #59327, .F. ) ;
#49762=VERTEX_POINT ( 'NONE', #122500 ) ;
#49790=EDGE_CURVE ( 'NONE', #70706, #142483, #3714, .T. ) ;
#49814=ORIENTED_EDGE ( 'NONE', *, *, #146413, .F. ) ;
#49851=EDGE_LOOP ( 'NONE', ( #151656, #58255, #198581, #52046 ) ) ;
#49881=AXIS2_PLACEMENT_3D ( 'NONE', #8703, #64814, #85627 ) ;
#49932=EDGE_CURVE ( 'NONE', #208853, #238489, #44244, .T. ) ;
#49935=CARTESIAN_POINT ( 'NONE',  ( 21.95218792049437795, 7.201507561257818324, -66.90097156020011937 ) ) ;
#49936=CIRCLE ( 'NONE', #141515, 11.70000000000000284 ) ;
#49957=AXIS2_PLACEMENT_3D ( 'NONE', #230297, #30851, #112930 ) ;
#49964=ADVANCED_FACE ( 'NONE', ( #105452 ), #191181, .T. ) ;
#49993=CARTESIAN_POINT ( 'NONE',  ( -20.94999999999999929, 11.65000000001115232, -100.5000000000000426 ) ) ;
#50002=DIRECTION ( 'NONE',  ( 1.000000000000000000, 0.000000000000000000, 0.000000000000000000 ) ) ;
#50008=EDGE_CURVE ( 'NONE', #120817, #70703, #99542, .T. ) ;
#50013=ORIENTED_EDGE ( 'NONE', *, *, #146857, .F. ) ;
#50016=CARTESIAN_POINT ( 'NONE',  ( 21.05000000000000071, 1.115600667400684642E-11, -104.5000000000000568 ) ) ;
#50060=EDGE_CURVE ( 'NONE', #56225, #209971, #28711, .T. ) ;
#50085=CARTESIAN_POINT ( 'NONE',  ( 22.49436431346199683, 11.64995094766461392, -66.93309647027778908 ) ) ;
#50091=CARTESIAN_POINT ( 'NONE',  ( 23.14999999999999503, 11.65000000001116298, -88.35000000000003695 ) ) ;
#50095=CIRCLE ( 'NONE', #12724, 0.1999999999999987899 ) ;
#50098=ADVANCED_FACE ( 'NONE', ( #212312 ), #11541, .T. ) ;
#50100=CARTESIAN_POINT ( 'NONE',  ( -21.13435531349821872, 6.493721063603322463, -67.00000000000004263 ) ) ;
#50110=ORIENTED_EDGE ( 'NONE', *, *, #121789, .T. ) ;
#50112=EDGE_CURVE ( 'NONE', #114130, #252230, #45605, .T. ) ;
#50122=LINE ( 'NONE', #30593, #113660 ) ;
#50126=CARTESIAN_POINT ( 'NONE',  ( -18.42609945526390902, -9.499999710479540838, -73.99936249024790413 ) ) ;
#50130=FACE_OUTER_BOUND ( 'NONE', #231101, .T. ) ;
#50136=ORIENTED_EDGE ( 'NONE', *, *, #17054, .F. ) ;
#50185=ORIENTED_EDGE ( 'NONE', *, *, #39440, .T. ) ;
#50206=CARTESIAN_POINT ( 'NONE',  ( 18.53691006697098942, 10.30215155716143016, -91.70219871729851491 ) ) ;
#50207=CIRCLE ( 'NONE', #143, 0.1000000000000028644 ) ;
#50225=CIRCLE ( 'NONE', #171106, 12.77500000000000036 ) ;
#50245=CARTESIAN_POINT ( 'NONE',  ( 20.94999999999999574, 10.47338541492405994, -74.57865446424858646 ) ) ;
#50314=CARTESIAN_POINT ( 'NONE',  ( 21.08832698747859169, 8.775364393428372267, -79.22871746646418956 ) ) ;
#50316=LINE ( 'NONE', #131156, #120459 ) ;
#50319=DIRECTION ( 'NONE',  ( 1.000000000000000000, 1.836970198721029934E-16, -0.000000000000000000 ) ) ;
#50345=AXIS2_PLACEMENT_3D ( 'NONE', #46149, #68296, #233478 ) ;
#50359=ORIENTED_EDGE ( 'NONE', *, *, #94742, .T. ) ;
#50363=DIRECTION ( 'NONE',  ( 1.000000000000000000, 0.000000000000000000, 0.000000000000000000 ) ) ;
#50365=TOROIDAL_SURFACE ( 'NONE', #166956, 0.9750000000000019762, 0.1000000000000000056 ) ;
#50387=LINE ( 'NONE', #248615, #1222 ) ;
#50429=DIRECTION ( 'NONE',  ( 4.336808689942128177E-15, 0.8660254037844330455, -0.5000000000000096589 ) ) ;
#50430=LINE ( 'NONE', #251207, #51915 ) ;
#50432=ORIENTED_EDGE ( 'NONE', *, *, #214466, .T. ) ;
#50436=EDGE_CURVE ( 'NONE', #111358, #237092, #50316, .T. ) ;
#50438=CARTESIAN_POINT ( 'NONE',  ( -20.85000000000000142, 7.070967871809997973, -104.2465642218683541 ) ) ;
#50456=DIRECTION ( 'NONE',  ( -0.000000000000000000, -0.000000000000000000, 1.000000000000000000 ) ) ;
#50462=CARTESIAN_POINT ( 'NONE',  ( -20.94999999999999929, -1.736257131586239844, -78.56865232901753870 ) ) ;
#50496=ORIENTED_EDGE ( 'NONE', *, *, #54484, .T. ) ;
#50501=ORIENTED_EDGE ( 'NONE', *, *, #159332, .T. ) ;
#50546=EDGE_LOOP ( 'NONE', ( #177204, #12424, #69498, #66159 ) ) ;
#50554=EDGE_CURVE ( 'NONE', #84058, #192064, #195653, .T. ) ;
#50555=CARTESIAN_POINT ( 'NONE',  ( 18.49999999999999289, 11.65000000001115943, -91.85000000000003695 ) ) ;
#50558=ORIENTED_EDGE ( 'NONE', *, *, #97876, .F. ) ;
#50577=EDGE_CURVE ( 'NONE', #217587, #75011, #91573, .T. ) ;
#50613=LINE ( 'NONE', #225398, #84765 ) ;
#50622=VERTEX_POINT ( 'NONE', #245363 ) ;
#50653=DIRECTION ( 'NONE',  ( 1.000000000000000000, 0.000000000000000000, 0.000000000000000000 ) ) ;
#50662=CYLINDRICAL_SURFACE ( 'NONE', #24603, 0.1000000000000028644 ) ;
#50667=CIRCLE ( 'NONE', #196426, 0.5000000000000004441 ) ;
#50672=CARTESIAN_POINT ( 'NONE',  ( -22.50000000000000000, 1.115600667400684642E-11, -67.00000000000004263 ) ) ;
#50695=FACE_OUTER_BOUND ( 'NONE', #177925, .T. ) ;
#50727=DIRECTION ( 'NONE',  ( 0.000000000000000000, 0.000000000000000000, -1.000000000000000000 ) ) ;
#50729=ORIENTED_EDGE ( 'NONE', *, *, #204805, .F. ) ;
#50734=DIRECTION ( 'NONE',  ( 1.000000000000000000, 0.000000000000000000, 0.000000000000000000 ) ) ;
#50753=ORIENTED_EDGE ( 'NONE', *, *, #41242, .T. ) ;
#50763=ORIENTED_EDGE ( 'NONE', *, *, #15201, .F. ) ;
#50782=ORIENTED_EDGE ( 'NONE', *, *, #176930, .F. ) ;
#50813=CARTESIAN_POINT ( 'NONE',  ( -18.50000000000000711, 11.65000000001115232, -74.01480577065404987 ) ) ;
#50824=EDGE_CURVE ( 'NONE', #96187, #68295, #70945, .T. ) ;
#50825=DIRECTION ( 'NONE',  ( 1.000000000000000000, 3.265361837132813093E-16, -0.000000000000000000 ) ) ;
#50835=PLANE ( 'NONE',  #194774 ) ;
#50866=DIRECTION ( 'NONE',  ( 2.952720810173289112E-16, -1.000000000000000000, 0.000000000000000000 ) ) ;
#50870=ORIENTED_EDGE ( 'NONE', *, *, #78279, .F. ) ;
#50892=VERTEX_POINT ( 'NONE', #102942 ) ;
#50899=EDGE_LOOP ( 'NONE', ( #63060, #167992, #32341, #218525 ) ) ;
#50919=ADVANCED_FACE ( 'NONE', ( #198207 ), #179946, .T. ) ;
#50929=DIRECTION ( 'NONE',  ( -1.000000000000000000, -0.000000000000000000, -0.000000000000000000 ) ) ;
#50934=EDGE_CURVE ( 'NONE', #172095, #231898, #19589, .T. ) ;
#50946=CARTESIAN_POINT ( 'NONE',  ( -21.14999999999999858, -11.74999999998884448, -69.90000000000004832 ) ) ;
#50953=AXIS2_PLACEMENT_3D ( 'NONE', #227554, #110172, #131025 ) ;
#50987=VERTEX_POINT ( 'NONE', #140811 ) ;
#51006=AXIS2_PLACEMENT_3D ( 'NONE', #3464, #139096, #119595 ) ;
#51031=FACE_BOUND ( 'NONE', #22472, .T. ) ;
#51045=EDGE_CURVE ( 'NONE', #17147, #190429, #137525, .T. ) ;
#51047=ORIENTED_EDGE ( 'NONE', *, *, #21642, .F. ) ;
#51071=CARTESIAN_POINT ( 'NONE',  ( -18.59999999999999787, 9.350000000011156942, -88.15000000000004832 ) ) ;
#51078=CYLINDRICAL_SURFACE ( 'NONE', #128747, 12.87499999999999822 ) ;
#51083=CARTESIAN_POINT ( 'NONE',  ( 23.14999999999999147, 1.115600667400684642E-11, -67.00000000000004263 ) ) ;
#51113=AXIS2_PLACEMENT_3D ( 'NONE', #179400, #39901, #162404 ) ;
#51115=EDGE_CURVE ( 'NONE', #6867, #106375, #220747, .T. ) ;
#51119=CIRCLE ( 'NONE', #213461, 0.1000000000000028644 ) ;
#51124=ORIENTED_EDGE ( 'NONE', *, *, #51259, .T. ) ;
#51153=AXIS2_PLACEMENT_3D ( 'NONE', #71095, #133610, #230149 ) ;
#51182=ORIENTED_EDGE ( 'NONE', *, *, #44064, .F. ) ;
#51193=ORIENTED_EDGE ( 'NONE', *, *, #71784, .F. ) ;
#51196=DIRECTION ( 'NONE',  ( 0.000000000000000000, 0.000000000000000000, -1.000000000000000000 ) ) ;
#51206=CARTESIAN_POINT ( 'NONE',  ( 21.06086055315989114, 8.774707514967413857, -79.20232215515413543 ) ) ;
#51215=FACE_OUTER_BOUND ( 'NONE', #174642, .T. ) ;
#51254=CARTESIAN_POINT ( 'NONE',  ( 22.57320508075687826, 11.75000000001115552, -67.00000000000004263 ) ) ;
#51259=EDGE_CURVE ( 'NONE', #205048, #116760, #58359, .T. ) ;
#51268=CARTESIAN_POINT ( 'NONE',  ( 20.84999999999998721, 10.33248238083634440, -106.0948465439131922 ) ) ;
#51301=CARTESIAN_POINT ( 'NONE',  ( -23.24999999999999645, -9.599999999988845900, -107.1001893912220879 ) ) ;
#51318=CIRCLE ( 'NONE', #30715, 0.5000000000000004441 ) ;
#51323=DIRECTION ( 'NONE',  ( 0.000000000000000000, -0.9908441862701596881, -0.1350103645451901924 ) ) ;
#51339=EDGE_CURVE ( 'NONE', #95768, #24665, #216829, .T. ) ;
#51342=CARTESIAN_POINT ( 'NONE',  ( -20.54999999999999716, 1.115600667400684642E-11, -67.00000000000004263 ) ) ;
#51377=CARTESIAN_POINT ( 'NONE',  ( 23.24999999999999645, 1.115600667400684642E-11, -67.00000000000004263 ) ) ;
#51379=VERTEX_POINT ( 'NONE', #248578 ) ;
#51390=CARTESIAN_POINT ( 'NONE',  ( 18.49999999999998934, 11.65000000001115943, -91.75000000000005684 ) ) ;
#51395=CARTESIAN_POINT ( 'NONE',  ( 22.49999999999998579, 0.1008583691098678958, -55.25043287651065071 ) ) ;
#51407=ORIENTED_EDGE ( 'NONE', *, *, #73637, .T. ) ;
#51417=ADVANCED_FACE ( 'NONE', ( #165193 ), #146886, .T. ) ;
#51425=EDGE_CURVE ( 'NONE', #210821, #115244, #220914, .T. ) ;
#51443=AXIS2_PLACEMENT_3D ( 'NONE', #14326, #93826, #13039 ) ;
#51481=AXIS2_PLACEMENT_3D ( 'NONE', #145407, #227512, #74902 ) ;
#51511=CARTESIAN_POINT ( 'NONE',  ( 20.77526135991775291, 8.932009016633136511, -75.46856854272438397 ) ) ;
#51533=CARTESIAN_POINT ( 'NONE',  ( 18.59999999999999787, -11.74999999998883737, -88.35000000000003695 ) ) ;
#51544=CYLINDRICAL_SURFACE ( 'NONE', #1183, 0.09999999999999939493 ) ;
#51552=ORIENTED_EDGE ( 'NONE', *, *, #106748, .F. ) ;
#51574=SPHERICAL_SURFACE ( 'NONE', #257850, 0.1000000000000000056 ) ;
#51592=CARTESIAN_POINT ( 'NONE',  ( 21.05000000000000071, -9.399999999988844834, -90.60603087734760663 ) ) ;
#51594=CARTESIAN_POINT ( 'NONE',  ( -21.05000000000000071, 6.400000000011158541, -76.93042463006162279 ) ) ;
#51601=ORIENTED_EDGE ( 'NONE', *, *, #23377, .T. ) ;
#51618=DIRECTION ( 'NONE',  ( 0.000000000000000000, 0.000000000000000000, -1.000000000000000000 ) ) ;
#51624=DIRECTION ( 'NONE',  ( 0.000000000000000000, 0.000000000000000000, 1.000000000000000000 ) ) ;
#51650=EDGE_CURVE ( 'NONE', #231082, #153266, #146279, .T. ) ;
#51675=PLANE ( 'NONE',  #243919 ) ;
#51717=CARTESIAN_POINT ( 'NONE',  ( -20.54999999999999716, 1.115600667400684642E-11, -100.5000000000000426 ) ) ;
#51727=EDGE_CURVE ( 'NONE', #252613, #7494, #54706, .T. ) ;
#51736=VERTEX_POINT ( 'NONE', #147911 ) ;
#51746=EDGE_CURVE ( 'NONE', #163852, #201338, #250342, .T. ) ;
#51748=AXIS2_PLACEMENT_3D ( 'NONE', #98671, #17885, #177006 ) ;
#51785=DIRECTION ( 'NONE',  ( 0.7071067811865474617, 0.7071067811865474617, -0.000000000000000000 ) ) ;
#51788=DIRECTION ( 'NONE',  ( 1.000000000000000000, 0.000000000000000000, 0.000000000000000000 ) ) ;
#51804=ORIENTED_EDGE ( 'NONE', *, *, #82417, .F. ) ;
#51807=CARTESIAN_POINT ( 'NONE',  ( -22.45354308602430038, 2.198891012223663321E-07, -55.24956710953974692 ) ) ;
#51814=ADVANCED_FACE ( 'NONE', ( #43664 ), #123198, .T. ) ;
#51815=AXIS2_PLACEMENT_3D ( 'NONE', #2248, #19265, #98758 ) ;
#51818=ORIENTED_EDGE ( 'NONE', *, *, #240178, .T. ) ;
#51819=CARTESIAN_POINT ( 'NONE',  ( -23.25000000000000000, 2.000000000011154189, -87.27537807723794572 ) ) ;
#51873=CARTESIAN_POINT ( 'NONE',  ( -20.85000000000000142, -11.64999999998884306, -100.5000000000000426 ) ) ;
#51882=DIRECTION ( 'NONE',  ( 0.000000000000000000, 0.000000000000000000, -1.000000000000000000 ) ) ;
#51884=VERTEX_POINT ( 'NONE', #211741 ) ;
#51915=VECTOR ( 'NONE', #229101, 1000.000000000000000 ) ;
#51928=LINE ( 'NONE', #94917, #251876 ) ;
#51931=EDGE_LOOP ( 'NONE', ( #229915, #255076, #160919, #33065 ) ) ;
#52008=CYLINDRICAL_SURFACE ( 'NONE', #219833, 0.5000000000000004441 ) ;
#52012=AXIS2_PLACEMENT_3D ( 'NONE', #85037, #221985, #107197 ) ;
#52014=AXIS2_PLACEMENT_3D ( 'NONE', #10499, #247814, #169611 ) ;
#52034=AXIS2_PLACEMENT_3D ( 'NONE', #170523, #229166, #231736 ) ;
#52038=DIRECTION ( 'NONE',  ( 1.000000000000000000, 0.000000000000000000, 0.000000000000000000 ) ) ;
#52046=ORIENTED_EDGE ( 'NONE', *, *, #10623, .F. ) ;
#52066=VERTEX_POINT ( 'NONE', #68055 ) ;
#52081=ORIENTED_EDGE ( 'NONE', *, *, #7788, .F. ) ;
#52085=ORIENTED_EDGE ( 'NONE', *, *, #200338, .F. ) ;
#52110=AXIS2_PLACEMENT_3D ( 'NONE', #6450, #165547, #120025 ) ;
#52156=EDGE_LOOP ( 'NONE', ( #50110, #129269, #56168, #43401, #39042 ) ) ;
#52186=CIRCLE ( 'NONE', #110449, 0.2000000000000057288 ) ;
#52190=DIRECTION ( 'NONE',  ( 0.000000000000000000, 0.000000000000000000, -1.000000000000000000 ) ) ;
#52229=ORIENTED_EDGE ( 'NONE', *, *, #254966, .T. ) ;
#52255=ORIENTED_EDGE ( 'NONE', *, *, #92089, .T. ) ;
#52267=DIRECTION ( 'NONE',  ( 0.000000000000000000, 1.000000000000000000, 0.000000000000000000 ) ) ;
#52273=VECTOR ( 'NONE', #221078, 1000.000000000000000 ) ;
#52282=CARTESIAN_POINT ( 'NONE',  ( -20.85000000000000142, 1.115600667400684642E-11, -100.5000000000000426 ) ) ;
#52322=CIRCLE ( 'NONE', #214830, 0.1000000000000028644 ) ;
#52332=AXIS2_PLACEMENT_3D ( 'NONE', #150241, #108526, #208908 ) ;
#52363=ORIENTED_EDGE ( 'NONE', *, *, #50554, .T. ) ;
#52408=ORIENTED_EDGE ( 'NONE', *, *, #112335, .T. ) ;
#52428=CARTESIAN_POINT ( 'NONE',  ( 23.14999999999999503, 11.75000000001115552, -88.25000000000005684 ) ) ;
#52454=CARTESIAN_POINT ( 'NONE',  ( -20.94999999999999929, -1.851028230129704522, -78.65391326942254580 ) ) ;
#52460=LINE ( 'NONE', #206418, #139731 ) ;
#52479=CIRCLE ( 'NONE', #219075, 2.000000000000001776 ) ;
#52481=( BOUNDED_CURVE ( )  B_SPLINE_CURVE ( 3, ( #83381, #5123, #105506, #84652 ),
 .UNSPECIFIED., .F., .F. ) 
 B_SPLINE_CURVE_WITH_KNOTS ( ( 4, 4 ),
 ( 0.000000000000000000, 1.570796326794908992 ),
 .UNSPECIFIED. ) 
 CURVE ( )  GEOMETRIC_REPRESENTATION_ITEM ( )  RATIONAL_B_SPLINE_CURVE ( ( 1.000000000000000000, 0.8047378541243619399, 0.8047378541243619399, 1.000000000000000000 ) ) 
 REPRESENTATION_ITEM ( '' )  );
#52492=CARTESIAN_POINT ( 'NONE',  ( 21.30740335185486245, 6.556657922039159203, -66.90106547422419681 ) ) ;
#52500=CARTESIAN_POINT ( 'NONE',  ( -21.33487959338958362, 6.725558151922345296, -67.00000000000004263 ) ) ;
#52535=DIRECTION ( 'NONE',  ( 0.000000000000000000, 0.000000000000000000, -1.000000000000000000 ) ) ;
#52560=AXIS2_PLACEMENT_3D ( 'NONE', #137959, #15488, #94998 ) ;
#52564=LINE ( 'NONE', #227358, #167457 ) ;
#52581=ADVANCED_FACE ( 'NONE', ( #208231 ), #25866, .T. ) ;
#52626=TOROIDAL_SURFACE ( 'NONE', #214946, 6.258578643762712446, 0.1000000000000000056 ) ;
#52641=CARTESIAN_POINT ( 'NONE',  ( 21.08035267497491105, 6.331706839794169817, -66.91731137522391748 ) ) ;
#52654=VECTOR ( 'NONE', #126649, 1000.000000000000000 ) ;
#52666=ORIENTED_EDGE ( 'NONE', *, *, #50436, .T. ) ;
#52690=AXIS2_PLACEMENT_3D ( 'NONE', #201453, #118071, #101024 ) ;
#52693=CARTESIAN_POINT ( 'NONE',  ( -18.43599941264910314, -9.519327428583675754, -73.97297678952132571 ) ) ;
#52752=AXIS2_PLACEMENT_3D ( 'NONE', #189196, #50929, #91378 ) ;
#52780=AXIS2_PLACEMENT_3D ( 'NONE', #168143, #29895, #229367 ) ;
#52798=B_SPLINE_CURVE_WITH_KNOTS ( 'NONE', 3,
 ( #50245, #227610, #48976, #69853, #105057, #209329, #226309, #204193, #228908, #163808, #4698, #67259, #184637, #208077, #25581, #85499, #145506, #243319, #245909, #29461, #225027, #26881 ),
 .UNSPECIFIED., .F., .F.,
 ( 4, 3, 3, 3, 3, 3, 3, 4 ),
 ( 0.000000000000000000, 7.307836821080901168E-06, 4.161455748548376624E-05, 7.576591810647682044E-05, 0.0001098090429817505560, 0.0001438003617351163335, 0.0001777914035423660871, 0.0002117966137403033873 ),
 .UNSPECIFIED. ) ;
#52801=CARTESIAN_POINT ( 'NONE',  ( -20.85000000000000142, -1.835859311432481045, -112.0044391687985694 ) ) ;
#52814=CARTESIAN_POINT ( 'NONE',  ( 23.15000000000000213, -11.48912529306489994, -97.40000000000004832 ) ) ;
#52834=DIRECTION ( 'NONE',  ( 0.000000000000000000, 0.000000000000000000, 1.000000000000000000 ) ) ;
#52840=AXIS2_PLACEMENT_3D ( 'NONE', #76938, #157814, #58641 ) ;
#52844=ORIENTED_EDGE ( 'NONE', *, *, #163325, .T. ) ;
#52848=ORIENTED_EDGE ( 'NONE', *, *, #97769, .T. ) ;
#52864=CARTESIAN_POINT ( 'NONE',  ( -21.05000000000000071, -1.835341550213255957, -78.55515129256302487 ) ) ;
#52874=ADVANCED_FACE ( 'NONE', ( #223688 ), #24247, .T. ) ;
#52911=EDGE_LOOP ( 'NONE', ( #225695, #1913, #96577, #123278 ) ) ;
#52913=DIRECTION ( 'NONE',  ( 1.000000000000000000, -0.000000000000000000, -0.000000000000000000 ) ) ;
#52948=CARTESIAN_POINT ( 'NONE',  ( 21.04999999999999716, 8.894723818389266512, -75.48708432315146410 ) ) ;
#52955=DIRECTION ( 'NONE',  ( 0.000000000000000000, 1.000000000000000000, 0.000000000000000000 ) ) ;
#52961=ORIENTED_EDGE ( 'NONE', *, *, #157827, .F. ) ;
#52965=ADVANCED_FACE ( 'NONE', ( #209274 ), #167609, .F. ) ;
#52970=VERTEX_POINT ( 'NONE', #151904 ) ;
#52975=ADVANCED_FACE ( 'NONE', ( #30674 ), #31955, .F. ) ;
#52978=ORIENTED_EDGE ( 'NONE', *, *, #5093, .T. ) ;
#52982=EDGE_LOOP ( 'NONE', ( #134387, #190107 ) ) ;
#53007=ORIENTED_EDGE ( 'NONE', *, *, #219729, .T. ) ;
#53057=DIRECTION ( 'NONE',  ( 0.000000000000000000, 0.9908441862701596881, -0.1350103645451904977 ) ) ;
#53137=DIRECTION ( 'NONE',  ( -0.000000000000000000, 0.000000000000000000, 1.000000000000000000 ) ) ;
#53138=EDGE_LOOP ( 'NONE', ( #85595, #74200, #213963, #111404 ) ) ;
#53157=LINE ( 'NONE', #192682, #61354 ) ;
#53167=DIRECTION ( 'NONE',  ( 0.000000000000000000, 0.6728971962616697722, 0.7397360091702875895 ) ) ;
#53179=EDGE_LOOP ( 'NONE', ( #24482, #209859, #208511, #124269 ) ) ;
#53185=DIRECTION ( 'NONE',  ( 0.1538461538461510236, 0.9880948137434718559, 0.000000000000000000 ) ) ;
#53208=EDGE_CURVE ( 'NONE', #248066, #11990, #225531, .T. ) ;
#53259=AXIS2_PLACEMENT_3D ( 'NONE', #92129, #97215, #191261 ) ;
#53273=CARTESIAN_POINT ( 'NONE',  ( 21.14999999999999858, 11.65000000001116298, -79.15000000000004832 ) ) ;
#53280=AXIS2_PLACEMENT_3D ( 'NONE', #252552, #110483, #11404 ) ;
#53289=DIRECTION ( 'NONE',  ( -1.000000000000000000, -0.000000000000000000, -0.000000000000000000 ) ) ;
#53293=EDGE_CURVE ( 'NONE', #244409, #247770, #83845, .T. ) ;
#53305=CARTESIAN_POINT ( 'NONE',  ( 21.00000000000000000, 9.750000000011153745, -88.15000000000004832 ) ) ;
#53316=CARTESIAN_POINT ( 'NONE',  ( -18.50000000000000711, 11.75000000001115197, -74.01480577065404987 ) ) ;
#53318=ORIENTED_EDGE ( 'NONE', *, *, #55155, .T. ) ;
#53323=DIRECTION ( 'NONE',  ( 0.000000000000000000, 0.000000000000000000, -1.000000000000000000 ) ) ;
#53327=AXIS2_PLACEMENT_3D ( 'NONE', #46816, #188920, #222897 ) ;
#53335=VERTEX_POINT ( 'NONE', #220829 ) ;
#53372=EDGE_LOOP ( 'NONE', ( #109258, #253790, #222394, #62234, #32305 ) ) ;
#53378=CYLINDRICAL_SURFACE ( 'NONE', #125745, 0.09999999999999939493 ) ;
#53392=ORIENTED_EDGE ( 'NONE', *, *, #201426, .F. ) ;
#53447=EDGE_CURVE ( 'NONE', #187354, #18995, #225937, .T. ) ;
#53471=ADVANCED_FACE ( 'NONE', ( #188135 ), #208818, .T. ) ;
#53483=CARTESIAN_POINT ( 'NONE',  ( -23.25000000000000000, -1.249999999988843369, -108.3004807544151191 ) ) ;
#53499=CARTESIAN_POINT ( 'NONE',  ( 21.14999999999999858, 6.257814610487280937, -66.90220970869124528 ) ) ;
#53502=DIRECTION ( 'NONE',  ( -1.000000000000000000, -0.000000000000000000, -0.000000000000000000 ) ) ;
#53504=ORIENTED_EDGE ( 'NONE', *, *, #69115, .T. ) ;
#53517=CARTESIAN_POINT ( 'NONE',  ( -21.05000000000000071, 1.115600667400684642E-11, -67.00000000000004263 ) ) ;
#53576=CIRCLE ( 'NONE', #141066, 0.1000000000000028644 ) ;
#53620=VERTEX_POINT ( 'NONE', #52454 ) ;
#53634=VERTEX_POINT ( 'NONE', #113730 ) ;
#53649=FACE_OUTER_BOUND ( 'NONE', #112603, .T. ) ;
#53736=EDGE_CURVE ( 'NONE', #24899, #27072, #9082, .T. ) ;
#53740=ORIENTED_EDGE ( 'NONE', *, *, #190902, .T. ) ;
#53773=DIRECTION ( 'NONE',  ( -0.7071067811865474617, 0.7071067811865474617, 0.000000000000000000 ) ) ;
#53783=DIRECTION ( 'NONE',  ( 0.000000000000000000, -0.4791956752371546169, -0.8777080977375152360 ) ) ;
#53797=DIRECTION ( 'NONE',  ( 0.000000000000000000, -0.8700118002898359348, 0.4930308989875165082 ) ) ;
#53815=EDGE_CURVE ( 'NONE', #143381, #16002, #246578, .T. ) ;
#53857=CARTESIAN_POINT ( 'NONE',  ( 18.49999999999998934, 6.550000000011156231, -88.15000000000004832 ) ) ;
#53885=AXIS2_PLACEMENT_3D ( 'NONE', #254016, #75424, #233210 ) ;
#53893=DIRECTION ( 'NONE',  ( 1.000000000000000000, 0.000000000000000000, -0.000000000000000000 ) ) ;
#53946=CARTESIAN_POINT ( 'NONE',  ( 22.39999999999999503, 0.1000000000111554016, -59.20922040162665922 ) ) ;
#53962=DIRECTION ( 'NONE',  ( -0.000000000000000000, -0.000000000000000000, 1.000000000000000000 ) ) ;
#53983=FACE_OUTER_BOUND ( 'NONE', #63343, .T. ) ;
#54013=ORIENTED_EDGE ( 'NONE', *, *, #159332, .F. ) ;
#54024=CARTESIAN_POINT ( 'NONE',  ( 23.14999999999999858, 4.775700934590591196, -88.65123189595408348 ) ) ;
#54025=AXIS2_PLACEMENT_3D ( 'NONE', #185979, #167729, #225079 ) ;
#54076=ORIENTED_EDGE ( 'NONE', *, *, #215702, .F. ) ;
#54090=ORIENTED_EDGE ( 'NONE', *, *, #196586, .T. ) ;
#54107=CARTESIAN_POINT ( 'NONE',  ( 18.39999999999999858, -9.599999999988845900, -107.1001893912220879 ) ) ;
#54148=CARTESIAN_POINT ( 'NONE',  ( -21.05000000000000071, 1.115600667400684642E-11, -100.5000000000000426 ) ) ;
#54164=CARTESIAN_POINT ( 'NONE',  ( 20.94999999999999929, -8.999999999988842703, -90.60603087734760663 ) ) ;
#54167=EDGE_CURVE ( 'NONE', #70706, #144450, #167655, .T. ) ;
#54191=DIRECTION ( 'NONE',  ( 1.000000000000000000, 3.265361837132813093E-16, -0.000000000000000000 ) ) ;
#54197=DIRECTION ( 'NONE',  ( -0.000000000000000000, -0.000000000000000000, -1.000000000000000000 ) ) ;
#54214=CARTESIAN_POINT ( 'NONE',  ( 21.97500000000000497, 9.750000000011153745, -79.35000000000005116 ) ) ;
#54235=CARTESIAN_POINT ( 'NONE',  ( 20.94999999999999929, -1.835341550213257733, -78.55515129256302487 ) ) ;
#54300=CARTESIAN_POINT ( 'NONE',  ( -20.54999999999999716, 1.940186915899004161, -87.67088078894671810 ) ) ;
#54362=CARTESIAN_POINT ( 'NONE',  ( -20.64999999999999858, 4.350000000011156054, -79.25000000000004263 ) ) ;
#54386=DIRECTION ( 'NONE',  ( 1.000000000000000000, 0.000000000000000000, 0.000000000000000000 ) ) ;
#54441=ADVANCED_FACE ( 'NONE', ( #99615 ), #234471, .T. ) ;
#54459=AXIS2_PLACEMENT_3D ( 'NONE', #224438, #204868, #45810 ) ;
#54463=CYLINDRICAL_SURFACE ( 'NONE', #146415, 0.1000000000000006162 ) ;
#54468=EDGE_LOOP ( 'NONE', ( #254888, #53740, #14247, #105897 ) ) ;
#54478=CIRCLE ( 'NONE', #162846, 0.09999999999999939493 ) ;
#54484=EDGE_CURVE ( 'NONE', #256436, #247484, #171989, .T. ) ;
#54494=DIRECTION ( 'NONE',  ( 1.000000000000000000, 0.000000000000000000, 0.000000000000000000 ) ) ;
#54497=EDGE_CURVE ( 'NONE', #104861, #247198, #55375, .T. ) ;
#54501=CARTESIAN_POINT ( 'NONE',  ( -20.94999999999999929, -1.835341550213255957, -78.65515129256303339 ) ) ;
#54503=CIRCLE ( 'NONE', #58760, 4.049999999999998046 ) ;
#54506=CARTESIAN_POINT ( 'NONE',  ( -21.02374657821582105, 11.60000000083146077, -93.57179677019813369 ) ) ;
#54519=VERTEX_POINT ( 'NONE', #184310 ) ;
#54573=CARTESIAN_POINT ( 'NONE',  ( 20.94999999999999574, 1.835341550235567887, -78.65515129256303339 ) ) ;
#54582=EDGE_LOOP ( 'NONE', ( #127617, #186098, #122293 ) ) ;
#54604=CARTESIAN_POINT ( 'NONE',  ( 18.49351773456764292, -9.443025695134114272, -74.18532552602735564 ) ) ;
#54643=EDGE_CURVE ( 'NONE', #152543, #175862, #76252, .T. ) ;
#54661=ADVANCED_FACE ( 'NONE', ( #250707 ), #229874, .F. ) ;
#54679=CARTESIAN_POINT ( 'NONE',  ( 18.47654891039378811, -9.465274948371156682, -74.12597590519470714 ) ) ;
#54706=CIRCLE ( 'NONE', #158784, 0.2000000000000057288 ) ;
#54710=EDGE_CURVE ( 'NONE', #203487, #104152, #192990, .T. ) ;
#54750=EDGE_CURVE ( 'NONE', #39792, #135788, #176247, .T. ) ;
#54764=CARTESIAN_POINT ( 'NONE',  ( 21.05000000000000071, -9.499999999988848032, -76.89396912265249284 ) ) ;
#54842=CARTESIAN_POINT ( 'NONE',  ( 21.14999999999998082, -11.74999999998884448, -67.00000000000004263 ) ) ;
#54851=DIRECTION ( 'NONE',  ( 0.000000000000000000, 0.000000000000000000, 1.000000000000000000 ) ) ;
#54885=ORIENTED_EDGE ( 'NONE', *, *, #77257, .F. ) ;
#54890=CARTESIAN_POINT ( 'NONE',  ( 21.13435531349813701, 1.115486826172573664E-11, -60.50627893640798050 ) ) ;
#54891=CARTESIAN_POINT ( 'NONE',  ( 23.14999999999999147, 1.115600667400684642E-11, -67.00000000000004263 ) ) ;
#54892=CARTESIAN_POINT ( 'NONE',  ( -23.15000000000000213, 4.350000000011156054, -88.25000000000005684 ) ) ;
#54901=ORIENTED_EDGE ( 'NONE', *, *, #171673, .F. ) ;
#54913=EDGE_CURVE ( 'NONE', #50622, #121769, #130431, .T. ) ;
#54968=ORIENTED_EDGE ( 'NONE', *, *, #8817, .F. ) ;
#54971=ORIENTED_EDGE ( 'NONE', *, *, #156545, .F. ) ;
#55000=EDGE_LOOP ( 'NONE', ( #46009, #226030, #122165, #164063 ) ) ;
#55009=DIRECTION ( 'NONE',  ( 0.000000000000000000, 0.000000000000000000, -1.000000000000000000 ) ) ;
#55012=CIRCLE ( 'NONE', #38467, 0.1000000000000002831 ) ;
#55023=CARTESIAN_POINT ( 'NONE',  ( -20.94999999999999929, -11.48912529306490349, -70.00000000000004263 ) ) ;
#55033=AXIS2_PLACEMENT_3D ( 'NONE', #72100, #250713, #13407 ) ;
#55035=FACE_OUTER_BOUND ( 'NONE', #22365, .T. ) ;
#55043=EDGE_CURVE ( 'NONE', #105777, #201510, #55743, .T. ) ;
#55109=ORIENTED_EDGE ( 'NONE', *, *, #49151, .F. ) ;
#55117=CARTESIAN_POINT ( 'NONE',  ( -23.25000000000000000, -9.599999999988847676, -76.89396912265249284 ) ) ;
#55122=EDGE_CURVE ( 'NONE', #53620, #72835, #84786, .T. ) ;
#55135=CARTESIAN_POINT ( 'NONE',  ( 22.39999999999999503, 1.115541036281197940E-11, -59.20922040162666633 ) ) ;
#55155=EDGE_CURVE ( 'NONE', #111358, #223130, #201521, .T. ) ;
#55157=EDGE_LOOP ( 'NONE', ( #254529, #27434, #205682 ) ) ;
#55160=EDGE_CURVE ( 'NONE', #176751, #31646, #89095, .T. ) ;
#55201=VECTOR ( 'NONE', #9158, 1000.000000000000000 ) ;
#55218=DIRECTION ( 'NONE',  ( 1.000000000000000000, 0.000000000000000000, 0.000000000000000000 ) ) ;
#55233=FACE_OUTER_BOUND ( 'NONE', #71395, .T. ) ;
#55237=DIRECTION ( 'NONE',  ( 1.000000000000000000, 0.000000000000000000, 0.000000000000000000 ) ) ;
#55274=DIRECTION ( 'NONE',  ( 3.469446951953635015E-14, -0.000000000000000000, 1.000000000000000000 ) ) ;
#55346=CIRCLE ( 'NONE', #146950, 0.09999999999999939493 ) ;
#55357=VECTOR ( 'NONE', #10540, 1000.000000000000000 ) ;
#55375=CIRCLE ( 'NONE', #163577, 0.09999999999999741040 ) ;
#55385=CIRCLE ( 'NONE', #201167, 0.1000000000000028644 ) ;
#55399=CARTESIAN_POINT ( 'NONE',  ( -21.14999999999999858, -0.09999999998884338825, -60.45934304829880546 ) ) ;
#55413=VERTEX_POINT ( 'NONE', #91982 ) ;
#55434=CARTESIAN_POINT ( 'NONE',  ( -20.54999999999999716, -8.999999999988846255, -76.89396912265249284 ) ) ;
#55435=FACE_OUTER_BOUND ( 'NONE', #220410, .T. ) ;
#55450=LINE ( 'NONE', #230265, #64606 ) ;
#55486=CARTESIAN_POINT ( 'NONE',  ( 21.05000000000000071, 8.876614585098257848, -75.38508047884472774 ) ) ;
#55489=CARTESIAN_POINT ( 'NONE',  ( -20.64999999999999858, -8.999999999988844479, -90.60603087734760663 ) ) ;
#55528=CIRCLE ( 'NONE', #126304, 0.09999999999999741040 ) ;
#55535=CARTESIAN_POINT ( 'NONE',  ( -21.12757541349819590, 0.005161215820883788274, -60.52661942874848222 ) ) ;
#55559=EDGE_CURVE ( 'NONE', #153327, #95642, #55938, .T. ) ;
#55562=CIRCLE ( 'NONE', #122247, 0.09999999999999939493 ) ;
#55565=EDGE_CURVE ( 'NONE', #71736, #118383, #243209, .T. ) ;
#55568=CIRCLE ( 'NONE', #234688, 0.5000000000000004441 ) ;
#55597=LINE ( 'NONE', #193871, #93579 ) ;
#55608=ORIENTED_EDGE ( 'NONE', *, *, #104327, .F. ) ;
#55618=ORIENTED_EDGE ( 'NONE', *, *, #150387, .F. ) ;
#55624=FACE_OUTER_BOUND ( 'NONE', #3934, .T. ) ;
#55646=AXIS2_PLACEMENT_3D ( 'NONE', #630, #58040, #138845 ) ;
#55668=AXIS2_PLACEMENT_3D ( 'NONE', #168939, #46357, #64650 ) ;
#55671=DIRECTION ( 'NONE',  ( 0.000000000000000000, -0.000000000000000000, 1.000000000000000000 ) ) ;
#55672=CIRCLE ( 'NONE', #63909, 0.1000000000000020595 ) ;
#55675=ORIENTED_EDGE ( 'NONE', *, *, #117083, .F. ) ;
#55680=DIRECTION ( 'NONE',  ( -1.000000000000000000, 0.000000000000000000, 0.000000000000000000 ) ) ;
#55695=ORIENTED_EDGE ( 'NONE', *, *, #173932, .F. ) ;
#55702=EDGE_CURVE ( 'NONE', #101410, #3545, #245628, .T. ) ;
#55723=CYLINDRICAL_SURFACE ( 'NONE', #222144, 0.09999999999999939493 ) ;
#55743=CIRCLE ( 'NONE', #243033, 0.1000000000000000472 ) ;
#55746=CARTESIAN_POINT ( 'NONE',  ( -18.59999999999999787, 11.65000000001115232, -74.01480577065404987 ) ) ;
#55754=CARTESIAN_POINT ( 'NONE',  ( -18.50000000000000000, -1.687074390080403941, -54.18542703345839584 ) ) ;
#55762=CARTESIAN_POINT ( 'NONE',  ( -23.15000000000000213, 4.350000000011156054, -79.35000000000005116 ) ) ;
#55789=FACE_OUTER_BOUND ( 'NONE', #137189, .T. ) ;
#55802=AXIS2_PLACEMENT_3D ( 'NONE', #242484, #221620, #44307 ) ;
#55830=CARTESIAN_POINT ( 'NONE',  ( 18.49999999999999645, -1.835859311432484375, -112.0044391687985694 ) ) ;
#55847=DIRECTION ( 'NONE',  ( 1.000000000000000000, -0.000000000000000000, -0.000000000000000000 ) ) ;
#55864=CARTESIAN_POINT ( 'NONE',  ( 18.46947024752519084, -9.509297157144997570, -73.98668944869785946 ) ) ;
#55867=ORIENTED_EDGE ( 'NONE', *, *, #4485, .T. ) ;
#55869=EDGE_LOOP ( 'NONE', ( #203478, #242335 ) ) ;
#55879=CIRCLE ( 'NONE', #1728, 0.1000000000000028644 ) ;
#55890=VERTEX_POINT ( 'NONE', #94246 ) ;
#55920=CIRCLE ( 'NONE', #93348, 0.1000000000000028644 ) ;
#55938=CIRCLE ( 'NONE', #201706, 0.1999999999999987899 ) ;
#55942=LINE ( 'NONE', #37716, #78304 ) ;
#55960=ORIENTED_EDGE ( 'NONE', *, *, #47273, .T. ) ;
#55981=AXIS2_PLACEMENT_3D ( 'NONE', #210356, #151690, #111248 ) ;
#55997=VERTEX_POINT ( 'NONE', #26282 ) ;
#56043=DIRECTION ( 'NONE',  ( 0.000000000000000000, 0.000000000000000000, 1.000000000000000000 ) ) ;
#56046=CARTESIAN_POINT ( 'NONE',  ( 23.14999999999998437, 1.115600667400684642E-11, -67.00000000000004263 ) ) ;
#56047=CIRCLE ( 'NONE', #210393, 0.09999999999999939493 ) ;
#56053=CYLINDRICAL_SURFACE ( 'NONE', #71496, 0.09999999999999939493 ) ;
#56068=FACE_OUTER_BOUND ( 'NONE', #121963, .T. ) ;
#56087=EDGE_LOOP ( 'NONE', ( #234654, #230800, #45815, #240328 ) ) ;
#56090=B_SPLINE_CURVE_WITH_KNOTS ( 'NONE', 3,
 ( #232060, #156389, #113380, #54679, #213758, #35166, #114660, #194227, #15590, #95096 ),
 .UNSPECIFIED., .F., .F.,
 ( 4, 2, 2, 2, 4 ),
 ( 0.000000000000000000, 0.0001584437871625023631, 0.0002376656807437556318, 0.0002772766275343830386, 0.0003168875743250104725 ),
 .UNSPECIFIED. ) ;
#56106=DIRECTION ( 'NONE',  ( 0.000000000000000000, -0.9893560106964500722, 0.1455152366551550613 ) ) ;
#56151=EDGE_CURVE ( 'NONE', #133700, #214401, #134338, .T. ) ;
#56152=CARTESIAN_POINT ( 'NONE',  ( 21.05000000000000071, 5.000000000011153745, -88.09473398108696074 ) ) ;
#56162=AXIS2_PLACEMENT_3D ( 'NONE', #208665, #146092, #27487 ) ;
#56167=DIRECTION ( 'NONE',  ( -0.000000000000000000, -1.000000000000000000, 0.000000000000000000 ) ) ;
#56168=ORIENTED_EDGE ( 'NONE', *, *, #38787, .T. ) ;
#56186=CIRCLE ( 'NONE', #131209, 0.09999999999999939493 ) ;
#56192=CARTESIAN_POINT ( 'NONE',  ( -18.41418431465368144, -9.499999999989071853, -107.1001893912215195 ) ) ;
#56195=CARTESIAN_POINT ( 'NONE',  ( -22.50000000000000000, 1.115600667400684642E-11, -67.00000000000004263 ) ) ;
#56199=EDGE_CURVE ( 'NONE', #203190, #62297, #210284, .T. ) ;
#56207=ADVANCED_FACE ( 'NONE', ( #95230 ), #213894, .F. ) ;
#56225=VERTEX_POINT ( 'NONE', #172250 ) ;
#56240=ORIENTED_EDGE ( 'NONE', *, *, #174241, .T. ) ;
#56265=ADVANCED_FACE ( 'NONE', ( #28432, #88328 ), #152217, .F. ) ;
#56270=CARTESIAN_POINT ( 'NONE',  ( -20.94999999999999929, 1.835341550235569663, -78.55515129256302487 ) ) ;
#56281=TOROIDAL_SURFACE ( 'NONE', #226985, 12.97499999999999609, 0.1000000000000000056 ) ;
#56282=CARTESIAN_POINT ( 'NONE',  ( 18.50000000000000000, -9.399999999988843058, -73.99928567783889832 ) ) ;
#56305=CIRCLE ( 'NONE', #202075, 0.1000000000000028644 ) ;
#56312=ORIENTED_EDGE ( 'NONE', *, *, #186651, .T. ) ;
#56321=DIRECTION ( 'NONE',  ( 0.000000000000000000, 0.000000000000000000, -1.000000000000000000 ) ) ;
#56336=EDGE_CURVE ( 'NONE', #58672, #189831, #44798, .T. ) ;
#56383=CARTESIAN_POINT ( 'NONE',  ( 18.59999999999999076, 10.25000000001115552, -91.75000000000005684 ) ) ;
#56411=DIRECTION ( 'NONE',  ( 0.000000000000000000, 0.000000000000000000, -1.000000000000000000 ) ) ;
#56412=AXIS2_PLACEMENT_3D ( 'NONE', #199271, #59723, #1023 ) ;
#56423=CIRCLE ( 'NONE', #39895, 0.1000000000000008937 ) ;
#56430=VERTEX_POINT ( 'NONE', #90534 ) ;
#56438=CARTESIAN_POINT ( 'NONE',  ( 21.07016717457011623, 1.115539956314190190E-11, -60.67905916189912574 ) ) ;
#56453=CARTESIAN_POINT ( 'NONE',  ( 21.05000000000000071, -11.64999999998883595, -97.60000000000005116 ) ) ;
#56473=ORIENTED_EDGE ( 'NONE', *, *, #167381, .T. ) ;
#56510=CARTESIAN_POINT ( 'NONE',  ( 20.94999999999999929, 10.29270135741298731, -105.9573618871519756 ) ) ;
#56520=CONICAL_SURFACE ( 'NONE', #177207, 4.299999999999956302, 0.7853981633974466137 ) ;
#56527=CARTESIAN_POINT ( 'NONE',  ( -18.46093223321774701, -9.480682968263366206, -74.08455051392672885 ) ) ;
#56528=CARTESIAN_POINT ( 'NONE',  ( 21.05000000000000071, -8.730841121484166578, -90.90192528101570701 ) ) ;
#56591=CARTESIAN_POINT ( 'NONE',  ( 20.02499999999999858, 9.750000000011153745, -88.15000000000004832 ) ) ;
#56612=SPHERICAL_SURFACE ( 'NONE', #94304, 0.1000000000000000056 ) ;
#56623=EDGE_CURVE ( 'NONE', #73311, #98112, #31609, .T. ) ;
#56630=CARTESIAN_POINT ( 'NONE',  ( 22.47071067811865319, 7.720074744509199505, -66.90090754529744288 ) ) ;
#56675=EDGE_CURVE ( 'NONE', #253099, #155361, #231321, .T. ) ;
#56678=ADVANCED_FACE ( 'NONE', ( #147325 ), #254290, .T. ) ;
#56687=FACE_OUTER_BOUND ( 'NONE', #239468, .T. ) ;
#56712=ORIENTED_EDGE ( 'NONE', *, *, #23220, .F. ) ;
#56727=CARTESIAN_POINT ( 'NONE',  ( 20.94999999999999574, 1.162701749949165642, -75.10000000000003695 ) ) ;
#56730=B_SPLINE_CURVE_WITH_KNOTS ( 'NONE', 3,
 ( #35775, #194852, #17467, #179145, #96964, #159560, #175298 ),
 .UNSPECIFIED., .F., .F.,
 ( 4, 3, 4 ),
 ( 0.000000000000000000, 1.860045280646151707E-05, 5.251155757305330614E-05 ),
 .UNSPECIFIED. ) ;
#56740=EDGE_CURVE ( 'NONE', #68386, #133700, #102267, .T. ) ;
#56745=VERTEX_POINT ( 'NONE', #194179 ) ;
#56747=AXIS2_PLACEMENT_3D ( 'NONE', #33199, #213067, #249647 ) ;
#56749=ADVANCED_FACE ( 'NONE', ( #117192 ), #18908, .T. ) ;
#56793=DIRECTION ( 'NONE',  ( 1.000000000000000000, 0.000000000000000000, -0.000000000000000000 ) ) ;
#56804=FACE_OUTER_BOUND ( 'NONE', #155410, .T. ) ;
#56835=ORIENTED_EDGE ( 'NONE', *, *, #183317, .F. ) ;
#56861=ORIENTED_EDGE ( 'NONE', *, *, #224395, .T. ) ;
#56869=LINE ( 'NONE', #179442, #190124 ) ;
#56879=AXIS2_PLACEMENT_3D ( 'NONE', #171972, #93672, #195367 ) ;
#56883=DIRECTION ( 'NONE',  ( 0.000000000000000000, 0.8660254037844384856, -0.5000000000000003331 ) ) ;
#56894=VERTEX_POINT ( 'NONE', #240992 ) ;
#56910=DIRECTION ( 'NONE',  ( -0.000000000000000000, -0.000000000000000000, 1.000000000000000000 ) ) ;
#56918=AXIS2_PLACEMENT_3D ( 'NONE', #72331, #227524, #28080 ) ;
#56919=DIRECTION ( 'NONE',  ( -3.469446951953635015E-14, -1.000000000000000000, 0.000000000000000000 ) ) ;
#56946=LINE ( 'NONE', #137784, #5228 ) ;
#56967=CARTESIAN_POINT ( 'NONE',  ( 20.95159278453404283, 8.907896337960206523, -75.48472018510929615 ) ) ;
#57023=PLANE ( 'NONE',  #199286 ) ;
#57025=TOROIDAL_SURFACE ( 'NONE', #219535, 0.9750000000000019762, 0.1000000000000000056 ) ;
#57048=CARTESIAN_POINT ( 'NONE',  ( 21.04116576186320486, 10.62466307876251115, -79.32858176862818311 ) ) ;
#57054=( BOUNDED_SURFACE ( )  B_SPLINE_SURFACE ( 3, 2, ( 
 ( #92444, #117162, #97555 ),
 ( #156317, #256603, #233280 ),
 ( #54604, #177159, #213684 ),
 ( #72931, #128055, #78015 ),
 ( #172036, #132880, #16792 ),
 ( #114591, #255323, #55864 ),
 ( #157608, #135420, #211124 ),
 ( #112035, #113302, #14230 ) ),
 .UNSPECIFIED., .F., .F., .T. ) 
 B_SPLINE_SURFACE_WITH_KNOTS ( ( 4, 2, 2, 4 ),
 ( 3, 3 ),
 ( 0.0001704874539069910233, 0.0003809798300636651949, 0.0004862260181420022536, 0.0005914722062203393122 ),
 ( 0.000000000000000000, 1.000000000000000000 ),
 .UNSPECIFIED. ) 
 GEOMETRIC_REPRESENTATION_ITEM ( )  RATIONAL_B_SPLINE_SURFACE ( (
 ( 1.000000000000000000, 0.7071067811864942820, 1.000000000000000000),
 ( 1.000000000000000000, 0.7670648383577298723, 1.000000000000000000),
 ( 1.000000000000000000, 0.8204820770251111117, 1.000000000000000000),
 ( 1.000000000000000000, 0.8877218296114299800, 1.000000000000000000),
 ( 1.000000000000000000, 0.9080815932667398727, 1.000000000000000000),
 ( 1.000000000000000000, 0.9395541505860036668, 1.000000000000000000),
 ( 1.000000000000000000, 0.9506520335380280740, 1.000000000000000000),
 ( 1.000000000000000000, 0.9504532311154628710, 1.000000000000000000) ) ) 
 REPRESENTATION_ITEM ( '' )  SURFACE ( )  );
#57077=CARTESIAN_POINT ( 'NONE',  ( 23.14999999999999858, 5.500000000011153745, -88.09473398108696074 ) ) ;
#57083=DIRECTION ( 'NONE',  ( 1.000000000000000000, 0.000000000000000000, 0.000000000000000000 ) ) ;
#57100=DIRECTION ( 'NONE',  ( 1.000000000000000000, 0.000000000000000000, 0.000000000000000000 ) ) ;
#57110=ORIENTED_EDGE ( 'NONE', *, *, #230723, .F. ) ;
#57114=VECTOR ( 'NONE', #81898, 1000.000000000000000 ) ;
#57137=CIRCLE ( 'NONE', #44703, 0.1000000000000028644 ) ;
#57143=AXIS2_PLACEMENT_3D ( 'NONE', #18356, #138278, #70974 ) ;
#57169=LINE ( 'NONE', #216256, #164998 ) ;
#57199=EDGE_CURVE ( 'NONE', #31018, #64899, #77512, .T. ) ;
#57227=DIRECTION ( 'NONE',  ( -1.000000000000000000, -0.000000000000000000, -0.000000000000000000 ) ) ;
#57239=B_SPLINE_CURVE_WITH_KNOTS ( 'NONE', 3,
 ( #193816, #16476, #219771, #58118, #75170, #235488, #215914, #95970, #195118, #17713, #116837, #97224, #15184, #154710, #175551, #55535, #254992, #76408, #137658 ),
 .UNSPECIFIED., .F., .F.,
 ( 4, 3, 3, 3, 3, 3, 4 ),
 ( 0.000000000000000000, 1.655171619026035414E-05, 2.773500582848695921E-05, 5.941817267378355548E-05, 0.0001114174635873587483, 0.0001914169455916365928, 0.0002627181070750677803 ),
 .UNSPECIFIED. ) ;
#57241=DIRECTION ( 'NONE',  ( 0.000000000000000000, 1.224646799142015331E-16, 1.000000000000000000 ) ) ;
#57262=CIRCLE ( 'NONE', #90586, 0.09999999999999982514 ) ;
#57314=EDGE_CURVE ( 'NONE', #48905, #82676, #31958, .T. ) ;
#57347=DIRECTION ( 'NONE',  ( 0.000000000000000000, 0.000000000000000000, -1.000000000000000000 ) ) ;
#57377=CARTESIAN_POINT ( 'NONE',  ( -23.25000000000000000, 11.65000000001115588, -67.00000000000004263 ) ) ;
#57402=DIRECTION ( 'NONE',  ( 0.000000000000000000, -0.4930308989875324399, -0.8700118002898268310 ) ) ;
#57414=CARTESIAN_POINT ( 'NONE',  ( 21.14999999999999503, 11.65000000001116298, -67.00000000000004263 ) ) ;
#57438=DIRECTION ( 'NONE',  ( -4.801466763864313332E-15, -0.2605042016806672911, -0.9654727137038716656 ) ) ;
#57442=EDGE_CURVE ( 'NONE', #97847, #76842, #23605, .T. ) ;
#57458=CARTESIAN_POINT ( 'NONE',  ( 21.05000000000000071, -0.02138556592644301479, -60.69503888731549068 ) ) ;
#57490=ORIENTED_EDGE ( 'NONE', *, *, #137902, .T. ) ;
#57525=CYLINDRICAL_SURFACE ( 'NONE', #152935, 0.09999999999999939493 ) ;
#57551=ORIENTED_EDGE ( 'NONE', *, *, #4107, .F. ) ;
#57567=CIRCLE ( 'NONE', #199243, 0.1000000000000028644 ) ;
#57575=ORIENTED_EDGE ( 'NONE', *, *, #54497, .T. ) ;
#57585=ORIENTED_EDGE ( 'NONE', *, *, #48641, .T. ) ;
#57588=DIRECTION ( 'NONE',  ( -0.7071067811865474617, -0.7071067811865474617, -0.000000000000000000 ) ) ;
#57626=DIRECTION ( 'NONE',  ( 0.000000000000000000, 0.000000000000000000, -1.000000000000000000 ) ) ;
#57634=DIRECTION ( 'NONE',  ( -1.000000000000000000, 0.000000000000000000, -0.000000000000000000 ) ) ;
#57663=FACE_OUTER_BOUND ( 'NONE', #237216, .T. ) ;
#57693=ORIENTED_EDGE ( 'NONE', *, *, #22280, .F. ) ;
#57701=DIRECTION ( 'NONE',  ( -3.469446951953605354E-14, 1.000000000000000000, 0.000000000000000000 ) ) ;
#57750=AXIS2_PLACEMENT_3D ( 'NONE', #66595, #126563, #31351 ) ;
#57791=DIRECTION ( 'NONE',  ( -1.000000000000000000, -0.000000000000000000, -0.000000000000000000 ) ) ;
#57798=ORIENTED_EDGE ( 'NONE', *, *, #42473, .F. ) ;
#57862=DIRECTION ( 'NONE',  ( 0.000000000000000000, 1.265107689135680095E-16, -1.000000000000000000 ) ) ;
#57920=DIRECTION ( 'NONE',  ( -0.000000000000000000, -0.000000000000000000, 1.000000000000000000 ) ) ;
#57947=CARTESIAN_POINT ( 'NONE',  ( -23.25000000000000000, 5.950000000011167245, -90.19429769496522908 ) ) ;
#57959=LINE ( 'NONE', #97062, #151081 ) ;
#57960=VERTEX_POINT ( 'NONE', #250631 ) ;
#57969=EDGE_CURVE ( 'NONE', #75011, #202644, #193875, .T. ) ;
#57971=CARTESIAN_POINT ( 'NONE',  ( -20.94999999999999929, -1.162701749926853712, -75.10000000000003695 ) ) ;
#57973=VECTOR ( 'NONE', #194630, 1000.000000000000000 ) ;
#58020=EDGE_CURVE ( 'NONE', #126808, #60368, #181422, .T. ) ;
#58039=EDGE_CURVE ( 'NONE', #184752, #177157, #172438, .T. ) ;
#58040=DIRECTION ( 'NONE',  ( -1.000000000000000000, 0.000000000000000000, 0.000000000000000000 ) ) ;
#58078=AXIS2_PLACEMENT_3D ( 'NONE', #226460, #252139, #206928 ) ;
#58083=AXIS2_PLACEMENT_3D ( 'NONE', #34663, #54191, #72500 ) ;
#58113=DIRECTION ( 'NONE',  ( -1.000000000000000000, 0.000000000000000000, 0.000000000000000000 ) ) ;
#58118=CARTESIAN_POINT ( 'NONE',  ( -21.08035267497491816, 0.08268862478717949049, -60.66829316021700436 ) ) ;
#58127=CARTESIAN_POINT ( 'NONE',  ( 20.85000000000000142, 11.75000000001115907, -100.5000000000000426 ) ) ;
#58141=ORIENTED_EDGE ( 'NONE', *, *, #124089, .F. ) ;
#58167=DIRECTION ( 'NONE',  ( -1.000000000000000000, 6.938893903907270030E-14, 0.000000000000000000 ) ) ;
#58189=ORIENTED_EDGE ( 'NONE', *, *, #49932, .F. ) ;
#58197=CARTESIAN_POINT ( 'NONE',  ( 21.00000000000000000, 9.750000000011153745, -79.35000000000005116 ) ) ;
#58223=CARTESIAN_POINT ( 'NONE',  ( -23.25000000000000000, 1.115600667400684642E-11, -71.05000000000003979 ) ) ;
#58233=ADVANCED_FACE ( 'NONE', ( #26176 ), #163124, .T. ) ;
#58245=ADVANCED_FACE ( 'NONE', ( #122718 ), #245222, .T. ) ;
#58255=ORIENTED_EDGE ( 'NONE', *, *, #181365, .F. ) ;
#58275=DIRECTION ( 'NONE',  ( 0.000000000000000000, 0.000000000000000000, -1.000000000000000000 ) ) ;
#58279=DIRECTION ( 'NONE',  ( 0.000000000000000000, -1.000000000000000000, 0.000000000000000000 ) ) ;
#58314=ORIENTED_EDGE ( 'NONE', *, *, #255960, .T. ) ;
#58325=CARTESIAN_POINT ( 'NONE',  ( -18.54270223418606633, -9.624105502871746154, -107.2409350504074723 ) ) ;
#58329=CARTESIAN_POINT ( 'NONE',  ( -18.59999999999999787, 1.115600667400684642E-11, -67.00000000000004263 ) ) ;
#58333=DIRECTION ( 'NONE',  ( -1.000000000000000000, 0.000000000000000000, 0.000000000000000000 ) ) ;
#58336=EDGE_LOOP ( 'NONE', ( #51818, #222756, #251620, #160544 ) ) ;
#58354=ADVANCED_FACE ( 'NONE', ( #27493 ), #104259, .T. ) ;
#58359=LINE ( 'NONE', #178365, #79448 ) ;
#58371=TOROIDAL_SURFACE ( 'NONE', #170704, 0.2000000000000000111, 0.1000000000000000056 ) ;
#58435=DIRECTION ( 'NONE',  ( 0.000000000000000000, 0.000000000000000000, -1.000000000000000000 ) ) ;
#58451=VERTEX_POINT ( 'NONE', #69165 ) ;
#58462=EDGE_CURVE ( 'NONE', #181640, #106717, #249364, .T. ) ;
#58478=DIRECTION ( 'NONE',  ( 0.000000000000000000, -0.1350103645451904977, -0.9908441862701596881 ) ) ;
#58480=AXIS2_PLACEMENT_3D ( 'NONE', #224642, #9456, #6885 ) ;
#58508=EDGE_CURVE ( 'NONE', #154967, #10263, #227540, .T. ) ;
#58510=CARTESIAN_POINT ( 'NONE',  ( 20.94999999999999929, -8.999999999988844479, -76.89396912265249284 ) ) ;
#58515=ADVANCED_FACE ( 'NONE', ( #39985 ), #60782, .F. ) ;
#58532=ORIENTED_EDGE ( 'NONE', *, *, #55160, .T. ) ;
#58554=CARTESIAN_POINT ( 'NONE',  ( 18.59999999999999076, 11.65000000001115943, -55.25000000000004974 ) ) ;
#58562=FACE_OUTER_BOUND ( 'NONE', #167473, .T. ) ;
#58572=ORIENTED_EDGE ( 'NONE', *, *, #202223, .T. ) ;
#58577=EDGE_LOOP ( 'NONE', ( #130661, #229871, #125360, #73650, #60938, #29970 ) ) ;
#58601=AXIS2_PLACEMENT_3D ( 'NONE', #243439, #169084, #9969 ) ;
#58607=DIRECTION ( 'NONE',  ( 0.000000000000000000, 0.4930308989875230585, 0.8700118002898322711 ) ) ;
#58641=DIRECTION ( 'NONE',  ( 0.000000000000000000, 0.000000000000000000, 1.000000000000000000 ) ) ;
#58644=CARTESIAN_POINT ( 'NONE',  ( 23.24999999999999289, 11.65000000001116298, -55.25000000000004974 ) ) ;
#58647=EDGE_LOOP ( 'NONE', ( #232283, #127420, #184316, #172510 ) ) ;
#58672=VERTEX_POINT ( 'NONE', #163760 ) ;
#58680=ADVANCED_FACE ( 'NONE', ( #31967 ), #249709, .T. ) ;
#58708=ORIENTED_EDGE ( 'NONE', *, *, #79931, .F. ) ;
#58722=VERTEX_POINT ( 'NONE', #254786 ) ;
#58729=CARTESIAN_POINT ( 'NONE',  ( 21.05000000000000071, 0.09779029132038050132, -60.74218538951851798 ) ) ;
#58749=ORIENTED_EDGE ( 'NONE', *, *, #137570, .T. ) ;
#58751=EDGE_LOOP ( 'NONE', ( #229747, #41710, #234577, #157481, #41067 ) ) ;
#58752=EDGE_CURVE ( 'NONE', #23868, #214700, #44227, .T. ) ;
#58759=CARTESIAN_POINT ( 'NONE',  ( 20.94999999999999929, 5.000000000011153745, -79.40526601891313874 ) ) ;
#58760=AXIS2_PLACEMENT_3D ( 'NONE', #187316, #90747, #71224 ) ;
#58784=AXIS2_PLACEMENT_3D ( 'NONE', #111542, #174128, #192365 ) ;
#58805=DIRECTION ( 'NONE',  ( 0.000000000000000000, 0.000000000000000000, 1.000000000000000000 ) ) ;
#58806=ORIENTED_EDGE ( 'NONE', *, *, #204273, .F. ) ;
#58814=VERTEX_POINT ( 'NONE', #21393 ) ;
#58816=ORIENTED_EDGE ( 'NONE', *, *, #81626, .T. ) ;
#58823=CIRCLE ( 'NONE', #217229, 0.1000000000000028644 ) ;
#58871=CARTESIAN_POINT ( 'NONE',  ( -21.05000000000000071, -11.48912529306490349, -70.10000000000005116 ) ) ;
#58895=CARTESIAN_POINT ( 'NONE',  ( -23.15000000000000213, -9.499999999988848032, -76.89396912265249284 ) ) ;
#58972=CARTESIAN_POINT ( 'NONE',  ( 20.85000000000000142, -1.835859311432481045, -112.0044391687985694 ) ) ;
#58973=EDGE_CURVE ( 'NONE', #120817, #155038, #102812, .T. ) ;
#59009=DIRECTION ( 'NONE',  ( 1.000000000000000000, 0.000000000000000000, 0.000000000000000000 ) ) ;
#59033=CARTESIAN_POINT ( 'NONE',  ( 21.07933241753356768, 6.328645948390905218, -66.90662040958073931 ) ) ;
#59050=AXIS2_PLACEMENT_3D ( 'NONE', #249798, #169018, #30777 ) ;
#59096=CARTESIAN_POINT ( 'NONE',  ( -18.50000000000000000, 11.75000000001115552, -79.15000000000003411 ) ) ;
#59101=VERTEX_POINT ( 'NONE', #90312 ) ;
#59123=AXIS2_PLACEMENT_3D ( 'NONE', #188644, #169124, #20160 ) ;
#59130=DIRECTION ( 'NONE',  ( -1.000000000000000000, 0.000000000000000000, 0.000000000000000000 ) ) ;
#59133=DIRECTION ( 'NONE',  ( 0.000000000000000000, 0.000000000000000000, -1.000000000000000000 ) ) ;
#59142=ORIENTED_EDGE ( 'NONE', *, *, #8112, .F. ) ;
#59145=VERTEX_POINT ( 'NONE', #95462 ) ;
#59162=DIRECTION ( 'NONE',  ( -1.000000000000000000, -8.673617379884087537E-15, 0.000000000000000000 ) ) ;
#59163=FACE_OUTER_BOUND ( 'NONE', #136615, .T. ) ;
#59168=DIRECTION ( 'NONE',  ( -1.000000000000000000, 0.000000000000000000, 0.000000000000000000 ) ) ;
#59186=AXIS2_PLACEMENT_3D ( 'NONE', #43890, #123428, #243363 ) ;
#59218=DIRECTION ( 'NONE',  ( 0.000000000000000000, 1.000000000000000000, 0.000000000000000000 ) ) ;
#59244=CARTESIAN_POINT ( 'NONE',  ( 18.59999999999999076, -1.851617760457748618, -112.1031897196037050 ) ) ;
#59260=CARTESIAN_POINT ( 'NONE',  ( -20.94999999999999929, 7.031312794766356511, -104.1091509382273586 ) ) ;
#59271=CARTESIAN_POINT ( 'NONE',  ( -21.05000000000000071, 1.115600667400684642E-11, -100.5000000000000426 ) ) ;
#59274=CARTESIAN_POINT ( 'NONE',  ( -21.05000000000000071, 11.75000000001115197, -93.48519422934609224 ) ) ;
#59281=ORIENTED_EDGE ( 'NONE', *, *, #104438, .T. ) ;
#59291=B_SPLINE_CURVE_WITH_KNOTS ( 'NONE', 3,
 ( #128429, #207984, #189688, #170172, #108860, #249667, #25488, #256020 ),
 .UNSPECIFIED., .F., .F.,
 ( 4, 2, 2, 4 ),
 ( 0.000000000000000000, 6.534141206311282169E-05, 0.0001306828241262256434, 0.0002613656482524638093 ),
 .UNSPECIFIED. ) ;
#59305=DIRECTION ( 'NONE',  ( 0.000000000000000000, 1.000000000000000000, 0.000000000000000000 ) ) ;
#59325=ADVANCED_FACE ( 'NONE', ( #223109 ), #144853, .F. ) ;
#59327=EDGE_CURVE ( 'NONE', #50892, #70706, #146142, .T. ) ;
#59346=EDGE_CURVE ( 'NONE', #4064, #224664, #127880, .T. ) ;
#59354=ADVANCED_FACE ( 'NONE', ( #185284 ), #174391, .T. ) ;
#59376=DIRECTION ( 'NONE',  ( -0.000000000000000000, -0.000000000000000000, 1.000000000000000000 ) ) ;
#59410=ORIENTED_EDGE ( 'NONE', *, *, #196574, .T. ) ;
#59456=FACE_OUTER_BOUND ( 'NONE', #48952, .T. ) ;
#59459=ORIENTED_EDGE ( 'NONE', *, *, #184251, .T. ) ;
#59467=AXIS2_PLACEMENT_3D ( 'NONE', #5652, #205146, #81331 ) ;
#59479=DIRECTION ( 'NONE',  ( 0.000000000000000000, -0.9999176327611369874, 0.01283462868041984617 ) ) ;
#59487=CIRCLE ( 'NONE', #238596, 0.1000000000000028644 ) ;
#59488=CIRCLE ( 'NONE', #251044, 0.1000000000000028644 ) ;
#59494=LINE ( 'NONE', #219884, #122606 ) ;
#59507=ORIENTED_EDGE ( 'NONE', *, *, #129134, .F. ) ;
#59537=CARTESIAN_POINT ( 'NONE',  ( 20.04142135623730070, 11.65000000001115943, -88.35000000000003695 ) ) ;
#59581=CARTESIAN_POINT ( 'NONE',  ( -18.50000000000000000, 11.65000000001115232, -74.01480577065404987 ) ) ;
#59583=AXIS2_PLACEMENT_3D ( 'NONE', #163681, #140233, #25461 ) ;
#59599=DIRECTION ( 'NONE',  ( 0.000000000000000000, 8.881784197002011602E-16, -1.000000000000000000 ) ) ;
#59601=AXIS2_PLACEMENT_3D ( 'NONE', #42288, #4426, #241758 ) ;
#59616=DIRECTION ( 'NONE',  ( 0.000000000000000000, 2.891205793294679805E-16, -1.000000000000000000 ) ) ;
#59635=DIRECTION ( 'NONE',  ( 0.000000000000000000, 0.000000000000000000, -1.000000000000000000 ) ) ;
#59668=CARTESIAN_POINT ( 'NONE',  ( -21.14999999999999858, 11.75000000001115552, -73.78386566297820082 ) ) ;
#59687=FACE_OUTER_BOUND ( 'NONE', #147662, .T. ) ;
#59695=ADVANCED_FACE ( 'NONE', ( #165419 ), #37814, .T. ) ;
#59723=DIRECTION ( 'NONE',  ( -1.000000000000000000, 0.000000000000000000, 0.000000000000000000 ) ) ;
#59726=CARTESIAN_POINT ( 'NONE',  ( -23.25000000000000000, 2.600000000011156054, -87.27537807723794572 ) ) ;
#59733=DIRECTION ( 'NONE',  ( 1.000000000000000000, 1.875376730785737719E-16, 0.000000000000000000 ) ) ;
#59751=CARTESIAN_POINT ( 'NONE',  ( -23.15000000000000213, 2.600000000011156054, -80.22462192276213955 ) ) ;
#59809=ORIENTED_EDGE ( 'NONE', *, *, #97986, .F. ) ;
#59818=CARTESIAN_POINT ( 'NONE',  ( 20.94999999999999929, 6.550000000011156231, -77.01702717044007329 ) ) ;
#59821=ORIENTED_EDGE ( 'NONE', *, *, #236787, .F. ) ;
#59823=CARTESIAN_POINT ( 'NONE',  ( -23.15000000000000213, -8.596261682231835621, -76.45012751715033517 ) ) ;
#59838=EDGE_LOOP ( 'NONE', ( #231248, #100282, #237191, #161304 ) ) ;
#59858=AXIS2_PLACEMENT_3D ( 'NONE', #53499, #157784, #176038 ) ;
#59862=FACE_OUTER_BOUND ( 'NONE', #5893, .T. ) ;
#59917=DIRECTION ( 'NONE',  ( -6.938893903907222067E-15, 1.000000000000000000, 2.891205793294679805E-16 ) ) ;
#59942=FACE_OUTER_BOUND ( 'NONE', #252779, .T. ) ;
#59946=AXIS2_PLACEMENT_3D ( 'NONE', #61923, #164879, #102289 ) ;
#59954=DIRECTION ( 'NONE',  ( 1.000000000000000000, -7.304098846218134667E-16, 0.000000000000000000 ) ) ;
#59990=DIRECTION ( 'NONE',  ( 0.000000000000000000, 0.000000000000000000, -1.000000000000000000 ) ) ;
#59991=AXIS2_PLACEMENT_3D ( 'NONE', #187296, #88141, #230249 ) ;
#60007=CIRCLE ( 'NONE', #130939, 0.1000000000000028644 ) ;
#60079=CARTESIAN_POINT ( 'NONE',  ( -23.15000000000000213, -8.999999999988844479, -90.60603087734760663 ) ) ;
#60091=ORIENTED_EDGE ( 'NONE', *, *, #139438, .F. ) ;
#60093=SURFACE_STYLE_FILL_AREA ( #155394 ) ;
#60095=EDGE_LOOP ( 'NONE', ( #24856, #41401, #97332, #236826 ) ) ;
#60105=DIRECTION ( 'NONE',  ( 1.000000000000000000, 0.000000000000000000, 0.000000000000000000 ) ) ;
#60106=ORIENTED_EDGE ( 'NONE', *, *, #101715, .T. ) ;
#60109=CARTESIAN_POINT ( 'NONE',  ( -20.94999999999999929, 1.750000000011155743, -78.66951155790169992 ) ) ;
#60116=CIRCLE ( 'NONE', #39312, 0.6000000000000015321 ) ;
#60120=AXIS2_PLACEMENT_3D ( 'NONE', #227893, #104067, #222740 ) ;
#60151=CARTESIAN_POINT ( 'NONE',  ( -18.59999999999999787, -1.135018845899022466, -108.2169768834323662 ) ) ;
#60211=VERTEX_POINT ( 'NONE', #253976 ) ;
#60233=ORIENTED_EDGE ( 'NONE', *, *, #94036, .T. ) ;
#60241=DIRECTION ( 'NONE',  ( 0.000000000000000000, 1.000000000000000000, 0.000000000000000000 ) ) ;
#60250=DIRECTION ( 'NONE',  ( 0.000000000000000000, 0.000000000000000000, -1.000000000000000000 ) ) ;
#60325=EDGE_CURVE ( 'NONE', #87242, #238381, #64766, .T. ) ;
#60336=ORIENTED_EDGE ( 'NONE', *, *, #25039, .T. ) ;
#60368=VERTEX_POINT ( 'NONE', #180880 ) ;
#60399=DIRECTION ( 'NONE',  ( 0.000000000000000000, -1.000000000000000000, 0.000000000000000000 ) ) ;
#60416=DIRECTION ( 'NONE',  ( 0.000000000000000000, 0.000000000000000000, 1.000000000000000000 ) ) ;
#60434=LINE ( 'NONE', #136100, #15328 ) ;
#60443=AXIS2_PLACEMENT_3D ( 'NONE', #230133, #132313, #48922 ) ;
#60463=EDGE_CURVE ( 'NONE', #94787, #177719, #248542, .T. ) ;
#60479=CIRCLE ( 'NONE', #185579, 12.87500000000000000 ) ;
#60485=AXIS2_PLACEMENT_3D ( 'NONE', #49610, #144844, #44489 ) ;
#60503=CARTESIAN_POINT ( 'NONE',  ( 21.05000000000000071, 1.162701749949165642, -75.10000000000003695 ) ) ;
#60514=ORIENTED_EDGE ( 'NONE', *, *, #101106, .T. ) ;
#60517=DIRECTION ( 'NONE',  ( 1.000000000000000000, 0.000000000000000000, 0.000000000000000000 ) ) ;
#60534=CARTESIAN_POINT ( 'NONE',  ( -22.57848426163148403, -0.004264329271961148776, -55.24994169310969738 ) ) ;
#60536=DIRECTION ( 'NONE',  ( 1.000000000000000000, 0.000000000000000000, 0.000000000000000000 ) ) ;
#60545=DIRECTION ( 'NONE',  ( -0.4999999999999799050, 0.000000000000000000, -0.8660254037844502539 ) ) ;
#60547=EDGE_CURVE ( 'NONE', #119770, #147057, #13228, .T. ) ;
#60550=CARTESIAN_POINT ( 'NONE',  ( 23.24999999999999289, 6.650000000011155876, -79.35000000000005116 ) ) ;
#60561=DIRECTION ( 'NONE',  ( -4.408576920032448588E-17, 0.1350103645451876666, -0.9908441862701600211 ) ) ;
#60567=AXIS2_PLACEMENT_3D ( 'NONE', #158535, #238035, #222297 ) ;
#60593=DIRECTION ( 'NONE',  ( -1.000000000000000000, 0.000000000000000000, 0.000000000000000000 ) ) ;
#60622=TOROIDAL_SURFACE ( 'NONE', #31643, 11.90000000000000213, 0.1000000000000000056 ) ;
#60657=EDGE_CURVE ( 'NONE', #173700, #219131, #17476, .T. ) ;
#60682=AXIS2_PLACEMENT_3D ( 'NONE', #175830, #213655, #97518 ) ;
#60697=DIRECTION ( 'NONE',  ( 0.000000000000000000, -0.1298341882520079038, -0.9915357197604846018 ) ) ;
#60725=DIRECTION ( 'NONE',  ( -2.978066053179067751E-16, 1.000000000000000000, 0.000000000000000000 ) ) ;
#60726=EDGE_CURVE ( 'NONE', #214744, #64899, #141434, .T. ) ;
#60741=DIRECTION ( 'NONE',  ( -1.000000000000000000, 7.304098846218134667E-16, 4.217023435051625732E-16 ) ) ;
#60774=ORIENTED_EDGE ( 'NONE', *, *, #99353, .F. ) ;
#60782=CYLINDRICAL_SURFACE ( 'NONE', #60942, 0.1000000000000028644 ) ;
#60793=CARTESIAN_POINT ( 'NONE',  ( 22.39999999999999503, 0.1000000000111554016, -59.20922040162665922 ) ) ;
#60796=EDGE_LOOP ( 'NONE', ( #69292, #240156, #195503, #242403 ) ) ;
#60815=DIRECTION ( 'NONE',  ( -0.000000000000000000, 0.9876197685951279004, -0.1568667991644694115 ) ) ;
#60835=VECTOR ( 'NONE', #39305, 1000.000000000000000 ) ;
#60863=VERTEX_POINT ( 'NONE', #70927 ) ;
#60873=CARTESIAN_POINT ( 'NONE',  ( -23.25000000000000000, -1.835859311432481045, -112.0044391687985694 ) ) ;
#60888=VERTEX_POINT ( 'NONE', #205249 ) ;
#60895=AXIS2_PLACEMENT_3D ( 'NONE', #34494, #71050, #132278 ) ;
#60905=FACE_OUTER_BOUND ( 'NONE', #10920, .T. ) ;
#60909=CARTESIAN_POINT ( 'NONE',  ( 20.94999999999999929, 8.876614585098254295, -75.38508047884472774 ) ) ;
#60916=CARTESIAN_POINT ( 'NONE',  ( 23.24999999999999289, 11.65000000001116298, -88.35000000000003695 ) ) ;
#60932=AXIS2_PLACEMENT_3D ( 'NONE', #203194, #122383, #199365 ) ;
#60933=PLANE ( 'NONE',  #130867 ) ;
#60938=ORIENTED_EDGE ( 'NONE', *, *, #142725, .T. ) ;
#60942=AXIS2_PLACEMENT_3D ( 'NONE', #162484, #137748, #3371 ) ;
#60969=CARTESIAN_POINT ( 'NONE',  ( -23.25000000000000000, 6.982009704867601307, -104.1961521182563359 ) ) ;
#61002=CARTESIAN_POINT ( 'NONE',  ( 18.47149038651511077, -9.671457157995551057, -107.1727863347384613 ) ) ;
#61020=VERTEX_POINT ( 'NONE', #76026 ) ;
#61030=CARTESIAN_POINT ( 'NONE',  ( -20.94999999999999574, 11.62071067812980907, -93.63158334765908819 ) ) ;
#61039=ORIENTED_EDGE ( 'NONE', *, *, #202551, .F. ) ;
#61042=DIRECTION ( 'NONE',  ( 1.000000000000000000, 0.000000000000000000, 0.000000000000000000 ) ) ;
#61049=ORIENTED_EDGE ( 'NONE', *, *, #195377, .T. ) ;
#61056=DIRECTION ( 'NONE',  ( 1.000000000000000000, 0.000000000000000000, 0.000000000000000000 ) ) ;
#61079=ORIENTED_EDGE ( 'NONE', *, *, #166566, .T. ) ;
#61083=ORIENTED_EDGE ( 'NONE', *, *, #97876, .T. ) ;
#61092=CARTESIAN_POINT ( 'NONE',  ( 18.58725287972303875, -9.566626910680497531, -107.3225048057656181 ) ) ;
#61102=ORIENTED_EDGE ( 'NONE', *, *, #121372, .F. ) ;
#61126=EDGE_CURVE ( 'NONE', #100102, #50622, #197259, .T. ) ;
#61134=VERTEX_POINT ( 'NONE', #159434 ) ;
#61143=AXIS2_PLACEMENT_3D ( 'NONE', #242972, #248113, #27823 ) ;
#61149=CARTESIAN_POINT ( 'NONE',  ( -22.49544290803744317, 11.74987023786832552, -66.93468804074220202 ) ) ;
#61164=DIRECTION ( 'NONE',  ( 0.000000000000000000, 0.000000000000000000, 1.000000000000000000 ) ) ;
#61191=ORIENTED_EDGE ( 'NONE', *, *, #14581, .F. ) ;
#61197=CIRCLE ( 'NONE', #189810, 7.900000000000003908 ) ;
#61203=ORIENTED_EDGE ( 'NONE', *, *, #11392, .T. ) ;
#61208=FACE_OUTER_BOUND ( 'NONE', #240007, .T. ) ;
#61211=ORIENTED_EDGE ( 'NONE', *, *, #37225, .T. ) ;
#61224=CIRCLE ( 'NONE', #144398, 0.1000000000000028644 ) ;
#61242=ORIENTED_EDGE ( 'NONE', *, *, #197351, .F. ) ;
#61243=CARTESIAN_POINT ( 'NONE',  ( -20.64999999999999858, 4.350000000011156054, -88.15000000000004832 ) ) ;
#61244=DIRECTION ( 'NONE',  ( 0.000000000000000000, 0.000000000000000000, -1.000000000000000000 ) ) ;
#61270=CARTESIAN_POINT ( 'NONE',  ( -20.94999999999999929, 1.250000000011155299, -75.00000000000004263 ) ) ;
#61329=ORIENTED_EDGE ( 'NONE', *, *, #33667, .T. ) ;
#61330=DIRECTION ( 'NONE',  ( -1.000000000000000000, 0.000000000000000000, 0.000000000000000000 ) ) ;
#61354=VECTOR ( 'NONE', #10196, 1000.000000000000000 ) ;
#61380=EDGE_LOOP ( 'NONE', ( #107937, #196635, #247728, #147132 ) ) ;
#61436=FACE_OUTER_BOUND ( 'NONE', #196132, .T. ) ;
#61438=CARTESIAN_POINT ( 'NONE',  ( 19.75857864376268935, 11.75000000001116440, -91.75000000000004263 ) ) ;
#61459=CARTESIAN_POINT ( 'NONE',  ( -20.85882249326303040, 10.33248238083634796, -106.0948465439131922 ) ) ;
#61470=EDGE_CURVE ( 'NONE', #225548, #24943, #155451, .T. ) ;
#61474=CARTESIAN_POINT ( 'NONE',  ( 18.59999999999996945, 10.33248238083634440, -106.0948465439131922 ) ) ;
#61502=CIRCLE ( 'NONE', #223795, 0.09999999999999939493 ) ;
#61514=DIRECTION ( 'NONE',  ( 1.000000000000000000, -0.000000000000000000, -0.000000000000000000 ) ) ;
#61619=EDGE_CURVE ( 'NONE', #144450, #171778, #76281, .T. ) ;
#61677=AXIS2_PLACEMENT_3D ( 'NONE', #60503, #77487, #198743 ) ;
#61701=ORIENTED_EDGE ( 'NONE', *, *, #39771, .F. ) ;
#61708=EDGE_LOOP ( 'NONE', ( #115270, #44743, #117330, #165393, #185615, #113238, #168447, #199955, #131291, #29085 ) ) ;
#61738=DIRECTION ( 'NONE',  ( 0.000000000000000000, 0.000000000000000000, -1.000000000000000000 ) ) ;
#61753=EDGE_CURVE ( 'NONE', #168456, #140891, #69970, .T. ) ;
#61755=DIRECTION ( 'NONE',  ( 1.000000000000000000, -0.000000000000000000, -0.000000000000000000 ) ) ;
#61757=CIRCLE ( 'NONE', #207529, 0.09999999999999939493 ) ;
#61773=DIRECTION ( 'NONE',  ( 0.000000000000000000, -0.9893560106964500722, 0.1455152366551550613 ) ) ;
#61797=DIRECTION ( 'NONE',  ( -0.7071067811865389130, 0.000000000000000000, 0.7071067811865561215 ) ) ;
#61798=VERTEX_POINT ( 'NONE', #76343 ) ;
#61808=AXIS2_PLACEMENT_3D ( 'NONE', #58197, #235561, #114349 ) ;
#61835=CIRCLE ( 'NONE', #86737, 0.1000000000000001860 ) ;
#61872=AXIS2_PLACEMENT_3D ( 'NONE', #230872, #49640, #108343 ) ;
#61884=ORIENTED_EDGE ( 'NONE', *, *, #106254, .T. ) ;
#61891=DIRECTION ( 'NONE',  ( -1.000000000000000000, 0.000000000000000000, 0.000000000000000000 ) ) ;
#61923=CARTESIAN_POINT ( 'NONE',  ( -21.14999999999999858, 6.540656951712397138, -67.10000000000005116 ) ) ;
#61933=VERTEX_POINT ( 'NONE', #184449 ) ;
#61942=B_SPLINE_CURVE_WITH_KNOTS ( 'NONE', 3,
 ( #98940, #179812, #123679, #2419, #181097, #183657, #40323, #243613, #83227, #203203, #139359, #198068, #41595, #178542, #24598, #84490 ),
 .UNSPECIFIED., .F., .F.,
 ( 4, 3, 3, 3, 3, 4 ),
 ( 0.000000000000000000, 2.209833635978076120E-05, 5.595056164119274593E-05, 8.979992002655373272E-05, 0.0001236482757198912469, 0.0001574984039362985829 ),
 .UNSPECIFIED. ) ;
#62013=CARTESIAN_POINT ( 'NONE',  ( -1.739115166359751170E-14, 11.65000000001114699, -88.35000000000003695 ) ) ;
#62017=CARTESIAN_POINT ( 'NONE',  ( 18.50016250449482413, 10.29766095125182268, -105.9743663933279265 ) ) ;
#62031=CIRCLE ( 'NONE', #241117, 0.1000000000000028644 ) ;
#62068=ORIENTED_EDGE ( 'NONE', *, *, #197, .F. ) ;
#62077=CARTESIAN_POINT ( 'NONE',  ( -18.50000000000000000, -26.43935341558978891, -85.14150860750750383 ) ) ;
#62097=CARTESIAN_POINT ( 'NONE',  ( -20.85000000000000142, 6.933893972137497030, -104.2856458343736250 ) ) ;
#62104=AXIS2_PLACEMENT_3D ( 'NONE', #8271, #87771, #68235 ) ;
#62133=DIRECTION ( 'NONE',  ( 0.000000000000000000, 0.000000000000000000, -1.000000000000000000 ) ) ;
#62153=ADVANCED_FACE ( 'NONE', ( #48793 ), #234891, .T. ) ;
#62172=CARTESIAN_POINT ( 'NONE',  ( 18.50000000000000000, -10.35479209691423996, -94.25654098307380480 ) ) ;
#62178=CARTESIAN_POINT ( 'NONE',  ( -23.25000000000000000, -11.64999999998884483, -97.40000000000004832 ) ) ;
#62212=CARTESIAN_POINT ( 'NONE',  ( -22.47007471830798764, 7.720710651937634061, -67.00000000000004263 ) ) ;
#62234=ORIENTED_EDGE ( 'NONE', *, *, #131124, .F. ) ;
#62253=CARTESIAN_POINT ( 'NONE',  ( 18.59999999999997655, -1.164121893230052995, -108.4148480855716485 ) ) ;
#62254=DIRECTION ( 'NONE',  ( 0.000000000000000000, 0.000000000000000000, 1.000000000000000000 ) ) ;
#62297=VERTEX_POINT ( 'NONE', #93056 ) ;
#62311=EDGE_CURVE ( 'NONE', #80704, #124622, #156920, .T. ) ;
#62338=DIRECTION ( 'NONE',  ( 1.000000000000000000, -0.000000000000000000, -0.000000000000000000 ) ) ;
#62341=AXIS2_PLACEMENT_3D ( 'NONE', #202377, #161992, #223208 ) ;
#62342=EDGE_LOOP ( 'NONE', ( #122418, #227657, #152881, #7809 ) ) ;
#62361=FACE_OUTER_BOUND ( 'NONE', #58751, .T. ) ;
#62365=ORIENTED_EDGE ( 'NONE', *, *, #58508, .F. ) ;
#62376=ORIENTED_EDGE ( 'NONE', *, *, #55043, .T. ) ;
#62380=ORIENTED_EDGE ( 'NONE', *, *, #185638, .F. ) ;
#62382=CARTESIAN_POINT ( 'NONE',  ( 23.24999999999999645, 5.600000000011153389, -88.09473398108696074 ) ) ;
#62388=FACE_OUTER_BOUND ( 'NONE', #143027, .T. ) ;
#62394=AXIS2_PLACEMENT_3D ( 'NONE', #981, #194116, #115839 ) ;
#62417=CARTESIAN_POINT ( 'NONE',  ( -22.57320508075687115, 11.75000000001115552, -67.00000000000004263 ) ) ;
#62422=CARTESIAN_POINT ( 'NONE',  ( -20.94999999999999929, 1.115600667400684642E-11, -100.5000000000000426 ) ) ;
#62425=ORIENTED_EDGE ( 'NONE', *, *, #103898, .F. ) ;
#62435=CARTESIAN_POINT ( 'NONE',  ( 20.85000000000000142, -1.835859311432481045, -112.0044391687985694 ) ) ;
#62443=ORIENTED_EDGE ( 'NONE', *, *, #150887, .T. ) ;
#62464=CARTESIAN_POINT ( 'NONE',  ( 21.12642695952774119, 0.09890328320052040045, -60.62434007796486668 ) ) ;
#62466=DIRECTION ( 'NONE',  ( 1.000000000000000000, 0.000000000000000000, -0.000000000000000000 ) ) ;
#62472=CIRCLE ( 'NONE', #91674, 0.1000000000000017958 ) ;
#62515=CARTESIAN_POINT ( 'NONE',  ( 21.05000000000000071, 10.50253167713781544, -74.55882981707586055 ) ) ;
#62525=DIRECTION ( 'NONE',  ( 0.000000000000000000, 0.9654727137038715545, 0.2605042016806676242 ) ) ;
#62536=CARTESIAN_POINT ( 'NONE',  ( 20.94999999999999929, -1.362429037182151470, -108.3888812479212476 ) ) ;
#62560=DIRECTION ( 'NONE',  ( 0.000000000000000000, -0.8660254037844412611, -0.4999999999999956701 ) ) ;
#62586=CARTESIAN_POINT ( 'NONE',  ( -20.64999999999999858, 2.000000000011154189, -80.22462192276213955 ) ) ;
#62595=ORIENTED_EDGE ( 'NONE', *, *, #115559, .T. ) ;
#62611=PLANE ( 'NONE',  #220699 ) ;
#62627=CARTESIAN_POINT ( 'NONE',  ( -18.50000000000000000, 7.021664781911246322, -104.1335654018973287 ) ) ;
#62645=EDGE_CURVE ( 'NONE', #124622, #146995, #59488, .T. ) ;
#62709=VECTOR ( 'NONE', #194052, 1000.000000000000000 ) ;
#62759=CYLINDRICAL_SURFACE ( 'NONE', #119284, 0.1000000000000000472 ) ;
#62762=VERTEX_POINT ( 'NONE', #62627 ) ;
#62852=CARTESIAN_POINT ( 'NONE',  ( 20.85000000000000142, 1.115600667400684642E-11, -108.4000000000000483 ) ) ;
#62868=CARTESIAN_POINT ( 'NONE',  ( 21.05000000000000071, 6.650000000011155876, -76.84382208968317229 ) ) ;
#62872=EDGE_LOOP ( 'NONE', ( #49535, #204942, #219667, #185823 ) ) ;
#62881=ADVANCED_FACE ( 'NONE', ( #67754 ), #169466, .T. ) ;
#62890=TOROIDAL_SURFACE ( 'NONE', #237683, 0.4000000000000017431, 0.1000000000000000056 ) ;
#62931=ORIENTED_EDGE ( 'NONE', *, *, #65544, .F. ) ;
#62964=CARTESIAN_POINT ( 'NONE',  ( -23.15000000000000213, 11.75000000001115552, -88.35000000000003695 ) ) ;
#62965=AXIS2_PLACEMENT_3D ( 'NONE', #212238, #93547, #113118 ) ;
#63014=DIRECTION ( 'NONE',  ( -0.000000000000000000, -1.000000000000000000, 6.308085367188393199E-16 ) ) ;
#63049=DIRECTION ( 'NONE',  ( 0.000000000000000000, -1.000000000000000000, 0.000000000000000000 ) ) ;
#63060=ORIENTED_EDGE ( 'NONE', *, *, #117485, .T. ) ;
#63074=AXIS2_PLACEMENT_3D ( 'NONE', #135399, #196660, #114574 ) ;
#63098=DIRECTION ( 'NONE',  ( 0.000000000000000000, -1.000000000000000000, 0.000000000000000000 ) ) ;
#63138=TOROIDAL_SURFACE ( 'NONE', #150636, 0.6000000000000013101, 0.1000000000000000056 ) ;
#63141=EDGE_CURVE ( 'NONE', #238715, #181403, #42973, .T. ) ;
#63201=CARTESIAN_POINT ( 'NONE',  ( 21.05000000000000071, -8.999999999988842703, -91.00603087734759811 ) ) ;
#63239=LINE ( 'NONE', #142764, #134686 ) ;
#63250=DIRECTION ( 'NONE',  ( 0.000000000000000000, 0.000000000000000000, -1.000000000000000000 ) ) ;
#63259=VECTOR ( 'NONE', #218387, 1000.000000000000000 ) ;
#63260=CIRCLE ( 'NONE', #184081, 0.5000000000000013323 ) ;
#63266=CARTESIAN_POINT ( 'NONE',  ( 18.49999999999999289, 6.650000000011155876, -88.15000000000004832 ) ) ;
#63278=CIRCLE ( 'NONE', #21607, 4.150000000000001243 ) ;
#63339=CARTESIAN_POINT ( 'NONE',  ( -22.47071067811865319, 0.09909245471376171288, -59.27992525550198621 ) ) ;
#63343=EDGE_LOOP ( 'NONE', ( #205507, #209423, #128078, #100046 ) ) ;
#63354=DIRECTION ( 'NONE',  ( -4.336808689941752679E-15, 0.8660254037844482555, 0.4999999999999837907 ) ) ;
#63392=ADVANCED_FACE ( 'NONE', ( #213038 ), #22506, .F. ) ;
#63408=VERTEX_POINT ( 'NONE', #56510 ) ;
#63444=( BOUNDED_SURFACE ( )  B_SPLINE_SURFACE ( 3, 2, ( 
 ( #244304, #102201, #104770 ),
 ( #159655, #24010, #240466 ),
 ( #125650, #140058, #220888 ),
 ( #21446, #145203, #3117 ),
 ( #219604, #143924, #106062 ),
 ( #205170, #184330, #5677 ) ),
 .UNSPECIFIED., .F., .F., .T. ) 
 B_SPLINE_SURFACE_WITH_KNOTS ( ( 4, 2, 4 ),
 ( 3, 3 ),
 ( 0.0001792624049599543154, 0.0003686986002124625081, 0.0005581347954649706466 ),
 ( 0.000000000000000000, 1.000000000000000000 ),
 .UNSPECIFIED. ) 
 GEOMETRIC_REPRESENTATION_ITEM ( )  RATIONAL_B_SPLINE_SURFACE ( (
 ( 1.000000000000000000, 0.9238795325112830747, 1.000000000000000000),
 ( 1.000000000000000000, 0.9229318695234240977, 1.000000000000000000),
 ( 1.000000000000000000, 0.8926288119236353014, 1.000000000000000000),
 ( 1.000000000000000000, 0.8123777807265625261, 1.000000000000000000),
 ( 1.000000000000000000, 0.7629087100935785237, 1.000000000000000000),
 ( 1.000000000000000000, 0.7071067811865475727, 1.000000000000000000) ) ) 
 REPRESENTATION_ITEM ( '' )  SURFACE ( )  );
#63484=FACE_OUTER_BOUND ( 'NONE', #39342, .T. ) ;
#63485=EDGE_CURVE ( 'NONE', #121769, #21107, #154397, .T. ) ;
#63501=DIRECTION ( 'NONE',  ( 0.000000000000000000, 0.000000000000000000, -1.000000000000000000 ) ) ;
#63528=TOROIDAL_SURFACE ( 'NONE', #180083, 3.899999999999999467, 0.1000000000000000056 ) ;
#63545=VERTEX_POINT ( 'NONE', #399 ) ;
#63569=EDGE_CURVE ( 'NONE', #17165, #174644, #26594, .T. ) ;
#63578=CARTESIAN_POINT ( 'NONE',  ( -18.52139480978223318, -9.481358845055737561, -74.02455656711912013 ) ) ;
#63595=CIRCLE ( 'NONE', #38478, 0.1000000000000004496 ) ;
#63608=CIRCLE ( 'NONE', #155236, 0.1000000000000004496 ) ;
#63615=AXIS2_PLACEMENT_3D ( 'NONE', #89126, #186974, #210373 ) ;
#63623=ORIENTED_EDGE ( 'NONE', *, *, #163282, .T. ) ;
#63626=DIRECTION ( 'NONE',  ( 0.000000000000000000, 0.000000000000000000, -1.000000000000000000 ) ) ;
#63641=ORIENTED_EDGE ( 'NONE', *, *, #247156, .F. ) ;
#63647=VECTOR ( 'NONE', #24269, 1000.000000000000000 ) ;
#63651=DIRECTION ( 'NONE',  ( 0.000000000000000000, 1.000000000000000000, 0.000000000000000000 ) ) ;
#63661=CARTESIAN_POINT ( 'NONE',  ( 21.07946286933444924, 0.07668384326756234881, -60.67096268099236056 ) ) ;
#63663=CARTESIAN_POINT ( 'NONE',  ( -22.24259225415828567, 7.491937870576586889, -66.90093411654720512 ) ) ;
#63692=VECTOR ( 'NONE', #101327, 1000.000000000000000 ) ;
#63699=DIRECTION ( 'NONE',  ( 0.7071067811865487940, 0.000000000000000000, -0.7071067811865463515 ) ) ;
#63723=ORIENTED_EDGE ( 'NONE', *, *, #50008, .F. ) ;
#63748=DIRECTION ( 'NONE',  ( 0.000000000000000000, 1.000000000000000000, -0.000000000000000000 ) ) ;
#63778=DIRECTION ( 'NONE',  ( -1.000000000000000000, -2.952720810173289112E-16, 0.000000000000000000 ) ) ;
#63782=LINE ( 'NONE', #179899, #75346 ) ;
#63808=DIRECTION ( 'NONE',  ( 0.000000000000000000, 0.000000000000000000, -1.000000000000000000 ) ) ;
#63855=AXIS2_PLACEMENT_3D ( 'NONE', #119019, #96837, #198536 ) ;
#63870=ORIENTED_EDGE ( 'NONE', *, *, #193486, .T. ) ;
#63885=CYLINDRICAL_SURFACE ( 'NONE', #18349, 11.74999999999999645 ) ;
#63886=ORIENTED_EDGE ( 'NONE', *, *, #155788, .F. ) ;
#63909=AXIS2_PLACEMENT_3D ( 'NONE', #8356, #150444, #194714 ) ;
#63945=ADVANCED_FACE ( 'NONE', ( #254131 ), #243220, .T. ) ;
#63965=ORIENTED_EDGE ( 'NONE', *, *, #247835, .F. ) ;
#63996=ORIENTED_EDGE ( 'NONE', *, *, #140077, .T. ) ;
#63997=CARTESIAN_POINT ( 'NONE',  ( 18.59999999999999787, -1.835341550213255957, -78.55515129256302487 ) ) ;
#64011=CIRCLE ( 'NONE', #138428, 0.1000000000000028644 ) ;
#64018=ORIENTED_EDGE ( 'NONE', *, *, #78214, .T. ) ;
#64053=DIRECTION ( 'NONE',  ( -1.000000000000000000, 0.000000000000000000, 0.000000000000000000 ) ) ;
#64057=TOROIDAL_SURFACE ( 'NONE', #84862, 7.791421356237316687, 0.1000000000000000056 ) ;
#64169=ORIENTED_EDGE ( 'NONE', *, *, #174407, .T. ) ;
#64199=ORIENTED_EDGE ( 'NONE', *, *, #94114, .T. ) ;
#64201=LINE ( 'NONE', #143723, #104393 ) ;
#64221=ORIENTED_EDGE ( 'NONE', *, *, #60463, .F. ) ;
#64223=DIRECTION ( 'NONE',  ( 0.000000000000000000, -1.734723475983068283E-15, 1.000000000000000000 ) ) ;
#64249=AXIS2_PLACEMENT_3D ( 'NONE', #74497, #57438, #134400 ) ;
#64297=ADVANCED_FACE ( 'NONE', ( #238109 ), #118180, .F. ) ;
#64313=CARTESIAN_POINT ( 'NONE',  ( -18.59999999999999787, -26.43935341558978891, -85.14150860750750383 ) ) ;
#64343=EDGE_CURVE ( 'NONE', #120362, #197089, #55597, .T. ) ;
#64345=CARTESIAN_POINT ( 'NONE',  ( 23.14999999999999858, 1.115600667400684642E-11, -100.5000000000000426 ) ) ;
#64364=ORIENTED_EDGE ( 'NONE', *, *, #80885, .F. ) ;
#64371=VERTEX_POINT ( 'NONE', #94755 ) ;
#64375=DIRECTION ( 'NONE',  ( 1.000000000000000000, 0.000000000000000000, 0.000000000000000000 ) ) ;
#64420=VECTOR ( 'NONE', #81965, 1000.000000000000000 ) ;
#64471=LINE ( 'NONE', #82702, #154945 ) ;
#64508=CARTESIAN_POINT ( 'NONE',  ( 21.14999999999999858, 11.65000000001115943, -67.10000000000005116 ) ) ;
#64532=ADVANCED_FACE ( 'NONE', ( #202840 ), #24232, .T. ) ;
#64539=CARTESIAN_POINT ( 'NONE',  ( -23.25000000000000000, 1.115600667400684642E-11, -100.5000000000000426 ) ) ;
#64550=ORIENTED_EDGE ( 'NONE', *, *, #256516, .F. ) ;
#64564=ORIENTED_EDGE ( 'NONE', *, *, #47354, .F. ) ;
#64572=DIRECTION ( 'NONE',  ( 0.000000000000000000, 0.000000000000000000, -1.000000000000000000 ) ) ;
#64601=FACE_OUTER_BOUND ( 'NONE', #75770, .T. ) ;
#64606=VECTOR ( 'NONE', #52913, 1000.000000000000000 ) ;
#64645=ORIENTED_EDGE ( 'NONE', *, *, #231666, .T. ) ;
#64650=DIRECTION ( 'NONE',  ( -0.7071067811865388020, 0.7071067811865561215, 0.000000000000000000 ) ) ;
#64651=CARTESIAN_POINT ( 'NONE',  ( 23.14999999999999858, -11.74999999998883560, -55.25000000000004974 ) ) ;
#64652=ORIENTED_EDGE ( 'NONE', *, *, #92454, .T. ) ;
#64678=FACE_OUTER_BOUND ( 'NONE', #206074, .T. ) ;
#64695=AXIS2_PLACEMENT_3D ( 'NONE', #207130, #225378, #182437 ) ;
#64723=DIRECTION ( 'NONE',  ( 0.000000000000000000, 0.000000000000000000, 1.000000000000000000 ) ) ;
#64758=DIRECTION ( 'NONE',  ( 0.000000000000000000, -0.8660254037844384856, 0.5000000000000003331 ) ) ;
#64766=LINE ( 'NONE', #21810, #146454 ) ;
#64770=VECTOR ( 'NONE', #47815, 1000.000000000000000 ) ;
#64772=CIRCLE ( 'NONE', #106440, 0.5000000000000004441 ) ;
#64814=DIRECTION ( 'NONE',  ( 7.589415207398576792E-15, -1.000000000000000000, -0.000000000000000000 ) ) ;
#64833=DIRECTION ( 'NONE',  ( 0.000000000000000000, 0.000000000000000000, -1.000000000000000000 ) ) ;
#64848=ORIENTED_EDGE ( 'NONE', *, *, #139422, .F. ) ;
#64850=CARTESIAN_POINT ( 'NONE',  ( 21.05000000000000426, 6.258817194692632313, -66.96636726466641676 ) ) ;
#64878=AXIS2_PLACEMENT_3D ( 'NONE', #56528, #203459, #137366 ) ;
#64899=VERTEX_POINT ( 'NONE', #173429 ) ;
#64900=EDGE_LOOP ( 'NONE', ( #161729, #4916, #220987, #70113, #206968 ) ) ;
#64944=CARTESIAN_POINT ( 'NONE',  ( -23.15000000000000213, -11.41227409413852811, -97.50000000000004263 ) ) ;
#64968=DIRECTION ( 'NONE',  ( 3.616040088954497272E-32, -1.224646799147352961E-16, 1.000000000000000000 ) ) ;
#64989=DIRECTION ( 'NONE',  ( 0.000000000000000000, 0.000000000000000000, 1.000000000000000000 ) ) ;
#64994=CARTESIAN_POINT ( 'NONE',  ( 21.08489247129321242, 8.877675190881227252, -79.35000000000005116 ) ) ;
#65038=ORIENTED_EDGE ( 'NONE', *, *, #56675, .T. ) ;
#65059=DIRECTION ( 'NONE',  ( 2.952720810173289112E-16, -1.000000000000000000, -0.000000000000000000 ) ) ;
#65074=CARTESIAN_POINT ( 'NONE',  ( 20.94999999999999929, 1.115600667400684642E-11, -100.5000000000000426 ) ) ;
#65079=CARTESIAN_POINT ( 'NONE',  ( -18.47653818581419927, -9.465280387751805691, -74.12596081613986598 ) ) ;
#65084=FACE_OUTER_BOUND ( 'NONE', #104321, .T. ) ;
#65137=CIRCLE ( 'NONE', #15084, 0.1000000000000028644 ) ;
#65152=EDGE_CURVE ( 'NONE', #19542, #55997, #202279, .T. ) ;
#65175=CARTESIAN_POINT ( 'NONE',  ( 20.94999999999999929, -8.999999999988842703, -90.60603087734760663 ) ) ;
#65183=EDGE_CURVE ( 'NONE', #233091, #137562, #135801, .T. ) ;
#65184=ORIENTED_EDGE ( 'NONE', *, *, #193337, .F. ) ;
#65188=CARTESIAN_POINT ( 'NONE',  ( 21.14999999999999858, 6.550000000011156231, -79.35000000000005116 ) ) ;
#65189=ORIENTED_EDGE ( 'NONE', *, *, #101064, .F. ) ;
#65236=DIRECTION ( 'NONE',  ( -1.000000000000000000, -1.836970198721029934E-16, 0.000000000000000000 ) ) ;
#65244=ADVANCED_FACE ( 'NONE', ( #147063 ), #67725, .T. ) ;
#65250=ORIENTED_EDGE ( 'NONE', *, *, #215464, .F. ) ;
#65254=AXIS2_PLACEMENT_3D ( 'NONE', #184539, #28079, #85411 ) ;
#65284=CARTESIAN_POINT ( 'NONE',  ( -22.39999999999999858, 1.115600667400684642E-11, -66.90000000000004832 ) ) ;
#65296=EDGE_LOOP ( 'NONE', ( #62595, #212929, #209921, #102850 ) ) ;
#65302=CARTESIAN_POINT ( 'NONE',  ( 21.00000000000000000, 9.750000000011153745, -79.25000000000004263 ) ) ;
#65309=ORIENTED_EDGE ( 'NONE', *, *, #249459, .T. ) ;
#65320=DIRECTION ( 'NONE',  ( 1.000000000000000000, 0.000000000000000000, 0.000000000000000000 ) ) ;
#65324=CARTESIAN_POINT ( 'NONE',  ( -21.04999999999999716, -0.01465611850199566996, -60.50331341423223108 ) ) ;
#65346=DIRECTION ( 'NONE',  ( -1.000000000000000000, -0.000000000000000000, 0.000000000000000000 ) ) ;
#65347=VECTOR ( 'NONE', #100743, 1000.000000000000000 ) ;
#65356=CARTESIAN_POINT ( 'NONE',  ( -20.54999999999999716, -8.730841121484170131, -90.90192528101572123 ) ) ;
#65361=AXIS2_PLACEMENT_3D ( 'NONE', #60151, #160583, #180129 ) ;
#65363=CARTESIAN_POINT ( 'NONE',  ( 18.59999999999999076, 6.450000000011156587, -77.01702717044007329 ) ) ;
#65377=EDGE_LOOP ( 'NONE', ( #45448, #247030, #122675, #211819 ) ) ;
#65412=EDGE_LOOP ( 'NONE', ( #253570, #120239, #225844, #227613 ) ) ;
#65415=CIRCLE ( 'NONE', #111208, 0.09999999999999939493 ) ;
#65443=CARTESIAN_POINT ( 'NONE',  ( 23.24999999999999289, 11.75000000001116263, -79.15000000000004832 ) ) ;
#65469=ORIENTED_EDGE ( 'NONE', *, *, #55043, .F. ) ;
#65471=LINE ( 'NONE', #109723, #221108 ) ;
#65521=CARTESIAN_POINT ( 'NONE',  ( 18.49999999999999645, 1.637172712981537659, -78.58215336547205254 ) ) ;
#65544=EDGE_CURVE ( 'NONE', #237980, #246766, #42591, .T. ) ;
#65585=CARTESIAN_POINT ( 'NONE',  ( -21.04999999999999716, -0.08574093702224443170, -60.58617371118707240 ) ) ;
#65591=VECTOR ( 'NONE', #241850, 1000.000000000000000 ) ;
#65598=EDGE_LOOP ( 'NONE', ( #95938, #45329, #34374, #68327, #219403 ) ) ;
#65604=FACE_OUTER_BOUND ( 'NONE', #114351, .T. ) ;
#65632=AXIS2_PLACEMENT_3D ( 'NONE', #215119, #116038, #195582 ) ;
#65639=SPHERICAL_SURFACE ( 'NONE', #169478, 0.1000000000000000056 ) ;
#65652=EDGE_CURVE ( 'NONE', #111358, #114655, #152614, .T. ) ;
#65670=CIRCLE ( 'NONE', #198936, 0.9750000000000036415 ) ;
#65692=ORIENTED_EDGE ( 'NONE', *, *, #11750, .F. ) ;
#65709=EDGE_CURVE ( 'NONE', #143962, #20178, #91923, .T. ) ;
#65725=VECTOR ( 'NONE', #128099, 1000.000000000000000 ) ;
#65759=DIRECTION ( 'NONE',  ( 1.000000000000000000, 2.952720810173289112E-16, -0.000000000000000000 ) ) ;
#65762=AXIS2_PLACEMENT_3D ( 'NONE', #68158, #241658, #146388 ) ;
#65788=DIRECTION ( 'NONE',  ( 0.000000000000000000, 0.000000000000000000, -1.000000000000000000 ) ) ;
#65807=DIRECTION ( 'NONE',  ( 1.000000000000000000, 0.000000000000000000, 0.000000000000000000 ) ) ;
#65810=AXIS2_PLACEMENT_3D ( 'NONE', #254587, #14753, #212925 ) ;
#65819=ORIENTED_EDGE ( 'NONE', *, *, #223331, .F. ) ;
#65831=VECTOR ( 'NONE', #79362, 1000.000000000000000 ) ;
#65864=ORIENTED_EDGE ( 'NONE', *, *, #122398, .T. ) ;
#65870=ADVANCED_FACE ( 'NONE', ( #38381 ), #56612, .F. ) ;
#65874=AXIS2_PLACEMENT_3D ( 'NONE', #22540, #257229, #40836 ) ;
#65877=EDGE_CURVE ( 'NONE', #209971, #240643, #215711, .T. ) ;
#65897=DIRECTION ( 'NONE',  ( 0.000000000000000000, 1.000000000000000000, 2.891205793294679805E-16 ) ) ;
#65911=ORIENTED_EDGE ( 'NONE', *, *, #146857, .T. ) ;
#65953=CARTESIAN_POINT ( 'NONE',  ( 18.59999999999999076, 10.49142135624846439, -91.75000000000005684 ) ) ;
#65956=AXIS2_PLACEMENT_3D ( 'NONE', #247843, #187886, #190466 ) ;
#66047=DIRECTION ( 'NONE',  ( 0.000000000000000000, 0.9908441862701596881, -0.1350103645451904977 ) ) ;
#66048=CARTESIAN_POINT ( 'NONE',  ( -22.00356870142746146, 7.254242362487302032, -67.00000000000005684 ) ) ;
#66052=AXIS2_PLACEMENT_3D ( 'NONE', #123904, #164314, #132554 ) ;
#66061=CARTESIAN_POINT ( 'NONE',  ( -20.85000000000000142, -11.74999999998884448, -100.5000000000000426 ) ) ;
#66125=CIRCLE ( 'NONE', #78595, 0.09999999999999693856 ) ;
#66138=CIRCLE ( 'NONE', #37125, 4.049999999999998046 ) ;
#66159=ORIENTED_EDGE ( 'NONE', *, *, #66866, .F. ) ;
#66176=CARTESIAN_POINT ( 'NONE',  ( 22.60000000000000142, 0.1008583691098682150, -55.25043287651065782 ) ) ;
#66186=EDGE_CURVE ( 'NONE', #197986, #70815, #223646, .T. ) ;
#66224=ORIENTED_EDGE ( 'NONE', *, *, #213966, .T. ) ;
#66230=EDGE_LOOP ( 'NONE', ( #59459, #177770, #74131, #97533 ) ) ;
#66266=CARTESIAN_POINT ( 'NONE',  ( -22.59080734064477625, 11.75000000001115907, -66.96925029190302325 ) ) ;
#66276=AXIS2_PLACEMENT_3D ( 'NONE', #203221, #107978, #64989 ) ;
#66278=ORIENTED_EDGE ( 'NONE', *, *, #80885, .T. ) ;
#66329=DIRECTION ( 'NONE',  ( -1.000000000000000000, 0.000000000000000000, 0.000000000000000000 ) ) ;
#66384=ADVANCED_FACE ( 'NONE', ( #204518 ), #25906, .F. ) ;
#66394=AXIS2_PLACEMENT_3D ( 'NONE', #184754, #3547, #86919 ) ;
#66420=VECTOR ( 'NONE', #187656, 1000.000000000000000 ) ;
#66428=DIRECTION ( 'NONE',  ( -3.265361837132813093E-16, 1.000000000000000000, 0.000000000000000000 ) ) ;
#66430=EDGE_CURVE ( 'NONE', #224607, #179279, #53157, .T. ) ;
#66444=CARTESIAN_POINT ( 'NONE',  ( -23.25000000000000000, 5.950000000011163692, -90.19429769496522908 ) ) ;
#66455=CARTESIAN_POINT ( 'NONE',  ( -23.25000000000000000, 1.115600667400684642E-11, -100.5000000000000426 ) ) ;
#66456=ORIENTED_EDGE ( 'NONE', *, *, #79480, .T. ) ;
#66489=ORIENTED_EDGE ( 'NONE', *, *, #138253, .F. ) ;
#66575=CARTESIAN_POINT ( 'NONE',  ( 18.59999999999999432, -1.835859311432481045, -112.0044391687985694 ) ) ;
#66577=ORIENTED_EDGE ( 'NONE', *, *, #115343, .F. ) ;
#66579=( BOUNDED_CURVE ( )  B_SPLINE_CURVE ( 3, ( #148459, #210992, #29821, #10232 ),
 .UNSPECIFIED., .F., .F. ) 
 B_SPLINE_CURVE_WITH_KNOTS ( ( 4, 4 ),
 ( 1.570796326794896558, 3.141592653589793116 ),
 .UNSPECIFIED. ) 
 CURVE ( )  GEOMETRIC_REPRESENTATION_ITEM ( )  RATIONAL_B_SPLINE_CURVE ( ( 1.000000000000000000, 0.8047378541243649375, 0.8047378541243649375, 1.000000000000000000 ) ) 
 REPRESENTATION_ITEM ( '' )  );
#66589=VERTEX_POINT ( 'NONE', #158709 ) ;
#66595=CARTESIAN_POINT ( 'NONE',  ( -23.25000000000000000, 1.115600667400684642E-11, -100.5000000000000426 ) ) ;
#66617=DIRECTION ( 'NONE',  ( 1.000000000000000000, 0.000000000000000000, 0.000000000000000000 ) ) ;
#66682=CARTESIAN_POINT ( 'NONE',  ( -23.15000000000000213, 2.000000000011154189, -87.27537807723794572 ) ) ;
#66700=ORIENTED_EDGE ( 'NONE', *, *, #91509, .F. ) ;
#66712=CARTESIAN_POINT ( 'NONE',  ( 18.59999999999999076, -1.249999999988843369, -75.00000000000004263 ) ) ;
#66719=EDGE_CURVE ( 'NONE', #128108, #113878, #141670, .T. ) ;
#66745=LINE ( 'NONE', #148857, #89834 ) ;
#66775=VERTEX_POINT ( 'NONE', #28184 ) ;
#66789=CIRCLE ( 'NONE', #229292, 0.1000000000000000472 ) ;
#66793=CARTESIAN_POINT ( 'NONE',  ( -20.94999999999999929, 1.116121084443477685E-11, -69.90000000000003411 ) ) ;
#66809=DIRECTION ( 'NONE',  ( 1.000000000000000000, 0.000000000000000000, 0.000000000000000000 ) ) ;
#66813=CARTESIAN_POINT ( 'NONE',  ( -20.95613430942427513, 11.75000000001115552, -73.85716264821988375 ) ) ;
#66829=CARTESIAN_POINT ( 'NONE',  ( 21.30000000000002558, 1.115600667400684642E-11, -67.00000000000004263 ) ) ;
#66835=CYLINDRICAL_SURFACE ( 'NONE', #257670, 4.049999999999998046 ) ;
#66852=EDGE_CURVE ( 'NONE', #75869, #164855, #115712, .T. ) ;
#66864=VERTEX_POINT ( 'NONE', #176664 ) ;
#66866=EDGE_CURVE ( 'NONE', #20400, #77369, #111237, .T. ) ;
#66874=CARTESIAN_POINT ( 'NONE',  ( -21.05000000000000071, 0.09779029131994770863, -60.74218538952393232 ) ) ;
#66915=CARTESIAN_POINT ( 'NONE',  ( 18.59999999999999076, 6.550000000011156231, -77.01702717044007329 ) ) ;
#66935=ORIENTED_EDGE ( 'NONE', *, *, #175460, .F. ) ;
#66945=CARTESIAN_POINT ( 'NONE',  ( -21.05000000000000071, 1.115600667400684642E-11, -67.00000000000004263 ) ) ;
#66948=CARTESIAN_POINT ( 'NONE',  ( 21.09546886439553504, 8.878553113026075749, -79.23709385055506971 ) ) ;
#66965=CIRCLE ( 'NONE', #237835, 0.1000000000000028644 ) ;
#66974=DIRECTION ( 'NONE',  ( 0.000000000000000000, 0.000000000000000000, -1.000000000000000000 ) ) ;
#66978=CYLINDRICAL_SURFACE ( 'NONE', #172112, 0.09999999999999892308 ) ;
#67029=CARTESIAN_POINT ( 'NONE',  ( 20.88420186297724257, 10.33025634372637391, -106.0870929282639281 ) ) ;
#67040=CARTESIAN_POINT ( 'NONE',  ( 19.88284271247461987, 11.69142135624847256, -91.75000000000005684 ) ) ;
#67110=VERTEX_POINT ( 'NONE', #210342 ) ;
#67141=CARTESIAN_POINT ( 'NONE',  ( 18.51024323315077069, 10.31104185824064245, -106.0204516983106373 ) ) ;
#67149=AXIS2_PLACEMENT_3D ( 'NONE', #118624, #244960, #3795 ) ;
#67184=AXIS2_PLACEMENT_3D ( 'NONE', #148507, #54197, #197563 ) ;
#67206=CARTESIAN_POINT ( 'NONE',  ( -18.59999999999999787, -1.835859311432481045, -112.0044391687985694 ) ) ;
#67218=CARTESIAN_POINT ( 'NONE',  ( 18.49999999999978328, 10.28015861706823841, -91.72457207120132239 ) ) ;
#67240=EDGE_LOOP ( 'NONE', ( #4239, #2660, #95860, #191995 ) ) ;
#67258=ORIENTED_EDGE ( 'NONE', *, *, #27712, .F. ) ;
#67259=CARTESIAN_POINT ( 'NONE',  ( 20.95496329884391784, 10.56743320610419445, -74.57430993228486216 ) ) ;
#67292=DIRECTION ( 'NONE',  ( 1.000000000000000000, 0.000000000000000000, 0.000000000000000000 ) ) ;
#67321=EDGE_CURVE ( 'NONE', #84452, #248210, #198466, .T. ) ;
#67330=CARTESIAN_POINT ( 'NONE',  ( 21.05095171578076574, 8.776179878782192745, -79.16587327663792450 ) ) ;
#67340=EDGE_CURVE ( 'NONE', #190222, #100804, #181964, .T. ) ;
#67342=FACE_OUTER_BOUND ( 'NONE', #78276, .T. ) ;
#67358=CARTESIAN_POINT ( 'NONE',  ( -21.55000000000000426, 7.750000000011159074, -88.25000000000005684 ) ) ;
#67422=ORIENTED_EDGE ( 'NONE', *, *, #210836, .T. ) ;
#67426=AXIS2_PLACEMENT_3D ( 'NONE', #51819, #165383, #244906 ) ;
#67451=DIRECTION ( 'NONE',  ( 0.000000000000000000, 0.000000000000000000, -1.000000000000000000 ) ) ;
#67456=ORIENTED_EDGE ( 'NONE', *, *, #189941, .F. ) ;
#67462=ORIENTED_EDGE ( 'NONE', *, *, #194246, .F. ) ;
#67463=ADVANCED_FACE ( 'NONE', ( #130185 ), #76084, .T. ) ;
#67466=ORIENTED_EDGE ( 'NONE', *, *, #157343, .F. ) ;
#67509=LINE ( 'NONE', #28433, #6073 ) ;
#67533=AXIS2_PLACEMENT_3D ( 'NONE', #11183, #248504, #189821 ) ;
#67539=CARTESIAN_POINT ( 'NONE',  ( -22.59999999999999787, 11.74956712350054744, -66.89914163090134025 ) ) ;
#67553=EDGE_LOOP ( 'NONE', ( #160680, #107314, #178096, #253054 ) ) ;
#67557=DIRECTION ( 'NONE',  ( 1.000000000000000000, 0.000000000000000000, -0.000000000000000000 ) ) ;
#67569=ORIENTED_EDGE ( 'NONE', *, *, #48174, .F. ) ;
#67589=CARTESIAN_POINT ( 'NONE',  ( 18.59999999999999076, 14.05000000001116689, -72.51369507076103105 ) ) ;
#67592=DIRECTION ( 'NONE',  ( 1.000000000000000000, -0.000000000000000000, -0.000000000000000000 ) ) ;
#67599=ORIENTED_EDGE ( 'NONE', *, *, #68904, .T. ) ;
#67624=ORIENTED_EDGE ( 'NONE', *, *, #121800, .F. ) ;
#67626=EDGE_CURVE ( 'NONE', #169137, #211645, #226070, .T. ) ;
#67648=CIRCLE ( 'NONE', #100913, 0.5000000000000004441 ) ;
#67654=ORIENTED_EDGE ( 'NONE', *, *, #111768, .T. ) ;
#67705=DIRECTION ( 'NONE',  ( 0.000000000000000000, -1.000000000000000000, 0.000000000000000000 ) ) ;
#67706=CARTESIAN_POINT ( 'NONE',  ( 18.59999999999999076, 1.115600667400684642E-11, -100.5000000000000426 ) ) ;
#67712=DIRECTION ( 'NONE',  ( 0.000000000000000000, -0.5000000000000078826, -0.8660254037844340447 ) ) ;
#67719=ORIENTED_EDGE ( 'NONE', *, *, #56199, .F. ) ;
#67725=( BOUNDED_SURFACE ( )  B_SPLINE_SURFACE ( 3, 2, ( 
 ( #241063, #222750, #70144 ),
 ( #227903, #51807, #49260 ),
 ( #28461, #152247, #130073 ),
 ( #231767, #171819, #14002 ) ),
 .UNSPECIFIED., .F., .F., .F. ) 
 B_SPLINE_SURFACE_WITH_KNOTS ( ( 4, 4 ),
 ( 3, 3 ),
 ( -1.355252715606880543E-20, 0.0003124336117481266921 ),
 ( 0.000000000000000000, 1.000000000000000000 ),
 .UNSPECIFIED. ) 
 GEOMETRIC_REPRESENTATION_ITEM ( )  RATIONAL_B_SPLINE_SURFACE ( (
 ( 1.000000000000000000, 0.7040654476015972829, 1.000000000000000000),
 ( 1.000000000000000000, 0.7039193538781918225, 1.000000000000000000),
 ( 1.000000000000000000, 0.7089171279145408677, 1.000000000000000000),
 ( 1.000000000000000000, 0.7071067811865506814, 1.000000000000000000) ) ) 
 REPRESENTATION_ITEM ( '' )  SURFACE ( )  );
#67746=ORIENTED_EDGE ( 'NONE', *, *, #146159, .T. ) ;
#67754=FACE_OUTER_BOUND ( 'NONE', #37294, .T. ) ;
#67778=ADVANCED_FACE ( 'NONE', ( #25359 ), #57025, .F. ) ;
#67806=ORIENTED_EDGE ( 'NONE', *, *, #158386, .T. ) ;
#67863=AXIS2_PLACEMENT_3D ( 'NONE', #231102, #212811, #112428 ) ;
#67873=ADVANCED_FACE ( 'NONE', ( #231264 ), #129402, .F. ) ;
#67885=EDGE_LOOP ( 'NONE', ( #106945, #4603, #177563, #82605 ) ) ;
#67900=CYLINDRICAL_SURFACE ( 'NONE', #78885, 0.09999999999999954758 ) ;
#67915=FACE_OUTER_BOUND ( 'NONE', #18909, .T. ) ;
#67919=AXIS2_PLACEMENT_3D ( 'NONE', #86961, #246076, #90823 ) ;
#67920=AXIS2_PLACEMENT_3D ( 'NONE', #204402, #84420, #222676 ) ;
#67928=DIRECTION ( 'NONE',  ( 0.000000000000000000, 0.9274965247785529332, 0.3738317757009255171 ) ) ;
#67937=ORIENTED_EDGE ( 'NONE', *, *, #76177, .T. ) ;
#67994=VECTOR ( 'NONE', #162148, 1000.000000000000000 ) ;
#68001=EDGE_LOOP ( 'NONE', ( #28317, #58708, #116244, #112016 ) ) ;
#68023=ADVANCED_FACE ( 'NONE', ( #6749 ), #184100, .T. ) ;
#68055=CARTESIAN_POINT ( 'NONE',  ( 23.14999999999999503, 11.75000000001116263, -79.15000000000004832 ) ) ;
#68060=AXIS2_PLACEMENT_3D ( 'NONE', #101798, #23621, #182673 ) ;
#68061=AXIS2_PLACEMENT_3D ( 'NONE', #179747, #143153, #240998 ) ;
#68064=ORIENTED_EDGE ( 'NONE', *, *, #233482, .T. ) ;
#68091=FACE_OUTER_BOUND ( 'NONE', #99599, .T. ) ;
#68093=FACE_OUTER_BOUND ( 'NONE', #160250, .T. ) ;
#68102=CARTESIAN_POINT ( 'NONE',  ( 23.15000000000000213, -11.64999999998883595, -97.40000000000004832 ) ) ;
#68123=CARTESIAN_POINT ( 'NONE',  ( -18.50000000000000000, 9.250000000011157297, -79.35000000000005116 ) ) ;
#68143=ORIENTED_EDGE ( 'NONE', *, *, #201300, .T. ) ;
#68148=ORIENTED_EDGE ( 'NONE', *, *, #143841, .F. ) ;
#68158=CARTESIAN_POINT ( 'NONE',  ( -21.05000000000000071, -11.74999999998884448, -97.60000000000005116 ) ) ;
#68192=CARTESIAN_POINT ( 'NONE',  ( 23.14999999999999503, 6.650000000011155876, -79.25000000000004263 ) ) ;
#68235=DIRECTION ( 'NONE',  ( 0.000000000000000000, 3.469446951953515108E-14, 1.000000000000000000 ) ) ;
#68238=CARTESIAN_POINT ( 'NONE',  ( 23.14999999999999147, -4.149999999988843058, -67.00000000000004263 ) ) ;
#68254=AXIS2_PLACEMENT_3D ( 'NONE', #177168, #257897, #19347 ) ;
#68279=AXIS2_PLACEMENT_3D ( 'NONE', #200105, #25341, #21484 ) ;
#68295=VERTEX_POINT ( 'NONE', #22178 ) ;
#68296=DIRECTION ( 'NONE',  ( 0.000000000000000000, -0.9908441862701600211, -0.1350103645451876666 ) ) ;
#68300=CIRCLE ( 'NONE', #101571, 0.8750000000000007772 ) ;
#68327=ORIENTED_EDGE ( 'NONE', *, *, #74520, .F. ) ;
#68344=CIRCLE ( 'NONE', #143342, 0.09999999999999721612 ) ;
#68366=CARTESIAN_POINT ( 'NONE',  ( -23.25000000000000000, 2.600000000011156054, -80.22462192276213955 ) ) ;
#68367=CARTESIAN_POINT ( 'NONE',  ( 18.59999999999999076, 11.65000000001115943, -91.85000000000003695 ) ) ;
#68386=VERTEX_POINT ( 'NONE', #20903 ) ;
#68420=EDGE_CURVE ( 'NONE', #181065, #103372, #106814, .T. ) ;
#68433=CARTESIAN_POINT ( 'NONE',  ( 22.49999999999999645, 0.1000000000111554016, -55.35042919245523763 ) ) ;
#68442=VERTEX_POINT ( 'NONE', #144657 ) ;
#68446=LINE ( 'NONE', #33208, #4278 ) ;
#68461=DIRECTION ( 'NONE',  ( -0.000000000000000000, -0.8660254037844411501, -0.4999999999999956701 ) ) ;
#68491=EDGE_CURVE ( 'NONE', #144504, #257922, #52481, .T. ) ;
#68519=AXIS2_PLACEMENT_3D ( 'NONE', #118583, #198097, #2450 ) ;
#68527=CARTESIAN_POINT ( 'NONE',  ( 21.14999999999999858, -11.74999999998884448, -79.25000000000004263 ) ) ;
#68549=CARTESIAN_POINT ( 'NONE',  ( 20.44999100639894962, 10.43971070322319683, -74.75907572597057538 ) ) ;
#68571=VERTEX_POINT ( 'NONE', #131523 ) ;
#68584=ORIENTED_EDGE ( 'NONE', *, *, #43789, .F. ) ;
#68598=LINE ( 'NONE', #226351, #79777 ) ;
#68648=ORIENTED_EDGE ( 'NONE', *, *, #227229, .T. ) ;
#68655=DIRECTION ( 'NONE',  ( 1.000000000000000000, -0.000000000000000000, -0.000000000000000000 ) ) ;
#68663=DIRECTION ( 'NONE',  ( 0.000000000000000000, 0.000000000000000000, -1.000000000000000000 ) ) ;
#68691=ORIENTED_EDGE ( 'NONE', *, *, #98709, .T. ) ;
#68692=EDGE_CURVE ( 'NONE', #81812, #141973, #94954, .T. ) ;
#68710=DIRECTION ( 'NONE',  ( 1.000000000000000000, -0.000000000000000000, -0.000000000000000000 ) ) ;
#68718=CARTESIAN_POINT ( 'NONE',  ( -21.55000000000000071, 7.150000000011155876, -88.25000000000005684 ) ) ;
#68737=ORIENTED_EDGE ( 'NONE', *, *, #22818, .F. ) ;
#68831=EDGE_CURVE ( 'NONE', #202762, #222218, #179104, .T. ) ;
#68835=DIRECTION ( 'NONE',  ( 0.000000000000000000, 0.000000000000000000, -1.000000000000000000 ) ) ;
#68836=AXIS2_PLACEMENT_3D ( 'NONE', #151748, #166181, #47459 ) ;
#68843=VERTEX_POINT ( 'NONE', #105182 ) ;
#68844=LINE ( 'NONE', #191374, #118502 ) ;
#68852=EDGE_CURVE ( 'NONE', #198075, #137562, #70767, .T. ) ;
#68893=DIRECTION ( 'NONE',  ( 0.000000000000000000, -0.000000000000000000, 1.000000000000000000 ) ) ;
#68894=CARTESIAN_POINT ( 'NONE',  ( 21.14999999999999858, 6.540656951712400691, -67.00000000000004263 ) ) ;
#68903=DIRECTION ( 'NONE',  ( 0.000000000000000000, 0.000000000000000000, -1.000000000000000000 ) ) ;
#68904=EDGE_CURVE ( 'NONE', #169584, #39555, #166451, .T. ) ;
#68915=DIRECTION ( 'NONE',  ( 0.000000000000000000, -0.000000000000000000, -1.000000000000000000 ) ) ;
#68923=VECTOR ( 'NONE', #8765, 1000.000000000000000 ) ;
#68930=CARTESIAN_POINT ( 'NONE',  ( 21.05000000000000071, 8.776282895303632259, -67.00000000000004263 ) ) ;
#68967=CARTESIAN_POINT ( 'NONE',  ( -20.85000000000000142, 11.75000000001115197, -93.71613433702194129 ) ) ;
#68985=AXIS2_PLACEMENT_3D ( 'NONE', #41158, #4554, #200210 ) ;
#68992=CARTESIAN_POINT ( 'NONE',  ( 21.30000000000002558, 1.115650265596050101E-11, -71.05000000000003979 ) ) ;
#69010=CARTESIAN_POINT ( 'NONE',  ( -21.37071067811865532, 8.070710678129811910, -88.25000000000005684 ) ) ;
#69033=ORIENTED_EDGE ( 'NONE', *, *, #237892, .F. ) ;
#69036=EDGE_CURVE ( 'NONE', #11297, #24624, #222301, .T. ) ;
#69067=CARTESIAN_POINT ( 'NONE',  ( 23.14999999999999503, 11.65000000001116298, -79.15000000000004832 ) ) ;
#69093=CARTESIAN_POINT ( 'NONE',  ( -18.44204374631830134, -9.491036389587220512, -107.1262012702210455 ) ) ;
#69096=CARTESIAN_POINT ( 'NONE',  ( -23.15000000000000213, 1.925233644870967487, -87.76975646687391475 ) ) ;
#69113=AXIS2_PLACEMENT_3D ( 'NONE', #113562, #54851, #176130 ) ;
#69114=EDGE_CURVE ( 'NONE', #220040, #163227, #176571, .T. ) ;
#69115=EDGE_CURVE ( 'NONE', #77390, #153546, #212794, .T. ) ;
#69121=CIRCLE ( 'NONE', #169100, 0.1000000000000028644 ) ;
#69146=B_SPLINE_CURVE_WITH_KNOTS ( 'NONE', 3,
 ( #160560, #41899, #49578, #127841, #187825, #87404, #206087, #245221 ),
 .UNSPECIFIED., .F., .F.,
 ( 4, 2, 2, 4 ),
 ( 0.000000000000000000, 9.550056980124257001E-05, 0.0001910011396024851400, 0.0003820022792049893620 ),
 .UNSPECIFIED. ) ;
#69157=FACE_OUTER_BOUND ( 'NONE', #73942, .T. ) ;
#69162=CARTESIAN_POINT ( 'NONE',  ( 21.05000000000000071, 1.115600667400684642E-11, -100.5000000000000426 ) ) ;
#69163=CARTESIAN_POINT ( 'NONE',  ( -21.05000000000000071, 1.162701749949165642, -75.00000000000004263 ) ) ;
#69165=CARTESIAN_POINT ( 'NONE',  ( -23.15000000000000213, -11.39257802169451139, -97.42605042016811012 ) ) ;
#69171=AXIS2_PLACEMENT_3D ( 'NONE', #1692, #126791, #42139 ) ;
#69184=VECTOR ( 'NONE', #13329, 1000.000000000000000 ) ;
#69186=DIRECTION ( 'NONE',  ( 2.952720810173289112E-16, -1.000000000000000000, 0.000000000000000000 ) ) ;
#69231=DIRECTION ( 'NONE',  ( 0.000000000000000000, -0.9908441862701596881, 0.1350103645451904977 ) ) ;
#69250=ORIENTED_EDGE ( 'NONE', *, *, #208024, .F. ) ;
#69292=ORIENTED_EDGE ( 'NONE', *, *, #195152, .F. ) ;
#69349=ORIENTED_EDGE ( 'NONE', *, *, #56623, .F. ) ;
#69379=FACE_OUTER_BOUND ( 'NONE', #180669, .T. ) ;
#69405=DIRECTION ( 'NONE',  ( 1.000000000000000000, 0.000000000000000000, 0.000000000000000000 ) ) ;
#69430=ORIENTED_EDGE ( 'NONE', *, *, #56151, .F. ) ;
#69431=ORIENTED_EDGE ( 'NONE', *, *, #150998, .T. ) ;
#69447=CIRCLE ( 'NONE', #173540, 0.1999999999999987899 ) ;
#69498=ORIENTED_EDGE ( 'NONE', *, *, #144208, .F. ) ;
#69504=ORIENTED_EDGE ( 'NONE', *, *, #89513, .F. ) ;
#69508=CARTESIAN_POINT ( 'NONE',  ( -18.59999999999999787, 1.115600667400684642E-11, -108.4000000000000483 ) ) ;
#69517=ORIENTED_EDGE ( 'NONE', *, *, #150293, .T. ) ;
#69531=DIRECTION ( 'NONE',  ( 0.000000000000000000, -1.000000000000000000, 0.000000000000000000 ) ) ;
#69548=CARTESIAN_POINT ( 'NONE',  ( 20.94999999999999574, 1.250000000011155299, -74.90000000000004832 ) ) ;
#69554=CARTESIAN_POINT ( 'NONE',  ( 20.94999999999999929, -8.730841121484171907, -76.59807471898437825 ) ) ;
#69583=DIRECTION ( 'NONE',  ( 0.000000000000000000, 0.000000000000000000, 1.000000000000000000 ) ) ;
#69604=ADVANCED_FACE ( 'NONE', ( #117457 ), #182579, .T. ) ;
#69606=DIRECTION ( 'NONE',  ( 0.000000000000000000, 1.000000000000000000, 0.000000000000000000 ) ) ;
#69615=ORIENTED_EDGE ( 'NONE', *, *, #28836, .F. ) ;
#69654=AXIS2_PLACEMENT_3D ( 'NONE', #128030, #125462, #247956 ) ;
#69659=ADVANCED_FACE ( 'NONE', ( #9053 ), #203413, .F. ) ;
#69700=DIRECTION ( 'NONE',  ( 1.000000000000000000, 0.000000000000000000, 0.000000000000000000 ) ) ;
#69704=ORIENTED_EDGE ( 'NONE', *, *, #151870, .T. ) ;
#69709=ORIENTED_EDGE ( 'NONE', *, *, #3245, .T. ) ;
#69718=CARTESIAN_POINT ( 'NONE',  ( -18.40000000000000213, -9.499999999988851584, -74.03206939669971121 ) ) ;
#69728=CARTESIAN_POINT ( 'NONE',  ( 22.59999999999999432, 0.1008583691098678403, -55.25043287651065071 ) ) ;
#69762=FACE_OUTER_BOUND ( 'NONE', #107223, .T. ) ;
#69771=EDGE_CURVE ( 'NONE', #188971, #91651, #248963, .T. ) ;
#69776=ADVANCED_FACE ( 'NONE', ( #251504 ), #131570, .T. ) ;
#69820=ORIENTED_EDGE ( 'NONE', *, *, #115174, .F. ) ;
#69832=ORIENTED_EDGE ( 'NONE', *, *, #71784, .T. ) ;
#69853=CARTESIAN_POINT ( 'NONE',  ( 20.95052659398289308, 10.47982436779105875, -74.57523875586565509 ) ) ;
#69872=CARTESIAN_POINT ( 'NONE',  ( 18.59999999999999076, 10.49142135624846439, -91.75000000000005684 ) ) ;
#69874=VECTOR ( 'NONE', #171822, 1000.000000000000000 ) ;
#69876=CARTESIAN_POINT ( 'NONE',  ( -18.50000000000000000, 1.866714910068465239, -78.75267524628205251 ) ) ;
#69880=AXIS2_PLACEMENT_3D ( 'NONE', #248386, #37070, #121733 ) ;
#69886=EDGE_CURVE ( 'NONE', #87571, #210308, #97778, .T. ) ;
#69948=ORIENTED_EDGE ( 'NONE', *, *, #11210, .F. ) ;
#69957=EDGE_LOOP ( 'NONE', ( #32593, #46685, #36149, #91588, #155320, #130481, #73360, #87173, #85042 ) ) ;
#69958=CARTESIAN_POINT ( 'NONE',  ( 21.13461538461538325, 10.61458296203669249, -79.35000000000005116 ) ) ;
#69960=CARTESIAN_POINT ( 'NONE',  ( 21.05000000000000071, 14.05000000001115623, -94.98630492923912527 ) ) ;
#69970=LINE ( 'NONE', #189896, #234703 ) ;
#70005=DIRECTION ( 'NONE',  ( -0.000000000000000000, -0.000000000000000000, 1.000000000000000000 ) ) ;
#70010=DIRECTION ( 'NONE',  ( 1.000000000000000000, 0.000000000000000000, 0.000000000000000000 ) ) ;
#70021=ORIENTED_EDGE ( 'NONE', *, *, #137671, .F. ) ;
#70042=DIRECTION ( 'NONE',  ( -0.000000000000000000, -0.000000000000000000, -1.000000000000000000 ) ) ;
#70044=ORIENTED_EDGE ( 'NONE', *, *, #199859, .T. ) ;
#70056=AXIS2_PLACEMENT_3D ( 'NONE', #130288, #91172, #31248 ) ;
#70075=CIRCLE ( 'NONE', #3392, 0.1000000000000001860 ) ;
#70088=EDGE_CURVE ( 'NONE', #214056, #13993, #244768, .T. ) ;
#70103=EDGE_CURVE ( 'NONE', #16002, #249989, #135202, .T. ) ;
#70113=ORIENTED_EDGE ( 'NONE', *, *, #184710, .F. ) ;
#70120=ORIENTED_EDGE ( 'NONE', *, *, #120521, .T. ) ;
#70122=B_SPLINE_CURVE_WITH_KNOTS ( 'NONE', 3,
 ( #239749, #23291, #162789, #242298, #104054, #140632, #218876, #220185, #63663, #143194 ),
 .UNSPECIFIED., .F., .F.,
 ( 4, 3, 3, 4 ),
 ( 0.000000000000000000, 0.0002000000000008585893, 0.001000000000082977483, 0.001967863649483336721 ),
 .UNSPECIFIED. ) ;
#70134=CARTESIAN_POINT ( 'NONE',  ( 20.94999999999999574, -1.162701749926853712, -75.10000000000003695 ) ) ;
#70143=ADVANCED_FACE ( 'NONE', ( #90825 ), #129948, .F. ) ;
#70144=CARTESIAN_POINT ( 'NONE',  ( -22.39999999999999858, -0.1008583690875575894, -55.25043287651065782 ) ) ;
#70168=ORIENTED_EDGE ( 'NONE', *, *, #124089, .T. ) ;
#70170=CARTESIAN_POINT ( 'NONE',  ( -20.94999999999999929, -1.135018845899022466, -108.2169768834323662 ) ) ;
#70184=AXIS2_PLACEMENT_3D ( 'NONE', #233790, #50002, #129551 ) ;
#70192=FACE_OUTER_BOUND ( 'NONE', #73493, .T. ) ;
#70199=ORIENTED_EDGE ( 'NONE', *, *, #155694, .F. ) ;
#70223=AXIS2_PLACEMENT_3D ( 'NONE', #183529, #47837, #145666 ) ;
#70253=LINE ( 'NONE', #11544, #166056 ) ;
#70270=VERTEX_POINT ( 'NONE', #171699 ) ;
#70340=DIRECTION ( 'NONE',  ( 1.000000000000000000, 0.000000000000000000, 0.000000000000000000 ) ) ;
#70357=FACE_OUTER_BOUND ( 'NONE', #49422, .T. ) ;
#70365=ORIENTED_EDGE ( 'NONE', *, *, #193486, .F. ) ;
#70379=AXIS2_PLACEMENT_3D ( 'NONE', #191560, #71604, #108148 ) ;
#70383=EDGE_CURVE ( 'NONE', #75395, #4930, #178102, .T. ) ;
#70390=CIRCLE ( 'NONE', #220766, 2.000000000000002665 ) ;
#70407=CIRCLE ( 'NONE', #103655, 0.1000000000000004496 ) ;
#70439=CARTESIAN_POINT ( 'NONE',  ( 22.39999999999999503, 1.115600667400684642E-11, -55.35042919245524473 ) ) ;
#70447=DIRECTION ( 'NONE',  ( -1.000000000000000000, -0.000000000000000000, -0.000000000000000000 ) ) ;
#70452=CARTESIAN_POINT ( 'NONE',  ( -20.54999999999999716, 9.350000000011156942, -88.25000000000005684 ) ) ;
#70474=ORIENTED_EDGE ( 'NONE', *, *, #43645, .F. ) ;
#70477=EDGE_LOOP ( 'NONE', ( #175820, #45166, #236457, #164916 ) ) ;
#70487=ORIENTED_EDGE ( 'NONE', *, *, #2110, .F. ) ;
#70502=EDGE_LOOP ( 'NONE', ( #209049, #575, #16363, #120134 ) ) ;
#70537=CARTESIAN_POINT ( 'NONE',  ( 21.14999999999999858, 11.65000000001115943, -79.15000000000004832 ) ) ;
#70599=CARTESIAN_POINT ( 'NONE',  ( 18.59999999999999787, -1.736705739456431807, -112.0174225876237699 ) ) ;
#70600=DIRECTION ( 'NONE',  ( 1.000000000000000000, 0.000000000000000000, 0.000000000000000000 ) ) ;
#70644=DIRECTION ( 'NONE',  ( 0.000000000000000000, 0.000000000000000000, -1.000000000000000000 ) ) ;
#70662=CYLINDRICAL_SURFACE ( 'NONE', #36447, 0.09999999999999781286 ) ;
#70673=CARTESIAN_POINT ( 'NONE',  ( 21.05000000000000071, -11.48912529306490349, -69.90000000000004832 ) ) ;
#70687=DIRECTION ( 'NONE',  ( 1.000000000000000000, -0.000000000000000000, -0.000000000000000000 ) ) ;
#70691=APPLICATION_CONTEXT ( 'automotive_design' ) ;
#70703=VERTEX_POINT ( 'NONE', #65521 ) ;
#70706=VERTEX_POINT ( 'NONE', #62964 ) ;
#70711=FACE_OUTER_BOUND ( 'NONE', #112878, .T. ) ;
#70712=EDGE_LOOP ( 'NONE', ( #5845, #199412, #123317, #185358 ) ) ;
#70713=CARTESIAN_POINT ( 'NONE',  ( -23.25000000000000000, 6.933893972137497030, -104.2856458343736250 ) ) ;
#70723=EDGE_LOOP ( 'NONE', ( #212757, #6979, #190958, #185886, #146566, #205523, #209305, #232031, #10107, #6005, #190937, #33792, #9834, #208219, #134644, #71602, #115926, #114970 ) ) ;
#70736=ADVANCED_FACE ( 'NONE', ( #185486 ), #106519, .F. ) ;
#70750=DIRECTION ( 'NONE',  ( -0.7071067811865474617, -0.7071067811865474617, -0.000000000000000000 ) ) ;
#70767=CIRCLE ( 'NONE', #224843, 3.999999999999999112 ) ;
#70768=EDGE_LOOP ( 'NONE', ( #150298, #82783, #204071, #138539 ) ) ;
#70777=ORIENTED_EDGE ( 'NONE', *, *, #33221, .F. ) ;
#70815=VERTEX_POINT ( 'NONE', #27733 ) ;
#70828=DIRECTION ( 'NONE',  ( 0.000000000000000000, 0.000000000000000000, -1.000000000000000000 ) ) ;
#70834=CARTESIAN_POINT ( 'NONE',  ( 20.97462148592268250, 8.874737576461731337, -79.25464433173107182 ) ) ;
#70835=ADVANCED_FACE ( 'NONE', ( #207635 ), #148940, .T. ) ;
#70840=CARTESIAN_POINT ( 'NONE',  ( 21.05000000000000426, -0.08561306079281312542, -60.58624026618976188 ) ) ;
#70885=ORIENTED_EDGE ( 'NONE', *, *, #12463, .T. ) ;
#70892=ORIENTED_EDGE ( 'NONE', *, *, #206020, .T. ) ;
#70925=CARTESIAN_POINT ( 'NONE',  ( -21.14999999999999858, 11.65000000001115588, -73.78386566297820082 ) ) ;
#70927=CARTESIAN_POINT ( 'NONE',  ( 20.94999999999999574, -11.39257802169451672, -70.07394957983198935 ) ) ;
#70928=ORIENTED_EDGE ( 'NONE', *, *, #223844, .T. ) ;
#70941=CIRCLE ( 'NONE', #37598, 0.09999999999999939493 ) ;
#70945=CIRCLE ( 'NONE', #45958, 0.1000000000000028644 ) ;
#70969=CARTESIAN_POINT ( 'NONE',  ( -23.25000000000000000, 1.115600667400684642E-11, -108.4000000000000483 ) ) ;
#70974=DIRECTION ( 'NONE',  ( 1.000000000000000000, 0.000000000000000000, 0.000000000000000000 ) ) ;
#70975=CARTESIAN_POINT ( 'NONE',  ( 18.59999999999999076, -1.149570369564537842, -108.3159124845020074 ) ) ;
#70992=VERTEX_POINT ( 'NONE', #204591 ) ;
#70999=ORIENTED_EDGE ( 'NONE', *, *, #148500, .T. ) ;
#71021=CARTESIAN_POINT ( 'NONE',  ( 18.53317502108576420, 10.32263460347359896, -106.0605957968672470 ) ) ;
#71023=FACE_OUTER_BOUND ( 'NONE', #131799, .T. ) ;
#71047=ORIENTED_EDGE ( 'NONE', *, *, #182099, .T. ) ;
#71050=DIRECTION ( 'NONE',  ( -1.000000000000000000, -2.952720810173289112E-16, 0.000000000000000000 ) ) ;
#71064=DIRECTION ( 'NONE',  ( 0.000000000000000000, 0.000000000000000000, -1.000000000000000000 ) ) ;
#71079=DIRECTION ( 'NONE',  ( 1.000000000000000000, 0.000000000000000000, 0.000000000000000000 ) ) ;
#71081=DIRECTION ( 'NONE',  ( 0.000000000000000000, -0.9654727137038715545, 0.2605042016806676242 ) ) ;
#71089=DIRECTION ( 'NONE',  ( 0.000000000000000000, 0.000000000000000000, 1.000000000000000000 ) ) ;
#71091=CARTESIAN_POINT ( 'NONE',  ( -20.64999999999999858, 4.250000000011156409, -88.15000000000004832 ) ) ;
#71095=CARTESIAN_POINT ( 'NONE',  ( -20.94999999999999929, 11.65000000001115588, -74.01480577065404987 ) ) ;
#71102=AXIS2_PLACEMENT_3D ( 'NONE', #246, #84885, #83604 ) ;
#71120=CARTESIAN_POINT ( 'NONE',  ( -20.00857864376270001, 9.350000000011156942, -79.35000000000005116 ) ) ;
#71134=ORIENTED_EDGE ( 'NONE', *, *, #90257, .T. ) ;
#71139=ORIENTED_EDGE ( 'NONE', *, *, #132307, .T. ) ;
#71154=FACE_OUTER_BOUND ( 'NONE', #41625, .T. ) ;
#71156=CARTESIAN_POINT ( 'NONE',  ( 20.46382478191414833, 8.901379558713770734, -75.54572809488314533 ) ) ;
#71162=CARTESIAN_POINT ( 'NONE',  ( 21.05000000000000071, 1.115600667400684642E-11, -100.5000000000000426 ) ) ;
#71166=CARTESIAN_POINT ( 'NONE',  ( -18.59999999999999787, -1.164121893230052995, -108.4148480855716485 ) ) ;
#71178=DIRECTION ( 'NONE',  ( -0.000000000000000000, 1.265107689135680095E-16, -1.000000000000000000 ) ) ;
#71185=ORIENTED_EDGE ( 'NONE', *, *, #61126, .T. ) ;
#71205=CARTESIAN_POINT ( 'NONE',  ( 21.13920837816993270, 8.783247050131068434, -79.25000000000004263 ) ) ;
#71220=AXIS2_PLACEMENT_3D ( 'NONE', #166130, #43578, #206499 ) ;
#71221=EDGE_CURVE ( 'NONE', #195076, #253894, #119213, .T. ) ;
#71222=ORIENTED_EDGE ( 'NONE', *, *, #181183, .F. ) ;
#71224=DIRECTION ( 'NONE',  ( 0.000000000000000000, 0.000000000000000000, -1.000000000000000000 ) ) ;
#71228=CARTESIAN_POINT ( 'NONE',  ( 18.59999999999999432, -1.162701749926855266, -75.10000000000003695 ) ) ;
#71246=CYLINDRICAL_SURFACE ( 'NONE', #211445, 11.80000000000000426 ) ;
#71272=LINE ( 'NONE', #229049, #102549 ) ;
#71284=CARTESIAN_POINT ( 'NONE',  ( -21.52071067811865746, 7.779289321892505882, -79.35000000000005116 ) ) ;
#71292=CARTESIAN_POINT ( 'NONE',  ( -20.64999999999999858, 2.000000000011154189, -87.27537807723794572 ) ) ;
#71307=AXIS2_PLACEMENT_3D ( 'NONE', #99647, #144891, #236607 ) ;
#71327=CARTESIAN_POINT ( 'NONE',  ( -23.15000000000000213, 4.150000000011156764, -79.35000000000005116 ) ) ;
#71343=VECTOR ( 'NONE', #144195, 1000.000000000000000 ) ;
#71347=ADVANCED_FACE ( 'NONE', ( #98507 ), #257568, .F. ) ;
#71378=CARTESIAN_POINT ( 'NONE',  ( 21.05000000000000071, 5.500000000011153745, -88.09473398108696074 ) ) ;
#71379=DIRECTION ( 'NONE',  ( 0.000000000000000000, -0.1568667991644863147, -0.9876197685951252359 ) ) ;
#71388=DIRECTION ( 'NONE',  ( 0.000000000000000000, 0.000000000000000000, -1.000000000000000000 ) ) ;
#71395=EDGE_LOOP ( 'NONE', ( #129659, #161432, #58806, #137711 ) ) ;
#71443=VERTEX_POINT ( 'NONE', #234205 ) ;
#71493=DIRECTION ( 'NONE',  ( 0.000000000000000000, 0.9998779222360096863, -0.01562500000001061998 ) ) ;
#71496=AXIS2_PLACEMENT_3D ( 'NONE', #135600, #36555, #235990 ) ;
#71510=VERTEX_POINT ( 'NONE', #106238 ) ;
#71526=CARTESIAN_POINT ( 'NONE',  ( 18.49999999999999645, 1.835341550235567887, -78.55515129256302487 ) ) ;
#71529=DIRECTION ( 'NONE',  ( 1.000000000000000000, 0.000000000000000000, 0.000000000000000000 ) ) ;
#71547=VERTEX_POINT ( 'NONE', #42432 ) ;
#71549=EDGE_LOOP ( 'NONE', ( #257552, #121159, #27165, #88410 ) ) ;
#71556=AXIS2_PLACEMENT_3D ( 'NONE', #7703, #147196, #109334 ) ;
#71597=DIRECTION ( 'NONE',  ( 6.938893903907224433E-15, -1.000000000000000000, -2.891205793294679805E-16 ) ) ;
#71602=ORIENTED_EDGE ( 'NONE', *, *, #227089, .T. ) ;
#71604=DIRECTION ( 'NONE',  ( 1.000000000000000000, 2.952720810173289112E-16, -0.000000000000000000 ) ) ;
#71623=CARTESIAN_POINT ( 'NONE',  ( -21.05000000000000071, 1.261786168576181755, -75.08649896354552311 ) ) ;
#71625=B_SPLINE_CURVE_WITH_KNOTS ( 'NONE', 3,
 ( #171604, #33381, #67330, #107739, #170336, #231554, #189849, #206846, #11218, #50314, #32084, #88144, #90731, #249827, #71205, #132442 ),
 .UNSPECIFIED., .F., .F.,
 ( 4, 3, 3, 3, 3, 4 ),
 ( 0.000000000000000000, 2.372700795693552043E-05, 5.739057815867001201E-05, 9.073899019179670509E-05, 0.0001243544287365731219, 0.0001585386695601224125 ),
 .UNSPECIFIED. ) ;
#71638=CARTESIAN_POINT ( 'NONE',  ( 23.14999999999999503, 11.65000000001116298, -93.48519422934610645 ) ) ;
#71678=ADVANCED_FACE ( 'NONE', ( #50130 ), #230064, .F. ) ;
#71736=VERTEX_POINT ( 'NONE', #128397 ) ;
#71755=LINE ( 'NONE', #30070, #212371 ) ;
#71765=B_SPLINE_CURVE_WITH_KNOTS ( 'NONE', 3,
 ( #185029, #83328, #162925, #5075, #84597, #243722, #65079, #245002, #224146, #6389 ),
 .UNSPECIFIED., .F., .F.,
 ( 4, 2, 2, 2, 4 ),
 ( 0.000000000000000000, 3.990160268013353780E-05, 7.980320536026707561E-05, 0.0001596064107205310341, 0.0003192128214410546957 ),
 .UNSPECIFIED. ) ;
#71784=EDGE_CURVE ( 'NONE', #140921, #104099, #98680, .T. ) ;
#71805=DIRECTION ( 'NONE',  ( 0.000000000000000000, -1.000000000000000000, -0.000000000000000000 ) ) ;
#71834=DIRECTION ( 'NONE',  ( -1.000000000000000000, -2.952720810173289112E-16, 0.000000000000000000 ) ) ;
#71850=AXIS2_PLACEMENT_3D ( 'NONE', #7210, #107607, #148029 ) ;
#71868=FACE_OUTER_BOUND ( 'NONE', #192285, .T. ) ;
#71937=CARTESIAN_POINT ( 'NONE',  ( -18.39999999999999858, -9.499999999988849808, -107.1001893912220879 ) ) ;
#71942=VECTOR ( 'NONE', #143658, 1000.000000000000000 ) ;
#71957=ADVANCED_FACE ( 'NONE', ( #146353 ), #157006, .T. ) ;
#71967=AXIS2_PLACEMENT_3D ( 'NONE', #131666, #172124, #114675 ) ;
#72010=CIRCLE ( 'NONE', #38686, 0.09999999999999939493 ) ;
#72059=EDGE_CURVE ( 'NONE', #112516, #76379, #197032, .T. ) ;
#72081=ORIENTED_EDGE ( 'NONE', *, *, #59346, .T. ) ;
#72095=DIRECTION ( 'NONE',  ( 0.000000000000000000, 0.000000000000000000, -1.000000000000000000 ) ) ;
#72100=CARTESIAN_POINT ( 'NONE',  ( 18.59999999999999787, -1.835859311432481045, -112.0044391687985694 ) ) ;
#72154=CARTESIAN_POINT ( 'NONE',  ( 22.48660254037843842, 11.75000000001115907, -66.95000000000003126 ) ) ;
#72187=DIRECTION ( 'NONE',  ( 1.000000000000000000, 0.000000000000000000, 0.000000000000000000 ) ) ;
#72254=EDGE_LOOP ( 'NONE', ( #13999, #230751, #191195, #214583 ) ) ;
#72283=FACE_OUTER_BOUND ( 'NONE', #53138, .T. ) ;
#72297=EDGE_LOOP ( 'NONE', ( #41377, #94309, #253285, #37124, #13683, #57585, #110760, #160222, #80307, #156075, #229222, #24677 ) ) ;
#72314=DIRECTION ( 'NONE',  ( -2.812466655313719426E-14, 0.1350103645451904977, 0.9908441862701596881 ) ) ;
#72331=CARTESIAN_POINT ( 'NONE',  ( 21.14999999999999858, -0.09999999998884338825, -55.35042919245524473 ) ) ;
#72373=AXIS2_PLACEMENT_3D ( 'NONE', #81876, #226531, #200577 ) ;
#72383=VECTOR ( 'NONE', #257251, 1000.000000000000114 ) ;
#72403=DIRECTION ( 'NONE',  ( 0.000000000000000000, 1.000000000000000000, 0.000000000000000000 ) ) ;
#72408=DIRECTION ( 'NONE',  ( 0.000000000000000000, 1.734723475976805517E-14, -1.000000000000000000 ) ) ;
#72413=CARTESIAN_POINT ( 'NONE',  ( 20.74625933824090396, 8.882913521095439080, -75.55517102412177621 ) ) ;
#72430=DIRECTION ( 'NONE',  ( 0.000000000000000000, -1.000000000000000000, 0.000000000000000000 ) ) ;
#72431=DIRECTION ( 'NONE',  ( -1.000000000000000000, -0.000000000000000000, -0.000000000000000000 ) ) ;
#72454=DIRECTION ( 'NONE',  ( 0.000000000000000000, 0.000000000000000000, -1.000000000000000000 ) ) ;
#72460=AXIS2_PLACEMENT_3D ( 'NONE', #140151, #219695, #81449 ) ;
#72480=VERTEX_POINT ( 'NONE', #176879 ) ;
#72500=DIRECTION ( 'NONE',  ( -3.265361837132813093E-16, 1.000000000000000000, 0.000000000000000000 ) ) ;
#72528=AXIS2_PLACEMENT_3D ( 'NONE', #82993, #162588, #242094 ) ;
#72541=CIRCLE ( 'NONE', #26754, 0.09999999999999939493 ) ;
#72566=CARTESIAN_POINT ( 'NONE',  ( -21.44999999999999929, 7.150000000011155876, -79.35000000000005116 ) ) ;
#72571=EDGE_CURVE ( 'NONE', #197089, #118463, #56869, .T. ) ;
#72609=CIRCLE ( 'NONE', #205859, 0.09999999999999749367 ) ;
#72645=CARTESIAN_POINT ( 'NONE',  ( -21.05000000000000071, -11.48912529306489994, -97.40000000000004832 ) ) ;
#72646=AXIS2_PLACEMENT_3D ( 'NONE', #151243, #173411, #15596 ) ;
#72672=ORIENTED_EDGE ( 'NONE', *, *, #154914, .T. ) ;
#72674=AXIS2_PLACEMENT_3D ( 'NONE', #16472, #236762, #173001 ) ;
#72729=CARTESIAN_POINT ( 'NONE',  ( -18.59999999999999787, -9.499999999988849808, -75.10000000000003695 ) ) ;
#72756=CARTESIAN_POINT ( 'NONE',  ( -18.59999999999999787, 1.115600667400684642E-11, -100.5000000000000426 ) ) ;
#72772=ORIENTED_EDGE ( 'NONE', *, *, #76734, .F. ) ;
#72786=CARTESIAN_POINT ( 'NONE',  ( 21.14999999999999858, 10.71339244341104013, -79.35000000000005116 ) ) ;
#72821=CARTESIAN_POINT ( 'NONE',  ( -20.94999999999999929, 1.115600667400684642E-11, -67.00000000000004263 ) ) ;
#72824=ORIENTED_EDGE ( 'NONE', *, *, #176735, .T. ) ;
#72835=VERTEX_POINT ( 'NONE', #11060 ) ;
#72837=EDGE_CURVE ( 'NONE', #189461, #192398, #136090, .T. ) ;
#72853=DIRECTION ( 'NONE',  ( 1.000000000000000000, 3.265361837132813093E-16, -0.000000000000000000 ) ) ;
#72859=AXIS2_PLACEMENT_3D ( 'NONE', #216840, #236411, #173925 ) ;
#72931=CARTESIAN_POINT ( 'NONE',  ( 18.47073956224748770, -9.471729412460723196, -74.10868575281796211 ) ) ;
#72955=ADVANCED_FACE ( 'NONE', ( #40925 ), #86204, .T. ) ;
#72995=EDGE_LOOP ( 'NONE', ( #236793, #210182, #30274, #40662 ) ) ;
#73008=CARTESIAN_POINT ( 'NONE',  ( -23.15000000000000213, 1.115600667400684642E-11, -100.5000000000000426 ) ) ;
#73027=DIRECTION ( 'NONE',  ( -3.265361837132813093E-16, 1.000000000000000000, 0.000000000000000000 ) ) ;
#73034=DIRECTION ( 'NONE',  ( -1.000000000000000000, -2.952720810173289112E-16, 0.000000000000000000 ) ) ;
#73047=( BOUNDED_SURFACE ( )  B_SPLINE_SURFACE ( 3, 2, ( 
 ( #68433, #51395, #69728 ),
 ( #130971, #151843, #228798 ),
 ( #227486, #48856, #128402 ),
 ( #207959, #171421, #250901 ) ),
 .UNSPECIFIED., .F., .F., .F. ) 
 B_SPLINE_SURFACE_WITH_KNOTS ( ( 4, 4 ),
 ( 3, 3 ),
 ( -2.710505431213761085E-20, 0.0003124336600439509004 ),
 ( 0.000000000000000000, 1.000000000000000000 ),
 .UNSPECIFIED. ) 
 GEOMETRIC_REPRESENTATION_ITEM ( )  RATIONAL_B_SPLINE_SURFACE ( (
 ( 1.000000000000000000, 0.7071067811865229258, 1.000000000000000000),
 ( 1.000000000000000000, 0.7089187706049977500, 1.000000000000000000),
 ( 1.000000000000000000, 0.7039288185052062774, 1.000000000000000000),
 ( 1.000000000000000000, 0.7040654476015933971, 1.000000000000000000) ) ) 
 REPRESENTATION_ITEM ( '' )  SURFACE ( )  );
#73079=CARTESIAN_POINT ( 'NONE',  ( -20.54999999999999716, -8.730841121484173684, -76.59807471898437825 ) ) ;
#73085=DIRECTION ( 'NONE',  ( 0.000000000000000000, -0.1298341882520022694, -0.9915357197604853789 ) ) ;
#73143=CARTESIAN_POINT ( 'NONE',  ( -23.25000000000000000, 1.115600667400684642E-11, -108.4000000000000483 ) ) ;
#73173=CARTESIAN_POINT ( 'NONE',  ( -20.54999999999999716, 2.500000000011154633, -87.27537807723794572 ) ) ;
#73192=CIRCLE ( 'NONE', #160486, 0.1000000000000020595 ) ;
#73272=ORIENTED_EDGE ( 'NONE', *, *, #217282, .T. ) ;
#73274=VECTOR ( 'NONE', #68710, 1000.000000000000000 ) ;
#73288=CARTESIAN_POINT ( 'NONE',  ( -18.50000000000000000, 11.65000000001115232, -55.25000000000004974 ) ) ;
#73298=ORIENTED_EDGE ( 'NONE', *, *, #53815, .T. ) ;
#73311=VERTEX_POINT ( 'NONE', #241374 ) ;
#73355=AXIS2_PLACEMENT_3D ( 'NONE', #44731, #124272, #141258 ) ;
#73360=ORIENTED_EDGE ( 'NONE', *, *, #150171, .T. ) ;
#73384=CARTESIAN_POINT ( 'NONE',  ( -18.59999999999999787, 6.846123162363745074, -104.2377262668499043 ) ) ;
#73392=CARTESIAN_POINT ( 'NONE',  ( 22.47071067811865319, 7.720074744509199505, -66.90090754529744288 ) ) ;
#73405=CARTESIAN_POINT ( 'NONE',  ( -20.94999999999999929, -11.39257802169451317, -97.42605042016811012 ) ) ;
#73416=ORIENTED_EDGE ( 'NONE', *, *, #195409, .F. ) ;
#73485=ADVANCED_FACE ( 'NONE', ( #131683 ), #50835, .T. ) ;
#73491=CARTESIAN_POINT ( 'NONE',  ( 18.59999999999999076, 10.20857864377385127, -88.35000000000003695 ) ) ;
#73493=EDGE_LOOP ( 'NONE', ( #212046, #241573, #115891, #78689 ) ) ;
#73502=AXIS2_PLACEMENT_3D ( 'NONE', #48945, #131054, #250984 ) ;
#73503=AXIS2_PLACEMENT_3D ( 'NONE', #62586, #99109, #59990 ) ;
#73533=CARTESIAN_POINT ( 'NONE',  ( 21.08884785362045378, 6.357193367436396514, -66.95021690493318545 ) ) ;
#73565=DIRECTION ( 'NONE',  ( -1.000000000000000000, 9.012599976028471648E-15, 6.882867235861662930E-14 ) ) ;
#73591=CARTESIAN_POINT ( 'NONE',  ( 22.59999999999999432, 0.1000000000111554016, -55.35042919245524473 ) ) ;
#73617=ADVANCED_FACE ( 'NONE', ( #216346 ), #74167, .T. ) ;
#73633=CYLINDRICAL_SURFACE ( 'NONE', #164321, 12.87499999999999822 ) ;
#73637=EDGE_CURVE ( 'NONE', #201851, #140921, #61942, .T. ) ;
#73638=EDGE_CURVE ( 'NONE', #11990, #60888, #223952, .T. ) ;
#73650=ORIENTED_EDGE ( 'NONE', *, *, #84640, .T. ) ;
#73661=EDGE_LOOP ( 'NONE', ( #42480, #150220, #144732, #35758 ) ) ;
#73666=DIRECTION ( 'NONE',  ( 0.000000000000000000, -1.000000000000000000, 0.000000000000000000 ) ) ;
#73676=AXIS2_PLACEMENT_3D ( 'NONE', #165541, #245062, #126396 ) ;
#73688=AXIS2_PLACEMENT_3D ( 'NONE', #119247, #183072, #100903 ) ;
#73691=CIRCLE ( 'NONE', #177912, 0.1000000000000028644 ) ;
#73715=DIRECTION ( 'NONE',  ( 0.000000000000000000, 1.734723475976757554E-14, -1.000000000000000000 ) ) ;
#73743=CARTESIAN_POINT ( 'NONE',  ( -23.15000000000000213, 4.350000000011156054, -79.25000000000004263 ) ) ;
#73754=TOROIDAL_SURFACE ( 'NONE', #186152, 0.4000000000000015210, 0.1000000000000000056 ) ;
#73771=DIRECTION ( 'NONE',  ( 1.000000000000000000, 0.000000000000000000, 0.000000000000000000 ) ) ;
#73773=VECTOR ( 'NONE', #219211, 1000.000000000000000 ) ;
#73803=FACE_OUTER_BOUND ( 'NONE', #27070, .T. ) ;
#73807=EDGE_CURVE ( 'NONE', #154034, #39515, #199029, .T. ) ;
#73814=CIRCLE ( 'NONE', #194624, 0.1000000000000001860 ) ;
#73819=CARTESIAN_POINT ( 'NONE',  ( -21.05000000000000071, -11.39257802169451672, -70.07394957983198935 ) ) ;
#73838=CARTESIAN_POINT ( 'NONE',  ( 21.04999999999999716, 8.871279686006802834, -75.55862899514100661 ) ) ;
#73858=VERTEX_POINT ( 'NONE', #208366 ) ;
#73863=ORIENTED_EDGE ( 'NONE', *, *, #47471, .F. ) ;
#73868=ADVANCED_FACE ( 'NONE', ( #192640 ), #160901, .T. ) ;
#73916=EDGE_CURVE ( 'NONE', #66589, #5531, #20097, .T. ) ;
#73926=AXIS2_PLACEMENT_3D ( 'NONE', #173391, #233340, #229471 ) ;
#73942=EDGE_LOOP ( 'NONE', ( #61083, #17569, #64652, #19432 ) ) ;
#73943=EDGE_LOOP ( 'NONE', ( #107509, #95286, #2274, #201938 ) ) ;
#73975=DIRECTION ( 'NONE',  ( 0.000000000000000000, 1.000000000000000000, 0.000000000000000000 ) ) ;
#74029=ORIENTED_EDGE ( 'NONE', *, *, #98709, .F. ) ;
#74051=VECTOR ( 'NONE', #6002, 1000.000000000000000 ) ;
#74089=TOROIDAL_SURFACE ( 'NONE', #211428, 0.2000000000000000111, 0.1000000000000000056 ) ;
#74112=CARTESIAN_POINT ( 'NONE',  ( -20.95000000000000639, 11.75000000001115019, -93.71613433702195550 ) ) ;
#74115=CYLINDRICAL_SURFACE ( 'NONE', #132645, 0.1000000000000028644 ) ;
#74117=VERTEX_POINT ( 'NONE', #66915 ) ;
#74131=ORIENTED_EDGE ( 'NONE', *, *, #102538, .F. ) ;
#74151=ORIENTED_EDGE ( 'NONE', *, *, #242800, .F. ) ;
#74152=AXIS2_PLACEMENT_3D ( 'NONE', #138701, #20092, #39674 ) ;
#74164=CYLINDRICAL_SURFACE ( 'NONE', #14660, 0.09999999999999939493 ) ;
#74167=TOROIDAL_SURFACE ( 'NONE', #194953, 11.89999999999999858, 0.1000000000000000056 ) ;
#74180=SPHERICAL_SURFACE ( 'NONE', #138404, 0.1000000000000000056 ) ;
#74200=ORIENTED_EDGE ( 'NONE', *, *, #22695, .T. ) ;
#74218=FACE_OUTER_BOUND ( 'NONE', #55000, .T. ) ;
#74228=CARTESIAN_POINT ( 'NONE',  ( 18.49999999999998934, 6.550000000011156231, -77.01702717044007329 ) ) ;
#74248=CARTESIAN_POINT ( 'NONE',  ( -23.15000000000000213, 1.115600667400684642E-11, -67.00000000000004263 ) ) ;
#74258=ORIENTED_EDGE ( 'NONE', *, *, #44922, .T. ) ;
#74291=DIRECTION ( 'NONE',  ( 0.000000000000000000, 1.000000000000000000, 0.000000000000000000 ) ) ;
#74316=CARTESIAN_POINT ( 'NONE',  ( 20.94999999999999929, -11.48912529306489994, -97.60000000000005116 ) ) ;
#74345=DIRECTION ( 'NONE',  ( 0.000000000000000000, 0.000000000000000000, -1.000000000000000000 ) ) ;
#74349=DIRECTION ( 'NONE',  ( 0.000000000000000000, -1.000000000000000000, 0.000000000000000000 ) ) ;
#74367=DIRECTION ( 'NONE',  ( -1.000000000000000000, -0.000000000000000000, -0.000000000000000000 ) ) ;
#74385=CARTESIAN_POINT ( 'NONE',  ( -20.54999999999999716, 7.150000000011155876, -83.75000000000004263 ) ) ;
#74391=ADVANCED_FACE ( 'NONE', ( #131582 ), #129028, .F. ) ;
#74397=ADVANCED_FACE ( 'NONE', ( #112034 ), #33813, .T. ) ;
#74437=ORIENTED_EDGE ( 'NONE', *, *, #243414, .F. ) ;
#74438=AXIS2_PLACEMENT_3D ( 'NONE', #96929, #233909, #55237 ) ;
#74455=DIRECTION ( 'NONE',  ( 1.000000000000000000, 0.000000000000000000, 0.000000000000000000 ) ) ;
#74473=VERTEX_POINT ( 'NONE', #235805 ) ;
#74479=DIRECTION ( 'NONE',  ( 1.000000000000000000, 0.000000000000000000, 0.000000000000000000 ) ) ;
#74484=ORIENTED_EDGE ( 'NONE', *, *, #69115, .F. ) ;
#74487=TOROIDAL_SURFACE ( 'NONE', #124516, 0.2000000000000000111, 0.1000000000000000056 ) ;
#74497=CARTESIAN_POINT ( 'NONE',  ( 23.15000000000000213, -11.48912529306489816, -97.40000000000004832 ) ) ;
#74518=CARTESIAN_POINT ( 'NONE',  ( 21.05000000000000071, -0.09999999998884512298, -60.45934304829879835 ) ) ;
#74519=FACE_OUTER_BOUND ( 'NONE', #133851, .T. ) ;
#74520=EDGE_CURVE ( 'NONE', #44645, #208853, #207796, .T. ) ;
#74537=VECTOR ( 'NONE', #131531, 1000.000000000000114 ) ;
#74557=EDGE_CURVE ( 'NONE', #232336, #24864, #195329, .T. ) ;
#74566=ORIENTED_EDGE ( 'NONE', *, *, #58462, .T. ) ;
#74621=VECTOR ( 'NONE', #138011, 1000.000000000000000 ) ;
#74633=EDGE_LOOP ( 'NONE', ( #82965, #6248, #83778 ) ) ;
#74651=CIRCLE ( 'NONE', #199532, 0.1000000000000017958 ) ;
#74668=DIRECTION ( 'NONE',  ( -1.000000000000000000, -0.000000000000000000, -0.000000000000000000 ) ) ;
#74685=CARTESIAN_POINT ( 'NONE',  ( 22.14074124539698829, 7.390077851054901892, -66.90094710415597490 ) ) ;
#74690=AXIS2_PLACEMENT_3D ( 'NONE', #207176, #31134, #48082 ) ;
#74724=DIRECTION ( 'NONE',  ( 1.000000000000000000, 0.000000000000000000, 0.000000000000000000 ) ) ;
#74781=DIRECTION ( 'NONE',  ( 0.000000000000000000, 0.9908441862701596881, 0.1350103645451904977 ) ) ;
#74817=CARTESIAN_POINT ( 'NONE',  ( 18.59999999999999076, 11.65000000001115943, -91.75000000000005684 ) ) ;
#74858=ORIENTED_EDGE ( 'NONE', *, *, #161579, .T. ) ;
#74876=CARTESIAN_POINT ( 'NONE',  ( -18.45037301276668984, -9.490200447530813932, -74.01267413641436121 ) ) ;
#74890=DIRECTION ( 'NONE',  ( -1.000000000000000000, -2.952720810173289112E-16, 0.000000000000000000 ) ) ;
#74893=EDGE_LOOP ( 'NONE', ( #22245, #23084, #174903, #252406 ) ) ;
#74902=DIRECTION ( 'NONE',  ( 0.000000000000000000, -0.4999999999999949485, 0.8660254037844415942 ) ) ;
#74937=DIRECTION ( 'NONE',  ( 2.259780016855445309E-14, 0.9875055080513753802, -0.1575844902526748192 ) ) ;
#74948=CARTESIAN_POINT ( 'NONE',  ( -20.85000000000000142, 0.1610488207298751417, -100.2158101556398293 ) ) ;
#74996=EDGE_CURVE ( 'NONE', #38707, #214401, #12162, .T. ) ;
#74997=DIRECTION ( 'NONE',  ( -4.336808689942053235E-15, -0.8660254037844482555, -0.4999999999999836797 ) ) ;
#75011=VERTEX_POINT ( 'NONE', #54573 ) ;
#75013=EDGE_CURVE ( 'NONE', #194521, #102331, #92413, .T. ) ;
#75072=CARTESIAN_POINT ( 'NONE',  ( -21.64999999999999858, 7.250000000011148416, -88.25000000000005684 ) ) ;
#75124=CARTESIAN_POINT ( 'NONE',  ( -18.50596464788227635, 10.30632246271647112, -106.0041836778896283 ) ) ;
#75135=ORIENTED_EDGE ( 'NONE', *, *, #229019, .T. ) ;
#75143=AXIS2_PLACEMENT_3D ( 'NONE', #154568, #153288, #112839 ) ;
#75156=ORIENTED_EDGE ( 'NONE', *, *, #128319, .T. ) ;
#75161=EDGE_LOOP ( 'NONE', ( #107650, #152575, #197270 ) ) ;
#75170=CARTESIAN_POINT ( 'NONE',  ( -21.08078803292166725, 0.07918598716886154909, -60.66698703556290440 ) ) ;
#75173=DIRECTION ( 'NONE',  ( -0.000000000000000000, 0.000000000000000000, 1.000000000000000000 ) ) ;
#75208=EDGE_CURVE ( 'NONE', #96187, #190057, #129037, .T. ) ;
#75223=VERTEX_POINT ( 'NONE', #55830 ) ;
#75227=ORIENTED_EDGE ( 'NONE', *, *, #125298, .F. ) ;
#75235=ORIENTED_EDGE ( 'NONE', *, *, #228398, .T. ) ;
#75244=ADVANCED_FACE ( 'NONE', ( #59687 ), #4119, .T. ) ;
#75278=EDGE_CURVE ( 'NONE', #102720, #119208, #224686, .T. ) ;
#75287=TOROIDAL_SURFACE ( 'NONE', #8631, 0.4000000000000010214, 0.1000000000000000056 ) ;
#75331=CARTESIAN_POINT ( 'NONE',  ( 23.15000000000000213, -8.596261682231833845, -76.45012751715033517 ) ) ;
#75346=VECTOR ( 'NONE', #1219, 1000.000000000000000 ) ;
#75350=CARTESIAN_POINT ( 'NONE',  ( -18.59999999999999787, 11.65000000001115232, -79.25000000000004263 ) ) ;
#75352=DIRECTION ( 'NONE',  ( 0.000000000000000000, -0.1298341882520022694, -0.9915357197604852679 ) ) ;
#75395=VERTEX_POINT ( 'NONE', #16134 ) ;
#75410=AXIS2_PLACEMENT_3D ( 'NONE', #217803, #56167, #135706 ) ;
#75424=DIRECTION ( 'NONE',  ( 0.000000000000000000, -1.000000000000000000, 0.000000000000000000 ) ) ;
#75442=ADVANCED_FACE ( 'NONE', ( #112646 ), #13550, .T. ) ;
#75475=VECTOR ( 'NONE', #11086, 1000.000000000000000 ) ;
#75489=DIRECTION ( 'NONE',  ( -1.000000000000000000, -3.265361837132813093E-16, 0.000000000000000000 ) ) ;
#75506=ADVANCED_FACE ( 'NONE', ( #177775 ), #199900, .F. ) ;
#75508=ORIENTED_EDGE ( 'NONE', *, *, #88720, .F. ) ;
#75544=EDGE_LOOP ( 'NONE', ( #222201, #75723, #76386, #191385, #49814 ) ) ;
#75553=CARTESIAN_POINT ( 'NONE',  ( 18.46932045258644450, -9.670685200254593994, -107.1738603729966997 ) ) ;
#75556=DIRECTION ( 'NONE',  ( 0.000000000000000000, -0.000000000000000000, -1.000000000000000000 ) ) ;
#75570=VECTOR ( 'NONE', #41749, 1000.000000000000000 ) ;
#75619=ORIENTED_EDGE ( 'NONE', *, *, #50577, .T. ) ;
#75635=EDGE_LOOP ( 'NONE', ( #127178, #125542, #46258 ) ) ;
#75643=VERTEX_POINT ( 'NONE', #47204 ) ;
#75664=ADVANCED_FACE ( 'NONE', ( #69379 ), #164618, .F. ) ;
#75674=DIRECTION ( 'NONE',  ( 0.000000000000000000, 0.000000000000000000, -1.000000000000000000 ) ) ;
#75717=DIRECTION ( 'NONE',  ( 0.000000000000000000, 0.8660254037844411501, 0.4999999999999956701 ) ) ;
#75723=ORIENTED_EDGE ( 'NONE', *, *, #144072, .T. ) ;
#75742=VERTEX_POINT ( 'NONE', #30251 ) ;
#75748=DIRECTION ( 'NONE',  ( 0.000000000000000000, 0.6728971962616697722, -0.7397360091702875895 ) ) ;
#75754=ADVANCED_FACE ( 'NONE', ( #210167 ), #130614, .T. ) ;
#75768=CARTESIAN_POINT ( 'NONE',  ( 21.11825140030084569, 0.007203620643888101679, -60.55459243458003016 ) ) ;
#75770=EDGE_LOOP ( 'NONE', ( #182570, #144609, #29977, #209892 ) ) ;
#75779=AXIS2_PLACEMENT_3D ( 'NONE', #243937, #178878, #41922 ) ;
#75784=ORIENTED_EDGE ( 'NONE', *, *, #75013, .F. ) ;
#75797=EDGE_LOOP ( 'NONE', ( #38978, #70044 ) ) ;
#75823=FILL_AREA_STYLE_COLOUR ( '', #99198 ) ;
#75825=ORIENTED_EDGE ( 'NONE', *, *, #43180, .T. ) ;
#75840=EDGE_CURVE ( 'NONE', #158987, #89853, #91970, .T. ) ;
#75869=VERTEX_POINT ( 'NONE', #70673 ) ;
#75870=CIRCLE ( 'NONE', #242446, 0.8750000000000007772 ) ;
#75896=ADVANCED_FACE ( 'NONE', ( #238705 ), #39251, .F. ) ;
#75920=EDGE_CURVE ( 'NONE', #240894, #85481, #37963, .T. ) ;
#75957=ORIENTED_EDGE ( 'NONE', *, *, #204163, .F. ) ;
#75969=FACE_OUTER_BOUND ( 'NONE', #118554, .T. ) ;
#76026=CARTESIAN_POINT ( 'NONE',  ( -22.50000000000000000, 0.1000000000111554016, -59.20922040162664501 ) ) ;
#76030=ADVANCED_FACE ( 'NONE', ( #255655 ), #87317, .T. ) ;
#76045=AXIS2_PLACEMENT_3D ( 'NONE', #153855, #15607, #95109 ) ;
#76063=CARTESIAN_POINT ( 'NONE',  ( 21.08198257630413508, 6.336596734026219480, -66.92735667621543882 ) ) ;
#76068=AXIS2_PLACEMENT_3D ( 'NONE', #160119, #199232, #156279 ) ;
#76084=( BOUNDED_SURFACE ( )  B_SPLINE_SURFACE ( 3, 2, ( 
 ( #93640, #74112, #68967 ),
 ( #190190, #171937, #92349 ),
 ( #251430, #153676, #233181 ),
 ( #148489, #128927, #208478 ),
 ( #54506, #29847, #109332 ),
 ( #102260, #78860, #59274 ) ),
 .UNSPECIFIED., .F., .F., .F. ) 
 B_SPLINE_SURFACE_WITH_KNOTS ( ( 4, 2, 4 ),
 ( 3, 3 ),
 ( 1.570796326794897668, 2.356194490192346169, 3.141592653589794448 ),
 ( 0.000000000000000000, 1.000000000000000000 ),
 .UNSPECIFIED. ) 
 GEOMETRIC_REPRESENTATION_ITEM ( )  RATIONAL_B_SPLINE_SURFACE ( (
 ( 1.000000000000000000, 0.7071067811865475727, 1.000000000000000000),
 ( 1.000000000000000000, 0.6611148371772178622, 1.000000000000000000),
 ( 1.000000000000000000, 0.6092287576704737972, 1.000000000000000000),
 ( 1.000000000000000000, 0.5278258667049164909, 1.000000000000000000),
 ( 1.000000000000000000, 0.4993418825341195411, 1.000000000000000000),
 ( 1.000000000000000000, 0.4999999999999960587, 1.000000000000000000) ) ) 
 REPRESENTATION_ITEM ( '' )  SURFACE ( )  );
#76142=DIRECTION ( 'NONE',  ( 1.000000000000000000, -0.000000000000000000, -0.000000000000000000 ) ) ;
#76177=EDGE_CURVE ( 'NONE', #217530, #61798, #12900, .T. ) ;
#76182=EDGE_LOOP ( 'NONE', ( #83380, #67746, #244500, #128228 ) ) ;
#76183=CIRCLE ( 'NONE', #130361, 0.1000000000000028644 ) ;
#76231=CIRCLE ( 'NONE', #105432, 0.1000000000000028644 ) ;
#76244=ORIENTED_EDGE ( 'NONE', *, *, #155788, .T. ) ;
#76251=ORIENTED_EDGE ( 'NONE', *, *, #92751, .F. ) ;
#76252=CIRCLE ( 'NONE', #226254, 0.1000000000000028644 ) ;
#76258=CARTESIAN_POINT ( 'NONE',  ( -20.94999999999999929, 1.115600667400684642E-11, -100.5000000000000426 ) ) ;
#76281=CIRCLE ( 'NONE', #138616, 0.1000000000000028644 ) ;
#76320=DIRECTION ( 'NONE',  ( 0.000000000000000000, 1.776356839400155604E-15, 1.000000000000000000 ) ) ;
#76332=CARTESIAN_POINT ( 'NONE',  ( 18.59999999999999432, -9.480686695267811714, -107.4411151687579036 ) ) ;
#76343=CARTESIAN_POINT ( 'NONE',  ( 23.14999999999999503, 11.75000000001116263, -93.48519422934610645 ) ) ;
#76350=AXIS2_PLACEMENT_3D ( 'NONE', #14797, #53893, #215525 ) ;
#76379=VERTEX_POINT ( 'NONE', #206970 ) ;
#76386=ORIENTED_EDGE ( 'NONE', *, *, #213360, .F. ) ;
#76398=CIRCLE ( 'NONE', #51443, 0.09999999999999939493 ) ;
#76408=CARTESIAN_POINT ( 'NONE',  ( -21.14250536705909411, 1.115600667400684642E-11, -60.48182782311928918 ) ) ;
#76420=CARTESIAN_POINT ( 'NONE',  ( -23.15000000000000213, 4.350000000011156054, -79.15000000000004832 ) ) ;
#76466=VERTEX_POINT ( 'NONE', #132573 ) ;
#76478=ORIENTED_EDGE ( 'NONE', *, *, #88215, .F. ) ;
#76485=DIRECTION ( 'NONE',  ( -1.000000000000000000, 0.000000000000000000, 0.000000000000000000 ) ) ;
#76508=CARTESIAN_POINT ( 'NONE',  ( 20.94999999999999929, 5.850000000011156942, -90.36750277572211587 ) ) ;
#76525=TOROIDAL_SURFACE ( 'NONE', #97345, 0.2000000000000000111, 0.1000000000000000056 ) ;
#76554=FACE_OUTER_BOUND ( 'NONE', #58336, .T. ) ;
#76565=ORIENTED_EDGE ( 'NONE', *, *, #66186, .F. ) ;
#76570=VECTOR ( 'NONE', #110729, 1000.000000000000000 ) ;
#76588=ORIENTED_EDGE ( 'NONE', *, *, #105237, .T. ) ;
#76640=CARTESIAN_POINT ( 'NONE',  ( 18.49999999999999289, 11.75000000001115552, -91.85000000000003695 ) ) ;
#76653=AXIS2_PLACEMENT_3D ( 'NONE', #176562, #39636, #136097 ) ;
#76682=EDGE_CURVE ( 'NONE', #232467, #222218, #198948, .T. ) ;
#76710=LINE ( 'NONE', #53316, #207398 ) ;
#76733=CARTESIAN_POINT ( 'NONE',  ( -22.59999999999999787, 11.64957080755595520, -66.90000000000004832 ) ) ;
#76734=EDGE_CURVE ( 'NONE', #205600, #143381, #108897, .T. ) ;
#76744=VERTEX_POINT ( 'NONE', #184517 ) ;
#76787=( BOUNDED_CURVE ( )  B_SPLINE_CURVE ( 3, ( #37761, #14353, #155155, #173458 ),
 .UNSPECIFIED., .F., .F. ) 
 B_SPLINE_CURVE_WITH_KNOTS ( ( 4, 4 ),
 ( 4.712388980384689674, 6.231880751915386263 ),
 .UNSPECIFIED. ) 
 CURVE ( )  GEOMETRIC_REPRESENTATION_ITEM ( )  RATIONAL_B_SPLINE_CURVE ( ( 1.000000000000000000, 0.8166740347213228279, 0.8166740347213228279, 1.000000000000000000 ) ) 
 REPRESENTATION_ITEM ( '' )  );
#76808=CYLINDRICAL_SURFACE ( 'NONE', #232460, 0.1000000000000028644 ) ;
#76837=CARTESIAN_POINT ( 'NONE',  ( 23.14999999999999858, 1.115600667400684642E-11, -100.5000000000000426 ) ) ;
#76841=ADVANCED_FACE ( 'NONE', ( #146661 ), #96425, .T. ) ;
#76842=VERTEX_POINT ( 'NONE', #153153 ) ;
#76906=DIRECTION ( 'NONE',  ( 0.000000000000000000, -0.1455152366551522025, -0.9893560106964505163 ) ) ;
#76938=CARTESIAN_POINT ( 'NONE',  ( -18.59999999999999787, 1.115600667400684642E-11, -100.5000000000000426 ) ) ;
#76956=EDGE_CURVE ( 'NONE', #119208, #124485, #68446, .T. ) ;
#76967=DIRECTION ( 'NONE',  ( -1.000000000000000000, 0.000000000000000000, 0.000000000000000000 ) ) ;
#76987=EDGE_LOOP ( 'NONE', ( #121346, #209226, #14787, #194490 ) ) ;
#77002=LINE ( 'NONE', #255592, #110063 ) ;
#77048=ORIENTED_EDGE ( 'NONE', *, *, #192352, .F. ) ;
#77059=CARTESIAN_POINT ( 'NONE',  ( -21.00857864376268935, 11.60000000001115161, -73.92820323027561358 ) ) ;
#77098=AXIS2_PLACEMENT_3D ( 'NONE', #245383, #147555, #108432 ) ;
#77102=CARTESIAN_POINT ( 'NONE',  ( -20.54999999999999716, -9.499999999988846255, -90.60603087734760663 ) ) ;
#77103=VERTEX_POINT ( 'NONE', #84764 ) ;
#77104=ORIENTED_EDGE ( 'NONE', *, *, #156545, .T. ) ;
#77126=EDGE_CURVE ( 'NONE', #44645, #177357, #245913, .T. ) ;
#77148=VERTEX_POINT ( 'NONE', #164356 ) ;
#77179=ADVANCED_FACE ( 'NONE', ( #204737 ), #145929, .T. ) ;
#77236=VECTOR ( 'NONE', #146919, 1000.000000000000000 ) ;
#77247=CYLINDRICAL_SURFACE ( 'NONE', #215763, 0.1000000000000028644 ) ;
#77257=EDGE_CURVE ( 'NONE', #62762, #70815, #83370, .T. ) ;
#77266=AXIS2_PLACEMENT_3D ( 'NONE', #231678, #70042, #34775 ) ;
#77288=CIRCLE ( 'NONE', #156633, 0.5000000000000004441 ) ;
#77290=CARTESIAN_POINT ( 'NONE',  ( 21.07094088545368749, 0.09889370256337753906, -60.67983277808289699 ) ) ;
#77305=ORIENTED_EDGE ( 'NONE', *, *, #56336, .T. ) ;
#77360=ORIENTED_EDGE ( 'NONE', *, *, #171600, .F. ) ;
#77367=CARTESIAN_POINT ( 'NONE',  ( -23.15000000000000213, 11.75000000001115907, -93.65839931010299324 ) ) ;
#77369=VERTEX_POINT ( 'NONE', #217566 ) ;
#77390=VERTEX_POINT ( 'NONE', #221412 ) ;
#77415=EDGE_CURVE ( 'NONE', #95768, #154701, #250183, .T. ) ;
#77426=DIRECTION ( 'NONE',  ( -1.000000000000000000, -0.000000000000000000, -0.000000000000000000 ) ) ;
#77483=AXIS2_PLACEMENT_3D ( 'NONE', #136720, #175884, #59733 ) ;
#77487=DIRECTION ( 'NONE',  ( -1.000000000000000000, -0.000000000000000000, -0.000000000000000000 ) ) ;
#77491=DIRECTION ( 'NONE',  ( 0.000000000000000000, 0.9908441862701600211, -0.1350103645451876666 ) ) ;
#77500=DIRECTION ( 'NONE',  ( -1.000000000000000000, -0.000000000000000000, -0.000000000000000000 ) ) ;
#77506=DIRECTION ( 'NONE',  ( 0.000000000000000000, 1.000000000000000000, -6.308085367188393199E-16 ) ) ;
#77512=CIRCLE ( 'NONE', #256551, 0.1000000000000002554 ) ;
#77541=ORIENTED_EDGE ( 'NONE', *, *, #104544, .F. ) ;
#77584=VERTEX_POINT ( 'NONE', #225265 ) ;
#77604=AXIS2_PLACEMENT_3D ( 'NONE', #244046, #146228, #186670 ) ;
#77630=ORIENTED_EDGE ( 'NONE', *, *, #137200, .F. ) ;
#77631=DIRECTION ( 'NONE',  ( 0.000000000000000000, 0.000000000000000000, -1.000000000000000000 ) ) ;
#77640=AXIS2_PLACEMENT_3D ( 'NONE', #51717, #33515, #173031 ) ;
#77650=DIRECTION ( 'NONE',  ( 1.000000000000000000, 3.265361837132813093E-16, -0.000000000000000000 ) ) ;
#77656=CARTESIAN_POINT ( 'NONE',  ( 22.48660254037844197, 11.65000000001116298, -66.95000000000004547 ) ) ;
#77692=DIRECTION ( 'NONE',  ( -7.304098846218201720E-16, 1.000000000000000000, 0.000000000000000000 ) ) ;
#77735=CARTESIAN_POINT ( 'NONE',  ( 20.04142135623730070, 11.65000000001115943, -91.65000000000004832 ) ) ;
#77772=CARTESIAN_POINT ( 'NONE',  ( 20.94999999999999929, 8.776282895303632259, -88.25000000000005684 ) ) ;
#77837=CARTESIAN_POINT ( 'NONE',  ( 23.14999999999999503, 6.650000000011155876, -88.15000000000004832 ) ) ;
#77840=CARTESIAN_POINT ( 'NONE',  ( -18.59999999999999787, 9.350000000011156942, -88.15000000000004832 ) ) ;
#77874=ORIENTED_EDGE ( 'NONE', *, *, #150998, .F. ) ;
#77893=ORIENTED_EDGE ( 'NONE', *, *, #69771, .F. ) ;
#77902=CARTESIAN_POINT ( 'NONE',  ( -20.64999999999999858, 4.350000000011156054, -88.25000000000005684 ) ) ;
#77919=CARTESIAN_POINT ( 'NONE',  ( -21.65000000000000213, 7.708578643773852157, -79.35000000000005116 ) ) ;
#77921=EDGE_CURVE ( 'NONE', #147057, #150331, #194737, .T. ) ;
#77927=AXIS2_PLACEMENT_3D ( 'NONE', #129301, #128025, #45908 ) ;
#78012=VERTEX_POINT ( 'NONE', #160752 ) ;
#78014=EDGE_CURVE ( 'NONE', #23243, #202405, #117738, .T. ) ;
#78015=CARTESIAN_POINT ( 'NONE',  ( 18.54147908293611735, -9.463261657916946845, -74.04894889675584579 ) ) ;
#78058=VERTEX_POINT ( 'NONE', #78602 ) ;
#78086=CARTESIAN_POINT ( 'NONE',  ( 21.05000000000000071, -8.999999999988842703, -90.60603087734760663 ) ) ;
#78098=CARTESIAN_POINT ( 'NONE',  ( -23.15000000000000213, 1.115648428625851357E-11, -96.60000000000005116 ) ) ;
#78112=EDGE_CURVE ( 'NONE', #24864, #190429, #5467, .T. ) ;
#78118=ORIENTED_EDGE ( 'NONE', *, *, #55702, .T. ) ;
#78120=EDGE_CURVE ( 'NONE', #74117, #205048, #226212, .T. ) ;
#78133=PLANE ( 'NONE',  #137585 ) ;
#78149=CYLINDRICAL_SURFACE ( 'NONE', #257046, 11.80000000000000426 ) ;
#78161=EDGE_LOOP ( 'NONE', ( #130970, #144367, #146591, #138041, #159747 ) ) ;
#78214=EDGE_CURVE ( 'NONE', #75742, #198610, #1774, .T. ) ;
#78259=VERTEX_POINT ( 'NONE', #248102 ) ;
#78276=EDGE_LOOP ( 'NONE', ( #104213, #102471, #103557, #170702 ) ) ;
#78279=EDGE_CURVE ( 'NONE', #215522, #12719, #155375, .T. ) ;
#78304=VECTOR ( 'NONE', #198035, 1000.000000000000000 ) ;
#78307=CARTESIAN_POINT ( 'NONE',  ( 21.05000000000080362, 0.05148288189288811878, -60.69982018208269636 ) ) ;
#78344=EDGE_LOOP ( 'NONE', ( #92050, #209259, #83001, #62380 ) ) ;
#78357=AXIS2_PLACEMENT_3D ( 'NONE', #21803, #240846, #180874 ) ;
#78360=CIRCLE ( 'NONE', #198598, 0.1000000000000028644 ) ;
#78364=AXIS2_PLACEMENT_3D ( 'NONE', #21011, #234907, #177531 ) ;
#78376=PRESENTATION_STYLE_ASSIGNMENT (( #135778 ) ) ;
#78397=EDGE_LOOP ( 'NONE', ( #16076, #23283, #59410, #170703 ) ) ;
#78398=ORIENTED_EDGE ( 'NONE', *, *, #242800, .T. ) ;
#78456=CARTESIAN_POINT ( 'NONE',  ( -21.05000000000000071, 1.851028230152016674, -78.65391326942254580 ) ) ;
#78487=DIRECTION ( 'NONE',  ( -1.000000000000000000, 0.000000000000000000, -0.000000000000000000 ) ) ;
#78500=CARTESIAN_POINT ( 'NONE',  ( -23.25000000000000000, 11.75000000001115552, -100.5000000000000426 ) ) ;
#78517=DIRECTION ( 'NONE',  ( 0.000000000000000000, 0.000000000000000000, 1.000000000000000000 ) ) ;
#78524=EDGE_CURVE ( 'NONE', #71510, #217161, #39365, .T. ) ;
#78556=CIRCLE ( 'NONE', #157722, 0.1000000000000028644 ) ;
#78567=CARTESIAN_POINT ( 'NONE',  ( -21.05000000000000071, -1.162701749926853712, -74.90000000000004832 ) ) ;
#78588=AXIS2_PLACEMENT_3D ( 'NONE', #41486, #75489, #155027 ) ;
#78595=AXIS2_PLACEMENT_3D ( 'NONE', #159926, #63354, #140321 ) ;
#78602=CARTESIAN_POINT ( 'NONE',  ( -21.05000000000000071, -11.39257802169451139, -97.42605042016811012 ) ) ;
#78603=AXIS2_PLACEMENT_3D ( 'NONE', #221535, #122480, #83305 ) ;
#78627=CYLINDRICAL_SURFACE ( 'NONE', #65874, 0.1000000000000028644 ) ;
#78631=DIRECTION ( 'NONE',  ( 0.000000000000000000, -0.9908441862701596881, 0.1350103645451904977 ) ) ;
#78655=ORIENTED_EDGE ( 'NONE', *, *, #38809, .T. ) ;
#78674=DIRECTION ( 'NONE',  ( 0.000000000000000000, 0.000000000000000000, -1.000000000000000000 ) ) ;
#78682=CARTESIAN_POINT ( 'NONE',  ( 23.14999999999999858, 6.650000000011155876, -79.35000000000005116 ) ) ;
#78689=ORIENTED_EDGE ( 'NONE', *, *, #125498, .F. ) ;
#78711=FACE_OUTER_BOUND ( 'NONE', #130310, .T. ) ;
#78721=AXIS2_PLACEMENT_3D ( 'NONE', #89958, #70447, #91261 ) ;
#78722=DIRECTION ( 'NONE',  ( 1.000000000000000000, 0.000000000000000000, -0.000000000000000000 ) ) ;
#78779=DIRECTION ( 'NONE',  ( 0.000000000000000000, 0.000000000000000000, -1.000000000000000000 ) ) ;
#78780=EDGE_CURVE ( 'NONE', #153266, #231082, #180468, .T. ) ;
#78811=AXIS2_PLACEMENT_3D ( 'NONE', #106987, #224372, #7918 ) ;
#78817=EDGE_LOOP ( 'NONE', ( #2058, #166241, #124849, #1891, #69504, #113165, #179404, #205889, #134391, #195478 ) ) ;
#78819=DIRECTION ( 'NONE',  ( 1.836970198721029934E-16, -1.000000000000000000, -0.000000000000000000 ) ) ;
#78842=AXIS2_PLACEMENT_3D ( 'NONE', #58871, #135848, #115023 ) ;
#78843=EDGE_LOOP ( 'NONE', ( #93838, #51407, #147754, #169825 ) ) ;
#78860=CARTESIAN_POINT ( 'NONE',  ( -21.05000000000000071, 11.75000000001115552, -93.65839931010299324 ) ) ;
#78872=ORIENTED_EDGE ( 'NONE', *, *, #134930, .F. ) ;
#78885=AXIS2_PLACEMENT_3D ( 'NONE', #246530, #190440, #11809 ) ;
#78921=EDGE_LOOP ( 'NONE', ( #164095, #55675, #15631, #26336 ) ) ;
#78929=CIRCLE ( 'NONE', #220447, 0.3999999999999975797 ) ;
#78961=DIRECTION ( 'NONE',  ( 0.000000000000000000, 0.000000000000000000, -1.000000000000000000 ) ) ;
#78966=DIRECTION ( 'NONE',  ( 0.000000000000000000, 0.000000000000000000, -1.000000000000000000 ) ) ;
#78979=ORIENTED_EDGE ( 'NONE', *, *, #154194, .T. ) ;
#79034=AXIS2_PLACEMENT_3D ( 'NONE', #14359, #252927, #233403 ) ;
#79042=EDGE_CURVE ( 'NONE', #188126, #116664, #206557, .T. ) ;
#79048=CARTESIAN_POINT ( 'NONE',  ( 21.05000000000000071, 6.450000000011156587, -77.01702717044007329 ) ) ;
#79073=EDGE_CURVE ( 'NONE', #32089, #142573, #185715, .T. ) ;
#79111=ADVANCED_FACE ( 'NONE', ( #30723 ), #11134, .T. ) ;
#79115=ORIENTED_EDGE ( 'NONE', *, *, #115989, .F. ) ;
#79146=DIRECTION ( 'NONE',  ( 0.000000000000000000, 0.000000000000000000, 1.000000000000000000 ) ) ;
#79166=AXIS2_PLACEMENT_3D ( 'NONE', #54362, #71388, #76485 ) ;
#79190=CARTESIAN_POINT ( 'NONE',  ( 20.95512820512820440, 10.62384868372303259, -79.15000000000003411 ) ) ;
#79261=EDGE_LOOP ( 'NONE', ( #190665, #23412, #218831, #66700 ) ) ;
#79268=AXIS2_PLACEMENT_3D ( 'NONE', #238537, #241132, #133348 ) ;
#79319=DIRECTION ( 'NONE',  ( 0.000000000000000000, 0.000000000000000000, -1.000000000000000000 ) ) ;
#79323=DIRECTION ( 'NONE',  ( 0.000000000000000000, 0.000000000000000000, 1.000000000000000000 ) ) ;
#79341=ADVANCED_FACE ( 'NONE', ( #123078 ), #43541, .F. ) ;
#79342=ORIENTED_EDGE ( 'NONE', *, *, #159032, .F. ) ;
#79344=EDGE_CURVE ( 'NONE', #31293, #52970, #99617, .T. ) ;
#79362=DIRECTION ( 'NONE',  ( 0.000000000000000000, 0.000000000000000000, -1.000000000000000000 ) ) ;
#79384=DIRECTION ( 'NONE',  ( 1.000000000000000000, 7.304098846218133681E-16, -4.607487905232622991E-31 ) ) ;
#79396=DIRECTION ( 'NONE',  ( 0.000000000000000000, -0.7397360091702744889, 0.6728971962616842051 ) ) ;
#79402=DIRECTION ( 'NONE',  ( -1.000000000000000000, 0.000000000000000000, 0.000000000000000000 ) ) ;
#79409=DIRECTION ( 'NONE',  ( 0.000000000000000000, 0.000000000000000000, -1.000000000000000000 ) ) ;
#79416=TOROIDAL_SURFACE ( 'NONE', #33695, 11.70000000000000107, 0.1000000000000000056 ) ;
#79420=EDGE_LOOP ( 'NONE', ( #132335, #212730, #24085, #155457 ) ) ;
#79437=AXIS2_PLACEMENT_3D ( 'NONE', #4780, #84284, #45218 ) ;
#79448=VECTOR ( 'NONE', #140478, 1000.000000000000000 ) ;
#79449=DIRECTION ( 'NONE',  ( 0.000000000000000000, 0.000000000000000000, 1.000000000000000000 ) ) ;
#79477=EDGE_LOOP ( 'NONE', ( #9947, #153463, #78872, #160623 ) ) ;
#79480=EDGE_CURVE ( 'NONE', #109372, #100102, #148484, .T. ) ;
#79490=DIRECTION ( 'NONE',  ( 0.000000000000000000, 0.000000000000000000, 1.000000000000000000 ) ) ;
#79521=ORIENTED_EDGE ( 'NONE', *, *, #14390, .T. ) ;
#79529=CARTESIAN_POINT ( 'NONE',  ( 20.85000000000000142, 0.1610488207298751417, -100.2158101556398293 ) ) ;
#79560=VECTOR ( 'NONE', #217048, 1000.000000000000000 ) ;
#79583=EDGE_CURVE ( 'NONE', #71736, #24624, #214162, .T. ) ;
#79599=B_SPLINE_CURVE_WITH_KNOTS ( 'NONE', 3,
 ( #161506, #141913, #221431, #83197, #44109, #242296, #63661, #123654 ),
 .UNSPECIFIED., .F., .F.,
 ( 4, 2, 2, 4 ),
 ( 0.000000000000000000, 0.0001306511400391352018, 0.0001959767100587012307, 0.0002613022800782672595 ),
 .UNSPECIFIED. ) ;
#79610=EDGE_LOOP ( 'NONE', ( #215204, #223227, #39617, #217756, #159901 ) ) ;
#79653=EDGE_LOOP ( 'NONE', ( #223930, #183627, #221631, #90500 ) ) ;
#79680=DIRECTION ( 'NONE',  ( 0.000000000000000000, -0.000000000000000000, 1.000000000000000000 ) ) ;
#79695=LINE ( 'NONE', #219214, #33015 ) ;
#79772=CARTESIAN_POINT ( 'NONE',  ( -21.05000000000000071, -11.48912529306490349, -69.90000000000004832 ) ) ;
#79776=AXIS2_PLACEMENT_3D ( 'NONE', #224426, #203587, #168364 ) ;
#79777=VECTOR ( 'NONE', #71178, 1000.000000000000000 ) ;
#79781=ORIENTED_EDGE ( 'NONE', *, *, #69886, .F. ) ;
#79783=AXIS2_PLACEMENT_3D ( 'NONE', #249403, #186867, #147728 ) ;
#79798=ORIENTED_EDGE ( 'NONE', *, *, #147617, .F. ) ;
#79828=( BOUNDED_SURFACE ( )  B_SPLINE_SURFACE ( 3, 2, ( 
 ( #252728, #188924, #131510 ),
 ( #148519, #127672, #247611 ),
 ( #110667, #171967, #231918 ),
 ( #32451, #168124, #111969 ) ),
 .UNSPECIFIED., .F., .F., .T. ) 
 B_SPLINE_SURFACE_WITH_KNOTS ( ( 4, 4 ),
 ( 3, 3 ),
 ( 0.000000000000000000, 0.001979672783031562362 ),
 ( 0.000000000000000000, 1.000000000000000000 ),
 .UNSPECIFIED. ) 
 GEOMETRIC_REPRESENTATION_ITEM ( )  RATIONAL_B_SPLINE_SURFACE ( (
 ( 1.000000000000000000, 0.7103081912008026855, 1.000000000000000000),
 ( 1.000000000000000000, 0.7104998333558677492, 1.000000000000000000),
 ( 1.000000000000000000, 0.7107238315755500802, 1.000000000000000000),
 ( 1.000000000000000000, 0.7110073749539205235, 1.000000000000000000) ) ) 
 REPRESENTATION_ITEM ( '' )  SURFACE ( )  );
#79897=AXIS2_PLACEMENT_3D ( 'NONE', #182130, #42608, #201679 ) ;
#79931=EDGE_CURVE ( 'NONE', #102379, #220040, #177896, .T. ) ;
#79949=CIRCLE ( 'NONE', #113305, 0.09999999999999939493 ) ;
#79950=EDGE_CURVE ( 'NONE', #236070, #119208, #15687, .T. ) ;
#79967=VECTOR ( 'NONE', #226439, 1000.000000000000000 ) ;
#80001=DIRECTION ( 'NONE',  ( 0.000000000000000000, 0.000000000000000000, 1.000000000000000000 ) ) ;
#80028=ORIENTED_EDGE ( 'NONE', *, *, #63485, .F. ) ;
#80034=EDGE_LOOP ( 'NONE', ( #15861, #257270, #242195 ) ) ;
#80037=CIRCLE ( 'NONE', #51006, 0.1999999999999999833 ) ;
#80062=FACE_OUTER_BOUND ( 'NONE', #149079, .T. ) ;
#80080=CARTESIAN_POINT ( 'NONE',  ( -20.94999999999999929, 1.736257131608553550, -78.56865232901755292 ) ) ;
#80091=VERTEX_POINT ( 'NONE', #161612 ) ;
#80167=ORIENTED_EDGE ( 'NONE', *, *, #63141, .F. ) ;
#80211=VERTEX_POINT ( 'NONE', #88434 ) ;
#80215=DIRECTION ( 'NONE',  ( 0.000000000000000000, 2.891205793294679805E-16, -1.000000000000000000 ) ) ;
#80251=ORIENTED_EDGE ( 'NONE', *, *, #251354, .F. ) ;
#80277=DIRECTION ( 'NONE',  ( 0.000000000000000000, -1.000000000000000000, -2.891205793294679805E-16 ) ) ;
#80293=ORIENTED_EDGE ( 'NONE', *, *, #159504, .F. ) ;
#80307=ORIENTED_EDGE ( 'NONE', *, *, #39485, .T. ) ;
#80336=EDGE_LOOP ( 'NONE', ( #99959, #141703, #137054 ) ) ;
#80350=( NAMED_UNIT ( * ) PLANE_ANGLE_UNIT ( ) SI_UNIT ( $, .RADIAN. ) );
#80371=CARTESIAN_POINT ( 'NONE',  ( 18.49999999999999645, -1.637172712959225507, -78.58215336547205254 ) ) ;
#80377=ORIENTED_EDGE ( 'NONE', *, *, #32149, .F. ) ;
#80391=ADVANCED_FACE ( 'NONE', ( #229273 ), #130149, .T. ) ;
#80393=AXIS2_PLACEMENT_3D ( 'NONE', #196908, #193080, #217741 ) ;
#80457=CARTESIAN_POINT ( 'NONE',  ( -22.49072729836729678, 0.05648193274477467801, -55.34999175084509915 ) ) ;
#80472=ORIENTED_EDGE ( 'NONE', *, *, #115174, .T. ) ;
#80505=AXIS2_PLACEMENT_3D ( 'NONE', #248146, #86474, #51196 ) ;
#80526=ORIENTED_EDGE ( 'NONE', *, *, #171857, .T. ) ;
#80536=AXIS2_PLACEMENT_3D ( 'NONE', #30574, #210482, #230035 ) ;
#80548=( BOUNDED_SURFACE ( )  B_SPLINE_SURFACE ( 3, 2, ( 
 ( #132114, #190835, #189527 ),
 ( #146511, #250765, #128262 ),
 ( #10887, #12187, #229927 ),
 ( #51254, #72154, #151708 ) ),
 .UNSPECIFIED., .F., .F., .F. ) 
 B_SPLINE_SURFACE_WITH_KNOTS ( ( 4, 4 ),
 ( 3, 3 ),
 ( 0.0006461284895273917582, 0.0007503702773985995202 ),
 ( 0.000000000000000000, 1.000000000000000000 ),
 .UNSPECIFIED. ) 
 GEOMETRIC_REPRESENTATION_ITEM ( )  RATIONAL_B_SPLINE_SURFACE ( (
 ( 1.000000000000000000, 0.7071067811865475727, 1.000000000000000000),
 ( 1.000000000000000000, 0.7076476444648680530, 1.000000000000000000),
 ( 1.000000000000000000, 0.7075727925192004664, 1.000000000000000000),
 ( 1.000000000000000000, 0.7071067811865369146, 1.000000000000000000) ) ) 
 REPRESENTATION_ITEM ( '' )  SURFACE ( )  );
#80559=DIRECTION ( 'NONE',  ( -1.000000000000000000, -3.265361837132813093E-16, 0.000000000000000000 ) ) ;
#80573=CARTESIAN_POINT ( 'NONE',  ( -20.54999999999999716, 4.350000000011156054, -79.35000000000005116 ) ) ;
#80582=CIRCLE ( 'NONE', #5760, 0.1000000000000002554 ) ;
#80615=ORIENTED_EDGE ( 'NONE', *, *, #118951, .T. ) ;
#80619=DIRECTION ( 'NONE',  ( 0.000000000000000000, 0.000000000000000000, -1.000000000000000000 ) ) ;
#80629=ORIENTED_EDGE ( 'NONE', *, *, #101516, .T. ) ;
#80644=VECTOR ( 'NONE', #191792, 999.9999999999998863 ) ;
#80690=ORIENTED_EDGE ( 'NONE', *, *, #19664, .F. ) ;
#80692=CARTESIAN_POINT ( 'NONE',  ( -22.50000000000000000, 11.64957080755595520, -66.90000000000004832 ) ) ;
#80704=VERTEX_POINT ( 'NONE', #35603 ) ;
#80725=EDGE_CURVE ( 'NONE', #72480, #172095, #103387, .T. ) ;
#80748=DIRECTION ( 'NONE',  ( 1.000000000000000000, -0.000000000000000000, -0.000000000000000000 ) ) ;
#80749=ADVANCED_FACE ( 'NONE', ( #98072 ), #40907, .T. ) ;
#80757=CARTESIAN_POINT ( 'NONE',  ( 20.94999999999999929, 1.115600667400684642E-11, -79.87500000000004263 ) ) ;
#80761=ORIENTED_EDGE ( 'NONE', *, *, #100480, .F. ) ;
#80792=EDGE_LOOP ( 'NONE', ( #121563, #186672, #197984, #174637 ) ) ;
#80794=CARTESIAN_POINT ( 'NONE',  ( 23.14999999999999503, 11.65000000001116298, -88.35000000000003695 ) ) ;
#80832=DIRECTION ( 'NONE',  ( 1.000000000000000000, 0.000000000000000000, 0.000000000000000000 ) ) ;
#80851=ORIENTED_EDGE ( 'NONE', *, *, #256149, .F. ) ;
#80874=DIRECTION ( 'NONE',  ( 0.000000000000000000, 0.000000000000000000, -1.000000000000000000 ) ) ;
#80885=EDGE_CURVE ( 'NONE', #29232, #171778, #181518, .T. ) ;
#80902=EDGE_CURVE ( 'NONE', #68295, #193140, #11862, .T. ) ;
#80945=DIRECTION ( 'NONE',  ( 0.000000000000000000, 0.000000000000000000, 1.000000000000000000 ) ) ;
#80950=EDGE_CURVE ( 'NONE', #183134, #87663, #86627, .T. ) ;
#80953=DIRECTION ( 'NONE',  ( 0.000000000000000000, 1.000000000000000000, 0.000000000000000000 ) ) ;
#80974=VERTEX_POINT ( 'NONE', #50946 ) ;
#80999=CARTESIAN_POINT ( 'NONE',  ( -20.94999999999999929, 10.29288807859936661, -105.9580020160122160 ) ) ;
#81070=EDGE_LOOP ( 'NONE', ( #252555, #229628, #250163, #24078 ) ) ;
#81084=CARTESIAN_POINT ( 'NONE',  ( 18.50000000000000000, -9.419078080838367839, -107.3299253502083559 ) ) ;
#81108=ORIENTED_EDGE ( 'NONE', *, *, #24643, .F. ) ;
#81139=DIRECTION ( 'NONE',  ( 1.000000000000000000, 0.000000000000000000, 0.000000000000000000 ) ) ;
#81189=AXIS2_PLACEMENT_3D ( 'NONE', #227682, #114161, #228985 ) ;
#81192=AXIS2_PLACEMENT_3D ( 'NONE', #193199, #15860, #118790 ) ;
#81218=AXIS2_PLACEMENT_3D ( 'NONE', #214941, #235780, #173305 ) ;
#81248=ORIENTED_EDGE ( 'NONE', *, *, #147144, .F. ) ;
#81265=DIRECTION ( 'NONE',  ( 0.000000000000000000, 0.9908441862701596881, -0.1350103645451904977 ) ) ;
#81276=VECTOR ( 'NONE', #492, 1000.000000000000000 ) ;
#81291=DIRECTION ( 'NONE',  ( -1.000000000000000000, 0.000000000000000000, 0.000000000000000000 ) ) ;
#81320=FACE_OUTER_BOUND ( 'NONE', #91074, .T. ) ;
#81331=DIRECTION ( 'NONE',  ( -1.000000000000000000, 0.000000000000000000, 0.000000000000000000 ) ) ;
#81332=VECTOR ( 'NONE', #20546, 1000.000000000000000 ) ;
#81345=ORIENTED_EDGE ( 'NONE', *, *, #199004, .F. ) ;
#81353=CARTESIAN_POINT ( 'NONE',  ( 21.05000000000000071, 1.115600667400684642E-11, -67.10000000000005116 ) ) ;
#81354=EDGE_LOOP ( 'NONE', ( #194188, #151503, #16313, #64848 ) ) ;
#81358=ADVANCED_FACE ( 'NONE', ( #243733 ), #74115, .T. ) ;
#81371=DIRECTION ( 'NONE',  ( 1.000000000000000000, 0.000000000000000000, 0.000000000000000000 ) ) ;
#81417=VERTEX_POINT ( 'NONE', #34995 ) ;
#81444=ADVANCED_FACE ( 'NONE', ( #32424 ), #195337, .T. ) ;
#81449=DIRECTION ( 'NONE',  ( 0.000000000000000000, 0.000000000000000000, 1.000000000000000000 ) ) ;
#81455=ORIENTED_EDGE ( 'NONE', *, *, #54913, .T. ) ;
#81468=FACE_OUTER_BOUND ( 'NONE', #114617, .T. ) ;
#81544=VECTOR ( 'NONE', #169380, 1000.000000000000000 ) ;
#81598=CARTESIAN_POINT ( 'NONE',  ( -22.32929514600008503, 0.09907567812507747651, -59.42135243462354310 ) ) ;
#81626=EDGE_CURVE ( 'NONE', #205206, #135186, #41270, .T. ) ;
#81631=CIRCLE ( 'NONE', #181644, 0.09999999999999939493 ) ;
#81633=ORIENTED_EDGE ( 'NONE', *, *, #93626, .T. ) ;
#81637=AXIS2_PLACEMENT_3D ( 'NONE', #193718, #192431, #131161 ) ;
#81644=DIRECTION ( 'NONE',  ( -0.000000000000000000, -0.000000000000000000, -1.000000000000000000 ) ) ;
#81648=CARTESIAN_POINT ( 'NONE',  ( -23.15000000000000213, 1.115600667400684642E-11, -102.6000000000000512 ) ) ;
#81686=ORIENTED_EDGE ( 'NONE', *, *, #185164, .T. ) ;
#81742=ADVANCED_FACE ( 'NONE', ( #187297 ), #126010, .F. ) ;
#81775=EDGE_LOOP ( 'NONE', ( #246688, #74566, #117879, #96072 ) ) ;
#81804=DIRECTION ( 'NONE',  ( 0.000000000000000000, -0.000000000000000000, -1.000000000000000000 ) ) ;
#81812=VERTEX_POINT ( 'NONE', #94588 ) ;
#81818=CARTESIAN_POINT ( 'NONE',  ( 21.05000000000000071, 6.540656951712400691, -67.10000000000005116 ) ) ;
#81832=CARTESIAN_POINT ( 'NONE',  ( 18.59999999999999432, -1.866714910046153308, -78.75267524628205251 ) ) ;
#81876=CARTESIAN_POINT ( 'NONE',  ( 23.15000000000000213, -11.64999999998883595, -97.40000000000004832 ) ) ;
#81898=DIRECTION ( 'NONE',  ( -1.000000000000000000, 0.000000000000000000, 0.000000000000000000 ) ) ;
#81904=CARTESIAN_POINT ( 'NONE',  ( 18.48197441911674588, -9.517954794694565734, -107.3902116422077313 ) ) ;
#81906=DIRECTION ( 'NONE',  ( 1.000000000000000000, 7.304098846218134667E-16, 0.000000000000000000 ) ) ;
#81918=ADVANCED_FACE ( 'NONE', ( #55435 ), #253782, .T. ) ;
#81936=DIRECTION ( 'NONE',  ( 4.504528286903032433E-15, -0.1298341882520124002, -0.9915357197604841577 ) ) ;
#81965=DIRECTION ( 'NONE',  ( 0.000000000000000000, 0.000000000000000000, -1.000000000000000000 ) ) ;
#82017=CARTESIAN_POINT ( 'NONE',  ( -21.05000000000000071, 1.162701749949165642, -75.10000000000003695 ) ) ;
#82037=CARTESIAN_POINT ( 'NONE',  ( -23.15000000000000213, 11.65000000001115588, -88.35000000000003695 ) ) ;
#82057=AXIS2_PLACEMENT_3D ( 'NONE', #155748, #78722, #115295 ) ;
#82088=FACE_OUTER_BOUND ( 'NONE', #171476, .T. ) ;
#82146=ORIENTED_EDGE ( 'NONE', *, *, #181856, .F. ) ;
#82168=AXIS2_PLACEMENT_3D ( 'NONE', #174780, #133050, #134297 ) ;
#82197=LINE ( 'NONE', #240032, #217121 ) ;
#82219=DIRECTION ( 'NONE',  ( 1.000000000000000000, 0.000000000000000000, 0.000000000000000000 ) ) ;
#82221=ORIENTED_EDGE ( 'NONE', *, *, #218554, .T. ) ;
#82246=DIRECTION ( 'NONE',  ( 0.000000000000000000, 0.000000000000000000, -1.000000000000000000 ) ) ;
#82278=TOROIDAL_SURFACE ( 'NONE', #232175, 0.2000000000000000111, 0.1000000000000000056 ) ;
#82287=DIRECTION ( 'NONE',  ( -1.000000000000000000, 0.000000000000000000, 0.000000000000000000 ) ) ;
#82293=CARTESIAN_POINT ( 'NONE',  ( -21.09096482362056335, 0.03944827878534100385, -60.63645563459576948 ) ) ;
#82333=ORIENTED_EDGE ( 'NONE', *, *, #104727, .T. ) ;
#82338=ADVANCED_FACE ( 'NONE', ( #155601 ), #255890, .T. ) ;
#82340=ORIENTED_EDGE ( 'NONE', *, *, #60547, .T. ) ;
#82363=DIRECTION ( 'NONE',  ( 0.000000000000000000, 1.000000000000000000, -0.000000000000000000 ) ) ;
#82372=ORIENTED_EDGE ( 'NONE', *, *, #233274, .T. ) ;
#82376=AXIS2_PLACEMENT_3D ( 'NONE', #108720, #145258, #168749 ) ;
#82405=VERTEX_POINT ( 'NONE', #138535 ) ;
#82417=EDGE_CURVE ( 'NONE', #246051, #70703, #16681, .T. ) ;
#82446=CARTESIAN_POINT ( 'NONE',  ( -21.05000000000000071, 1.115600667400684642E-11, -100.5000000000000426 ) ) ;
#82448=DIRECTION ( 'NONE',  ( 0.000000000000000000, -1.000000000000000000, -1.734723475976807292E-15 ) ) ;
#82466=AXIS2_PLACEMENT_3D ( 'NONE', #140352, #41299, #218597 ) ;
#82481=VERTEX_POINT ( 'NONE', #182854 ) ;
#82540=DIRECTION ( 'NONE',  ( 1.000000000000000000, 0.000000000000000000, 0.000000000000000000 ) ) ;
#82575=DIRECTION ( 'NONE',  ( -0.000000000000000000, 0.000000000000000000, 1.000000000000000000 ) ) ;
#82605=ORIENTED_EDGE ( 'NONE', *, *, #141869, .F. ) ;
#82612=CARTESIAN_POINT ( 'NONE',  ( -18.59999999999999787, 11.65000000001115232, -79.15000000000003411 ) ) ;
#82636=AXIS2_PLACEMENT_3D ( 'NONE', #4871, #84384, #58435 ) ;
#82639=FACE_OUTER_BOUND ( 'NONE', #107517, .T. ) ;
#82676=VERTEX_POINT ( 'NONE', #249229 ) ;
#82687=EDGE_LOOP ( 'NONE', ( #140329, #28866, #131146, #122667 ) ) ;
#82697=DIRECTION ( 'NONE',  ( -1.000000000000000000, 0.000000000000000000, 0.000000000000000000 ) ) ;
#82702=CARTESIAN_POINT ( 'NONE',  ( -23.25000000000000000, -0.1008583690875562017, -55.25043287651065782 ) ) ;
#82709=ORIENTED_EDGE ( 'NONE', *, *, #227089, .F. ) ;
#82721=CARTESIAN_POINT ( 'NONE',  ( 21.05000000000000071, 10.72371710471867701, -79.15000000000004832 ) ) ;
#82780=FACE_OUTER_BOUND ( 'NONE', #179575, .T. ) ;
#82783=ORIENTED_EDGE ( 'NONE', *, *, #162865, .T. ) ;
#82808=DIRECTION ( 'NONE',  ( -1.000000000000000000, 0.000000000000000000, 0.000000000000000000 ) ) ;
#82811=AXIS2_PLACEMENT_3D ( 'NONE', #62013, #180672, #77692 ) ;
#82827=AXIS2_PLACEMENT_3D ( 'NONE', #28962, #84999, #104563 ) ;
#82844=VECTOR ( 'NONE', #220765, 999.9999999999998863 ) ;
#82853=EDGE_CURVE ( 'NONE', #233410, #113090, #112712, .T. ) ;
#82919=SURFACE_SIDE_STYLE ('',( #219894 ) ) ;
#82965=ORIENTED_EDGE ( 'NONE', *, *, #47979, .T. ) ;
#82972=DIRECTION ( 'NONE',  ( -1.000000000000000000, -0.000000000000000000, -0.000000000000000000 ) ) ;
#82993=CARTESIAN_POINT ( 'NONE',  ( -20.64999999999999858, 4.350000000011156054, -79.35000000000005116 ) ) ;
#82998=DIRECTION ( 'NONE',  ( 0.000000000000000000, 1.000000000000000000, -6.308085367188393199E-16 ) ) ;
#83001=ORIENTED_EDGE ( 'NONE', *, *, #80725, .F. ) ;
#83007=EDGE_CURVE ( 'NONE', #192064, #84058, #250260, .T. ) ;
#83034=ORIENTED_EDGE ( 'NONE', *, *, #65183, .T. ) ;
#83043=FACE_OUTER_BOUND ( 'NONE', #219001, .T. ) ;
#83093=ORIENTED_EDGE ( 'NONE', *, *, #47166, .T. ) ;
#83097=CARTESIAN_POINT ( 'NONE',  ( 18.43709777086140278, -9.682403433465237796, -107.1568433774128835 ) ) ;
#83129=CARTESIAN_POINT ( 'NONE',  ( -20.54999999999999716, -11.74999999998884626, -79.35000000000005116 ) ) ;
#83142=AXIS2_PLACEMENT_3D ( 'NONE', #7279, #201636, #101209 ) ;
#83150=CARTESIAN_POINT ( 'NONE',  ( 21.05000000000000071, 5.000000000011153745, -88.09473398108696074 ) ) ;
#83159=CARTESIAN_POINT ( 'NONE',  ( 23.15000000000000213, -11.39257802169451139, -97.42605042016811012 ) ) ;
#83172=CIRCLE ( 'NONE', #108173, 0.1000000000000029060 ) ;
#83195=DIRECTION ( 'NONE',  ( 0.000000000000000000, 0.000000000000000000, -1.000000000000000000 ) ) ;
#83197=CARTESIAN_POINT ( 'NONE',  ( 21.10257677756355932, 0.02495074957913740246, -60.60161825746730102 ) ) ;
#83227=CARTESIAN_POINT ( 'NONE',  ( 22.47110162079220785, 0.02879741281384913879, -55.35006406331571327 ) ) ;
#83240=FACE_OUTER_BOUND ( 'NONE', #208759, .T. ) ;
#83282=ORIENTED_EDGE ( 'NONE', *, *, #120711, .T. ) ;
#83305=DIRECTION ( 'NONE',  ( -3.469446951953515108E-14, 0.000000000000000000, 1.000000000000000000 ) ) ;
#83310=ORIENTED_EDGE ( 'NONE', *, *, #54643, .F. ) ;
#83313=CIRCLE ( 'NONE', #229094, 0.1000000000000028644 ) ;
#83328=CARTESIAN_POINT ( 'NONE',  ( -18.41353343127311248, -9.499999999988851584, -74.03206939669972542 ) ) ;
#83349=CARTESIAN_POINT ( 'NONE',  ( 22.60000000000000142, 11.74956712350054744, -66.89914163090134025 ) ) ;
#83350=AXIS2_PLACEMENT_3D ( 'NONE', #104226, #62560, #200780 ) ;
#83366=DIRECTION ( 'NONE',  ( 1.836970198721029934E-16, -1.000000000000000000, -0.000000000000000000 ) ) ;
#83367=CARTESIAN_POINT ( 'NONE',  ( -18.50000000000000000, 9.150000000011157653, -79.35000000000005116 ) ) ;
#83370=CIRCLE ( 'NONE', #229154, 0.2000000000000057288 ) ;
#83380=ORIENTED_EDGE ( 'NONE', *, *, #147771, .F. ) ;
#83381=CARTESIAN_POINT ( 'NONE',  ( 20.04142135623730070, 11.75000000001115907, -91.65000000000004832 ) ) ;
#83391=AXIS2_PLACEMENT_3D ( 'NONE', #24516, #45339, #205685 ) ;
#83410=ADVANCED_FACE ( 'NONE', ( #91772 ), #171357, .T. ) ;
#83428=CARTESIAN_POINT ( 'NONE',  ( 21.05000000000000071, -11.48912529306489994, -97.50000000000004263 ) ) ;
#83478=CARTESIAN_POINT ( 'NONE',  ( -20.54999999999999716, 4.350000000011156054, -88.25000000000005684 ) ) ;
#83540=AXIS2_PLACEMENT_3D ( 'NONE', #244954, #27233, #66329 ) ;
#83604=DIRECTION ( 'NONE',  ( 0.000000000000000000, 0.000000000000000000, -1.000000000000000000 ) ) ;
#83618=DIRECTION ( 'NONE',  ( -0.000000000000000000, -0.000000000000000000, 1.000000000000000000 ) ) ;
#83620=AXIS2_PLACEMENT_3D ( 'NONE', #192456, #195041, #175477 ) ;
#83665=CIRCLE ( 'NONE', #254376, 4.000000000000003553 ) ;
#83697=LINE ( 'NONE', #257191, #150393 ) ;
#83698=CIRCLE ( 'NONE', #229497, 0.1000000000000028644 ) ;
#83720=DIRECTION ( 'NONE',  ( 0.000000000000000000, 0.000000000000000000, 1.000000000000000000 ) ) ;
#83761=CARTESIAN_POINT ( 'NONE',  ( -18.50000000000000000, 1.835341550235567887, -78.55515129256302487 ) ) ;
#83778=ORIENTED_EDGE ( 'NONE', *, *, #128599, .T. ) ;
#83798=ORIENTED_EDGE ( 'NONE', *, *, #49109, .F. ) ;
#83831=VERTEX_POINT ( 'NONE', #54892 ) ;
#83845=LINE ( 'NONE', #119176, #21391 ) ;
#83868=DIRECTION ( 'NONE',  ( 0.000000000000000000, 0.000000000000000000, -1.000000000000000000 ) ) ;
#83870=ORIENTED_EDGE ( 'NONE', *, *, #191094, .F. ) ;
#83880=ORIENTED_EDGE ( 'NONE', *, *, #122398, .F. ) ;
#83940=VERTEX_POINT ( 'NONE', #120052 ) ;
#83950=ORIENTED_EDGE ( 'NONE', *, *, #254983, .T. ) ;
#83981=ORIENTED_EDGE ( 'NONE', *, *, #93778, .F. ) ;
#83997=VERTEX_POINT ( 'NONE', #121345 ) ;
#84011=DIRECTION ( 'NONE',  ( -1.000000000000000000, 0.000000000000000000, 0.000000000000000000 ) ) ;
#84029=DIRECTION ( 'NONE',  ( 0.000000000000000000, 0.000000000000000000, -1.000000000000000000 ) ) ;
#84058=VERTEX_POINT ( 'NONE', #132870 ) ;
#84083=DIRECTION ( 'NONE',  ( -1.000000000000000000, 0.000000000000000000, -0.000000000000000000 ) ) ;
#84137=CARTESIAN_POINT ( 'NONE',  ( -23.25000000000000000, -1.835859311432481045, -112.0044391687985694 ) ) ;
#84138=DIRECTION ( 'NONE',  ( 1.000000000000000000, 0.000000000000000000, 0.000000000000000000 ) ) ;
#84154=EDGE_LOOP ( 'NONE', ( #154778, #232723, #13338, #161449 ) ) ;
#84205=ORIENTED_EDGE ( 'NONE', *, *, #11543, .F. ) ;
#84234=LINE ( 'NONE', #62172, #246597 ) ;
#84275=DIRECTION ( 'NONE',  ( -0.000000000000000000, 0.8660254037844502539, 0.4999999999999799050 ) ) ;
#84284=DIRECTION ( 'NONE',  ( 0.000000000000000000, 1.000000000000000000, 0.000000000000000000 ) ) ;
#84322=CARTESIAN_POINT ( 'NONE',  ( -18.59999999999999787, 1.115600667400684642E-11, -100.5000000000000426 ) ) ;
#84329=LINE ( 'NONE', #7406, #79967 ) ;
#84360=VECTOR ( 'NONE', #90461, 1000.000000000000000 ) ;
#84384=DIRECTION ( 'NONE',  ( -0.000000000000000000, 1.000000000000000000, -0.000000000000000000 ) ) ;
#84420=DIRECTION ( 'NONE',  ( -0.000000000000000000, -0.2605042016806452532, -0.9654727137038777718 ) ) ;
#84426=DIRECTION ( 'NONE',  ( 0.000000000000000000, 0.000000000000000000, -1.000000000000000000 ) ) ;
#84452=VERTEX_POINT ( 'NONE', #175242 ) ;
#84490=CARTESIAN_POINT ( 'NONE',  ( 22.50000000000000000, 0.1000000000111554016, -55.35042919245524473 ) ) ;
#84510=ORIENTED_EDGE ( 'NONE', *, *, #7788, .T. ) ;
#84514=ORIENTED_EDGE ( 'NONE', *, *, #181856, .T. ) ;
#84522=AXIS2_PLACEMENT_3D ( 'NONE', #55434, #60593, #154605 ) ;
#84534=CARTESIAN_POINT ( 'NONE',  ( 21.70464131381650219, 7.095358018979006864, -67.00000000000004263 ) ) ;
#84597=CARTESIAN_POINT ( 'NONE',  ( -18.45068461519105796, -9.486506529077932015, -74.06877716890477359 ) ) ;
#84616=CARTESIAN_POINT ( 'NONE',  ( 22.59080734064468032, 11.75000000001115552, -66.96925029190298062 ) ) ;
#84626=DIRECTION ( 'NONE',  ( -1.000000000000000000, 0.000000000000000000, 0.000000000000000000 ) ) ;
#84638=LINE ( 'NONE', #243757, #164093 ) ;
#84640=EDGE_CURVE ( 'NONE', #163227, #89054, #220742, .T. ) ;
#84652=CARTESIAN_POINT ( 'NONE',  ( 19.75857864376268935, 11.75000000001115907, -91.85000000000003695 ) ) ;
#84656=AXIS2_PLACEMENT_3D ( 'NONE', #104541, #43328, #122869 ) ;
#84660=CARTESIAN_POINT ( 'NONE',  ( 20.85000000000000142, 11.75000000001115907, -93.71613433702195550 ) ) ;
#84723=ORIENTED_EDGE ( 'NONE', *, *, #54913, .F. ) ;
#84747=CARTESIAN_POINT ( 'NONE',  ( -23.25000000000000000, 10.33248238083634440, -106.0948465439131922 ) ) ;
#84764=CARTESIAN_POINT ( 'NONE',  ( -20.00857864376270001, 9.350000000011156942, -79.25000000000004263 ) ) ;
#84765=VECTOR ( 'NONE', #244979, 1000.000000000000000 ) ;
#84783=CARTESIAN_POINT ( 'NONE',  ( -21.05000000000000071, -11.64999999998884483, -70.00000000000004263 ) ) ;
#84784=ORIENTED_EDGE ( 'NONE', *, *, #147771, .T. ) ;
#84786=CIRCLE ( 'NONE', #159852, 11.80000000000000426 ) ;
#84818=CIRCLE ( 'NONE', #138974, 0.09999999999999939493 ) ;
#84819=VECTOR ( 'NONE', #236421, 1000.000000000000000 ) ;
#84862=AXIS2_PLACEMENT_3D ( 'NONE', #29861, #50653, #225441 ) ;
#84872=AXIS2_PLACEMENT_3D ( 'NONE', #15815, #117459, #20949 ) ;
#84877=CIRCLE ( 'NONE', #143158, 0.09999999999999736877 ) ;
#84885=DIRECTION ( 'NONE',  ( 1.000000000000000000, 0.000000000000000000, -0.000000000000000000 ) ) ;
#84890=CIRCLE ( 'NONE', #5794, 0.1000000000000000472 ) ;
#84945=EDGE_CURVE ( 'NONE', #248066, #95768, #10688, .T. ) ;
#84982=AXIS2_PLACEMENT_3D ( 'NONE', #89298, #207998, #91876 ) ;
#84999=DIRECTION ( 'NONE',  ( 1.000000000000000000, 2.952720810173289112E-16, -0.000000000000000000 ) ) ;
#85028=ORIENTED_EDGE ( 'NONE', *, *, #242992, .T. ) ;
#85037=CARTESIAN_POINT ( 'NONE',  ( 23.15000000000000213, -9.599999999988842347, -90.60603087734760663 ) ) ;
#85042=ORIENTED_EDGE ( 'NONE', *, *, #222057, .T. ) ;
#85058=EDGE_CURVE ( 'NONE', #81417, #127618, #50667, .T. ) ;
#85075=AXIS2_PLACEMENT_3D ( 'NONE', #238618, #40457, #59954 ) ;
#85078=AXIS2_PLACEMENT_3D ( 'NONE', #92057, #150760, #51618 ) ;
#85083=AXIS2_PLACEMENT_3D ( 'NONE', #197640, #58113, #97218 ) ;
#85119=ORIENTED_EDGE ( 'NONE', *, *, #232525, .F. ) ;
#85124=ORIENTED_EDGE ( 'NONE', *, *, #147990, .F. ) ;
#85175=FACE_OUTER_BOUND ( 'NONE', #257714, .T. ) ;
#85220=DIRECTION ( 'NONE',  ( 1.000000000000000000, 0.000000000000000000, 0.000000000000000000 ) ) ;
#85267=DIRECTION ( 'NONE',  ( 2.659396599871503635E-15, 0.6132151058540549204, -0.7899159663865520375 ) ) ;
#85272=CIRCLE ( 'NONE', #235157, 0.09999999999999939493 ) ;
#85402=DIRECTION ( 'NONE',  ( 0.000000000000000000, 0.000000000000000000, 1.000000000000000000 ) ) ;
#85406=DIRECTION ( 'NONE',  ( 0.000000000000000000, 1.000000000000000000, 0.000000000000000000 ) ) ;
#85411=DIRECTION ( 'NONE',  ( 0.7071067811865388020, -0.7071067811865561215, 0.000000000000000000 ) ) ;
#85412=DIRECTION ( 'NONE',  ( 0.000000000000000000, 0.000000000000000000, 1.000000000000000000 ) ) ;
#85417=CARTESIAN_POINT ( 'NONE',  ( -21.45000000000000284, 7.708578643773852157, -79.35000000000005116 ) ) ;
#85430=AXIS2_PLACEMENT_3D ( 'NONE', #175282, #236493, #237788 ) ;
#85434=EDGE_LOOP ( 'NONE', ( #158145, #79521, #105949, #190950 ) ) ;
#85436=EDGE_LOOP ( 'NONE', ( #207221, #716, #112715, #31256 ) ) ;
#85459=CARTESIAN_POINT ( 'NONE',  ( 18.50000000000189360, 10.44006789215571551, -91.76711774888565287 ) ) ;
#85463=ORIENTED_EDGE ( 'NONE', *, *, #145662, .T. ) ;
#85481=VERTEX_POINT ( 'NONE', #24536 ) ;
#85499=CARTESIAN_POINT ( 'NONE',  ( 20.95568717954149562, 10.60199405390297400, -74.60250836826870113 ) ) ;
#85515=CARTESIAN_POINT ( 'NONE',  ( 21.46681500593265568, 6.857511159395777156, -67.00000000000004263 ) ) ;
#85531=EDGE_CURVE ( 'NONE', #247198, #221706, #150874, .T. ) ;
#85550=CIRCLE ( 'NONE', #243813, 0.1000000000000028644 ) ;
#85595=ORIENTED_EDGE ( 'NONE', *, *, #199968, .F. ) ;
#85621=VERTEX_POINT ( 'NONE', #221107 ) ;
#85627=DIRECTION ( 'NONE',  ( -1.000000000000000000, 0.000000000000000000, 0.000000000000000000 ) ) ;
#85688=CARTESIAN_POINT ( 'NONE',  ( -23.15000000000000213, 11.65000000001115588, -79.15000000000003411 ) ) ;
#85702=CARTESIAN_POINT ( 'NONE',  ( -21.05000000000000071, 1.115600667400684642E-11, -100.5000000000000426 ) ) ;
#85745=AXIS2_PLACEMENT_3D ( 'NONE', #147681, #229775, #246759 ) ;
#85776=ORIENTED_EDGE ( 'NONE', *, *, #111502, .T. ) ;
#85802=CARTESIAN_POINT ( 'NONE',  ( -20.00857864376270001, 9.350000000011156942, -88.25000000000005684 ) ) ;
#85809=CARTESIAN_POINT ( 'NONE',  ( 20.97239005616516394, 8.874843841361279573, -79.25015280215322377 ) ) ;
#85811=EDGE_LOOP ( 'NONE', ( #72772, #122933, #212359 ) ) ;
#85818=EDGE_CURVE ( 'NONE', #143703, #135186, #26131, .T. ) ;
#85879=DIRECTION ( 'NONE',  ( 2.694716079187272946E-16, -1.000000000000000000, 0.000000000000000000 ) ) ;
#85887=FACE_OUTER_BOUND ( 'NONE', #81775, .T. ) ;
#85899=CARTESIAN_POINT ( 'NONE',  ( -23.15000000000000213, 1.115600667400684642E-11, -100.5000000000000426 ) ) ;
#85906=AXIS2_PLACEMENT_3D ( 'NONE', #182380, #106651, #166685 ) ;
#85954=CIRCLE ( 'NONE', #194347, 11.90000000000000213 ) ;
#85998=DIRECTION ( 'NONE',  ( 0.000000000000000000, -0.9908441862701596881, 0.1350103645451904977 ) ) ;
#86018=FACE_OUTER_BOUND ( 'NONE', #141055, .T. ) ;
#86072=DIRECTION ( 'NONE',  ( 0.000000000000000000, 0.000000000000000000, 1.000000000000000000 ) ) ;
#86085=AXIS2_PLACEMENT_3D ( 'NONE', #142745, #183190, #185748 ) ;
#86088=ORIENTED_EDGE ( 'NONE', *, *, #77257, .T. ) ;
#86089=LINE ( 'NONE', #126540, #55201 ) ;
#86097=CARTESIAN_POINT ( 'NONE',  ( -22.50000000000000000, 1.115600667400684642E-11, -55.35042919245524473 ) ) ;
#86138=DIRECTION ( 'NONE',  ( -0.000000000000000000, 0.000000000000000000, 1.000000000000000000 ) ) ;
#86161=ADVANCED_FACE ( 'NONE', ( #223368 ), #123013, .T. ) ;
#86162=EDGE_CURVE ( 'NONE', #232478, #29232, #131665, .T. ) ;
#86180=AXIS2_PLACEMENT_3D ( 'NONE', #123886, #243816, #219106 ) ;
#86204=TOROIDAL_SURFACE ( 'NONE', #219496, 4.149999999999999467, 0.1000000000000000056 ) ;
#86218=CIRCLE ( 'NONE', #40499, 0.1000000000000016431 ) ;
#86233=CARTESIAN_POINT ( 'NONE',  ( -23.25000000000000000, -11.74999999998884448, -97.40000000000004832 ) ) ;
#86289=CIRCLE ( 'NONE', #123748, 0.1000000000000008937 ) ;
#86317=ORIENTED_EDGE ( 'NONE', *, *, #83007, .F. ) ;
#86322=CIRCLE ( 'NONE', #173902, 0.1000000000000028644 ) ;
#86334=EDGE_CURVE ( 'NONE', #233410, #231082, #196982, .T. ) ;
#86434=DIRECTION ( 'NONE',  ( -1.000000000000000000, -2.952720810173289112E-16, 0.000000000000000000 ) ) ;
#86436=DIRECTION ( 'NONE',  ( -1.000000000000000000, 0.000000000000000000, 0.000000000000000000 ) ) ;
#86469=DIRECTION ( 'NONE',  ( 0.000000000000000000, -0.4930308989875248349, -0.8700118002898312719 ) ) ;
#86474=DIRECTION ( 'NONE',  ( 1.000000000000000000, -0.000000000000000000, -0.000000000000000000 ) ) ;
#86492=CIRCLE ( 'NONE', #37052, 0.1999999999999996503 ) ;
#86516=AXIS2_PLACEMENT_3D ( 'NONE', #174038, #214396, #96976 ) ;
#86534=CIRCLE ( 'NONE', #194913, 7.791421356237338003 ) ;
#86568=CARTESIAN_POINT ( 'NONE',  ( 19.97071067811864609, 11.72071067812981404, -91.65000000000004832 ) ) ;
#86598=ORIENTED_EDGE ( 'NONE', *, *, #178282, .F. ) ;
#86603=ADVANCED_FACE ( 'NONE', ( #226589 ), #167996, .F. ) ;
#86609=DIRECTION ( 'NONE',  ( 0.000000000000000000, 0.000000000000000000, 1.000000000000000000 ) ) ;
#86615=CARTESIAN_POINT ( 'NONE',  ( -21.05000000000000071, 1.115600667400684642E-11, -100.5000000000000426 ) ) ;
#86624=ORIENTED_EDGE ( 'NONE', *, *, #146413, .T. ) ;
#86627=CIRCLE ( 'NONE', #32537, 4.100000000000006750 ) ;
#86671=CARTESIAN_POINT ( 'NONE',  ( 18.55807992284871588, 10.32898536001801659, -106.0826683222764899 ) ) ;
#86678=CARTESIAN_POINT ( 'NONE',  ( -23.15000000000000213, 1.115626384983466744E-11, -98.40000000000004832 ) ) ;
#86700=CIRCLE ( 'NONE', #232508, 0.09999999999999939493 ) ;
#86717=CIRCLE ( 'NONE', #231954, 0.1000000000000028644 ) ;
#86737=AXIS2_PLACEMENT_3D ( 'NONE', #81832, #118452, #161434 ) ;
#86739=ORIENTED_EDGE ( 'NONE', *, *, #178282, .T. ) ;
#86747=DIRECTION ( 'NONE',  ( -3.890533409366484652E-14, -0.1298341882520124002, -0.9915357197604841577 ) ) ;
#86758=DIRECTION ( 'NONE',  ( -1.000000000000000000, 0.000000000000000000, 0.000000000000000000 ) ) ;
#86762=EDGE_CURVE ( 'NONE', #207164, #100804, #201256, .T. ) ;
#86777=VECTOR ( 'NONE', #124143, 1000.000000000000000 ) ;
#86814=EDGE_LOOP ( 'NONE', ( #130008, #66456, #180484, #200668 ) ) ;
#86852=VERTEX_POINT ( 'NONE', #62097 ) ;
#86906=AXIS2_PLACEMENT_3D ( 'NONE', #116580, #59130, #96967 ) ;
#86919=DIRECTION ( 'NONE',  ( 0.000000000000000000, 0.000000000000000000, 1.000000000000000000 ) ) ;
#86922=EDGE_LOOP ( 'NONE', ( #212496, #155563, #103060, #159980 ) ) ;
#86923=VERTEX_POINT ( 'NONE', #140327 ) ;
#86954=AXIS2_PLACEMENT_3D ( 'NONE', #189349, #150234, #208900 ) ;
#86961=CARTESIAN_POINT ( 'NONE',  ( -23.15000000000000213, 1.115651490242849210E-11, -62.85000000000004405 ) ) ;
#86974=DIRECTION ( 'NONE',  ( 1.734723475976817507E-14, 0.000000000000000000, -1.000000000000000000 ) ) ;
#87007=EDGE_CURVE ( 'NONE', #181065, #225548, #172461, .T. ) ;
#87049=EDGE_CURVE ( 'NONE', #229766, #237818, #206733, .T. ) ;
#87051=CARTESIAN_POINT ( 'NONE',  ( -22.39999999999999858, -0.1008583690875579364, -55.25043287651065782 ) ) ;
#87061=ORIENTED_EDGE ( 'NONE', *, *, #75840, .F. ) ;
#87075=ADVANCED_FACE ( 'NONE', ( #88038 ), #8538, .F. ) ;
#87084=CARTESIAN_POINT ( 'NONE',  ( -22.59999999999999787, 11.74987124438766273, -66.93457040898637445 ) ) ;
#87094=EDGE_CURVE ( 'NONE', #236288, #97847, #148051, .T. ) ;
#87138=ORIENTED_EDGE ( 'NONE', *, *, #205326, .T. ) ;
#87173=ORIENTED_EDGE ( 'NONE', *, *, #239903, .T. ) ;
#87178=CARTESIAN_POINT ( 'NONE',  ( -20.64999999999999858, 4.250000000011156409, -79.35000000000005116 ) ) ;
#87182=CARTESIAN_POINT ( 'NONE',  ( 21.05000000000000426, 10.62950747927179407, -74.62797939999673247 ) ) ;
#87187=DIRECTION ( 'NONE',  ( 0.000000000000000000, 0.000000000000000000, 1.000000000000000000 ) ) ;
#87210=CARTESIAN_POINT ( 'NONE',  ( -23.25000000000000000, 11.75000000001115552, -79.15000000000004832 ) ) ;
#87218=ORIENTED_EDGE ( 'NONE', *, *, #47273, .F. ) ;
#87242=VERTEX_POINT ( 'NONE', #138711 ) ;
#87285=EDGE_CURVE ( 'NONE', #76379, #127210, #201290, .T. ) ;
#87301=DIRECTION ( 'NONE',  ( 0.000000000000000000, -0.8777080977375132376, 0.4791956752371582251 ) ) ;
#87317=CYLINDRICAL_SURFACE ( 'NONE', #225046, 0.09999999999999939493 ) ;
#87329=ADVANCED_FACE ( 'NONE', ( #239141 ), #22781, .F. ) ;
#87353=DIRECTION ( 'NONE',  ( -1.836970198721029934E-16, 1.000000000000000000, 0.000000000000000000 ) ) ;
#87373=DIRECTION ( 'NONE',  ( 0.000000000000000000, 0.000000000000000000, -1.000000000000000000 ) ) ;
#87404=CARTESIAN_POINT ( 'NONE',  ( -21.05000000000000071, 6.413759733821438935, -67.08561306080399333 ) ) ;
#87406=TOROIDAL_SURFACE ( 'NONE', #162442, 0.2000000000000000111, 0.1000000000000000056 ) ;
#87440=CARTESIAN_POINT ( 'NONE',  ( 23.14999999999999503, 6.650000000011155876, -88.15000000000004832 ) ) ;
#87500=DIRECTION ( 'NONE',  ( 0.000000000000000000, 1.897661533703519897E-16, -1.000000000000000000 ) ) ;
#87515=LINE ( 'NONE', #49692, #110040 ) ;
#87521=AXIS2_PLACEMENT_3D ( 'NONE', #227365, #109980, #48723 ) ;
#87571=VERTEX_POINT ( 'NONE', #233718 ) ;
#87572=AXIS2_PLACEMENT_3D ( 'NONE', #71166, #232808, #209368 ) ;
#87588=ORIENTED_EDGE ( 'NONE', *, *, #201878, .T. ) ;
#87590=LINE ( 'NONE', #101021, #151394 ) ;
#87607=DIRECTION ( 'NONE',  ( 0.000000000000000000, 0.000000000000000000, -1.000000000000000000 ) ) ;
#87621=EDGE_CURVE ( 'NONE', #76842, #77103, #185062, .T. ) ;
#87663=VERTEX_POINT ( 'NONE', #1499 ) ;
#87673=VERTEX_POINT ( 'NONE', #160617 ) ;
#87694=ORIENTED_EDGE ( 'NONE', *, *, #119658, .F. ) ;
#87701=DIRECTION ( 'NONE',  ( 3.265361837132813093E-16, -1.000000000000000000, -0.000000000000000000 ) ) ;
#87746=CARTESIAN_POINT ( 'NONE',  ( 20.94999999999999929, 10.72371710471867701, -74.66491356908764487 ) ) ;
#87763=EDGE_CURVE ( 'NONE', #132550, #80211, #204832, .T. ) ;
#87765=CARTESIAN_POINT ( 'NONE',  ( -18.59999999999999787, -1.835859311432481045, -112.0044391687985694 ) ) ;
#87771=DIRECTION ( 'NONE',  ( 0.000000000000000000, 1.000000000000000000, -3.469446951953635015E-14 ) ) ;
#87792=ORIENTED_EDGE ( 'NONE', *, *, #183077, .F. ) ;
#87793=ORIENTED_EDGE ( 'NONE', *, *, #180063, .F. ) ;
#87801=CARTESIAN_POINT ( 'NONE',  ( -20.12071067811865888, 9.320710678129810134, -79.35000000000005116 ) ) ;
#87809=CYLINDRICAL_SURFACE ( 'NONE', #71220, 0.09999999999999939493 ) ;
#87833=FACE_OUTER_BOUND ( 'NONE', #231297, .T. ) ;
#87886=CYLINDRICAL_SURFACE ( 'NONE', #108475, 0.09999999999999939493 ) ;
#87907=DIRECTION ( 'NONE',  ( 1.000000000000000000, 0.000000000000000000, 0.000000000000000000 ) ) ;
#87946=CARTESIAN_POINT ( 'NONE',  ( -20.64999999999999858, 7.150000000011155876, -88.25000000000005684 ) ) ;
#87953=DIRECTION ( 'NONE',  ( 0.000000000000000000, 0.000000000000000000, -1.000000000000000000 ) ) ;
#87955=DIRECTION ( 'NONE',  ( 0.000000000000000000, -0.000000000000000000, -1.000000000000000000 ) ) ;
#87975=ORIENTED_EDGE ( 'NONE', *, *, #229030, .F. ) ;
#88006=EDGE_CURVE ( 'NONE', #252613, #114500, #177313, .T. ) ;
#88036=CARTESIAN_POINT ( 'NONE',  ( 18.50000000000022382, 10.37342005529079536, -91.76578812462599899 ) ) ;
#88038=FACE_OUTER_BOUND ( 'NONE', #142988, .T. ) ;
#88046=CARTESIAN_POINT ( 'NONE',  ( 19.58285714285715073, 10.38499851036257837, -74.62968466739000917 ) ) ;
#88072=CARTESIAN_POINT ( 'NONE',  ( 20.12518398540832365, 9.975088720679844201, -74.99666825246995927 ) ) ;
#88141=DIRECTION ( 'NONE',  ( -1.000000000000000000, -0.000000000000000000, 0.000000000000000000 ) ) ;
#88144=CARTESIAN_POINT ( 'NONE',  ( 21.10710606213542206, 8.776894023904366904, -79.24099652639947067 ) ) ;
#88147=AXIS2_PLACEMENT_3D ( 'NONE', #62435, #141954, #221475 ) ;
#88149=CARTESIAN_POINT ( 'NONE',  ( 18.49999999999999289, 11.75000000001115907, -75.10000000000003695 ) ) ;
#88157=TOROIDAL_SURFACE ( 'NONE', #92461, 0.4000000000000005773, 0.1000000000000000056 ) ;
#88179=CARTESIAN_POINT ( 'NONE',  ( -21.05000000000000071, 1.115600667400684642E-11, -100.5000000000000426 ) ) ;
#88199=DIRECTION ( 'NONE',  ( 0.000000000000000000, 0.000000000000000000, 1.000000000000000000 ) ) ;
#88215=EDGE_CURVE ( 'NONE', #177869, #114655, #156901, .T. ) ;
#88328=FACE_BOUND ( 'NONE', #52982, .T. ) ;
#88369=ADVANCED_FACE ( 'NONE', ( #80062 ), #177937, .F. ) ;
#88382=EDGE_CURVE ( 'NONE', #51736, #190222, #138752, .T. ) ;
#88383=CARTESIAN_POINT ( 'NONE',  ( -22.50000000000000000, 1.115600667400684642E-11, -67.00000000000004263 ) ) ;
#88410=ORIENTED_EDGE ( 'NONE', *, *, #163298, .F. ) ;
#88426=CARTESIAN_POINT ( 'NONE',  ( 20.94999999999999929, 1.115600667400684642E-11, -100.5000000000000426 ) ) ;
#88434=CARTESIAN_POINT ( 'NONE',  ( -23.15000000000000213, -9.499999999988848032, -76.89396912265249284 ) ) ;
#88466=CARTESIAN_POINT ( 'NONE',  ( -21.05000000000000071, -1.835341550213255957, -78.65515129256301918 ) ) ;
#88521=ORIENTED_EDGE ( 'NONE', *, *, #163325, .F. ) ;
#88524=DIRECTION ( 'NONE',  ( 0.000000000000000000, 0.000000000000000000, 1.000000000000000000 ) ) ;
#88587=DIRECTION ( 'NONE',  ( 0.000000000000000000, 0.000000000000000000, -1.000000000000000000 ) ) ;
#88599=CIRCLE ( 'NONE', #172051, 4.100000000000006750 ) ;
#88720=EDGE_CURVE ( 'NONE', #62297, #215522, #255823, .T. ) ;
#88741=VERTEX_POINT ( 'NONE', #79772 ) ;
#88776=FACE_OUTER_BOUND ( 'NONE', #76987, .T. ) ;
#88790=DIRECTION ( 'NONE',  ( 0.000000000000000000, 0.000000000000000000, 1.000000000000000000 ) ) ;
#88815=EDGE_CURVE ( 'NONE', #253894, #53634, #163920, .T. ) ;
#88826=ORIENTED_EDGE ( 'NONE', *, *, #210836, .F. ) ;
#88853=EDGE_CURVE ( 'NONE', #127618, #113007, #216279, .T. ) ;
#88882=AXIS2_PLACEMENT_3D ( 'NONE', #10238, #65059, #246275 ) ;
#88885=ADVANCED_FACE ( 'NONE', ( #62361 ), #251403, .T. ) ;
#88895=FACE_OUTER_BOUND ( 'NONE', #30854, .T. ) ;
#88921=CARTESIAN_POINT ( 'NONE',  ( -20.94999999999999929, 11.60000000001115339, -73.92820323027561358 ) ) ;
#88931=AXIS2_PLACEMENT_3D ( 'NONE', #175244, #119084, #18689 ) ;
#88941=ORIENTED_EDGE ( 'NONE', *, *, #202551, .T. ) ;
#89028=CARTESIAN_POINT ( 'NONE',  ( -20.54999999999999716, -8.663551401858004652, -76.52410111806734960 ) ) ;
#89041=DIRECTION ( 'NONE',  ( -7.304098846218134667E-16, -1.000000000000000000, 0.000000000000000000 ) ) ;
#89054=VERTEX_POINT ( 'NONE', #222862 ) ;
#89076=CARTESIAN_POINT ( 'NONE',  ( 21.05000000000000426, -0.09999999998884513686, -60.52295361821018105 ) ) ;
#89095=CIRCLE ( 'NONE', #59858, 0.1000000000000001027 ) ;
#89122=ORIENTED_EDGE ( 'NONE', *, *, #53293, .T. ) ;
#89126=CARTESIAN_POINT ( 'NONE',  ( -20.94999999999999929, -11.48912529306490349, -70.10000000000005116 ) ) ;
#89145=ORIENTED_EDGE ( 'NONE', *, *, #1272, .T. ) ;
#89198=DIRECTION ( 'NONE',  ( 3.469446951953728416E-14, -0.8660254037844309360, 0.5000000000000134337 ) ) ;
#89214=DIRECTION ( 'NONE',  ( -1.000000000000000000, 0.000000000000000000, 0.000000000000000000 ) ) ;
#89226=DIRECTION ( 'NONE',  ( 0.000000000000000000, 0.9908441862701596881, 0.1350103645451904977 ) ) ;
#89231=FACE_BOUND ( 'NONE', #237178, .T. ) ;
#89243=AXIS2_PLACEMENT_3D ( 'NONE', #161728, #183830, #27370 ) ;
#89261=FACE_OUTER_BOUND ( 'NONE', #210283, .T. ) ;
#89271=DIRECTION ( 'NONE',  ( 1.000000000000000000, 3.265361837132813093E-16, -0.000000000000000000 ) ) ;
#89273=AXIS2_PLACEMENT_3D ( 'NONE', #60550, #140080, #120564 ) ;
#89276=EDGE_LOOP ( 'NONE', ( #35463, #27209, #52081, #192881 ) ) ;
#89298=CARTESIAN_POINT ( 'NONE',  ( 22.39999999999999503, 11.65000000001116298, -66.90000000000004832 ) ) ;
#89314=ORIENTED_EDGE ( 'NONE', *, *, #166573, .F. ) ;
#89324=DIRECTION ( 'NONE',  ( 0.000000000000000000, 0.000000000000000000, -1.000000000000000000 ) ) ;
#89363=DIRECTION ( 'NONE',  ( 1.000000000000000000, 0.000000000000000000, 0.000000000000000000 ) ) ;
#89369=CARTESIAN_POINT ( 'NONE',  ( 20.22483756094572271, 9.501904678882469923, -75.13953912871474472 ) ) ;
#89393=DIRECTION ( 'NONE',  ( -0.000000000000000000, -0.9876197685951252359, -0.1568667991644863424 ) ) ;
#89395=DIRECTION ( 'NONE',  ( -0.000000000000000000, 0.000000000000000000, 1.000000000000000000 ) ) ;
#89399=AXIS2_PLACEMENT_3D ( 'NONE', #231940, #53289, #205938 ) ;
#89449=CARTESIAN_POINT ( 'NONE',  ( -23.15000000000000213, 1.115600667400684642E-11, -67.00000000000004263 ) ) ;
#89468=ORIENTED_EDGE ( 'NONE', *, *, #19513, .F. ) ;
#89513=EDGE_CURVE ( 'NONE', #80704, #197421, #163721, .T. ) ;
#89524=CARTESIAN_POINT ( 'NONE',  ( -21.55000000000000071, 7.350000000011155166, -88.15000000000004832 ) ) ;
#89533=EDGE_LOOP ( 'NONE', ( #123689, #254718, #213122 ) ) ;
#89536=DIRECTION ( 'NONE',  ( 0.000000000000000000, 0.000000000000000000, -1.000000000000000000 ) ) ;
#89537=EDGE_CURVE ( 'NONE', #71510, #8323, #243385, .T. ) ;
#89554=CARTESIAN_POINT ( 'NONE',  ( -18.59999999999999787, -9.321008403350132809, -74.23593824907793248 ) ) ;
#89562=LINE ( 'NONE', #169149, #184416 ) ;
#89581=FACE_OUTER_BOUND ( 'NONE', #98521, .T. ) ;
#89592=EDGE_CURVE ( 'NONE', #123054, #170816, #8649, .T. ) ;
#89599=CARTESIAN_POINT ( 'NONE',  ( -21.05000000000000071, 1.115600667400684642E-11, -67.00000000000004263 ) ) ;
#89664=AXIS2_PLACEMENT_3D ( 'NONE', #111476, #188435, #89324 ) ;
#89682=DIRECTION ( 'NONE',  ( 0.000000000000000000, -0.9908441862701596881, 0.1350103645451899148 ) ) ;
#89709=CYLINDRICAL_SURFACE ( 'NONE', #170931, 0.1000000000000028644 ) ;
#89821=FACE_OUTER_BOUND ( 'NONE', #197283, .T. ) ;
#89834=VECTOR ( 'NONE', #129282, 1000.000000000000000 ) ;
#89853=VERTEX_POINT ( 'NONE', #124138 ) ;
#89875=CARTESIAN_POINT ( 'NONE',  ( -18.59999999999999787, 11.65000000001115232, -74.01480577065404987 ) ) ;
#89910=CARTESIAN_POINT ( 'NONE',  ( 21.14999999999999858, -0.09999999998884338825, -67.00000000000004263 ) ) ;
#89930=AXIS2_PLACEMENT_3D ( 'NONE', #194222, #35161, #3342 ) ;
#89932=VERTEX_POINT ( 'NONE', #70599 ) ;
#89958=CARTESIAN_POINT ( 'NONE',  ( 20.94999999999999929, 1.115600667400684642E-11, -100.5000000000000426 ) ) ;
#89981=CARTESIAN_POINT ( 'NONE',  ( 20.94999999999999574, 1.115600667400684642E-11, -67.00000000000004263 ) ) ;
#89995=EDGE_CURVE ( 'NONE', #44654, #75742, #227061, .T. ) ;
#90022=DIRECTION ( 'NONE',  ( 1.000000000000000000, 0.000000000000000000, 0.000000000000000000 ) ) ;
#90066=DIRECTION ( 'NONE',  ( 1.000000000000000000, 0.000000000000000000, 0.000000000000000000 ) ) ;
#90088=CARTESIAN_POINT ( 'NONE',  ( 18.49999999999999645, -1.135018845899022466, -108.2169768834323662 ) ) ;
#90097=( BOUNDED_SURFACE ( )  B_SPLINE_SURFACE ( 3, 2, ( 
 ( #163885, #62212, #144277 ),
 ( #201712, #66048, #42639 ),
 ( #204265, #43923, #102581 ),
 ( #123466, #25652, #105133 ) ),
 .UNSPECIFIED., .F., .F., .T. ) 
 B_SPLINE_SURFACE_WITH_KNOTS ( ( 4, 4 ),
 ( 3, 3 ),
 ( 0.04058434257139457990, 0.04256401539001584966 ),
 ( 0.000000000000000000, 1.000000000000000000 ),
 .UNSPECIFIED. ) 
 GEOMETRIC_REPRESENTATION_ITEM ( )  RATIONAL_B_SPLINE_SURFACE ( (
 ( 1.000000000000000000, 0.7103081912008297749, 1.000000000000000000),
 ( 1.000000000000000000, 0.7104998333555360146, 1.000000000000000000),
 ( 1.000000000000000000, 0.7107238315755094460, 1.000000000000000000),
 ( 1.000000000000000000, 0.7110073749539291832, 1.000000000000000000) ) ) 
 REPRESENTATION_ITEM ( '' )  SURFACE ( )  );
#90155=AXIS2_PLACEMENT_3D ( 'NONE', #210222, #113664, #193220 ) ;
#90164=EDGE_CURVE ( 'NONE', #56894, #178238, #1945, .T. ) ;
#90214=FACE_OUTER_BOUND ( 'NONE', #171060, .T. ) ;
#90257=EDGE_CURVE ( 'NONE', #205409, #8169, #84638, .T. ) ;
#90265=CARTESIAN_POINT ( 'NONE',  ( 20.94999999999999929, 1.835341550235569663, -78.55515129256303908 ) ) ;
#90274=ORIENTED_EDGE ( 'NONE', *, *, #104628, .T. ) ;
#90279=ORIENTED_EDGE ( 'NONE', *, *, #2840, .T. ) ;
#90312=CARTESIAN_POINT ( 'NONE',  ( -20.94999999999999929, 7.021664781911246322, -104.1335654018973287 ) ) ;
#90351=ORIENTED_EDGE ( 'NONE', *, *, #47979, .F. ) ;
#90388=CARTESIAN_POINT ( 'NONE',  ( 19.99999999999998934, 11.65000000001115943, -88.25000000000005684 ) ) ;
#90423=FACE_OUTER_BOUND ( 'NONE', #72297, .T. ) ;
#90428=ORIENTED_EDGE ( 'NONE', *, *, #192352, .T. ) ;
#90461=DIRECTION ( 'NONE',  ( -0.000000000000000000, -0.000000000000000000, -1.000000000000000000 ) ) ;
#90480=CARTESIAN_POINT ( 'NONE',  ( -20.94999999999999929, -1.162701749926853712, -75.10000000000003695 ) ) ;
#90494=DIRECTION ( 'NONE',  ( -1.836970198721029934E-16, 1.000000000000000000, 0.000000000000000000 ) ) ;
#90500=ORIENTED_EDGE ( 'NONE', *, *, #28695, .F. ) ;
#90512=AXIS2_PLACEMENT_3D ( 'NONE', #129677, #252181, #87953 ) ;
#90533=DIRECTION ( 'NONE',  ( 1.441126678808781001E-14, 0.9876197685951252359, 0.1568667991644863424 ) ) ;
#90534=CARTESIAN_POINT ( 'NONE',  ( -23.15000000000000213, 11.75000000001115552, -79.15000000000004832 ) ) ;
#90539=EDGE_CURVE ( 'NONE', #102379, #133216, #171965, .T. ) ;
#90586=AXIS2_PLACEMENT_3D ( 'NONE', #228743, #185747, #223563 ) ;
#90594=EDGE_CURVE ( 'NONE', #101672, #24943, #201678, .T. ) ;
#90613=DIRECTION ( 'NONE',  ( 0.000000000000000000, 0.000000000000000000, -1.000000000000000000 ) ) ;
#90640=AXIS2_PLACEMENT_3D ( 'NONE', #26767, #127121, #189671 ) ;
#90649=CARTESIAN_POINT ( 'NONE',  ( -21.44999999999999929, 7.350000000011155166, -88.25000000000005684 ) ) ;
#90709=CIRCLE ( 'NONE', #61677, 0.2000000000000057288 ) ;
#90714=ORIENTED_EDGE ( 'NONE', *, *, #165084, .T. ) ;
#90731=CARTESIAN_POINT ( 'NONE',  ( 21.11747605621531321, 8.778708005504054057, -79.24456316978982784 ) ) ;
#90747=DIRECTION ( 'NONE',  ( -1.000000000000000000, -0.000000000000000000, 0.000000000000000000 ) ) ;
#90823=DIRECTION ( 'NONE',  ( 0.000000000000000000, 1.224646799142015331E-16, 1.000000000000000000 ) ) ;
#90825=FACE_OUTER_BOUND ( 'NONE', #40432, .T. ) ;
#90832=AXIS2_PLACEMENT_3D ( 'NONE', #213023, #215467, #219319 ) ;
#90835=CARTESIAN_POINT ( 'NONE',  ( 20.94999999999999929, 1.115600667400684642E-11, -104.6000000000000512 ) ) ;
#90887=ORIENTED_EDGE ( 'NONE', *, *, #8112, .T. ) ;
#90893=DIRECTION ( 'NONE',  ( -1.000000000000000000, -0.000000000000000000, -0.000000000000000000 ) ) ;
#90927=DIRECTION ( 'NONE',  ( 1.000000000000000000, 0.000000000000000000, 0.000000000000000000 ) ) ;
#90976=ORIENTED_EDGE ( 'NONE', *, *, #47881, .T. ) ;
#91007=CARTESIAN_POINT ( 'NONE',  ( -23.25000000000000000, -0.09999999998884338825, -55.35042919245524473 ) ) ;
#91054=VECTOR ( 'NONE', #230645, 1000.000000000000000 ) ;
#91063=DIRECTION ( 'NONE',  ( 0.000000000000000000, 1.000000000000000000, 0.000000000000000000 ) ) ;
#91067=CARTESIAN_POINT ( 'NONE',  ( -23.25000000000000000, 1.115600667400684642E-11, -100.5000000000000426 ) ) ;
#91074=EDGE_LOOP ( 'NONE', ( #65469, #179845, #42766 ) ) ;
#91081=CARTESIAN_POINT ( 'NONE',  ( 21.07928932188134397, 6.328516656404459262, -66.90110485434564680 ) ) ;
#91088=EDGE_CURVE ( 'NONE', #97606, #21107, #35319, .T. ) ;
#91092=VERTEX_POINT ( 'NONE', #7093 ) ;
#91143=CIRCLE ( 'NONE', #240990, 7.800000000000001599 ) ;
#91169=CARTESIAN_POINT ( 'NONE',  ( 20.99749315643149217, 11.75000000001115907, -93.48519423124028549 ) ) ;
#91172=DIRECTION ( 'NONE',  ( 1.000000000000000000, -0.000000000000000000, -0.000000000000000000 ) ) ;
#91186=ORIENTED_EDGE ( 'NONE', *, *, #82417, .T. ) ;
#91193=AXIS2_PLACEMENT_3D ( 'NONE', #5993, #165083, #185929 ) ;
#91207=AXIS2_PLACEMENT_3D ( 'NONE', #251971, #254514, #53773 ) ;
#91220=DIRECTION ( 'NONE',  ( 0.000000000000000000, 0.000000000000000000, -1.000000000000000000 ) ) ;
#91249=CARTESIAN_POINT ( 'NONE',  ( -21.04999999999999716, -9.599999999988844124, -74.03206939669971121 ) ) ;
#91261=DIRECTION ( 'NONE',  ( 0.000000000000000000, 0.000000000000000000, -1.000000000000000000 ) ) ;
#91375=ORIENTED_EDGE ( 'NONE', *, *, #73916, .F. ) ;
#91378=DIRECTION ( 'NONE',  ( 0.000000000000000000, 1.776356839400254803E-15, -1.000000000000000000 ) ) ;
#91379=DIRECTION ( 'NONE',  ( -1.000000000000000000, 0.000000000000000000, 0.000000000000000000 ) ) ;
#91437=ORIENTED_EDGE ( 'NONE', *, *, #256145, .T. ) ;
#91478=VERTEX_POINT ( 'NONE', #152434 ) ;
#91495=DIRECTION ( 'NONE',  ( 0.000000000000000000, 0.000000000000000000, -1.000000000000000000 ) ) ;
#91497=EDGE_CURVE ( 'NONE', #68843, #205409, #97971, .T. ) ;
#91509=EDGE_CURVE ( 'NONE', #68843, #50987, #18880, .T. ) ;
#91526=DIRECTION ( 'NONE',  ( 0.000000000000000000, 0.000000000000000000, -1.000000000000000000 ) ) ;
#91560=ADVANCED_FACE ( 'NONE', ( #257867 ), #157585, .T. ) ;
#91561=VECTOR ( 'NONE', #5110, 1000.000000000000000 ) ;
#91573=CIRCLE ( 'NONE', #253870, 0.1000000000000028644 ) ;
#91588=ORIENTED_EDGE ( 'NONE', *, *, #31493, .T. ) ;
#91627=ORIENTED_EDGE ( 'NONE', *, *, #180719, .T. ) ;
#91651=VERTEX_POINT ( 'NONE', #114564 ) ;
#91674=AXIS2_PLACEMENT_3D ( 'NONE', #223397, #61773, #42220 ) ;
#91690=CARTESIAN_POINT ( 'NONE',  ( 20.85000000000000142, -1.835859311432481045, -112.1044391687985780 ) ) ;
#91705=AXIS2_PLACEMENT_3D ( 'NONE', #92421, #136450, #252560 ) ;
#91764=CIRCLE ( 'NONE', #191571, 11.65000000000000746 ) ;
#91772=FACE_OUTER_BOUND ( 'NONE', #140127, .T. ) ;
#91781=CARTESIAN_POINT ( 'NONE',  ( -18.59999999999999787, -1.164121893230052995, -108.4148480855716485 ) ) ;
#91782=CARTESIAN_POINT ( 'NONE',  ( 21.11101077988997332, 6.423684734737198809, -66.98471473108573093 ) ) ;
#91785=ORIENTED_EDGE ( 'NONE', *, *, #94182, .F. ) ;
#91805=ORIENTED_EDGE ( 'NONE', *, *, #24774, .T. ) ;
#91843=CARTESIAN_POINT ( 'NONE',  ( 18.56579813702275317, 10.33025634372637924, -106.0870929282639281 ) ) ;
#91848=DIRECTION ( 'NONE',  ( 0.000000000000000000, 0.6728971962616792091, -0.7397360091702790408 ) ) ;
#91852=ADVANCED_FACE ( 'NONE', ( #230333 ), #51675, .F. ) ;
#91867=ORIENTED_EDGE ( 'NONE', *, *, #121153, .T. ) ;
#91876=DIRECTION ( 'NONE',  ( 1.000000000000000000, 0.000000000000000000, 0.000000000000000000 ) ) ;
#91905=EDGE_CURVE ( 'NONE', #193140, #22968, #7436, .T. ) ;
#91923=LINE ( 'NONE', #68527, #198357 ) ;
#91950=CARTESIAN_POINT ( 'NONE',  ( 20.54374330479337374, 10.50501031423420351, -74.72568363488957743 ) ) ;
#91953=CYLINDRICAL_SURFACE ( 'NONE', #185944, 0.09999999999999939493 ) ;
#91970=CIRCLE ( 'NONE', #129395, 11.65000000000000746 ) ;
#91982=CARTESIAN_POINT ( 'NONE',  ( -20.85000000000000142, -1.263275465206102233, -108.4018646667464481 ) ) ;
#92008=( BOUNDED_CURVE ( )  B_SPLINE_CURVE ( 3, ( #86568, #166174, #67040, #141430 ),
 .UNSPECIFIED., .F., .F. ) 
 B_SPLINE_CURVE_WITH_KNOTS ( ( 4, 4 ),
 ( 0.000000000000000000, 1.570796326794916320 ),
 .UNSPECIFIED. ) 
 CURVE ( )  GEOMETRIC_REPRESENTATION_ITEM ( )  RATIONAL_B_SPLINE_CURVE ( ( 1.000000000000000000, 0.8047378541243603856, 0.8047378541243603856, 1.000000000000000000 ) ) 
 REPRESENTATION_ITEM ( '' )  );
#92025=CYLINDRICAL_SURFACE ( 'NONE', #116135, 0.1000000000000028644 ) ;
#92027=CARTESIAN_POINT ( 'NONE',  ( -22.39999999999999858, 11.65000000001115588, -66.90000000000004832 ) ) ;
#92044=ADVANCED_FACE ( 'NONE', ( #56804 ), #173052, .T. ) ;
#92050=ORIENTED_EDGE ( 'NONE', *, *, #162197, .T. ) ;
#92057=CARTESIAN_POINT ( 'NONE',  ( -23.15000000000000213, 1.115600667400684642E-11, -104.4000000000000483 ) ) ;
#92076=DIRECTION ( 'NONE',  ( 1.000000000000000000, -0.000000000000000000, -0.000000000000000000 ) ) ;
#92089=EDGE_CURVE ( 'NONE', #208732, #143962, #35674, .T. ) ;
#92097=AXIS2_PLACEMENT_3D ( 'NONE', #174201, #197560, #97138 ) ;
#92120=EDGE_CURVE ( 'NONE', #137421, #169584, #185839, .T. ) ;
#92129=CARTESIAN_POINT ( 'NONE',  ( 23.14999999999999503, 11.65000000001116298, -93.48519422934610645 ) ) ;
#92160=CARTESIAN_POINT ( 'NONE',  ( -23.15000000000000213, 1.115600667400684642E-11, -100.5000000000000426 ) ) ;
#92167=ADVANCED_FACE ( 'NONE', ( #89231, #188344 ), #149240, .T. ) ;
#92172=CARTESIAN_POINT ( 'NONE',  ( -20.94999999999999929, -11.48912529306490349, -70.10000000000005116 ) ) ;
#92202=ORIENTED_EDGE ( 'NONE', *, *, #134222, .T. ) ;
#92214=AXIS2_PLACEMENT_3D ( 'NONE', #154942, #234434, #92363 ) ;
#92246=DIRECTION ( 'NONE',  ( 0.000000000000000000, 0.1298341882520022694, 0.9915357197604852679 ) ) ;
#92247=AXIS2_PLACEMENT_3D ( 'NONE', #191946, #130648, #210207 ) ;
#92253=EDGE_CURVE ( 'NONE', #174189, #91651, #256513, .T. ) ;
#92263=CIRCLE ( 'NONE', #117215, 0.5000000000000004441 ) ;
#92265=VECTOR ( 'NONE', #101890, 1000.000000000000000 ) ;
#92268=ORIENTED_EDGE ( 'NONE', *, *, #243027, .T. ) ;
#92297=DIRECTION ( 'NONE',  ( -1.000000000000000000, 0.000000000000000000, 0.000000000000000000 ) ) ;
#92304=DIRECTION ( 'NONE',  ( -0.9880948137434723000, 0.1538461538461483591, -0.000000000000000000 ) ) ;
#92343=FACE_OUTER_BOUND ( 'NONE', #9469, .T. ) ;
#92349=CARTESIAN_POINT ( 'NONE',  ( -20.85000000106584750, 11.75000000001115197, -93.65550465647375233 ) ) ;
#92352=EDGE_CURVE ( 'NONE', #189474, #18191, #137337, .T. ) ;
#92363=DIRECTION ( 'NONE',  ( 1.000000000000000000, 0.000000000000000000, 0.000000000000000000 ) ) ;
#92379=CARTESIAN_POINT ( 'NONE',  ( -21.05000000000000071, 5.900000000011162093, -90.28090023534366537 ) ) ;
#92381=ORIENTED_EDGE ( 'NONE', *, *, #137489, .T. ) ;
#92413=LINE ( 'NONE', #250217, #3946 ) ;
#92421=CARTESIAN_POINT ( 'NONE',  ( 18.59999999999999076, 11.65000000001115943, -91.85000000000003695 ) ) ;
#92429=EDGE_LOOP ( 'NONE', ( #202353, #227618, #196359, #93110 ) ) ;
#92440=AXIS2_PLACEMENT_3D ( 'NONE', #233468, #134322, #148785 ) ;
#92444=CARTESIAN_POINT ( 'NONE',  ( 18.50000000000000000, -9.399999999988823518, -74.29725975966330509 ) ) ;
#92454=EDGE_CURVE ( 'NONE', #39964, #211866, #173439, .T. ) ;
#92461=AXIS2_PLACEMENT_3D ( 'NONE', #160101, #234467, #100070 ) ;
#92468=AXIS2_PLACEMENT_3D ( 'NONE', #6024, #82972, #205513 ) ;
#92562=EDGE_LOOP ( 'NONE', ( #95950, #99432, #159743, #137371 ) ) ;
#92564=CARTESIAN_POINT ( 'NONE',  ( -23.24999999999999645, -9.599999999988845900, -107.1001893912220879 ) ) ;
#92568=DIRECTION ( 'NONE',  ( 1.000000000000000000, 0.000000000000000000, -0.000000000000000000 ) ) ;
#92603=FACE_OUTER_BOUND ( 'NONE', #79420, .T. ) ;
#92613=FACE_OUTER_BOUND ( 'NONE', #104174, .T. ) ;
#92625=CIRCLE ( 'NONE', #134133, 0.5000000000000004441 ) ;
#92652=CARTESIAN_POINT ( 'NONE',  ( 20.94999999999999574, 10.62357026049396680, -74.49194520323059976 ) ) ;
#92691=SPHERICAL_SURFACE ( 'NONE', #124295, 0.1000000000000000056 ) ;
#92694=DIRECTION ( 'NONE',  ( 1.000000000000000000, 0.000000000000000000, 0.000000000000000000 ) ) ;
#92706=ADVANCED_FACE ( 'NONE', ( #68093 ), #123294, .T. ) ;
#92717=EDGE_CURVE ( 'NONE', #188088, #144636, #238494, .T. ) ;
#92730=DIRECTION ( 'NONE',  ( 5.603264701231745086E-32, -1.897661533703520636E-16, 1.000000000000000000 ) ) ;
#92751=EDGE_CURVE ( 'NONE', #214401, #154034, #248388, .T. ) ;
#92801=DIRECTION ( 'NONE',  ( -0.000000000000000000, -0.000000000000000000, 1.000000000000000000 ) ) ;
#92808=ORIENTED_EDGE ( 'NONE', *, *, #233453, .T. ) ;
#92848=FACE_OUTER_BOUND ( 'NONE', #79653, .T. ) ;
#92849=ADVANCED_FACE ( 'NONE', ( #157727 ), #98952, .T. ) ;
#92851=CARTESIAN_POINT ( 'NONE',  ( 18.39999999999999858, -9.519327731081283162, -73.97297637655937308 ) ) ;
#92863=CARTESIAN_POINT ( 'NONE',  ( 21.14999999999999858, 8.786607556611267356, -79.25000000000004263 ) ) ;
#92885=SPHERICAL_SURFACE ( 'NONE', #110084, 0.1000000000000000056 ) ;
#92915=CARTESIAN_POINT ( 'NONE',  ( -22.39999999999999858, 7.790779598384560245, -67.00000000000004263 ) ) ;
#92930=CYLINDRICAL_SURFACE ( 'NONE', #150215, 0.1000000000000028644 ) ;
#93017=AXIS2_PLACEMENT_3D ( 'NONE', #94195, #156779, #18527 ) ;
#93029=EDGE_CURVE ( 'NONE', #155038, #205048, #229214, .T. ) ;
#93056=CARTESIAN_POINT ( 'NONE',  ( 18.59999999999997655, 11.75000000001115552, -100.5000000000000426 ) ) ;
#93090=CIRCLE ( 'NONE', #59946, 0.1000000000000028644 ) ;
#93110=ORIENTED_EDGE ( 'NONE', *, *, #70088, .F. ) ;
#93123=EDGE_LOOP ( 'NONE', ( #35347, #52848, #232047, #11435 ) ) ;
#93182=EDGE_LOOP ( 'NONE', ( #192264, #254101, #2796, #104072 ) ) ;
#93194=DIRECTION ( 'NONE',  ( 0.000000000000000000, 3.552713678800509607E-15, 1.000000000000000000 ) ) ;
#93213=AXIS2_PLACEMENT_3D ( 'NONE', #185472, #107208, #66809 ) ;
#93221=DIRECTION ( 'NONE',  ( 0.000000000000000000, 1.000000000000000000, 0.000000000000000000 ) ) ;
#93243=ORIENTED_EDGE ( 'NONE', *, *, #177048, .F. ) ;
#93257=EDGE_CURVE ( 'NONE', #53620, #192398, #232214, .T. ) ;
#93348=AXIS2_PLACEMENT_3D ( 'NONE', #222206, #186990, #246922 ) ;
#93378=DIRECTION ( 'NONE',  ( 0.000000000000000000, 0.000000000000000000, -1.000000000000000000 ) ) ;
#93380=CARTESIAN_POINT ( 'NONE',  ( -20.85000000000000142, -1.835859311432481045, -112.0044391687985694 ) ) ;
#93435=AXIS2_PLACEMENT_3D ( 'NONE', #46496, #68655, #229014 ) ;
#93452=EDGE_CURVE ( 'NONE', #201338, #257922, #202904, .T. ) ;
#93468=ORIENTED_EDGE ( 'NONE', *, *, #38787, .F. ) ;
#93476=AXIS2_PLACEMENT_3D ( 'NONE', #166764, #8940, #168053 ) ;
#93482=ADVANCED_FACE ( 'NONE', ( #171518 ), #149381, .T. ) ;
#93499=AXIS2_PLACEMENT_3D ( 'NONE', #190237, #188948, #67712 ) ;
#93529=VERTEX_POINT ( 'NONE', #193620 ) ;
#93531=TOROIDAL_SURFACE ( 'NONE', #122785, 0.2000000000000000111, 0.1000000000000000056 ) ;
#93547=DIRECTION ( 'NONE',  ( -1.000000000000000000, -0.000000000000000000, -0.000000000000000000 ) ) ;
#93548=VECTOR ( 'NONE', #140305, 1000.000000000000227 ) ;
#93553=CARTESIAN_POINT ( 'NONE',  ( 20.95483826173899899, 8.876166204781142710, -75.54627555289955865 ) ) ;
#93579=VECTOR ( 'NONE', #138985, 999.9999999999998863 ) ;
#93626=EDGE_CURVE ( 'NONE', #233528, #47237, #90709, .T. ) ;
#93632=DIRECTION ( 'NONE',  ( 0.000000000000000000, 0.000000000000000000, 1.000000000000000000 ) ) ;
#93640=CARTESIAN_POINT ( 'NONE',  ( -20.94999999999999929, 11.65000000001115055, -93.71613433702194129 ) ) ;
#93642=AXIS2_PLACEMENT_3D ( 'NONE', #41314, #98645, #120855 ) ;
#93659=EDGE_LOOP ( 'NONE', ( #112637, #143491, #111792, #99471 ) ) ;
#93669=DIRECTION ( 'NONE',  ( -0.7071067811865475727, -0.7071067811865475727, 0.000000000000000000 ) ) ;
#93672=DIRECTION ( 'NONE',  ( 0.000000000000000000, 0.000000000000000000, 1.000000000000000000 ) ) ;
#93693=LINE ( 'NONE', #173285, #106144 ) ;
#93696=DIRECTION ( 'NONE',  ( 0.000000000000000000, 0.000000000000000000, -1.000000000000000000 ) ) ;
#93723=CARTESIAN_POINT ( 'NONE',  ( -2.995603634470829482E-16, -11.74999999998884448, -91.75000000000005684 ) ) ;
#93734=VECTOR ( 'NONE', #82575, 1000.000000000000000 ) ;
#93742=VERTEX_POINT ( 'NONE', #202604 ) ;
#93753=CIRCLE ( 'NONE', #202102, 2.000000000000002665 ) ;
#93759=ORIENTED_EDGE ( 'NONE', *, *, #181674, .F. ) ;
#93774=CIRCLE ( 'NONE', #177026, 0.3999999999999975797 ) ;
#93778=EDGE_CURVE ( 'NONE', #110538, #153266, #203878, .T. ) ;
#93787=CIRCLE ( 'NONE', #18959, 0.1000000000000000472 ) ;
#93797=CARTESIAN_POINT ( 'NONE',  ( 18.41832399655374175, -9.682403266662738872, -107.1568436200277006 ) ) ;
#93805=ORIENTED_EDGE ( 'NONE', *, *, #197196, .T. ) ;
#93809=FACE_OUTER_BOUND ( 'NONE', #14352, .T. ) ;
#93815=CIRCLE ( 'NONE', #60485, 0.1000000000000028644 ) ;
#93826=DIRECTION ( 'NONE',  ( 0.000000000000000000, 0.000000000000000000, 1.000000000000000000 ) ) ;
#93838=ORIENTED_EDGE ( 'NONE', *, *, #99018, .F. ) ;
#93852=CIRCLE ( 'NONE', #43776, 0.1000000000000028644 ) ;
#93863=CIRCLE ( 'NONE', #239620, 0.1000000000000001860 ) ;
#93889=SPHERICAL_SURFACE ( 'NONE', #220056, 0.1000000000000000056 ) ;
#93916=EDGE_CURVE ( 'NONE', #102952, #58722, #174335, .T. ) ;
#93998=EDGE_LOOP ( 'NONE', ( #103911, #89122, #68648, #108336 ) ) ;
#94000=( GEOMETRIC_REPRESENTATION_CONTEXT ( 3 ) GLOBAL_UNCERTAINTY_ASSIGNED_CONTEXT ( ( #37559 ) ) GLOBAL_UNIT_ASSIGNED_CONTEXT ( ( #240756, #162510, #122088 ) ) REPRESENTATION_CONTEXT ( 'NONE', 'WORKASPACE' ) );
#94007=DIRECTION ( 'NONE',  ( 0.000000000000000000, -0.8660254037844411501, -0.4999999999999956146 ) ) ;
#94019=FACE_OUTER_BOUND ( 'NONE', #208924, .T. ) ;
#94036=EDGE_CURVE ( 'NONE', #256256, #223322, #57567, .T. ) ;
#94037=ORIENTED_EDGE ( 'NONE', *, *, #196042, .T. ) ;
#94051=DIRECTION ( 'NONE',  ( 0.000000000000000000, 0.1298341882520022694, 0.9915357197604852679 ) ) ;
#94069=ORIENTED_EDGE ( 'NONE', *, *, #12500, .F. ) ;
#94073=AXIS2_PLACEMENT_3D ( 'NONE', #189983, #109142, #110438 ) ;
#94078=CARTESIAN_POINT ( 'NONE',  ( -23.15000000000000213, 1.115600667400684642E-11, -79.87500000000004263 ) ) ;
#94079=DIRECTION ( 'NONE',  ( -1.000000000000000000, 0.000000000000000000, 0.000000000000000000 ) ) ;
#94080=ORIENTED_EDGE ( 'NONE', *, *, #56151, .T. ) ;
#94114=EDGE_CURVE ( 'NONE', #131327, #62762, #157584, .T. ) ;
#94116=AXIS2_PLACEMENT_3D ( 'NONE', #168965, #247158, #248461 ) ;
#94180=VERTEX_POINT ( 'NONE', #210015 ) ;
#94182=EDGE_CURVE ( 'NONE', #236296, #236185, #178414, .T. ) ;
#94185=CARTESIAN_POINT ( 'NONE',  ( -21.05000000000000071, 1.115600667400684642E-11, -67.00000000000004263 ) ) ;
#94195=CARTESIAN_POINT ( 'NONE',  ( -22.39999999999999858, 7.790779598384560245, -66.90000000000004832 ) ) ;
#94215=ADVANCED_FACE ( 'NONE', ( #92603 ), #167058, .T. ) ;
#94239=DIRECTION ( 'NONE',  ( 3.265361837132813093E-16, -1.000000000000000000, -0.000000000000000000 ) ) ;
#94245=ORIENTED_EDGE ( 'NONE', *, *, #222824, .F. ) ;
#94246=CARTESIAN_POINT ( 'NONE',  ( -20.94999999999999929, 11.75000000001115552, -74.01480577065404987 ) ) ;
#94290=CARTESIAN_POINT ( 'NONE',  ( 23.14999999999999858, 5.600000000011153389, -88.09473398108696074 ) ) ;
#94304=AXIS2_PLACEMENT_3D ( 'NONE', #198731, #119209, #20111 ) ;
#94309=ORIENTED_EDGE ( 'NONE', *, *, #249799, .T. ) ;
#94370=DIRECTION ( 'NONE',  ( -1.000000000000000000, -0.000000000000000000, -0.000000000000000000 ) ) ;
#94404=AXIS2_PLACEMENT_3D ( 'NONE', #244265, #123063, #3080 ) ;
#94473=CARTESIAN_POINT ( 'NONE',  ( -18.59999999999999787, 1.115600667400684642E-11, -67.00000000000004263 ) ) ;
#94518=CARTESIAN_POINT ( 'NONE',  ( 21.05000000000000071, -11.48912529306489994, -97.40000000000004832 ) ) ;
#94588=CARTESIAN_POINT ( 'NONE',  ( -20.00857864376270001, 9.250000000011157297, -88.15000000000004832 ) ) ;
#94590=ORIENTED_EDGE ( 'NONE', *, *, #156715, .T. ) ;
#94638=ORIENTED_EDGE ( 'NONE', *, *, #153350, .F. ) ;
#94656=DIRECTION ( 'NONE',  ( 0.000000000000000000, 0.000000000000000000, 1.000000000000000000 ) ) ;
#94666=DIRECTION ( 'NONE',  ( 0.000000000000000000, -3.339342691255258236E-13, 1.000000000000000000 ) ) ;
#94677=CIRCLE ( 'NONE', #128024, 0.09999999999999939493 ) ;
#94678=SPHERICAL_SURFACE ( 'NONE', #206684, 0.1000000000000000056 ) ;
#94727=ORIENTED_EDGE ( 'NONE', *, *, #53208, .F. ) ;
#94730=CIRCLE ( 'NONE', #98796, 0.1000000000000028644 ) ;
#94732=EDGE_CURVE ( 'NONE', #66589, #18615, #7307, .T. ) ;
#94742=EDGE_CURVE ( 'NONE', #144670, #55413, #173956, .T. ) ;
#94755=CARTESIAN_POINT ( 'NONE',  ( -21.05000000000000071, 11.65000000001115588, -67.10000000000005116 ) ) ;
#94777=ORIENTED_EDGE ( 'NONE', *, *, #79073, .T. ) ;
#94781=CARTESIAN_POINT ( 'NONE',  ( 23.24999999999999289, 6.550000000011156231, -88.35000000000003695 ) ) ;
#94787=VERTEX_POINT ( 'NONE', #145225 ) ;
#94796=CIRCLE ( 'NONE', #69880, 0.09999999999999939493 ) ;
#94814=ORIENTED_EDGE ( 'NONE', *, *, #217932, .F. ) ;
#94857=VERTEX_POINT ( 'NONE', #246897 ) ;
#94876=ORIENTED_EDGE ( 'NONE', *, *, #139948, .F. ) ;
#94883=ORIENTED_EDGE ( 'NONE', *, *, #100332, .T. ) ;
#94917=CARTESIAN_POINT ( 'NONE',  ( -23.25000000000000000, -1.835859311432481045, -112.1044391687985780 ) ) ;
#94936=CARTESIAN_POINT ( 'NONE',  ( 18.59999999999997655, 1.115600667400684642E-11, -100.5000000000000426 ) ) ;
#94938=CARTESIAN_POINT ( 'NONE',  ( 23.15000000000000213, -11.64999999998883595, -97.40000000000004832 ) ) ;
#94953=ORIENTED_EDGE ( 'NONE', *, *, #132307, .F. ) ;
#94954=LINE ( 'NONE', #254027, #48762 ) ;
#94998=DIRECTION ( 'NONE',  ( -1.000000000000000000, 0.000000000000000000, 0.000000000000000000 ) ) ;
#95002=EDGE_LOOP ( 'NONE', ( #211396, #123372, #234252, #80690 ) ) ;
#95044=DIRECTION ( 'NONE',  ( -1.000000000000000000, -0.000000000000000000, -0.000000000000000000 ) ) ;
#95051=DIRECTION ( 'NONE',  ( 1.000000000000000000, 0.000000000000000000, -0.000000000000000000 ) ) ;
#95065=ORIENTED_EDGE ( 'NONE', *, *, #133658, .F. ) ;
#95067=VERTEX_POINT ( 'NONE', #1559 ) ;
#95073=ADVANCED_FACE ( 'NONE', ( #176385 ), #77247, .F. ) ;
#95074=EDGE_LOOP ( 'NONE', ( #78979, #37020, #150036, #222321 ) ) ;
#95096=CARTESIAN_POINT ( 'NONE',  ( 18.39999999999999858, -9.499999999988842703, -74.03206939669971121 ) ) ;
#95099=EDGE_LOOP ( 'NONE', ( #80251, #9383, #135327, #142365 ) ) ;
#95107=CARTESIAN_POINT ( 'NONE',  ( -21.05000000000000071, 1.115600667400684642E-11, -67.00000000000004263 ) ) ;
#95109=DIRECTION ( 'NONE',  ( 0.000000000000000000, 0.000000000000000000, -1.000000000000000000 ) ) ;
#95110=CIRCLE ( 'NONE', #149295, 0.09999999999999693856 ) ;
#95132=ORIENTED_EDGE ( 'NONE', *, *, #180997, .T. ) ;
#95148=CYLINDRICAL_SURFACE ( 'NONE', #205683, 0.1000000000000028644 ) ;
#95156=VERTEX_POINT ( 'NONE', #16032 ) ;
#95205=AXIS2_PLACEMENT_3D ( 'NONE', #94936, #72853, #254011 ) ;
#95217=DIRECTION ( 'NONE',  ( -1.000000000000000000, 0.000000000000000000, 0.000000000000000000 ) ) ;
#95223=AXIS2_PLACEMENT_3D ( 'NONE', #54024, #18749, #115281 ) ;
#95230=FACE_OUTER_BOUND ( 'NONE', #102359, .T. ) ;
#95231=DIRECTION ( 'NONE',  ( -1.000000000000000000, -0.000000000000000000, -0.000000000000000000 ) ) ;
#95242=CIRCLE ( 'NONE', #157833, 0.1000000000000028644 ) ;
#95267=CARTESIAN_POINT ( 'NONE',  ( 20.94999999999999929, 1.835341550235569663, -78.55515129256303908 ) ) ;
#95286=ORIENTED_EDGE ( 'NONE', *, *, #110077, .T. ) ;
#95297=DIRECTION ( 'NONE',  ( -1.000000000000000000, -0.000000000000000000, -0.000000000000000000 ) ) ;
#95314=VERTEX_POINT ( 'NONE', #14442 ) ;
#95319=CARTESIAN_POINT ( 'NONE',  ( 21.07954640115360334, 0.06600770715084654239, -60.67071230397558423 ) ) ;
#95332=ORIENTED_EDGE ( 'NONE', *, *, #132319, .T. ) ;
#95356=ADVANCED_FACE ( 'NONE', ( #227034 ), #245004, .T. ) ;
#95362=ORIENTED_EDGE ( 'NONE', *, *, #2935, .F. ) ;
#95369=ORIENTED_EDGE ( 'NONE', *, *, #132898, .F. ) ;
#95370=ORIENTED_EDGE ( 'NONE', *, *, #199673, .F. ) ;
#95382=ORIENTED_EDGE ( 'NONE', *, *, #84, .F. ) ;
#95390=CARTESIAN_POINT ( 'NONE',  ( 18.59999999999999076, 6.450000000011156587, -77.01702717044007329 ) ) ;
#95455=AXIS2_PLACEMENT_3D ( 'NONE', #180428, #177873, #139985 ) ;
#95462=CARTESIAN_POINT ( 'NONE',  ( -18.59999999999999787, 1.835341550235567887, -78.65515129256301918 ) ) ;
#95487=DIRECTION ( 'NONE',  ( 0.000000000000000000, 0.000000000000000000, 1.000000000000000000 ) ) ;
#95490=EDGE_CURVE ( 'NONE', #248044, #151819, #232734, .T. ) ;
#95577=CARTESIAN_POINT ( 'NONE',  ( 21.46681500597990677, 1.115539681028482333E-11, -60.14248884057332134 ) ) ;
#95611=ORIENTED_EDGE ( 'NONE', *, *, #151543, .T. ) ;
#95622=CARTESIAN_POINT ( 'NONE',  ( 21.08621493067296626, 6.349294291182826733, -66.94380516052393659 ) ) ;
#95632=EDGE_CURVE ( 'NONE', #145626, #196062, #111936, .T. ) ;
#95642=VERTEX_POINT ( 'NONE', #121261 ) ;
#95656=ORIENTED_EDGE ( 'NONE', *, *, #100332, .F. ) ;
#95663=VECTOR ( 'NONE', #200436, 1000.000000000000000 ) ;
#95680=LINE ( 'NONE', #51390, #124004 ) ;
#95742=CYLINDRICAL_SURFACE ( 'NONE', #74152, 0.1000000000000028644 ) ;
#95755=ORIENTED_EDGE ( 'NONE', *, *, #65652, .T. ) ;
#95768=VERTEX_POINT ( 'NONE', #207187 ) ;
#95769=CIRCLE ( 'NONE', #91705, 0.1000000000000028644 ) ;
#95780=CARTESIAN_POINT ( 'NONE',  ( 23.24999999999999645, 3.900000000011155432, -100.5000000000000426 ) ) ;
#95797=DIRECTION ( 'NONE',  ( -1.000000000000000000, -2.952720810173289112E-16, 0.000000000000000000 ) ) ;
#95846=FACE_OUTER_BOUND ( 'NONE', #172979, .T. ) ;
#95855=ADVANCED_FACE ( 'NONE', ( #147195 ), #226722, .T. ) ;
#95860=ORIENTED_EDGE ( 'NONE', *, *, #162181, .T. ) ;
#95867=ADVANCED_FACE ( 'NONE', ( #113203 ), #221515, .F. ) ;
#95920=CARTESIAN_POINT ( 'NONE',  ( 21.05000000000000071, 8.926614585098253229, -75.47168301922316402 ) ) ;
#95938=ORIENTED_EDGE ( 'NONE', *, *, #20834, .T. ) ;
#95942=CIRCLE ( 'NONE', #87572, 0.1000000000000028644 ) ;
#95946=CARTESIAN_POINT ( 'NONE',  ( 21.14999999999999858, 6.650000000011155876, -79.35000000000005116 ) ) ;
#95950=ORIENTED_EDGE ( 'NONE', *, *, #195585, .T. ) ;
#95959=EDGE_LOOP ( 'NONE', ( #84514, #42572, #118102, #232402 ) ) ;
#95960=CARTESIAN_POINT ( 'NONE',  ( -18.39999999999999858, -9.499999999988849808, -73.99928567783889832 ) ) ;
#95970=CARTESIAN_POINT ( 'NONE',  ( -21.08376601933334271, 0.06377601094103593771, -60.65805272872431431 ) ) ;
#95981=VERTEX_POINT ( 'NONE', #179612 ) ;
#96009=CARTESIAN_POINT ( 'NONE',  ( 20.94999999999999929, 1.115649653272650466E-11, -96.50000000000004263 ) ) ;
#96043=VERTEX_POINT ( 'NONE', #60916 ) ;
#96059=CARTESIAN_POINT ( 'NONE',  ( 19.81427058490564264, 11.66856398039202070, -91.75000000000005684 ) ) ;
#96069=CARTESIAN_POINT ( 'NONE',  ( 20.94999999999999929, -1.135018845899022466, -108.2169768834323662 ) ) ;
#96072=ORIENTED_EDGE ( 'NONE', *, *, #119989, .F. ) ;
#96159=CARTESIAN_POINT ( 'NONE',  ( 20.85000000000000142, -1.263275465206102233, -108.4018646667464481 ) ) ;
#96187=VERTEX_POINT ( 'NONE', #112897 ) ;
#96195=TOROIDAL_SURFACE ( 'NONE', #154507, 11.70000000000000462, 0.1000000000000000056 ) ;
#96205=EDGE_CURVE ( 'NONE', #194152, #14603, #195518, .T. ) ;
#96239=DIRECTION ( 'NONE',  ( 0.000000000000000000, 0.3738317757009345654, 0.9274965247785492695 ) ) ;
#96249=ADVANCED_FACE ( 'NONE', ( #253671 ), #41576, .T. ) ;
#96291=DIRECTION ( 'NONE',  ( 1.000000000000000000, 0.000000000000000000, 0.000000000000000000 ) ) ;
#96293=VERTEX_POINT ( 'NONE', #132458 ) ;
#96307=SPHERICAL_SURFACE ( 'NONE', #241640, 0.1000000000000000056 ) ;
#96321=CARTESIAN_POINT ( 'NONE',  ( 20.94999999999999929, 4.850467289730772791, -79.03426740900172831 ) ) ;
#96350=CIRCLE ( 'NONE', #146254, 0.09999999999999939493 ) ;
#96371=ORIENTED_EDGE ( 'NONE', *, *, #127030, .T. ) ;
#96382=ADVANCED_FACE ( 'NONE', ( #155148 ), #150305, .T. ) ;
#96417=CARTESIAN_POINT ( 'NONE',  ( -20.64999999999999858, 7.250000000011155521, -88.25000000000005684 ) ) ;
#96425=TOROIDAL_SURFACE ( 'NONE', #129204, 0.2000000000000000111, 0.1000000000000000056 ) ;
#96430=CARTESIAN_POINT ( 'NONE',  ( -18.50000000000000000, 11.65000000001115588, -100.5000000000000426 ) ) ;
#96433=PLANE ( 'NONE',  #202999 ) ;
#96445=CARTESIAN_POINT ( 'NONE',  ( 21.05000000000000071, -9.399999999988846611, -76.89396912265249284 ) ) ;
#96492=DIRECTION ( 'NONE',  ( 1.000000000000000000, -0.000000000000000000, -0.000000000000000000 ) ) ;
#96543=CARTESIAN_POINT ( 'NONE',  ( -23.15000000000000213, 1.115600667400684642E-11, -79.77500000000003411 ) ) ;
#96577=ORIENTED_EDGE ( 'NONE', *, *, #144792, .F. ) ;
#96604=EDGE_LOOP ( 'NONE', ( #156699, #169413, #103036, #212685 ) ) ;
#96612=CARTESIAN_POINT ( 'NONE',  ( 21.14999999999999858, 1.115600667400684642E-11, -79.15000000000004832 ) ) ;
#96632=PLANE ( 'NONE',  #107587 ) ;
#96642=VERTEX_POINT ( 'NONE', #228150 ) ;
#96665=ORIENTED_EDGE ( 'NONE', *, *, #125377, .T. ) ;
#96684=CIRCLE ( 'NONE', #150881, 0.5000000000000004441 ) ;
#96695=AXIS2_PLACEMENT_3D ( 'NONE', #26075, #180017, #163024 ) ;
#96737=DIRECTION ( 'NONE',  ( -0.000000000000000000, -1.265107689135680095E-16, 1.000000000000000000 ) ) ;
#96740=AXIS2_PLACEMENT_3D ( 'NONE', #142676, #98389, #162283 ) ;
#96743=AXIS2_PLACEMENT_3D ( 'NONE', #176982, #219924, #221193 ) ;
#96794=ORIENTED_EDGE ( 'NONE', *, *, #28695, .T. ) ;
#96818=ADVANCED_FACE ( 'NONE', ( #134163 ), #96307, .T. ) ;
#96834=DIRECTION ( 'NONE',  ( -1.000000000000000000, 0.000000000000000000, 0.000000000000000000 ) ) ;
#96837=DIRECTION ( 'NONE',  ( -0.000000000000000000, -0.4791956752371546724, -0.8777080977375153470 ) ) ;
#96845=DIRECTION ( 'NONE',  ( 0.000000000000000000, 0.8700118002898321601, -0.4930308989875230030 ) ) ;
#96848=DIRECTION ( 'NONE',  ( -1.000000000000000000, 0.000000000000000000, 0.000000000000000000 ) ) ;
#96855=CARTESIAN_POINT ( 'NONE',  ( 23.25000000000000000, -8.999999999988842703, -90.60603087734760663 ) ) ;
#96878=VECTOR ( 'NONE', #143503, 1000.000000000000000 ) ;
#96885=ORIENTED_EDGE ( 'NONE', *, *, #33963, .F. ) ;
#96888=ADVANCED_FACE ( 'NONE', ( #161455 ), #21102, .F. ) ;
#96891=ORIENTED_EDGE ( 'NONE', *, *, #228523, .F. ) ;
#96893=VECTOR ( 'NONE', #32546, 1000.000000000000000 ) ;
#96898=VECTOR ( 'NONE', #25289, 1000.000000000000000 ) ;
#96929=CARTESIAN_POINT ( 'NONE',  ( -20.94999999999999929, 1.835341550235569663, -78.55515129256303908 ) ) ;
#96932=ORIENTED_EDGE ( 'NONE', *, *, #93916, .F. ) ;
#96964=CARTESIAN_POINT ( 'NONE',  ( -22.49806830649814415, 11.64988965485023620, -66.92253568367453909 ) ) ;
#96967=DIRECTION ( 'NONE',  ( 0.000000000000000000, 0.000000000000000000, 1.000000000000000000 ) ) ;
#96971=DIRECTION ( 'NONE',  ( 0.000000000000000000, 0.000000000000000000, 1.000000000000000000 ) ) ;
#96976=DIRECTION ( 'NONE',  ( 0.000000000000000000, 0.000000000000000000, -1.000000000000000000 ) ) ;
#96978=ADVANCED_FACE ( 'NONE', ( #20663 ), #195880, .T. ) ;
#96988=FACE_OUTER_BOUND ( 'NONE', #238972, .T. ) ;
#97038=CARTESIAN_POINT ( 'NONE',  ( -21.05000000000000071, -1.249999999988843369, -75.00000000000004263 ) ) ;
#97042=DIRECTION ( 'NONE',  ( 1.000000000000000000, 0.000000000000000000, 0.000000000000000000 ) ) ;
#97062=CARTESIAN_POINT ( 'NONE',  ( 20.94999999999999929, 4.813084112160680661, -78.94151775652387926 ) ) ;
#97076=LINE ( 'NONE', #181797, #133763 ) ;
#97077=ORIENTED_EDGE ( 'NONE', *, *, #4485, .F. ) ;
#97108=DIRECTION ( 'NONE',  ( 1.000000000000000000, 2.952720810173289112E-16, -0.000000000000000000 ) ) ;
#97126=DIRECTION ( 'NONE',  ( -1.000000000000000000, 0.000000000000000000, -0.000000000000000000 ) ) ;
#97138=DIRECTION ( 'NONE',  ( -6.938893903907209445E-14, -0.9999176327611370985, -0.01283462868040260302 ) ) ;
#97176=DIRECTION ( 'NONE',  ( 1.000000000000000000, 0.000000000000000000, -0.000000000000000000 ) ) ;
#97184=ORIENTED_EDGE ( 'NONE', *, *, #173188, .T. ) ;
#97199=EDGE_CURVE ( 'NONE', #64371, #87242, #192413, .T. ) ;
#97211=ORIENTED_EDGE ( 'NONE', *, *, #143665, .T. ) ;
#97215=DIRECTION ( 'NONE',  ( 0.000000000000000000, -1.000000000000000000, 0.000000000000000000 ) ) ;
#97218=DIRECTION ( 'NONE',  ( 0.000000000000000000, 0.000000000000000000, 1.000000000000000000 ) ) ;
#97224=CARTESIAN_POINT ( 'NONE',  ( -21.09813707148783379, 0.03135149954059018862, -60.61493789426336321 ) ) ;
#97259=AXIS2_PLACEMENT_3D ( 'NONE', #83761, #159508, #239030 ) ;
#97262=DIRECTION ( 'NONE',  ( -1.000000000000000000, -3.265361837132813093E-16, 0.000000000000000000 ) ) ;
#97285=CARTESIAN_POINT ( 'NONE',  ( -21.05000000000000071, 14.00000000001115374, -95.07290746961757577 ) ) ;
#97307=ORIENTED_EDGE ( 'NONE', *, *, #162636, .F. ) ;
#97329=DIRECTION ( 'NONE',  ( 0.7071359030027940529, 0.000000000000000000, -0.7070776581708850816 ) ) ;
#97332=ORIENTED_EDGE ( 'NONE', *, *, #130311, .F. ) ;
#97337=DIRECTION ( 'NONE',  ( 0.000000000000000000, -1.000000000000000000, -0.000000000000000000 ) ) ;
#97343=TOROIDAL_SURFACE ( 'NONE', #55646, 11.90000000000000391, 0.1000000000000000056 ) ;
#97345=AXIS2_PLACEMENT_3D ( 'NONE', #99146, #254365, #40523 ) ;
#97378=CARTESIAN_POINT ( 'NONE',  ( -20.94999999999999929, 1.851028230152016674, -78.65391326942254580 ) ) ;
#97403=DIRECTION ( 'NONE',  ( 0.000000000000000000, -1.000000000000000000, 0.000000000000000000 ) ) ;
#97409=AXIS2_PLACEMENT_3D ( 'NONE', #171664, #193758, #152087 ) ;
#97472=CARTESIAN_POINT ( 'NONE',  ( 20.94999999999999574, -1.249999999988843369, -75.00000000000004263 ) ) ;
#97518=DIRECTION ( 'NONE',  ( 0.7071359030027419834, 0.000000000000000000, 0.7070776581709371511 ) ) ;
#97532=CIRCLE ( 'NONE', #72646, 0.09999999999999911737 ) ;
#97533=ORIENTED_EDGE ( 'NONE', *, *, #45337, .F. ) ;
#97555=CARTESIAN_POINT ( 'NONE',  ( 18.59999999999999787, -9.321008403350148797, -74.23593824907790406 ) ) ;
#97571=CARTESIAN_POINT ( 'NONE',  ( -20.94999999999999929, 11.65000000001115232, -93.71613433702194129 ) ) ;
#97581=CARTESIAN_POINT ( 'NONE',  ( 21.05000000000000071, 5.900000000011162093, -90.28090023534366537 ) ) ;
#97606=VERTEX_POINT ( 'NONE', #233637 ) ;
#97614=AXIS2_PLACEMENT_3D ( 'NONE', #30808, #146850, #66047 ) ;
#97619=ADVANCED_FACE ( 'NONE', ( #161818 ), #241342, .T. ) ;
#97620=EDGE_LOOP ( 'NONE', ( #162765, #22642, #19452, #148822 ) ) ;
#97622=ORIENTED_EDGE ( 'NONE', *, *, #75840, .T. ) ;
#97630=EDGE_CURVE ( 'NONE', #71443, #17147, #142220, .T. ) ;
#97657=EDGE_LOOP ( 'NONE', ( #84205, #5063, #213804, #242450, #124862 ) ) ;
#97684=CARTESIAN_POINT ( 'NONE',  ( -18.59999999999999787, -1.162701749926853712, -75.10000000000003695 ) ) ;
#97705=CARTESIAN_POINT ( 'NONE',  ( -23.25000000000000000, 11.75000000001115552, -88.35000000000003695 ) ) ;
#97769=EDGE_CURVE ( 'NONE', #113878, #140349, #249049, .T. ) ;
#97778=CIRCLE ( 'NONE', #206145, 7.800000000000001599 ) ;
#97819=DIRECTION ( 'NONE',  ( 0.000000000000000000, 0.000000000000000000, -1.000000000000000000 ) ) ;
#97823=CARTESIAN_POINT ( 'NONE',  ( -20.54999999999999716, 1.115600667400684642E-11, -79.97500000000005116 ) ) ;
#97836=ADVANCED_FACE ( 'NONE', ( #106936 ), #7871, .T. ) ;
#97842=DIRECTION ( 'NONE',  ( 0.000000000000000000, 0.5000000000000004441, 0.8660254037844384856 ) ) ;
#97847=VERTEX_POINT ( 'NONE', #187788 ) ;
#97876=EDGE_CURVE ( 'NONE', #75223, #89932, #1015, .T. ) ;
#97889=ORIENTED_EDGE ( 'NONE', *, *, #213695, .T. ) ;
#97923=DIRECTION ( 'NONE',  ( -0.000000000000000000, 0.000000000000000000, 1.000000000000000000 ) ) ;
#97971=CIRCLE ( 'NONE', #122950, 0.1000000000000033223 ) ;
#97979=EDGE_LOOP ( 'NONE', ( #68064, #88521, #242943, #168470 ) ) ;
#97986=EDGE_CURVE ( 'NONE', #181640, #189831, #155098, .T. ) ;
#98009=CARTESIAN_POINT ( 'NONE',  ( 21.05000000000000071, 1.115650877919449575E-11, -96.40000000000003411 ) ) ;
#98014=ORIENTED_EDGE ( 'NONE', *, *, #12485, .T. ) ;
#98028=AXIS2_PLACEMENT_3D ( 'NONE', #177049, #157497, #38807 ) ;
#98032=DIRECTION ( 'NONE',  ( 0.000000000000000000, 0.000000000000000000, 1.000000000000000000 ) ) ;
#98072=FACE_OUTER_BOUND ( 'NONE', #220605, .T. ) ;
#98092=CARTESIAN_POINT ( 'NONE',  ( -21.45000000000000284, 7.708578643773852157, -79.35000000000005116 ) ) ;
#98112=VERTEX_POINT ( 'NONE', #1092 ) ;
#98161=CARTESIAN_POINT ( 'NONE',  ( -18.59999999999999787, -1.261786168553869603, -75.08649896354552311 ) ) ;
#98187=ORIENTED_EDGE ( 'NONE', *, *, #182149, .T. ) ;
#98207=ORIENTED_EDGE ( 'NONE', *, *, #138885, .F. ) ;
#98242=MECHANICAL_DESIGN_GEOMETRIC_PRESENTATION_REPRESENTATION('',(#239764),#181519);
#98244=EDGE_CURVE ( 'NONE', #174189, #224643, #188672, .T. ) ;
#98251=FACE_OUTER_BOUND ( 'NONE', #213984, .T. ) ;
#98272=CARTESIAN_POINT ( 'NONE',  ( -20.94999999999999929, 1.115600667400684642E-11, -74.90000000000004832 ) ) ;
#98284=ORIENTED_EDGE ( 'NONE', *, *, #231761, .T. ) ;
#98309=AXIS2_PLACEMENT_3D ( 'NONE', #5162, #181291, #207270 ) ;
#98328=AXIS2_PLACEMENT_3D ( 'NONE', #133601, #73666, #90613 ) ;
#98377=CARTESIAN_POINT ( 'NONE',  ( 21.14999999999999858, 11.75000000001116263, -67.10000000000005116 ) ) ;
#98389=DIRECTION ( 'NONE',  ( -1.000000000000000000, 0.000000000000000000, 0.000000000000000000 ) ) ;
#98394=AXIS2_PLACEMENT_3D ( 'NONE', #1420, #80953, #82219 ) ;
#98410=DIRECTION ( 'NONE',  ( -1.000000000000000000, -0.000000000000000000, -0.000000000000000000 ) ) ;
#98445=CARTESIAN_POINT ( 'NONE',  ( -23.15000000000000213, 1.115649653272650466E-11, -104.5000000000000568 ) ) ;
#98464=FACE_OUTER_BOUND ( 'NONE', #112412, .T. ) ;
#98495=ORIENTED_EDGE ( 'NONE', *, *, #249228, .T. ) ;
#98507=FACE_OUTER_BOUND ( 'NONE', #144740, .T. ) ;
#98521=EDGE_LOOP ( 'NONE', ( #37552, #120832, #96885, #97307 ) ) ;
#98540=ADVANCED_FACE ( 'NONE', ( #59456 ), #246133, .F. ) ;
#98548=DIRECTION ( 'NONE',  ( -1.000000000000000000, 0.000000000000000000, 0.000000000000000000 ) ) ;
#98629=DIRECTION ( 'NONE',  ( 0.000000000000000000, -0.1568667991644693838, -0.9876197685951279004 ) ) ;
#98633=DIRECTION ( 'NONE',  ( 0.000000000000000000, -0.9908441862701596881, -0.1350103645451904977 ) ) ;
#98645=DIRECTION ( 'NONE',  ( -1.000000000000000000, 0.000000000000000000, 0.000000000000000000 ) ) ;
#98661=ORIENTED_EDGE ( 'NONE', *, *, #31560, .T. ) ;
#98667=AXIS2_PLACEMENT_3D ( 'NONE', #178163, #21641, #120763 ) ;
#98671=CARTESIAN_POINT ( 'NONE',  ( -22.39999999999999858, 1.115600667400684642E-11, -67.00000000000004263 ) ) ;
#98680=CIRCLE ( 'NONE', #182120, 0.09999999999999741040 ) ;
#98685=AXIS2_PLACEMENT_3D ( 'NONE', #58554, #178555, #79402 ) ;
#98709=EDGE_CURVE ( 'NONE', #31018, #74117, #111466, .T. ) ;
#98718=DIRECTION ( 'NONE',  ( -0.000000000000000000, -0.000000000000000000, -1.000000000000000000 ) ) ;
#98731=CARTESIAN_POINT ( 'NONE',  ( 21.11344571971287465, 10.61787902352919666, -79.24602089239978397 ) ) ;
#98758=DIRECTION ( 'NONE',  ( 0.000000000000000000, 0.000000000000000000, -1.000000000000000000 ) ) ;
#98796=AXIS2_PLACEMENT_3D ( 'NONE', #184885, #63651, #25822 ) ;
#98799=AXIS2_PLACEMENT_3D ( 'NONE', #174425, #53137, #210934 ) ;
#98823=AXIS2_PLACEMENT_3D ( 'NONE', #36349, #53323, #237095 ) ;
#98855=CIRCLE ( 'NONE', #169863, 0.3999999999999975797 ) ;
#98884=LINE ( 'NONE', #181044, #28686 ) ;
#98901=CARTESIAN_POINT ( 'NONE',  ( -23.15000000000000213, -11.74999999998884448, -97.40000000000004832 ) ) ;
#98910=LINE ( 'NONE', #18124, #65831 ) ;
#98913=ORIENTED_EDGE ( 'NONE', *, *, #86762, .F. ) ;
#98940=CARTESIAN_POINT ( 'NONE',  ( 22.39999999999999503, 1.115600667400684642E-11, -55.35042919245524473 ) ) ;
#98943=CIRCLE ( 'NONE', #153364, 0.09999999999999820144 ) ;
#98952=CYLINDRICAL_SURFACE ( 'NONE', #98685, 0.09999999999999939493 ) ;
#98980=DIRECTION ( 'NONE',  ( 0.000000000000000000, -1.000000000000000000, -2.891205793294679805E-16 ) ) ;
#99018=EDGE_CURVE ( 'NONE', #201851, #247975, #124312, .T. ) ;
#99021=CYLINDRICAL_SURFACE ( 'NONE', #171282, 11.74999999999999645 ) ;
#99033=CARTESIAN_POINT ( 'NONE',  ( -20.64999999999999858, 4.250000000011156409, -79.25000000000004263 ) ) ;
#99109=DIRECTION ( 'NONE',  ( 1.000000000000000000, 0.000000000000000000, 0.000000000000000000 ) ) ;
#99114=AXIS2_PLACEMENT_3D ( 'NONE', #220607, #240177, #142334 ) ;
#99119=CIRCLE ( 'NONE', #32540, 0.1000000000000028644 ) ;
#99135=DIRECTION ( 'NONE',  ( -0.000000000000000000, -0.1298341882520022694, -0.9915357197604853789 ) ) ;
#99146=CARTESIAN_POINT ( 'NONE',  ( 18.59999999999999076, 6.650000000011155876, -88.15000000000004832 ) ) ;
#99161=EDGE_LOOP ( 'NONE', ( #195187, #18387, #181330, #221118 ) ) ;
#99168=ORIENTED_EDGE ( 'NONE', *, *, #13391, .F. ) ;
#99180=EDGE_CURVE ( 'NONE', #230047, #48218, #19456, .T. ) ;
#99198=COLOUR_RGB ( '', 0.08235294, 0.09019608, 0.10196078) ;
#99231=ORIENTED_EDGE ( 'NONE', *, *, #139679, .F. ) ;
#99265=TOROIDAL_SURFACE ( 'NONE', #149193, 4.149999999999999467, 0.1000000000000000056 ) ;
#99271=LINE ( 'NONE', #237530, #44733 ) ;
#99275=FACE_OUTER_BOUND ( 'NONE', #113795, .T. ) ;
#99278=VECTOR ( 'NONE', #229341, 1000.000000000000000 ) ;
#99279=CARTESIAN_POINT ( 'NONE',  ( -20.85000000000000142, 10.33248238083634440, -106.0948465439131922 ) ) ;
#99353=EDGE_CURVE ( 'NONE', #164187, #123901, #179877, .T. ) ;
#99416=DIRECTION ( 'NONE',  ( 0.000000000000000000, 0.000000000000000000, -1.000000000000000000 ) ) ;
#99432=ORIENTED_EDGE ( 'NONE', *, *, #200392, .F. ) ;
#99441=EDGE_CURVE ( 'NONE', #152197, #195076, #212631, .T. ) ;
#99463=EDGE_LOOP ( 'NONE', ( #209724, #71185, #81455, #123399 ) ) ;
#99471=ORIENTED_EDGE ( 'NONE', *, *, #107963, .F. ) ;
#99482=DIRECTION ( 'NONE',  ( 1.000000000000000000, 0.000000000000000000, 0.000000000000000000 ) ) ;
#99502=CARTESIAN_POINT ( 'NONE',  ( -20.64999999999999858, 2.500000000011154633, -87.27537807723794572 ) ) ;
#99507=CARTESIAN_POINT ( 'NONE',  ( -18.59999996769639097, -9.363273769819265624, -74.18149391546575089 ) ) ;
#99542=CIRCLE ( 'NONE', #132907, 0.2000000000000000944 ) ;
#99591=DIRECTION ( 'NONE',  ( -1.000000000000000000, -0.000000000000000000, -0.000000000000000000 ) ) ;
#99592=CARTESIAN_POINT ( 'NONE',  ( 18.59999999999997655, 1.115600667400684642E-11, -108.4000000000000483 ) ) ;
#99599=EDGE_LOOP ( 'NONE', ( #161950, #160340, #162387, #69250 ) ) ;
#99600=ORIENTED_EDGE ( 'NONE', *, *, #99752, .F. ) ;
#99606=ORIENTED_EDGE ( 'NONE', *, *, #66186, .T. ) ;
#99615=FACE_OUTER_BOUND ( 'NONE', #171390, .T. ) ;
#99617=LINE ( 'NONE', #23989, #185879 ) ;
#99621=CARTESIAN_POINT ( 'NONE',  ( -20.64999999999999858, 1.115623935689868526E-11, -98.60000000000005116 ) ) ;
#99626=CARTESIAN_POINT ( 'NONE',  ( 20.94999999999999929, 5.000000000011153745, -88.09473398108696074 ) ) ;
#99636=CARTESIAN_POINT ( 'NONE',  ( 18.49999999999999289, 7.120270961708750512, -104.1595630418393768 ) ) ;
#99647=CARTESIAN_POINT ( 'NONE',  ( -18.50000000000000000, 7.021664781911246322, -104.3335654018973315 ) ) ;
#99687=DIRECTION ( 'NONE',  ( 0.000000000000000000, -0.8700118002898321601, 0.4930308989875230030 ) ) ;
#99724=CARTESIAN_POINT ( 'NONE',  ( 21.11701782572533048, 10.72160911601861244, -79.24503742951125673 ) ) ;
#99747=EDGE_CURVE ( 'NONE', #131057, #21996, #127223, .T. ) ;
#99752=EDGE_CURVE ( 'NONE', #55413, #214700, #196213, .T. ) ;
#99824=PLANE ( 'NONE',  #135293 ) ;
#99852=ADVANCED_FACE ( 'NONE', ( #174096 ), #212803, .F. ) ;
#99858=ORIENTED_EDGE ( 'NONE', *, *, #42908, .T. ) ;
#99871=ORIENTED_EDGE ( 'NONE', *, *, #243872, .F. ) ;
#99886=EDGE_CURVE ( 'NONE', #141973, #77103, #188040, .T. ) ;
#99899=EDGE_LOOP ( 'NONE', ( #194830, #122868, #93243, #81633 ) ) ;
#99902=ADVANCED_FACE ( 'NONE', ( #172812 ), #193616, .T. ) ;
#99914=EDGE_CURVE ( 'NONE', #211426, #242521, #58823, .T. ) ;
#99921=VECTOR ( 'NONE', #17804, 1000.000000000000000 ) ;
#99932=CARTESIAN_POINT ( 'NONE',  ( -18.59999999999999787, 11.65000000001115232, -88.35000000000003695 ) ) ;
#99940=ORIENTED_EDGE ( 'NONE', *, *, #24196, .T. ) ;
#99950=EDGE_CURVE ( 'NONE', #143581, #78012, #42289, .T. ) ;
#99959=ORIENTED_EDGE ( 'NONE', *, *, #176643, .T. ) ;
#99960=EDGE_CURVE ( 'NONE', #171778, #76379, #154737, .T. ) ;
#99970=LINE ( 'NONE', #872, #104567 ) ;
#100004=CARTESIAN_POINT ( 'NONE',  ( 23.14999999999999503, 11.65000000001116298, -79.15000000000004832 ) ) ;
#100018=FACE_OUTER_BOUND ( 'NONE', #79261, .T. ) ;
#100021=CIRCLE ( 'NONE', #137448, 0.1000000000000028644 ) ;
#100025=VECTOR ( 'NONE', #149753, 1000.000000000000000 ) ;
#100027=EDGE_CURVE ( 'NONE', #205600, #16002, #121430, .T. ) ;
#100046=ORIENTED_EDGE ( 'NONE', *, *, #78014, .F. ) ;
#100067=EDGE_LOOP ( 'NONE', ( #10684, #257038, #83880, #106903 ) ) ;
#100070=DIRECTION ( 'NONE',  ( 0.000000000000000000, 0.000000000000000000, -1.000000000000000000 ) ) ;
#100078=EDGE_CURVE ( 'NONE', #198610, #102331, #108915, .T. ) ;
#100102=VERTEX_POINT ( 'NONE', #120524 ) ;
#100202=CARTESIAN_POINT ( 'NONE',  ( 21.05000000000000071, 1.115600667400684642E-11, -67.00000000000004263 ) ) ;
#100206=CIRCLE ( 'NONE', #150321, 0.1000000000000028644 ) ;
#100251=SPHERICAL_SURFACE ( 'NONE', #68519, 0.1000000000000000056 ) ;
#100261=ORIENTED_EDGE ( 'NONE', *, *, #8998, .T. ) ;
#100271=CARTESIAN_POINT ( 'NONE',  ( 21.78635804494511419, 0.09900506551883611617, -59.96433851484686528 ) ) ;
#100282=ORIENTED_EDGE ( 'NONE', *, *, #247308, .T. ) ;
#100285=ADVANCED_FACE ( 'NONE', ( #47075 ), #227010, .F. ) ;
#100309=CARTESIAN_POINT ( 'NONE',  ( 20.94999999999999929, 1.115600667400684642E-11, -100.5000000000000426 ) ) ;
#100332=EDGE_CURVE ( 'NONE', #74117, #208340, #179864, .T. ) ;
#100343=AXIS2_PLACEMENT_3D ( 'NONE', #249738, #133636, #170252 ) ;
#100345=DIRECTION ( 'NONE',  ( -0.000000000000000000, -0.000000000000000000, -1.000000000000000000 ) ) ;
#100356=EDGE_CURVE ( 'NONE', #89932, #128108, #189183, .T. ) ;
#100387=CARTESIAN_POINT ( 'NONE',  ( 20.93284271247462414, 11.75000000001116085, -93.48519422934610645 ) ) ;
#100417=DIRECTION ( 'NONE',  ( 0.000000000000000000, -0.8660254037844383745, 0.5000000000000003331 ) ) ;
#100447=DIRECTION ( 'NONE',  ( 1.000000000000000000, -0.000000000000000000, -0.000000000000000000 ) ) ;
#100465=EDGE_CURVE ( 'NONE', #14603, #178965, #254796, .T. ) ;
#100480=EDGE_CURVE ( 'NONE', #48218, #82481, #125667, .T. ) ;
#100489=DIRECTION ( 'NONE',  ( 1.000000000000000000, 0.000000000000000000, 0.000000000000000000 ) ) ;
#100502=VECTOR ( 'NONE', #218492, 1000.000000000000000 ) ;
#100525=DIRECTION ( 'NONE',  ( -0.000000000000000000, -1.000000000000000000, 0.000000000000000000 ) ) ;
#100551=ORIENTED_EDGE ( 'NONE', *, *, #101853, .F. ) ;
#100612=CIRCLE ( 'NONE', #38306, 0.1000000000000010186 ) ;
#100624=CARTESIAN_POINT ( 'NONE',  ( -20.94999999999999929, 1.162701749949165642, -74.90000000000004832 ) ) ;
#100631=CARTESIAN_POINT ( 'NONE',  ( 18.41416235934318024, -9.499999999988842703, -107.1001893912220879 ) ) ;
#100635=VERTEX_POINT ( 'NONE', #164180 ) ;
#100650=ORIENTED_EDGE ( 'NONE', *, *, #86334, .T. ) ;
#100656=AXIS2_PLACEMENT_3D ( 'NONE', #220304, #63778, #85879 ) ;
#100658=AXIS2_PLACEMENT_3D ( 'NONE', #208157, #230257, #186005 ) ;
#100683=DIRECTION ( 'NONE',  ( -0.000000000000000000, 0.000000000000000000, 1.000000000000000000 ) ) ;
#100727=VECTOR ( 'NONE', #249980, 1000.000000000000000 ) ;
#100730=ORIENTED_EDGE ( 'NONE', *, *, #58973, .F. ) ;
#100743=DIRECTION ( 'NONE',  ( -1.000000000000000000, -0.000000000000000000, -0.000000000000000000 ) ) ;
#100779=AXIS2_PLACEMENT_3D ( 'NONE', #169818, #12007, #91526 ) ;
#100804=VERTEX_POINT ( 'NONE', #98377 ) ;
#100808=CARTESIAN_POINT ( 'NONE',  ( -18.59999999999999787, 1.340746217944851715, -56.72713749457886223 ) ) ;
#100815=CYLINDRICAL_SURFACE ( 'NONE', #132759, 0.09999999999999939493 ) ;
#100833=ORIENTED_EDGE ( 'NONE', *, *, #66719, .F. ) ;
#100881=DIRECTION ( 'NONE',  ( 0.000000000000000000, 0.000000000000000000, -1.000000000000000000 ) ) ;
#100889=DIRECTION ( 'NONE',  ( -2.578261006436900068E-14, 0.1350103645451904977, -0.9908441862701597991 ) ) ;
#100894=DIRECTION ( 'NONE',  ( 1.000000000000000000, 3.265361837132813093E-16, -0.000000000000000000 ) ) ;
#100903=DIRECTION ( 'NONE',  ( 0.000000000000000000, 0.000000000000000000, -1.000000000000000000 ) ) ;
#100906=DIRECTION ( 'NONE',  ( 0.000000000000000000, 0.000000000000000000, -1.000000000000000000 ) ) ;
#100913=AXIS2_PLACEMENT_3D ( 'NONE', #78086, #57227, #117233 ) ;
#100929=DIRECTION ( 'NONE',  ( 0.000000000000000000, -1.000000000000000000, -0.000000000000000000 ) ) ;
#100937=CARTESIAN_POINT ( 'NONE',  ( 20.94999999999999929, 10.38178547073510316, -106.0078453638842149 ) ) ;
#100964=ORIENTED_EDGE ( 'NONE', *, *, #153591, .T. ) ;
#100973=VERTEX_POINT ( 'NONE', #108704 ) ;
#100988=CARTESIAN_POINT ( 'NONE',  ( -23.25000000000000000, -11.64999999998884483, -97.40000000000004832 ) ) ;
#100997=VECTOR ( 'NONE', #5111, 1000.000000000000000 ) ;
#101021=CARTESIAN_POINT ( 'NONE',  ( -21.52071067811865746, 7.779289321892505882, -88.25000000000005684 ) ) ;
#101024=DIRECTION ( 'NONE',  ( 1.000000000000000000, 0.000000000000000000, 0.000000000000000000 ) ) ;
#101055=CIRCLE ( 'NONE', #30403, 0.09999999999999913125 ) ;
#101064=EDGE_CURVE ( 'NONE', #53620, #199698, #201054, .T. ) ;
#101068=CIRCLE ( 'NONE', #205166, 0.2000000000000057288 ) ;
#101070=CYLINDRICAL_SURFACE ( 'NONE', #82811, 0.09999999999999939493 ) ;
#101106=EDGE_CURVE ( 'NONE', #34181, #33467, #88599, .T. ) ;
#101116=EDGE_CURVE ( 'NONE', #19842, #176730, #230263, .T. ) ;
#101190=ADVANCED_FACE ( 'NONE', ( #124123 ), #163249, .T. ) ;
#101209=DIRECTION ( 'NONE',  ( -1.000000000000000000, 0.000000000000000000, 0.000000000000000000 ) ) ;
#101241=FACE_OUTER_BOUND ( 'NONE', #174234, .T. ) ;
#101295=AXIS2_PLACEMENT_3D ( 'NONE', #131711, #92568, #74345 ) ;
#101320=DIRECTION ( 'NONE',  ( -0.000000000000000000, 1.000000000000000000, 1.734723475976807292E-15 ) ) ;
#101321=CARTESIAN_POINT ( 'NONE',  ( 23.14999999999999503, 11.75000000001116263, -88.35000000000003695 ) ) ;
#101322=AXIS2_PLACEMENT_3D ( 'NONE', #186843, #231113, #185544 ) ;
#101327=DIRECTION ( 'NONE',  ( -1.000000000000000000, -1.836970198721029934E-16, 0.000000000000000000 ) ) ;
#101372=ORIENTED_EDGE ( 'NONE', *, *, #117572, .T. ) ;
#101382=EDGE_LOOP ( 'NONE', ( #120627, #121069, #37763, #257162 ) ) ;
#101410=VERTEX_POINT ( 'NONE', #230932 ) ;
#101455=CARTESIAN_POINT ( 'NONE',  ( 18.54271179734052666, -9.624084290087616012, -107.2409648527002730 ) ) ;
#101480=ORIENTED_EDGE ( 'NONE', *, *, #171061, .T. ) ;
#101516=EDGE_CURVE ( 'NONE', #150821, #258086, #255342, .T. ) ;
#101522=CARTESIAN_POINT ( 'NONE',  ( -22.59066674512245498, 11.75000000001115552, -66.96949587636947854 ) ) ;
#101540=FACE_OUTER_BOUND ( 'NONE', #27477, .T. ) ;
#101571=AXIS2_PLACEMENT_3D ( 'NONE', #47799, #129913, #50363 ) ;
#101638=DIRECTION ( 'NONE',  ( -0.000000000000000000, -1.000000000000000000, -0.000000000000000000 ) ) ;
#101672=VERTEX_POINT ( 'NONE', #142064 ) ;
#101715=EDGE_CURVE ( 'NONE', #96043, #177157, #113925, .T. ) ;
#101752=CARTESIAN_POINT ( 'NONE',  ( 18.59999999999999787, -10.35479209691423996, -94.25654098307380480 ) ) ;
#101766=ORIENTED_EDGE ( 'NONE', *, *, #72571, .T. ) ;
#101790=EDGE_CURVE ( 'NONE', #117385, #91478, #80582, .T. ) ;
#101796=CIRCLE ( 'NONE', #168515, 0.1000000000000004496 ) ;
#101797=ADVANCED_FACE ( 'NONE', ( #110651 ), #64057, .F. ) ;
#101798=CARTESIAN_POINT ( 'NONE',  ( -21.44999999999999929, 7.150000000011155876, -88.15000000000004832 ) ) ;
#101810=DIRECTION ( 'NONE',  ( 0.000000000000000000, 6.308085367182471812E-16, 1.000000000000000000 ) ) ;
#101812=DIRECTION ( 'NONE',  ( 1.000000000000000000, 0.000000000000000000, 0.000000000000000000 ) ) ;
#101853=EDGE_CURVE ( 'NONE', #4064, #195562, #39133, .T. ) ;
#101855=CARTESIAN_POINT ( 'NONE',  ( 20.94999999999999929, 5.400000000011154988, -90.60603087734760663 ) ) ;
#101886=ORIENTED_EDGE ( 'NONE', *, *, #95632, .T. ) ;
#101890=DIRECTION ( 'NONE',  ( -1.000000000000000000, -0.000000000000000000, -0.000000000000000000 ) ) ;
#101896=VECTOR ( 'NONE', #219541, 1000.000000000000000 ) ;
#101943=DIRECTION ( 'NONE',  ( -0.000000000000000000, -0.000000000000000000, 1.000000000000000000 ) ) ;
#101950=EDGE_CURVE ( 'NONE', #82676, #219130, #195352, .T. ) ;
#101964=CARTESIAN_POINT ( 'NONE',  ( -20.85000000000000142, -1.164121893230052995, -108.4148480855716485 ) ) ;
#101976=DIRECTION ( 'NONE',  ( 0.000000000000000000, 0.000000000000000000, -1.000000000000000000 ) ) ;
#102018=AXIS2_PLACEMENT_3D ( 'NONE', #143029, #43950, #203017 ) ;
#102032=EDGE_CURVE ( 'NONE', #129552, #53634, #194062, .T. ) ;
#102055=EDGE_CURVE ( 'NONE', #93742, #50892, #160070, .T. ) ;
#102080=ORIENTED_EDGE ( 'NONE', *, *, #218554, .F. ) ;
#102081=DIRECTION ( 'NONE',  ( 0.000000000000000000, 3.122502256758250246E-14, -1.000000000000000000 ) ) ;
#102086=ORIENTED_EDGE ( 'NONE', *, *, #241751, .F. ) ;
#102090=ORIENTED_EDGE ( 'NONE', *, *, #88815, .T. ) ;
#102103=ADVANCED_FACE ( 'NONE', ( #24409 ), #60933, .F. ) ;
#102110=CARTESIAN_POINT ( 'NONE',  ( -20.85000000000000142, -1.149570369564537842, -108.3159124845020074 ) ) ;
#102135=AXIS2_PLACEMENT_3D ( 'NONE', #147982, #245797, #22919 ) ;
#102139=DIRECTION ( 'NONE',  ( 8.673617379884087537E-15, -0.000000000000000000, 1.000000000000000000 ) ) ;
#102201=CARTESIAN_POINT ( 'NONE',  ( 21.05000000000000071, 6.299230910098045477, -66.90156250000005400 ) ) ;
#102255=CARTESIAN_POINT ( 'NONE',  ( -22.47071067811865319, 7.720074744509219933, -66.90090754529744288 ) ) ;
#102260=CARTESIAN_POINT ( 'NONE',  ( -21.05000000000000071, 11.60000000001115339, -93.57179676972452853 ) ) ;
#102265=EDGE_CURVE ( 'NONE', #254405, #165054, #22549, .T. ) ;
#102267=CIRCLE ( 'NONE', #185515, 11.74999999999999645 ) ;
#102284=CARTESIAN_POINT ( 'NONE',  ( 21.05563370358598263, 10.72423035585766549, -79.18309081596311216 ) ) ;
#102289=DIRECTION ( 'NONE',  ( 0.000000000000000000, 0.000000000000000000, -1.000000000000000000 ) ) ;
#102303=SPHERICAL_SURFACE ( 'NONE', #240564, 0.1000000000000000056 ) ;
#102315=ORIENTED_EDGE ( 'NONE', *, *, #62645, .F. ) ;
#102323=DIRECTION ( 'NONE',  ( -2.952720810173289112E-16, 1.000000000000000000, -0.000000000000000000 ) ) ;
#102331=VERTEX_POINT ( 'NONE', #115467 ) ;
#102332=AXIS2_PLACEMENT_3D ( 'NONE', #67358, #28267, #123480 ) ;
#102352=CARTESIAN_POINT ( 'NONE',  ( -23.25000000000000000, 1.115600667400684642E-11, -100.5000000000000426 ) ) ;
#102355=VECTOR ( 'NONE', #136370, 1000.000000000000000 ) ;
#102359=EDGE_LOOP ( 'NONE', ( #222713, #170269, #11446 ) ) ;
#102362=CARTESIAN_POINT ( 'NONE',  ( -23.25000000000000000, -1.149570369564537842, -108.3159124845020074 ) ) ;
#102379=VERTEX_POINT ( 'NONE', #252396 ) ;
#102387=CARTESIAN_POINT ( 'NONE',  ( 20.85000000000000142, -1.835859311432481045, -112.0044391687985694 ) ) ;
#102454=CARTESIAN_POINT ( 'NONE',  ( 21.05000000000000071, 10.42338541492406279, -74.49205192387015018 ) ) ;
#102471=ORIENTED_EDGE ( 'NONE', *, *, #21088, .F. ) ;
#102489=DIRECTION ( 'NONE',  ( 1.000000000000000000, 7.304098846218134667E-16, -0.000000000000000000 ) ) ;
#102498=CARTESIAN_POINT ( 'NONE',  ( -21.05000000000000071, 1.835341550235567887, -78.65515129256301918 ) ) ;
#102504=ORIENTED_EDGE ( 'NONE', *, *, #131760, .F. ) ;
#102538=EDGE_CURVE ( 'NONE', #39792, #208354, #143517, .T. ) ;
#102549=VECTOR ( 'NONE', #28308, 1000.000000000000000 ) ;
#102581=CARTESIAN_POINT ( 'NONE',  ( -21.53752568617674967, 6.786807874515073280, -66.90102553872934266 ) ) ;
#102602=CARTESIAN_POINT ( 'NONE',  ( -23.25000000000000000, 11.75000000001115552, -93.48519422934610645 ) ) ;
#102617=DIRECTION ( 'NONE',  ( 0.000000000000000000, 0.1575844902526560010, 0.9875055080513781558 ) ) ;
#102652=EDGE_CURVE ( 'NONE', #140921, #208514, #189321, .T. ) ;
#102675=CARTESIAN_POINT ( 'NONE',  ( 18.39999999999999858, -9.682403433465241349, -107.1568433774128408 ) ) ;
#102687=CARTESIAN_POINT ( 'NONE',  ( -18.39999999999999858, -9.519327731081281385, -73.97297637655937308 ) ) ;
#102704=DIRECTION ( 'NONE',  ( 0.000000000000000000, 0.000000000000000000, 1.000000000000000000 ) ) ;
#102720=VERTEX_POINT ( 'NONE', #255595 ) ;
#102729=SPHERICAL_SURFACE ( 'NONE', #157595, 0.1000000000000000056 ) ;
#102731=VECTOR ( 'NONE', #83618, 1000.000000000000000 ) ;
#102760=AXIS2_PLACEMENT_3D ( 'NONE', #42328, #218370, #162291 ) ;
#102763=CARTESIAN_POINT ( 'NONE',  ( 18.49362639424898447, -9.442604367876999305, -107.2644409335118070 ) ) ;
#102775=ORIENTED_EDGE ( 'NONE', *, *, #233308, .T. ) ;
#102793=DIRECTION ( 'NONE',  ( 0.000000000000000000, 0.000000000000000000, 1.000000000000000000 ) ) ;
#102796=CIRCLE ( 'NONE', #248560, 0.3999999999999975797 ) ;
#102812=CIRCLE ( 'NONE', #61143, 11.90000000000000391 ) ;
#102833=VERTEX_POINT ( 'NONE', #97823 ) ;
#102850=ORIENTED_EDGE ( 'NONE', *, *, #77921, .F. ) ;
#102854=CYLINDRICAL_SURFACE ( 'NONE', #83540, 0.09999999999999939493 ) ;
#102886=EDGE_CURVE ( 'NONE', #68571, #49762, #224212, .T. ) ;
#102891=CARTESIAN_POINT ( 'NONE',  ( 20.94999999999999929, 10.47338541492405461, -74.57865446424858646 ) ) ;
#102908=ORIENTED_EDGE ( 'NONE', *, *, #79480, .F. ) ;
#102916=DIRECTION ( 'NONE',  ( 1.296989514748957922E-15, -0.9887567792719341719, 0.1495327102803664099 ) ) ;
#102922=CYLINDRICAL_SURFACE ( 'NONE', #251579, 7.900000000000003908 ) ;
#102942=CARTESIAN_POINT ( 'NONE',  ( -23.15000000000000213, 11.75000000001115552, -93.48519422934610645 ) ) ;
#102949=ORIENTED_EDGE ( 'NONE', *, *, #123914, .F. ) ;
#102952=VERTEX_POINT ( 'NONE', #22192 ) ;
#102961=ADVANCED_FACE ( 'NONE', ( #242496 ), #114486, .T. ) ;
#102964=DIRECTION ( 'NONE',  ( 1.000000000000000000, 0.000000000000000000, 0.000000000000000000 ) ) ;
#102969=CIRCLE ( 'NONE', #132204, 0.6000000000000015321 ) ;
#103001=EDGE_LOOP ( 'NONE', ( #37592, #64364, #35237, #207592 ) ) ;
#103025=CARTESIAN_POINT ( 'NONE',  ( -18.59999999999999787, 6.982009704867601307, -104.1961521182563359 ) ) ;
#103036=ORIENTED_EDGE ( 'NONE', *, *, #175401, .T. ) ;
#103059=CARTESIAN_POINT ( 'NONE',  ( 23.14999999999999858, 1.115600667400684642E-11, -67.00000000000004263 ) ) ;
#103060=ORIENTED_EDGE ( 'NONE', *, *, #172455, .F. ) ;
#103093=CIRCLE ( 'NONE', #119906, 0.1000000000000028644 ) ;
#103125=CARTESIAN_POINT ( 'NONE',  ( 23.25000000000000000, -8.999999999988844479, -76.89396912265249284 ) ) ;
#103132=CARTESIAN_POINT ( 'NONE',  ( -20.94999675878240808, 10.29307482169070909, -105.9586421466940749 ) ) ;
#103161=CARTESIAN_POINT ( 'NONE',  ( -20.54999999999999716, -9.499999999988848032, -76.89396912265249284 ) ) ;
#103188=TOROIDAL_SURFACE ( 'NONE', #49036, 0.2000000000000000111, 0.1000000000000000056 ) ;
#103205=CARTESIAN_POINT ( 'NONE',  ( 21.05000000000000071, -12.41227409413852811, -97.50000000000004263 ) ) ;
#103207=DIRECTION ( 'NONE',  ( 0.000000000000000000, -0.4999999999999949485, 0.8660254037844415942 ) ) ;
#103227=EDGE_CURVE ( 'NONE', #111464, #96293, #192809, .T. ) ;
#103235=CARTESIAN_POINT ( 'NONE',  ( -21.05000000000000071, 1.835341550235567887, -78.65515129256301918 ) ) ;
#103281=AXIS2_PLACEMENT_3D ( 'NONE', #100624, #60241, #115094 ) ;
#103306=FACE_OUTER_BOUND ( 'NONE', #16336, .T. ) ;
#103321=CARTESIAN_POINT ( 'NONE',  ( -20.94999999999999929, 1.115600667400684642E-11, -100.5000000000000426 ) ) ;
#103336=EDGE_LOOP ( 'NONE', ( #100964, #170149, #104579, #224802 ) ) ;
#103338=LINE ( 'NONE', #239022, #65347 ) ;
#103372=VERTEX_POINT ( 'NONE', #25712 ) ;
#103387=CIRCLE ( 'NONE', #65810, 0.1000000000000028644 ) ;
#103416=EDGE_CURVE ( 'NONE', #171778, #142483, #225165, .T. ) ;
#103419=( BOUNDED_SURFACE ( )  B_SPLINE_SURFACE ( 3, 2, ( 
 ( #80692, #44169, #141963 ),
 ( #23342, #143245, #123703 ),
 ( #118579, #61149, #101522 ),
 ( #239801, #140684, #258014 ) ),
 .UNSPECIFIED., .F., .F., .F. ) 
 B_SPLINE_SURFACE_WITH_KNOTS ( ( 4, 4 ),
 ( 3, 3 ),
 ( 0.0006461284895273902403, 0.0007503702773986321546 ),
 ( 0.000000000000000000, 1.000000000000000000 ),
 .UNSPECIFIED. ) 
 GEOMETRIC_REPRESENTATION_ITEM ( )  RATIONAL_B_SPLINE_SURFACE ( (
 ( 1.000000000000000000, 0.7071067811865475727, 1.000000000000000000),
 ( 1.000000000000000000, 0.7076476444648814867, 1.000000000000000000),
 ( 1.000000000000000000, 0.7075727925191799272, 1.000000000000000000),
 ( 1.000000000000000000, 0.7071067811865475727, 1.000000000000000000) ) ) 
 REPRESENTATION_ITEM ( '' )  SURFACE ( )  );
#103424=LINE ( 'NONE', #44768, #216534 ) ;
#103439=FACE_OUTER_BOUND ( 'NONE', #142967, .T. ) ;
#103464=CARTESIAN_POINT ( 'NONE',  ( -18.59999999999999787, -1.162701749926853712, -75.10000000000003695 ) ) ;
#103470=CARTESIAN_POINT ( 'NONE',  ( -18.59999999999999787, 1.637172712981537659, -78.58215336547205254 ) ) ;
#103497=EDGE_CURVE ( 'NONE', #138550, #6498, #170410, .T. ) ;
#103541=CIRCLE ( 'NONE', #145061, 0.09999999999999971412 ) ;
#103557=ORIENTED_EDGE ( 'NONE', *, *, #99180, .T. ) ;
#103567=FACE_OUTER_BOUND ( 'NONE', #60095, .T. ) ;
#103573=DIRECTION ( 'NONE',  ( 1.000000000000000000, -0.000000000000000000, -0.000000000000000000 ) ) ;
#103587=LINE ( 'NONE', #46199, #201425 ) ;
#103625=EDGE_CURVE ( 'NONE', #129928, #192087, #112955, .T. ) ;
#103655=AXIS2_PLACEMENT_3D ( 'NONE', #222755, #81936, #23319 ) ;
#103674=DIRECTION ( 'NONE',  ( 0.000000000000000000, 0.008583690987124697677, -0.9999631594459055250 ) ) ;
#103715=CARTESIAN_POINT ( 'NONE',  ( 18.59999999999999432, 5.699452464332755319, -54.45772604343021328 ) ) ;
#103807=ORIENTED_EDGE ( 'NONE', *, *, #250068, .T. ) ;
#103816=CARTESIAN_POINT ( 'NONE',  ( -18.59999999999999787, 11.65000000001115232, -100.5000000000000426 ) ) ;
#103819=CIRCLE ( 'NONE', #149089, 0.09999999999999693856 ) ;
#103820=ADVANCED_FACE ( 'NONE', ( #29297 ), #10975, .T. ) ;
#103874=DIRECTION ( 'NONE',  ( -1.000000000000000000, 7.304098846218135653E-16, -4.607487905232624742E-31 ) ) ;
#103888=CARTESIAN_POINT ( 'NONE',  ( -22.39999999999999858, 1.115600667400684642E-11, -55.35042919245524473 ) ) ;
#103898=EDGE_CURVE ( 'NONE', #142573, #247975, #56186, .T. ) ;
#103911=ORIENTED_EDGE ( 'NONE', *, *, #28471, .T. ) ;
#103932=TOROIDAL_SURFACE ( 'NONE', #33104, 11.70000000000000107, 0.1000000000000000056 ) ;
#103988=PLANE ( 'NONE',  #44373 ) ;
#104045=CARTESIAN_POINT ( 'NONE',  ( 18.49999999999999645, -9.480686695267818820, -107.4411151687579036 ) ) ;
#104054=CARTESIAN_POINT ( 'NONE',  ( -21.40925344232282512, 6.658518859401606704, -66.90104981138040330 ) ) ;
#104067=DIRECTION ( 'NONE',  ( 0.000000000000000000, 0.8660254037844309360, -0.5000000000000134337 ) ) ;
#104072=ORIENTED_EDGE ( 'NONE', *, *, #244060, .F. ) ;
#104099=VERTEX_POINT ( 'NONE', #66176 ) ;
#104102=EDGE_CURVE ( 'NONE', #154701, #24665, #43730, .T. ) ;
#104127=CARTESIAN_POINT ( 'NONE',  ( 22.39999999999999503, 7.790779598384535376, -67.00000000000004263 ) ) ;
#104152=VERTEX_POINT ( 'NONE', #50438 ) ;
#104163=ORIENTED_EDGE ( 'NONE', *, *, #4722, .F. ) ;
#104165=( BOUNDED_SURFACE ( )  B_SPLINE_SURFACE ( 3, 2, ( 
 ( #173629, #253094, #74518 ),
 ( #54890, #208847, #198262 ),
 ( #75768, #219099, #59 ),
 ( #256908, #120049, #57458 ),
 ( #95319, #78307, #37936 ),
 ( #155326, #217807, #58729 ) ),
 .UNSPECIFIED., .F., .F., .F. ) 
 B_SPLINE_SURFACE_WITH_KNOTS ( ( 4, 2, 4 ),
 ( 3, 3 ),
 ( 0.0001300404313046639351, 0.0003183318589266644245, 0.0005066232865486648869 ),
 ( 0.000000000000000000, 1.000000000000000000 ),
 .UNSPECIFIED. ) 
 GEOMETRIC_REPRESENTATION_ITEM ( )  RATIONAL_B_SPLINE_SURFACE ( (
 ( 1.000000000000000000, 0.7071067811865475727, 1.000000000000000000),
 ( 1.000000000000000000, 0.7625113560541101343, 1.000000000000000000),
 ( 1.000000000000000000, 0.8126073484687262871, 1.000000000000000000),
 ( 1.000000000000000000, 0.8923049332733591354, 1.000000000000000000),
 ( 1.000000000000000000, 0.9231914937768681551, 1.000000000000000000),
 ( 1.000000000000000000, 0.9238795325112909573, 1.000000000000000000) ) ) 
 REPRESENTATION_ITEM ( '' )  SURFACE ( )  );
#104174=EDGE_LOOP ( 'NONE', ( #204908, #198324, #106377, #154078 ) ) ;
#104179=ORIENTED_EDGE ( 'NONE', *, *, #33667, .F. ) ;
#104187=DIRECTION ( 'NONE',  ( 1.000000000000000000, -0.000000000000000000, -0.000000000000000000 ) ) ;
#104213=ORIENTED_EDGE ( 'NONE', *, *, #180665, .F. ) ;
#104226=CARTESIAN_POINT ( 'NONE',  ( -18.59999999999999787, 3.912899247244609580, -78.48182297301100618 ) ) ;
#104246=AXIS2_PLACEMENT_3D ( 'NONE', #40841, #119069, #78631 ) ;
#104252=ORIENTED_EDGE ( 'NONE', *, *, #161579, .F. ) ;
#104259=( BOUNDED_SURFACE ( )  B_SPLINE_SURFACE ( 3, 2, ( 
 ( #166998, #61438, #116925 ),
 ( #96059, #247775, #190394 ),
 ( #226928, #151262, #129119 ),
 ( #216003, #109534, #175631 ),
 ( #209953, #31338, #131680 ),
 ( #207384, #36120, #115642 ) ),
 .UNSPECIFIED., .F., .F., .F. ) 
 B_SPLINE_SURFACE_WITH_KNOTS ( ( 4, 2, 4 ),
 ( 3, 3 ),
 ( 4.712388980384689674, 5.497787143782137953, 6.283185307179586232 ),
 ( 0.000000000000000000, 1.000000000000000000 ),
 .UNSPECIFIED. ) 
 GEOMETRIC_REPRESENTATION_ITEM ( )  RATIONAL_B_SPLINE_SURFACE ( (
 ( 1.000000000000000000, 0.7071067811865536790, 1.000000000000000000),
 ( 1.000000000000000000, 0.7727932973486136836, 1.000000000000000000),
 ( 1.000000000000000000, 0.8282379607656571441, 1.000000000000000000),
 ( 1.000000000000000000, 0.9038128468032184948, 1.000000000000000000),
 ( 1.000000000000000000, 0.9240297172249232194, 1.000000000000000000),
 ( 1.000000000000000000, 0.9238795325112914014, 1.000000000000000000) ) ) 
 REPRESENTATION_ITEM ( '' )  SURFACE ( )  );
#104311=ADVANCED_FACE ( 'NONE', ( #180691 ), #99824, .F. ) ;
#104321=EDGE_LOOP ( 'NONE', ( #173909, #186113, #112568, #14986, #21078 ) ) ;
#104322=VECTOR ( 'NONE', #228311, 999.9999999999998863 ) ;
#104327=EDGE_CURVE ( 'NONE', #152504, #165054, #235510, .T. ) ;
#104380=ORIENTED_EDGE ( 'NONE', *, *, #47147, .F. ) ;
#104393=VECTOR ( 'NONE', #164588, 999.9999999999998863 ) ;
#104411=EDGE_CURVE ( 'NONE', #199698, #217161, #110547, .T. ) ;
#104428=CARTESIAN_POINT ( 'NONE',  ( -21.13422380239058640, 1.115662971600936638E-11, -60.50667348519461797 ) ) ;
#104438=EDGE_CURVE ( 'NONE', #140891, #95981, #10611, .T. ) ;
#104473=CARTESIAN_POINT ( 'NONE',  ( 20.94999999999999929, -9.399999999988844834, -90.60603087734760663 ) ) ;
#104533=ORIENTED_EDGE ( 'NONE', *, *, #12557, .T. ) ;
#104541=CARTESIAN_POINT ( 'NONE',  ( 20.94999999999999574, 14.00000000001115730, -72.42709253038259476 ) ) ;
#104544=EDGE_CURVE ( 'NONE', #4905, #123054, #43910, .T. ) ;
#104546=EDGE_CURVE ( 'NONE', #217161, #192398, #93787, .T. ) ;
#104563=DIRECTION ( 'NONE',  ( 2.715809747126116508E-16, -1.000000000000000000, -2.172647797700893206E-15 ) ) ;
#104567=VECTOR ( 'NONE', #216086, 1000.000000000000000 ) ;
#104575=ORIENTED_EDGE ( 'NONE', *, *, #191410, .T. ) ;
#104579=ORIENTED_EDGE ( 'NONE', *, *, #188421, .F. ) ;
#104628=EDGE_CURVE ( 'NONE', #188126, #200601, #441, .T. ) ;
#104679=CARTESIAN_POINT ( 'NONE',  ( 22.50000000000000000, 7.750000000011162626, -66.90000000000004832 ) ) ;
#104696=DIRECTION ( 'NONE',  ( 0.000000000000000000, 0.000000000000000000, -1.000000000000000000 ) ) ;
#104727=EDGE_CURVE ( 'NONE', #206992, #45948, #256412, .T. ) ;
#104739=DIRECTION ( 'NONE',  ( -2.342056488767301376E-15, -0.1350103645451904977, 0.9908441862701596881 ) ) ;
#104768=CIRCLE ( 'NONE', #75779, 0.09999999999999939493 ) ;
#104770=CARTESIAN_POINT ( 'NONE',  ( 21.05000000000000071, 6.257814610487288043, -66.90220970869125949 ) ) ;
#104852=ADVANCED_FACE ( 'NONE', ( #143809 ), #188087, .T. ) ;
#104853=CARTESIAN_POINT ( 'NONE',  ( -23.15000000000000213, 5.900000000011162093, -90.28090023534366537 ) ) ;
#104861=VERTEX_POINT ( 'NONE', #248055 ) ;
#104897=CIRCLE ( 'NONE', #117422, 0.1000000000000028644 ) ;
#104906=CARTESIAN_POINT ( 'NONE',  ( -21.09107601085569428, 6.363877975371215356, -66.96069283528275662 ) ) ;
#105016=EDGE_CURVE ( 'NONE', #38637, #4064, #176249, .T. ) ;
#105057=CARTESIAN_POINT ( 'NONE',  ( 20.95132126680579887, 10.48994987015794322, -74.57032453843456210 ) ) ;
#105074=CARTESIAN_POINT ( 'NONE',  ( 21.07094088545303734, 6.320167221927647461, -66.90110629744782500 ) ) ;
#105082=CIRCLE ( 'NONE', #9260, 0.1000000000000001027 ) ;
#105133=CARTESIAN_POINT ( 'NONE',  ( -21.07094088545304089, 6.320167221927643020, -66.90110629744782500 ) ) ;
#105137=CARTESIAN_POINT ( 'NONE',  ( 18.59999999999999076, 6.550000000011156231, -88.15000000000004832 ) ) ;
#105182=CARTESIAN_POINT ( 'NONE',  ( -18.59999999999999787, -9.321008403350132809, -74.23593824907793248 ) ) ;
#105200=EDGE_LOOP ( 'NONE', ( #203511, #166980, #245327, #42859, #222233 ) ) ;
#105223=ADVANCED_FACE ( 'NONE', ( #46962 ), #206058, .T. ) ;
#105234=CIRCLE ( 'NONE', #226055, 0.2000000000000057288 ) ;
#105237=EDGE_CURVE ( 'NONE', #152197, #115296, #132955, .T. ) ;
#105245=ORIENTED_EDGE ( 'NONE', *, *, #101116, .F. ) ;
#105267=ORIENTED_EDGE ( 'NONE', *, *, #181183, .T. ) ;
#105276=AXIS2_PLACEMENT_3D ( 'NONE', #42274, #63098, #181781 ) ;
#105333=AXIS2_PLACEMENT_3D ( 'NONE', #242754, #101943, #199817 ) ;
#105385=CIRCLE ( 'NONE', #163687, 0.1000000000000028644 ) ;
#105390=DIRECTION ( 'NONE',  ( 1.000000000000000000, 0.000000000000000000, 0.000000000000000000 ) ) ;
#105392=CARTESIAN_POINT ( 'NONE',  ( 22.16821283564876666, 7.558973340791918183, -67.00000000000004263 ) ) ;
#105408=ORIENTED_EDGE ( 'NONE', *, *, #249567, .F. ) ;
#105432=AXIS2_PLACEMENT_3D ( 'NONE', #70537, #71805, #49653 ) ;
#105435=AXIS2_PLACEMENT_3D ( 'NONE', #51377, #189649, #11006 ) ;
#105451=DIRECTION ( 'NONE',  ( 1.000000000000000000, 0.000000000000000000, 0.000000000000000000 ) ) ;
#105452=FACE_OUTER_BOUND ( 'NONE', #25945, .T. ) ;
#105475=ORIENTED_EDGE ( 'NONE', *, *, #95632, .F. ) ;
#105484=AXIS2_PLACEMENT_3D ( 'NONE', #219816, #114302, #37353 ) ;
#105506=CARTESIAN_POINT ( 'NONE',  ( 19.92426406871192412, 11.75000000001116085, -91.85000000000003695 ) ) ;
#105509=EDGE_CURVE ( 'NONE', #109568, #84452, #240111, .T. ) ;
#105581=CIRCLE ( 'NONE', #118078, 0.1000000000000028644 ) ;
#105604=CARTESIAN_POINT ( 'NONE',  ( -18.44232395689904536, -9.552282557039346145, -107.3422519848068362 ) ) ;
#105605=ORIENTED_EDGE ( 'NONE', *, *, #55155, .F. ) ;
#105628=CIRCLE ( 'NONE', #101322, 0.09999999999999939493 ) ;
#105630=CARTESIAN_POINT ( 'NONE',  ( -23.15000000000000213, 11.65000000001115588, -88.25000000000005684 ) ) ;
#105655=AXIS2_PLACEMENT_3D ( 'NONE', #241943, #215950, #85402 ) ;
#105662=CARTESIAN_POINT ( 'NONE',  ( -21.52071067811865746, 7.779289321892505882, -88.15000000000004832 ) ) ;
#105695=DIRECTION ( 'NONE',  ( 1.000000000000000000, 0.000000000000000000, 0.000000000000000000 ) ) ;
#105708=CARTESIAN_POINT ( 'NONE',  ( -21.07954763557493294, 0.06587591862955510802, -60.67070900996179716 ) ) ;
#105711=CARTESIAN_POINT ( 'NONE',  ( -23.15000000000000213, 2.000000000011154189, -87.87537807723795424 ) ) ;
#105719=VECTOR ( 'NONE', #154943, 1000.000000000000000 ) ;
#105750=CARTESIAN_POINT ( 'NONE',  ( 20.04142135623730070, 11.75000000001115907, -88.35000000000003695 ) ) ;
#105754=CARTESIAN_POINT ( 'NONE',  ( 20.94999999999999929, -1.349153571964892606, -108.2874973355899328 ) ) ;
#105777=VERTEX_POINT ( 'NONE', #119167 ) ;
#105797=ORIENTED_EDGE ( 'NONE', *, *, #234714, .F. ) ;
#105824=ORIENTED_EDGE ( 'NONE', *, *, #208768, .T. ) ;
#105897=ORIENTED_EDGE ( 'NONE', *, *, #172415, .T. ) ;
#105903=CYLINDRICAL_SURFACE ( 'NONE', #93213, 0.09999999999999939493 ) ;
#105905=CARTESIAN_POINT ( 'NONE',  ( -21.05439746398122836, 11.75000000001115197, -73.98991648748463490 ) ) ;
#105912=CIRCLE ( 'NONE', #64249, 0.09999999999999971412 ) ;
#105949=ORIENTED_EDGE ( 'NONE', *, *, #111502, .F. ) ;
#105971=CARTESIAN_POINT ( 'NONE',  ( -21.05000000000000071, -0.09999999998884338825, -60.45934304829880546 ) ) ;
#105972=CARTESIAN_POINT ( 'NONE',  ( 18.59999999999999076, 1.250000000011167511, -75.00000000000004263 ) ) ;
#105999=DIRECTION ( 'NONE',  ( 0.000000000000000000, 2.664535259100343354E-15, -1.000000000000000000 ) ) ;
#106004=LINE ( 'NONE', #58223, #240216 ) ;
#106040=DIRECTION ( 'NONE',  ( 1.000000000000000000, 0.000000000000000000, 0.000000000000000000 ) ) ;
#106043=CIRCLE ( 'NONE', #31107, 0.1000000000000028644 ) ;
#106049=CARTESIAN_POINT ( 'NONE',  ( 21.12400222705975494, 8.778511907088235589, -79.25000000000004263 ) ) ;
#106062=CARTESIAN_POINT ( 'NONE',  ( 21.05000000000000071, 6.477552182504599187, -67.09999996529958821 ) ) ;
#106088=FACE_OUTER_BOUND ( 'NONE', #33567, .T. ) ;
#106090=EDGE_LOOP ( 'NONE', ( #70999, #122113, #83282, #255599 ) ) ;
#106110=DIRECTION ( 'NONE',  ( 0.000000000000000000, 0.000000000000000000, 1.000000000000000000 ) ) ;
#106135=CARTESIAN_POINT ( 'NONE',  ( 22.60000000000000142, 1.115600667400684642E-11, -67.00000000000004263 ) ) ;
#106144=VECTOR ( 'NONE', #213637, 1000.000000000000000 ) ;
#106163=EDGE_CURVE ( 'NONE', #208514, #187772, #115550, .T. ) ;
#106186=CARTESIAN_POINT ( 'NONE',  ( -21.05000000000000071, 1.115600667400684642E-11, -74.90000000000004832 ) ) ;
#106193=CARTESIAN_POINT ( 'NONE',  ( 20.94999999999999929, 1.115650877919449413E-11, -96.40000000000003411 ) ) ;
#106198=ADVANCED_FACE ( 'NONE', ( #99275 ), #1469, .F. ) ;
#106203=FACE_OUTER_BOUND ( 'NONE', #257719, .T. ) ;
#106238=CARTESIAN_POINT ( 'NONE',  ( -20.94999999999999929, -1.261786168553869603, -75.08649896354552311 ) ) ;
#106252=FACE_OUTER_BOUND ( 'NONE', #37129, .T. ) ;
#106254=EDGE_CURVE ( 'NONE', #231898, #208732, #65670, .T. ) ;
#106256=ORIENTED_EDGE ( 'NONE', *, *, #135206, .T. ) ;
#106270=FACE_OUTER_BOUND ( 'NONE', #95959, .T. ) ;
#106312=AXIS2_PLACEMENT_3D ( 'NONE', #195075, #192485, #94656 ) ;
#106331=EDGE_CURVE ( 'NONE', #223322, #183920, #203536, .T. ) ;
#106341=ORIENTED_EDGE ( 'NONE', *, *, #150074, .T. ) ;
#106370=AXIS2_PLACEMENT_3D ( 'NONE', #51873, #68915, #128879 ) ;
#106371=CARTESIAN_POINT ( 'NONE',  ( -18.59999999999999787, -9.499999999988842703, -79.15000000000004832 ) ) ;
#106375=VERTEX_POINT ( 'NONE', #226946 ) ;
#106377=ORIENTED_EDGE ( 'NONE', *, *, #39429, .F. ) ;
#106378=CARTESIAN_POINT ( 'NONE',  ( 22.00411653962179059, 7.253442868381116959, -66.90096189419941197 ) ) ;
#106404=ADVANCED_FACE ( 'NONE', ( #9182 ), #74089, .T. ) ;
#106440=AXIS2_PLACEMENT_3D ( 'NONE', #43552, #147789, #162231 ) ;
#106463=DIRECTION ( 'NONE',  ( -1.000000000000000000, -0.000000000000000000, 0.000000000000000000 ) ) ;
#106483=ORIENTED_EDGE ( 'NONE', *, *, #233274, .F. ) ;
#106498=ORIENTED_EDGE ( 'NONE', *, *, #237462, .F. ) ;
#106515=ORIENTED_EDGE ( 'NONE', *, *, #204477, .F. ) ;
#106519=TOROIDAL_SURFACE ( 'NONE', #69171, 0.4000000000000009104, 0.1000000000000000056 ) ;
#106526=ORIENTED_EDGE ( 'NONE', *, *, #157099, .T. ) ;
#106567=DIRECTION ( 'NONE',  ( -0.000000000000000000, -0.000000000000000000, 1.000000000000000000 ) ) ;
#106589=CIRCLE ( 'NONE', #235785, 2.000000000000001776 ) ;
#106603=ORIENTED_EDGE ( 'NONE', *, *, #33190, .T. ) ;
#106626=FACE_OUTER_BOUND ( 'NONE', #65412, .T. ) ;
#106651=DIRECTION ( 'NONE',  ( -1.836970198721029934E-16, 1.000000000000000000, 0.000000000000000000 ) ) ;
#106653=ORIENTED_EDGE ( 'NONE', *, *, #32149, .T. ) ;
#106673=CARTESIAN_POINT ( 'NONE',  ( 20.95512820512820440, 8.876151316299271343, -79.15000000000004832 ) ) ;
#106683=CARTESIAN_POINT ( 'NONE',  ( 23.14999999999999858, 5.000000000011153745, -88.09473398108696074 ) ) ;
#106695=AXIS2_PLACEMENT_3D ( 'NONE', #143123, #243526, #223950 ) ;
#106699=CARTESIAN_POINT ( 'NONE',  ( -23.15000000000000213, 2.000000000011154189, -87.27537807723794572 ) ) ;
#106717=VERTEX_POINT ( 'NONE', #186237 ) ;
#106737=ADVANCED_FACE ( 'NONE', ( #149696 ), #257689, .T. ) ;
#106748=EDGE_CURVE ( 'NONE', #243244, #206950, #61757, .T. ) ;
#106750=ORIENTED_EDGE ( 'NONE', *, *, #191884, .T. ) ;
#106768=DIRECTION ( 'NONE',  ( -0.000000000000000000, -0.000000000000000000, 1.000000000000000000 ) ) ;
#106814=LINE ( 'NONE', #69010, #203160 ) ;
#106877=ORIENTED_EDGE ( 'NONE', *, *, #184251, .F. ) ;
#106890=DIRECTION ( 'NONE',  ( 0.000000000000000000, -0.8660254037844459241, -0.4999999999999873990 ) ) ;
#106903=ORIENTED_EDGE ( 'NONE', *, *, #41242, .F. ) ;
#106908=CARTESIAN_POINT ( 'NONE',  ( -18.40000000000000213, -9.499999999988851584, -107.1001893912220879 ) ) ;
#106930=ORIENTED_EDGE ( 'NONE', *, *, #22280, .T. ) ;
#106936=FACE_OUTER_BOUND ( 'NONE', #181085, .T. ) ;
#106945=ORIENTED_EDGE ( 'NONE', *, *, #47341, .T. ) ;
#106974=VECTOR ( 'NONE', #77506, 1000.000000000000000 ) ;
#106987=CARTESIAN_POINT ( 'NONE',  ( 20.85000000000000142, 11.65000000001115943, -100.5000000000000426 ) ) ;
#107012=EDGE_CURVE ( 'NONE', #252230, #197089, #53576, .T. ) ;
#107013=TOROIDAL_SURFACE ( 'NONE', #119502, 11.65000000000000036, 0.1000000000000000056 ) ;
#107028=DIRECTION ( 'NONE',  ( 0.000000000000000000, -0.1350103645451904977, -0.9908441862701596881 ) ) ;
#107034=EDGE_CURVE ( 'NONE', #144450, #76379, #203426, .T. ) ;
#107075=DIRECTION ( 'NONE',  ( 0.000000000000000000, 0.000000000000000000, -1.000000000000000000 ) ) ;
#107086=DIRECTION ( 'NONE',  ( -1.000000000000000000, -0.000000000000000000, -0.000000000000000000 ) ) ;
#107090=DIRECTION ( 'NONE',  ( 0.000000000000000000, 0.000000000000000000, 1.000000000000000000 ) ) ;
#107092=DIRECTION ( 'NONE',  ( -0.000000000000000000, 0.000000000000000000, 1.000000000000000000 ) ) ;
#107116=CARTESIAN_POINT ( 'NONE',  ( -18.50000000000000000, 11.75000000001115197, -67.10000000000005116 ) ) ;
#107148=LINE ( 'NONE', #122881, #117356 ) ;
#107192=DIRECTION ( 'NONE',  ( 0.000000000000000000, 0.000000000000000000, -1.000000000000000000 ) ) ;
#107197=DIRECTION ( 'NONE',  ( 0.000000000000000000, 1.000000000000000000, 0.000000000000000000 ) ) ;
#107208=DIRECTION ( 'NONE',  ( -0.000000000000000000, 0.000000000000000000, 1.000000000000000000 ) ) ;
#107212=CARTESIAN_POINT ( 'NONE',  ( -21.00250684356852560, 11.75000000001115197, -74.01480576875988504 ) ) ;
#107223=EDGE_LOOP ( 'NONE', ( #149944, #146746 ) ) ;
#107249=ORIENTED_EDGE ( 'NONE', *, *, #161379, .F. ) ;
#107258=CIRCLE ( 'NONE', #248931, 0.1000000000000053069 ) ;
#107299=PLANE ( 'NONE',  #224444 ) ;
#107314=ORIENTED_EDGE ( 'NONE', *, *, #136699, .T. ) ;
#107328=ORIENTED_EDGE ( 'NONE', *, *, #250035, .T. ) ;
#107329=ORIENTED_EDGE ( 'NONE', *, *, #133658, .T. ) ;
#107331=EDGE_LOOP ( 'NONE', ( #42329, #206335, #234973, #80293 ) ) ;
#107347=EDGE_CURVE ( 'NONE', #256436, #236070, #223126, .T. ) ;
#107364=CIRCLE ( 'NONE', #161567, 0.09999999999999939493 ) ;
#107399=DIRECTION ( 'NONE',  ( 1.000000000000000000, 0.000000000000000000, -0.000000000000000000 ) ) ;
#107424=EDGE_CURVE ( 'NONE', #245368, #201917, #238271, .T. ) ;
#107434=CARTESIAN_POINT ( 'NONE',  ( 20.94788355080264353, 10.30207779525983014, -105.9895520716782897 ) ) ;
#107468=VECTOR ( 'NONE', #27854, 1000.000000000000000 ) ;
#107488=ORIENTED_EDGE ( 'NONE', *, *, #21088, .T. ) ;
#107496=EDGE_LOOP ( 'NONE', ( #67599, #200954, #119386, #225022 ) ) ;
#107509=ORIENTED_EDGE ( 'NONE', *, *, #232525, .T. ) ;
#107517=EDGE_LOOP ( 'NONE', ( #220622, #58532, #53392, #106653 ) ) ;
#107526=ORIENTED_EDGE ( 'NONE', *, *, #181284, .T. ) ;
#107543=CIRCLE ( 'NONE', #253292, 0.09999999999999939493 ) ;
#107584=CIRCLE ( 'NONE', #253339, 0.1000000000000028644 ) ;
#107587=AXIS2_PLACEMENT_3D ( 'NONE', #77102, #118816, #156679 ) ;
#107607=DIRECTION ( 'NONE',  ( 0.000000000000000000, -0.000000000000000000, 1.000000000000000000 ) ) ;
#107610=EDGE_CURVE ( 'NONE', #217530, #96043, #162817, .T. ) ;
#107623=CARTESIAN_POINT ( 'NONE',  ( 18.49999999999999289, 10.49142135624846439, -91.85000000000005116 ) ) ;
#107624=AXIS2_PLACEMENT_3D ( 'NONE', #61243, #160373, #45531 ) ;
#107639=DIRECTION ( 'NONE',  ( -1.000000000000000000, 0.000000000000000000, 0.000000000000000000 ) ) ;
#107648=CIRCLE ( 'NONE', #236643, 0.09999999999999939493 ) ;
#107650=ORIENTED_EDGE ( 'NONE', *, *, #34328, .F. ) ;
#107661=CARTESIAN_POINT ( 'NONE',  ( 20.21567752745019320, 10.19811410124265905, -74.88262034765169517 ) ) ;
#107688=DIRECTION ( 'NONE',  ( -0.000000000000000000, 0.8660254037844383745, -0.5000000000000003331 ) ) ;
#107716=AXIS2_PLACEMENT_3D ( 'NONE', #6924, #40951, #200001 ) ;
#107717=ORIENTED_EDGE ( 'NONE', *, *, #60547, .F. ) ;
#107733=CARTESIAN_POINT ( 'NONE',  ( -20.54999999999999716, 2.400000000011155432, -80.22462192276213955 ) ) ;
#107734=ORIENTED_EDGE ( 'NONE', *, *, #197409, .F. ) ;
#107739=CARTESIAN_POINT ( 'NONE',  ( 21.05281448260627641, 8.776010158548784190, -79.17355791181147140 ) ) ;
#107747=CARTESIAN_POINT ( 'NONE',  ( -18.39999999999999858, -9.599999999988844124, -74.03206939669971121 ) ) ;
#107764=CARTESIAN_POINT ( 'NONE',  ( -21.05000000000000071, -1.835341550213255957, -78.65515129256301918 ) ) ;
#107791=DIRECTION ( 'NONE',  ( 0.000000000000000000, 0.000000000000000000, -1.000000000000000000 ) ) ;
#107830=AXIS2_PLACEMENT_3D ( 'NONE', #124246, #158265, #119102 ) ;
#107838=DIRECTION ( 'NONE',  ( -1.000000000000000000, 0.000000000000000000, 0.000000000000000000 ) ) ;
#107862=FACE_OUTER_BOUND ( 'NONE', #188095, .T. ) ;
#107872=DIRECTION ( 'NONE',  ( 0.000000000000000000, 1.000000000000000000, -0.000000000000000000 ) ) ;
#107878=ORIENTED_EDGE ( 'NONE', *, *, #101853, .T. ) ;
#107881=ORIENTED_EDGE ( 'NONE', *, *, #87007, .T. ) ;
#107883=FACE_OUTER_BOUND ( 'NONE', #180133, .T. ) ;
#107908=ORIENTED_EDGE ( 'NONE', *, *, #193284, .T. ) ;
#107937=ORIENTED_EDGE ( 'NONE', *, *, #106163, .T. ) ;
#107963=EDGE_CURVE ( 'NONE', #10085, #174644, #244235, .T. ) ;
#107978=DIRECTION ( 'NONE',  ( -1.000000000000000000, 0.000000000000000000, 0.000000000000000000 ) ) ;
#107993=DIRECTION ( 'NONE',  ( 0.000000000000000000, -1.000000000000000000, 2.775557561562884094E-14 ) ) ;
#108001=ORIENTED_EDGE ( 'NONE', *, *, #255197, .F. ) ;
#108016=DIRECTION ( 'NONE',  ( 1.000000000000000000, 0.000000000000000000, 0.000000000000000000 ) ) ;
#108032=CIRCLE ( 'NONE', #253744, 0.1000000000000010186 ) ;
#108041=LINE ( 'NONE', #145861, #112546 ) ;
#108058=ORIENTED_EDGE ( 'NONE', *, *, #2840, .F. ) ;
#108060=CARTESIAN_POINT ( 'NONE',  ( 20.95429693346636313, 10.54330487990693044, -74.56088253831309487 ) ) ;
#108067=DIRECTION ( 'NONE',  ( -0.000000000000000000, 0.000000000000000000, 1.000000000000000000 ) ) ;
#108074=DIRECTION ( 'NONE',  ( -0.000000000000000000, 3.469446951953635015E-14, 1.000000000000000000 ) ) ;
#108075=TOROIDAL_SURFACE ( 'NONE', #45704, 0.6000000000000017542, 0.1000000000000000056 ) ;
#108123=CARTESIAN_POINT ( 'NONE',  ( -21.05000000000000071, 11.75000000001115552, -93.48519422934610645 ) ) ;
#108124=DIRECTION ( 'NONE',  ( -1.000000000000000000, 0.000000000000000000, 0.000000000000000000 ) ) ;
#108148=DIRECTION ( 'NONE',  ( 0.000000000000000000, -1.000000000000000000, 0.000000000000000000 ) ) ;
#108173=AXIS2_PLACEMENT_3D ( 'NONE', #253851, #59479, #176929 ) ;
#108177=CARTESIAN_POINT ( 'NONE',  ( 20.94560253601876809, 11.75000000001115907, -93.51008351251552142 ) ) ;
#108200=ORIENTED_EDGE ( 'NONE', *, *, #239759, .F. ) ;
#108255=AXIS2_PLACEMENT_3D ( 'NONE', #115152, #199846, #74781 ) ;
#108257=AXIS2_PLACEMENT_3D ( 'NONE', #155770, #218255, #59162 ) ;
#108269=ADVANCED_FACE ( 'NONE', ( #44803 ), #27838, .F. ) ;
#108273=EDGE_CURVE ( 'NONE', #66775, #130783, #42238, .T. ) ;
#108300=DIRECTION ( 'NONE',  ( 0.7071067811865487940, 8.659560562354918067E-17, 0.7071067811865463515 ) ) ;
#108330=ADVANCED_FACE ( 'NONE', ( #81320 ), #65639, .T. ) ;
#108335=DIRECTION ( 'NONE',  ( 0.000000000000000000, -0.4999999999999949485, 0.8660254037844415942 ) ) ;
#108336=ORIENTED_EDGE ( 'NONE', *, *, #216147, .F. ) ;
#108343=DIRECTION ( 'NONE',  ( 1.000000000000000000, 0.000000000000000000, 0.000000000000000000 ) ) ;
#108370=AXIS2_PLACEMENT_3D ( 'NONE', #66793, #126763, #64223 ) ;
#108376=DIRECTION ( 'NONE',  ( 0.000000000000000000, -0.000000000000000000, -1.000000000000000000 ) ) ;
#108387=CARTESIAN_POINT ( 'NONE',  ( -20.94999999999999929, 1.115600667400684642E-11, -100.5000000000000426 ) ) ;
#108405=( BOUNDED_CURVE ( )  B_SPLINE_CURVE ( 3, ( #84660, #44308, #100387, #22 ),
 .UNSPECIFIED., .F., .T. ) 
 B_SPLINE_CURVE_WITH_KNOTS ( ( 4, 4 ),
 ( 4.712388980384690562, 6.283185307179586232 ),
 .UNSPECIFIED. ) 
 CURVE ( )  GEOMETRIC_REPRESENTATION_ITEM ( )  RATIONAL_B_SPLINE_CURVE ( ( 1.000000000000000000, 0.8047378541243652705, 0.8047378541243652705, 1.000000000000000000 ) ) 
 REPRESENTATION_ITEM ( '' )  );
#108414=DIRECTION ( 'NONE',  ( -0.000000000000000000, 1.000000000000000000, 2.891205793294679805E-16 ) ) ;
#108432=DIRECTION ( 'NONE',  ( 0.000000000000000000, 0.000000000000000000, -1.000000000000000000 ) ) ;
#108475=AXIS2_PLACEMENT_3D ( 'NONE', #167481, #226112, #111340 ) ;
#108526=DIRECTION ( 'NONE',  ( 0.000000000000000000, 0.9876197685951252359, -0.1568667991644863424 ) ) ;
#108545=ORIENTED_EDGE ( 'NONE', *, *, #11489, .T. ) ;
#108592=ORIENTED_EDGE ( 'NONE', *, *, #136699, .F. ) ;
#108617=ADVANCED_FACE ( 'NONE', ( #201973 ), #78149, .F. ) ;
#108665=EDGE_CURVE ( 'NONE', #208340, #195188, #183697, .T. ) ;
#108677=DIRECTION ( 'NONE',  ( -0.7071067811865388020, 0.7071067811865561215, 0.000000000000000000 ) ) ;
#108689=ORIENTED_EDGE ( 'NONE', *, *, #185164, .F. ) ;
#108704=CARTESIAN_POINT ( 'NONE',  ( 18.52928932188133970, 10.27928932189250411, -88.35000000000003695 ) ) ;
#108720=CARTESIAN_POINT ( 'NONE',  ( -20.64999999999999858, 4.350000000011156054, -88.15000000000004832 ) ) ;
#108753=ADVANCED_FACE ( 'NONE', ( #49306, #109267 ), #144543, .T. ) ;
#108756=AXIS2_PLACEMENT_3D ( 'NONE', #208943, #207676, #29063 ) ;
#108777=CARTESIAN_POINT ( 'NONE',  ( 22.48660254037844197, 11.65000000001116298, -66.95000000000004547 ) ) ;
#108860=CARTESIAN_POINT ( 'NONE',  ( -21.10257677756356642, 6.398381742543891804, -66.97504925043209312 ) ) ;
#108883=ORIENTED_EDGE ( 'NONE', *, *, #38809, .F. ) ;
#108897=CIRCLE ( 'NONE', #208872, 0.1000000000000028644 ) ;
#108910=DIRECTION ( 'NONE',  ( -1.000000000000000000, 0.000000000000000000, 0.000000000000000000 ) ) ;
#108915=CIRCLE ( 'NONE', #33970, 0.1000000000000028644 ) ;
#108933=CARTESIAN_POINT ( 'NONE',  ( -23.15000000000000213, 11.65000000001115588, -88.35000000000003695 ) ) ;
#108940=CARTESIAN_POINT ( 'NONE',  ( 20.30466543256828160, 9.304236939266628426, -75.25366265139203392 ) ) ;
#108955=DIRECTION ( 'NONE',  ( 0.000000000000000000, 0.000000000000000000, -1.000000000000000000 ) ) ;
#108958=VERTEX_POINT ( 'NONE', #119572 ) ;
#108988=FACE_OUTER_BOUND ( 'NONE', #78397, .T. ) ;
#109018=CARTESIAN_POINT ( 'NONE',  ( -20.94999999999999929, -11.74999999998884448, -97.40000000000004832 ) ) ;
#109053=DIRECTION ( 'NONE',  ( 0.000000000000000000, -1.000000000000000000, -0.000000000000000000 ) ) ;
#109073=VECTOR ( 'NONE', #189112, 1000.000000000000000 ) ;
#109124=ORIENTED_EDGE ( 'NONE', *, *, #141869, .T. ) ;
#109142=DIRECTION ( 'NONE',  ( 0.000000000000000000, 0.000000000000000000, 1.000000000000000000 ) ) ;
#109145=ADVANCED_FACE ( 'NONE', ( #112823 ), #213190, .F. ) ;
#109157=ADVANCED_FACE ( 'NONE', ( #228924 ), #82278, .T. ) ;
#109159=CARTESIAN_POINT ( 'NONE',  ( 21.04999999999998650, 6.650000000011155876, -79.25000000000004263 ) ) ;
#109195=LINE ( 'NONE', #111788, #45175 ) ;
#109213=LINE ( 'NONE', #188758, #222326 ) ;
#109258=ORIENTED_EDGE ( 'NONE', *, *, #196761, .T. ) ;
#109267=FACE_OUTER_BOUND ( 'NONE', #52156, .T. ) ;
#109287=DIRECTION ( 'NONE',  ( 1.000000000000000000, 0.000000000000000000, 0.000000000000000000 ) ) ;
#109311=ORIENTED_EDGE ( 'NONE', *, *, #33415, .T. ) ;
#109332=CARTESIAN_POINT ( 'NONE',  ( -20.99749315643149217, 11.75000000001115197, -93.48519423124027128 ) ) ;
#109334=DIRECTION ( 'NONE',  ( -2.940209281316621016E-16, 1.000000000000000000, 0.000000000000000000 ) ) ;
#109372=VERTEX_POINT ( 'NONE', #41014 ) ;
#109390=CYLINDRICAL_SURFACE ( 'NONE', #93499, 0.09999999999999781286 ) ;
#109431=EDGE_LOOP ( 'NONE', ( #82221, #82709, #122685, #38126 ) ) ;
#109461=ORIENTED_EDGE ( 'NONE', *, *, #16228, .F. ) ;
#109467=CARTESIAN_POINT ( 'NONE',  ( -18.50000000000000000, -9.399999999988850163, -107.3820418481727046 ) ) ;
#109470=DIRECTION ( 'NONE',  ( 1.000000000000000000, 0.000000000000000000, -0.000000000000000000 ) ) ;
#109473=CARTESIAN_POINT ( 'NONE',  ( -20.64999999999999858, 2.400000000011155432, -87.27537807723794572 ) ) ;
#109534=CARTESIAN_POINT ( 'NONE',  ( 19.96984138294287092, 11.75000000001137934, -91.72457207120136502 ) ) ;
#109545=CYLINDRICAL_SURFACE ( 'NONE', #57750, 7.900000000000003908 ) ;
#109568=VERTEX_POINT ( 'NONE', #69554 ) ;
#109574=DIRECTION ( 'NONE',  ( 0.000000000000000000, 0.000000000000000000, -1.000000000000000000 ) ) ;
#109627=DIRECTION ( 'NONE',  ( -4.239556034732056743E-17, 0.1298341882520022694, 0.9915357197604853789 ) ) ;
#109658=CARTESIAN_POINT ( 'NONE',  ( -23.15000000000000213, 1.115600667400684642E-11, -98.50000000000004263 ) ) ;
#109660=ORIENTED_EDGE ( 'NONE', *, *, #194135, .T. ) ;
#109700=CARTESIAN_POINT ( 'NONE',  ( 23.14999999999999858, 1.115600667400684642E-11, -67.00000000000004263 ) ) ;
#109714=AXIS2_PLACEMENT_3D ( 'NONE', #58972, #138509, #118992 ) ;
#109721=EDGE_LOOP ( 'NONE', ( #69832, #211388, #224825, #207971 ) ) ;
#109723=CARTESIAN_POINT ( 'NONE',  ( 23.25000000000000000, -9.599999999988849453, -55.25000000000004974 ) ) ;
#109726=CIRCLE ( 'NONE', #117917, 11.74999999999999645 ) ;
#109739=VECTOR ( 'NONE', #115242, 1000.000000000000000 ) ;
#109816=CYLINDRICAL_SURFACE ( 'NONE', #152336, 0.09999999999999939493 ) ;
#109837=DIRECTION ( 'NONE',  ( -1.000000000000000000, -2.952720810173289112E-16, 0.000000000000000000 ) ) ;
#109872=CARTESIAN_POINT ( 'NONE',  ( -21.05000000000000071, -1.835341550213257733, -78.55515129256303908 ) ) ;
#109878=CIRCLE ( 'NONE', #176553, 4.149999999999999467 ) ;
#109907=VECTOR ( 'NONE', #44633, 1000.000000000000000 ) ;
#109916=FACE_OUTER_BOUND ( 'NONE', #250944, .T. ) ;
#109943=AXIS2_PLACEMENT_3D ( 'NONE', #85417, #244524, #65897 ) ;
#109974=DIRECTION ( 'NONE',  ( 0.000000000000000000, 0.000000000000000000, -1.000000000000000000 ) ) ;
#109980=DIRECTION ( 'NONE',  ( 0.000000000000000000, 2.891205793294679805E-16, -1.000000000000000000 ) ) ;
#110040=VECTOR ( 'NONE', #150103, 1000.000000000000000 ) ;
#110048=DIRECTION ( 'NONE',  ( 1.000000000000000000, 0.000000000000000000, 0.000000000000000000 ) ) ;
#110063=VECTOR ( 'NONE', #254338, 1000.000000000000000 ) ;
#110070=ADVANCED_FACE ( 'NONE', ( #235999 ), #157747, .T. ) ;
#110071=ORIENTED_EDGE ( 'NONE', *, *, #135621, .T. ) ;
#110077=EDGE_CURVE ( 'NONE', #247484, #145626, #237298, .T. ) ;
#110084=AXIS2_PLACEMENT_3D ( 'NONE', #195873, #112476, #194597 ) ;
#110095=EDGE_CURVE ( 'NONE', #94180, #120362, #213874, .T. ) ;
#110117=CARTESIAN_POINT ( 'NONE',  ( 18.51697539158856642, 10.31565961587946134, -106.0364194119178904 ) ) ;
#110130=CARTESIAN_POINT ( 'NONE',  ( -1.739115166359751170E-14, 11.65000000001114699, -91.85000000000003695 ) ) ;
#110133=EDGE_LOOP ( 'NONE', ( #150702, #229036, #149838, #212484 ) ) ;
#110163=ORIENTED_EDGE ( 'NONE', *, *, #183077, .T. ) ;
#110171=AXIS2_PLACEMENT_3D ( 'NONE', #209144, #110048, #207898 ) ;
#110172=DIRECTION ( 'NONE',  ( 0.000000000000000000, -0.9908441862701600211, -0.1350103645451876666 ) ) ;
#110180=ORIENTED_EDGE ( 'NONE', *, *, #89537, .F. ) ;
#110196=CARTESIAN_POINT ( 'NONE',  ( 19.58285714285715073, 9.015001489659738354, -75.42065281608175553 ) ) ;
#110216=VECTOR ( 'NONE', #100345, 1000.000000000000000 ) ;
#110224=EDGE_LOOP ( 'NONE', ( #238121, #156894, #22347, #169910 ) ) ;
#110225=CARTESIAN_POINT ( 'NONE',  ( 20.58091095332318332, 9.018470153363605135, -75.41865018215861483 ) ) ;
#110271=DIRECTION ( 'NONE',  ( 0.000000000000000000, -0.01283462868041947667, -0.9999176327611367654 ) ) ;
#110309=FACE_OUTER_BOUND ( 'NONE', #148060, .T. ) ;
#110339=CARTESIAN_POINT ( 'NONE',  ( 20.95512820512820795, 10.62384868372303615, -79.20016201942446799 ) ) ;
#110356=DIRECTION ( 'NONE',  ( 1.000000000000000000, 0.000000000000000000, 0.000000000000000000 ) ) ;
#110358=ORIENTED_EDGE ( 'NONE', *, *, #66852, .F. ) ;
#110370=ORIENTED_EDGE ( 'NONE', *, *, #481, .T. ) ;
#110399=CIRCLE ( 'NONE', #131249, 0.1999999999999996503 ) ;
#110411=CIRCLE ( 'NONE', #2061, 11.80000000000000426 ) ;
#110425=DIRECTION ( 'NONE',  ( 0.000000000000000000, -0.000000000000000000, 1.000000000000000000 ) ) ;
#110438=DIRECTION ( 'NONE',  ( 1.000000000000000000, 0.000000000000000000, 0.000000000000000000 ) ) ;
#110449=AXIS2_PLACEMENT_3D ( 'NONE', #128657, #148202, #227734 ) ;
#110466=DIRECTION ( 'NONE',  ( 0.000000000000000000, -1.000000000000000000, 0.000000000000000000 ) ) ;
#110483=DIRECTION ( 'NONE',  ( 1.000000000000000000, 1.836970198721029934E-16, 0.000000000000000000 ) ) ;
#110498=ORIENTED_EDGE ( 'NONE', *, *, #212387, .T. ) ;
#110538=VERTEX_POINT ( 'NONE', #163546 ) ;
#110547=CIRCLE ( 'NONE', #102135, 0.1000000000000028644 ) ;
#110586=CARTESIAN_POINT ( 'NONE',  ( -18.50000000000000000, -1.736257131586239844, -78.56865232901753870 ) ) ;
#110624=DIRECTION ( 'NONE',  ( 0.000000000000000000, -0.000000000000000000, 1.000000000000000000 ) ) ;
#110651=FACE_OUTER_BOUND ( 'NONE', #207318, .T. ) ;
#110656=DIRECTION ( 'NONE',  ( 1.000000000000000000, -0.000000000000000000, -0.000000000000000000 ) ) ;
#110658=EDGE_CURVE ( 'NONE', #250043, #140759, #69146, .T. ) ;
#110667=CARTESIAN_POINT ( 'NONE',  ( -21.53752568622136820, 0.09897446127752260181, -60.21319212545143529 ) ) ;
#110711=DIRECTION ( 'NONE',  ( 0.000000000000000000, 1.000000000000000000, 0.000000000000000000 ) ) ;
#110729=DIRECTION ( 'NONE',  ( 1.000000000000000000, 0.000000000000000000, 0.000000000000000000 ) ) ;
#110744=CIRCLE ( 'NONE', #256428, 3.999999999999999112 ) ;
#110747=AXIS2_PLACEMENT_3D ( 'NONE', #50091, #244440, #65807 ) ;
#110760=ORIENTED_EDGE ( 'NONE', *, *, #55565, .F. ) ;
#110762=CARTESIAN_POINT ( 'NONE',  ( -18.33682934331516279, -9.511185591082426782, -107.4056547686733580 ) ) ;
#110766=CARTESIAN_POINT ( 'NONE',  ( -23.15000000000000213, -8.999999999988846255, -76.89396912265249284 ) ) ;
#110773=ORIENTED_EDGE ( 'NONE', *, *, #144522, .F. ) ;
#110829=DIRECTION ( 'NONE',  ( 0.000000000000000000, 1.000000000000000000, 2.891205793294679805E-16 ) ) ;
#110841=ORIENTED_EDGE ( 'NONE', *, *, #195152, .T. ) ;
#110849=CARTESIAN_POINT ( 'NONE',  ( 20.94999999999999929, 6.450000000011156587, -77.01702717044007329 ) ) ;
#110865=ORIENTED_EDGE ( 'NONE', *, *, #88815, .F. ) ;
#110898=VECTOR ( 'NONE', #86138, 1000.000000000000000 ) ;
#110920=CARTESIAN_POINT ( 'NONE',  ( -20.05000000000000426, 9.250000000011157297, -88.25000000000005684 ) ) ;
#110927=EDGE_CURVE ( 'NONE', #149634, #144636, #257372, .T. ) ;
#110953=EDGE_CURVE ( 'NONE', #241599, #237434, #25246, .T. ) ;
#110959=ORIENTED_EDGE ( 'NONE', *, *, #134930, .T. ) ;
#111019=CARTESIAN_POINT ( 'NONE',  ( 21.14999999999999503, -0.09999999998884338825, -55.35042919245524473 ) ) ;
#111023=ORIENTED_EDGE ( 'NONE', *, *, #87007, .F. ) ;
#111049=CARTESIAN_POINT ( 'NONE',  ( -18.46907102845854354, -9.473727364752953406, -107.1760347387365897 ) ) ;
#111131=CARTESIAN_POINT ( 'NONE',  ( 23.14999999999999503, 6.650000000011155876, -88.25000000000005684 ) ) ;
#111174=CARTESIAN_POINT ( 'NONE',  ( 23.14999999999999858, 5.000000000011153745, -88.59473398108696074 ) ) ;
#111189=CARTESIAN_POINT ( 'NONE',  ( -18.50000000000000000, -1.362429037182155023, -108.3888812479212476 ) ) ;
#111208=AXIS2_PLACEMENT_3D ( 'NONE', #10420, #228182, #31297 ) ;
#111215=CARTESIAN_POINT ( 'NONE',  ( 21.11345278033261508, 8.882122073382229033, -79.24602217075594979 ) ) ;
#111228=ORIENTED_EDGE ( 'NONE', *, *, #121748, .T. ) ;
#111237=B_SPLINE_CURVE_WITH_KNOTS ( 'NONE', 3,
 ( #174124, #155821, #157100, #60534, #239185, #116667 ),
 .UNSPECIFIED., .F., .F.,
 ( 4, 2, 4 ),
 ( 0.000000000000000000, 0.0001568709654583421050, 0.0003137419309166841557 ),
 .UNSPECIFIED. ) ;
#111248=DIRECTION ( 'NONE',  ( 0.000000000000000000, 0.000000000000000000, -1.000000000000000000 ) ) ;
#111260=CARTESIAN_POINT ( 'NONE',  ( 23.14999999999999858, -1.999999999988846699, -100.5000000000000426 ) ) ;
#111293=PLANE ( 'NONE',  #15459 ) ;
#111298=CARTESIAN_POINT ( 'NONE',  ( 20.87600722750343252, 10.33112638556969465, -106.0901228926975080 ) ) ;
#111340=DIRECTION ( 'NONE',  ( 1.000000000000000000, 0.000000000000000000, 0.000000000000000000 ) ) ;
#111348=CARTESIAN_POINT ( 'NONE',  ( 21.09813707148777340, 6.385062105747657313, -66.96864850047053608 ) ) ;
#111358=VERTEX_POINT ( 'NONE', #74316 ) ;
#111364=ORIENTED_EDGE ( 'NONE', *, *, #135592, .F. ) ;
#111388=DIRECTION ( 'NONE',  ( 0.000000000000000000, 0.000000000000000000, -1.000000000000000000 ) ) ;
#111389=EDGE_LOOP ( 'NONE', ( #60106, #148342, #69033, #141459 ) ) ;
#111404=ORIENTED_EDGE ( 'NONE', *, *, #30093, .F. ) ;
#111408=LINE ( 'NONE', #171418, #26226 ) ;
#111429=AXIS2_PLACEMENT_3D ( 'NONE', #32680, #74367, #152613 ) ;
#111443=AXIS2_PLACEMENT_3D ( 'NONE', #204587, #202037, #25974 ) ;
#111460=AXIS2_PLACEMENT_3D ( 'NONE', #236235, #176290, #198396 ) ;
#111464=VERTEX_POINT ( 'NONE', #59818 ) ;
#111466=LINE ( 'NONE', #193575, #75475 ) ;
#111476=CARTESIAN_POINT ( 'NONE',  ( -23.25000000000000000, 1.115600667400684642E-11, -67.00000000000004263 ) ) ;
#111502=EDGE_CURVE ( 'NONE', #244178, #128108, #70407, .T. ) ;
#111524=CARTESIAN_POINT ( 'NONE',  ( 23.15000000000000213, -11.64999999998883595, -55.25000000000004974 ) ) ;
#111540=CARTESIAN_POINT ( 'NONE',  ( 23.14999999999999503, 6.650000000011155876, -79.15000000000004832 ) ) ;
#111542=CARTESIAN_POINT ( 'NONE',  ( -23.15000000000000213, 11.65000000001115588, -79.15000000000003411 ) ) ;
#111566=LINE ( 'NONE', #131116, #188334 ) ;
#111581=ORIENTED_EDGE ( 'NONE', *, *, #11084, .T. ) ;
#111599=DIRECTION ( 'NONE',  ( -1.000000000000000000, 0.000000000000000000, 0.000000000000000000 ) ) ;
#111645=CARTESIAN_POINT ( 'NONE',  ( 21.05000000000000071, 8.776282648982402179, -75.48759237851896842 ) ) ;
#111670=AXIS2_PLACEMENT_3D ( 'NONE', #44553, #7996, #47085 ) ;
#111682=CARTESIAN_POINT ( 'NONE',  ( 21.05000000000000071, -11.64999999998883595, -69.90000000000004832 ) ) ;
#111691=VECTOR ( 'NONE', #112454, 1000.000000000000114 ) ;
#111692=VERTEX_POINT ( 'NONE', #148373 ) ;
#111717=DIRECTION ( 'NONE',  ( 1.000000000000000000, 0.000000000000000000, 0.000000000000000000 ) ) ;
#111759=DIRECTION ( 'NONE',  ( 1.000000000000000000, -0.000000000000000000, 0.000000000000000000 ) ) ;
#111768=EDGE_CURVE ( 'NONE', #131787, #71547, #245352, .T. ) ;
#111788=CARTESIAN_POINT ( 'NONE',  ( -18.50000000000000000, -9.499999999988849808, -75.10000000000003695 ) ) ;
#111792=ORIENTED_EDGE ( 'NONE', *, *, #119051, .F. ) ;
#111793=CARTESIAN_POINT ( 'NONE',  ( -22.39999999999999858, 7.790779598384560245, -66.90000000000004832 ) ) ;
#111810=VERTEX_POINT ( 'NONE', #99592 ) ;
#111827=ORIENTED_EDGE ( 'NONE', *, *, #124742, .T. ) ;
#111876=AXIS2_PLACEMENT_3D ( 'NONE', #236009, #196882, #157811 ) ;
#111886=DIRECTION ( 'NONE',  ( 0.000000000000000000, 0.000000000000000000, -1.000000000000000000 ) ) ;
#111893=CIRCLE ( 'NONE', #32805, 0.1999999999999987899 ) ;
#111903=CIRCLE ( 'NONE', #32821, 0.1000000000000028644 ) ;
#111908=TOROIDAL_SURFACE ( 'NONE', #86906, 7.800000000000000711, 0.1000000000000000056 ) ;
#111936=CIRCLE ( 'NONE', #107624, 0.1000000000000028644 ) ;
#111938=DIRECTION ( 'NONE',  ( 0.000000000000000000, -1.000000000000000000, 6.938893903907228378E-14 ) ) ;
#111969=CARTESIAN_POINT ( 'NONE',  ( -21.00023020733502932, 1.115542391533913547E-11, -60.60913075473169442 ) ) ;
#111981=FACE_OUTER_BOUND ( 'NONE', #99463, .T. ) ;
#111990=ORIENTED_EDGE ( 'NONE', *, *, #239559, .F. ) ;
#112001=PLANE ( 'NONE',  #159304 ) ;
#112016=ORIENTED_EDGE ( 'NONE', *, *, #145991, .F. ) ;
#112034=FACE_OUTER_BOUND ( 'NONE', #156538, .T. ) ;
#112035=CARTESIAN_POINT ( 'NONE',  ( 18.39999999999999858, -9.499999999988844479, -74.03206939669972542 ) ) ;
#112036=DIRECTION ( 'NONE',  ( 0.000000000000000000, 0.000000000000000000, -1.000000000000000000 ) ) ;
#112038=VECTOR ( 'NONE', #178684, 1000.000000000000000 ) ;
#112050=ORIENTED_EDGE ( 'NONE', *, *, #97199, .T. ) ;
#112140=DIRECTION ( 'NONE',  ( -1.000000000000000000, -0.000000000000000000, -0.000000000000000000 ) ) ;
#112167=DIRECTION ( 'NONE',  ( 0.7071067811865474617, 0.7071067811865474617, 0.000000000000000000 ) ) ;
#112199=AXIS2_PLACEMENT_3D ( 'NONE', #180186, #5354, #143608 ) ;
#112208=DIRECTION ( 'NONE',  ( -2.827886303505249259E-16, 0.8660254037844412611, 0.4999999999999956701 ) ) ;
#112224=ORIENTED_EDGE ( 'NONE', *, *, #148810, .T. ) ;
#112226=DIRECTION ( 'NONE',  ( 1.000000000000000000, 2.952720810173289112E-16, -0.000000000000000000 ) ) ;
#112227=AXIS2_PLACEMENT_3D ( 'NONE', #36606, #116119, #195671 ) ;
#112298=CARTESIAN_POINT ( 'NONE',  ( -21.05000000000000071, 6.300000000011169554, -67.10000000000005116 ) ) ;
#112304=ORIENTED_EDGE ( 'NONE', *, *, #209904, .F. ) ;
#112330=B_SPLINE_CURVE_WITH_KNOTS ( 'NONE', 3,
 ( #40445, #84616, #221582, #83349 ),
 .UNSPECIFIED., .F., .F.,
 ( 4, 4 ),
 ( 3.469446951953614189E-18, 0.0001058379652594581074 ),
 .UNSPECIFIED. ) ;
#112335=EDGE_CURVE ( 'NONE', #187772, #104099, #150049, .T. ) ;
#112340=TOROIDAL_SURFACE ( 'NONE', #49957, 0.2000000000000000111, 0.1000000000000000056 ) ;
#112346=DIRECTION ( 'NONE',  ( 0.000000000000000000, -1.000000000000000000, 0.000000000000000000 ) ) ;
#112378=DIRECTION ( 'NONE',  ( 0.000000000000000000, 1.000000000000000000, 0.000000000000000000 ) ) ;
#112381=ORIENTED_EDGE ( 'NONE', *, *, #47341, .F. ) ;
#112399=EDGE_CURVE ( 'NONE', #14463, #61798, #169621, .T. ) ;
#112402=ORIENTED_EDGE ( 'NONE', *, *, #185928, .T. ) ;
#112412=EDGE_LOOP ( 'NONE', ( #126722, #253262, #95065, #2996 ) ) ;
#112428=DIRECTION ( 'NONE',  ( 0.000000000000000000, -8.673617379883787770E-15, 1.000000000000000000 ) ) ;
#112454=DIRECTION ( 'NONE',  ( -0.7071067811865474617, -0.7071067811865474617, -2.044391222244499837E-16 ) ) ;
#112476=DIRECTION ( 'NONE',  ( 0.000000000000000000, 1.000000000000000000, 0.000000000000000000 ) ) ;
#112498=AXIS2_PLACEMENT_3D ( 'NONE', #234254, #12683, #53057 ) ;
#112516=VERTEX_POINT ( 'NONE', #96430 ) ;
#112546=VECTOR ( 'NONE', #190152, 1000.000000000000000 ) ;
#112562=EDGE_LOOP ( 'NONE', ( #84510, #183573, #119041, #206652 ) ) ;
#112568=ORIENTED_EDGE ( 'NONE', *, *, #137109, .F. ) ;
#112588=CARTESIAN_POINT ( 'NONE',  ( 21.93340585898645401, 1.115541036281197940E-11, -59.67585297787184118 ) ) ;
#112595=DIRECTION ( 'NONE',  ( 1.734723475976817507E-14, 0.000000000000000000, -1.000000000000000000 ) ) ;
#112603=EDGE_LOOP ( 'NONE', ( #244989, #8915, #57693, #155555 ) ) ;
#112634=CARTESIAN_POINT ( 'NONE',  ( 21.13498764882293557, 6.495618143485025975, -66.99834360526871535 ) ) ;
#112637=ORIENTED_EDGE ( 'NONE', *, *, #256666, .T. ) ;
#112643=CARTESIAN_POINT ( 'NONE',  ( 20.94999999999999574, -11.64999999998883595, -69.90000000000004832 ) ) ;
#112645=ORIENTED_EDGE ( 'NONE', *, *, #120984, .T. ) ;
#112646=FACE_OUTER_BOUND ( 'NONE', #224859, .T. ) ;
#112647=AXIS2_PLACEMENT_3D ( 'NONE', #58759, #100447, #216572 ) ;
#112661=ADVANCED_FACE ( 'NONE', ( #70192 ), #89709, .T. ) ;
#112709=ADVANCED_FACE ( 'NONE', ( #168026 ), #250088, .F. ) ;
#112712=CIRCLE ( 'NONE', #245985, 3.900000000000000799 ) ;
#112715=ORIENTED_EDGE ( 'NONE', *, *, #44638, .T. ) ;
#112730=DIRECTION ( 'NONE',  ( 0.000000000000000000, 0.000000000000000000, -1.000000000000000000 ) ) ;
#112740=CARTESIAN_POINT ( 'NONE',  ( 20.94999999999999574, -11.48912529306490349, -70.10000000000005116 ) ) ;
#112757=DIRECTION ( 'NONE',  ( 0.000000000000000000, -1.000000000000000000, 0.000000000000000000 ) ) ;
#112764=CARTESIAN_POINT ( 'NONE',  ( -20.54999999999999716, -9.399999999988846611, -90.60603087734760663 ) ) ;
#112765=CYLINDRICAL_SURFACE ( 'NONE', #15306, 0.09999999999999939493 ) ;
#112798=DIRECTION ( 'NONE',  ( 1.000000000000000000, 0.000000000000000000, -0.000000000000000000 ) ) ;
#112803=DIRECTION ( 'NONE',  ( 0.000000000000000000, 0.6728971962616697722, 0.7397360091702875895 ) ) ;
#112823=FACE_OUTER_BOUND ( 'NONE', #250616, .T. ) ;
#112830=CARTESIAN_POINT ( 'NONE',  ( 20.12500000000000355, 9.258049272928479567, -75.36333883714247861 ) ) ;
#112839=DIRECTION ( 'NONE',  ( 1.000000000000000000, 0.000000000000000000, 0.000000000000000000 ) ) ;
#112849=ORIENTED_EDGE ( 'NONE', *, *, #131884, .F. ) ;
#112861=AXIS2_PLACEMENT_3D ( 'NONE', #56270, #114979, #175004 ) ;
#112867=DIRECTION ( 'NONE',  ( 0.000000000000000000, 0.000000000000000000, -1.000000000000000000 ) ) ;
#112878=EDGE_LOOP ( 'NONE', ( #41841, #244600, #255361, #96794 ) ) ;
#112895=CARTESIAN_POINT ( 'NONE',  ( 23.25000000000000000, -9.599999999988845900, -76.89396912265249284 ) ) ;
#112897=CARTESIAN_POINT ( 'NONE',  ( 20.94999999999999929, 1.115600667400684642E-11, -102.4000000000000483 ) ) ;
#112930=DIRECTION ( 'NONE',  ( 0.000000000000000000, 0.000000000000000000, -1.000000000000000000 ) ) ;
#112937=CARTESIAN_POINT ( 'NONE',  ( 21.05000000000000071, 8.872080675389140580, -75.52104741882936878 ) ) ;
#112939=AXIS2_PLACEMENT_3D ( 'NONE', #192502, #212077, #251164 ) ;
#112955=LINE ( 'NONE', #192489, #177429 ) ;
#112968=EDGE_CURVE ( 'NONE', #124815, #160493, #37810, .T. ) ;
#113001=ORIENTED_EDGE ( 'NONE', *, *, #100465, .F. ) ;
#113007=VERTEX_POINT ( 'NONE', #199093 ) ;
#113017=B_SPLINE_CURVE_WITH_KNOTS ( 'NONE', 3,
 ( #71937, #56192, #154079, #13250, #31553, #111049, #173654, #251839, #131898, #211435 ),
 .UNSPECIFIED., .F., .F.,
 ( 4, 2, 2, 2, 4 ),
 ( 0.000000000000000000, 4.221631689686210128E-05, 8.443263379372420256E-05, 0.0001688652675874484051, 0.0003377305351748950755 ),
 .UNSPECIFIED. ) ;
#113021=DIRECTION ( 'NONE',  ( 0.000000000000000000, -1.000000000000000000, 6.308085367188393199E-16 ) ) ;
#113043=CARTESIAN_POINT ( 'NONE',  ( 21.05000000000000071, -8.999999999988844479, -76.89396912265249284 ) ) ;
#113044=VERTEX_POINT ( 'NONE', #187249 ) ;
#113052=DIRECTION ( 'NONE',  ( 1.713247197920696616E-14, 0.9876197685951252359, -0.1568667991644863424 ) ) ;
#113090=VERTEX_POINT ( 'NONE', #167693 ) ;
#113118=DIRECTION ( 'NONE',  ( 0.000000000000000000, 0.000000000000000000, -1.000000000000000000 ) ) ;
#113122=PLANE ( 'NONE',  #25291 ) ;
#113142=VECTOR ( 'NONE', #194092, 1000.000000000000000 ) ;
#113165=ORIENTED_EDGE ( 'NONE', *, *, #62311, .T. ) ;
#113174=DIRECTION ( 'NONE',  ( 0.000000000000000000, 1.265107689135680095E-16, -1.000000000000000000 ) ) ;
#113203=FACE_OUTER_BOUND ( 'NONE', #7449, .T. ) ;
#113205=AXIS2_PLACEMENT_3D ( 'NONE', #53517, #14420, #116072 ) ;
#113220=ADVANCED_FACE ( 'NONE', ( #71154 ), #115382, .T. ) ;
#113226=DIRECTION ( 'NONE',  ( 0.000000000000000000, 1.000000000000000000, 0.000000000000000000 ) ) ;
#113227=CARTESIAN_POINT ( 'NONE',  ( -20.54999999999999716, -9.499999999988846255, -90.60603087734760663 ) ) ;
#113228=CARTESIAN_POINT ( 'NONE',  ( -21.59142135623730852, 7.850000000011158718, -79.35000000000005116 ) ) ;
#113237=DIRECTION ( 'NONE',  ( 1.000000000000000000, 7.304098846218134667E-16, -0.000000000000000000 ) ) ;
#113238=ORIENTED_EDGE ( 'NONE', *, *, #163298, .T. ) ;
#113242=ORIENTED_EDGE ( 'NONE', *, *, #70383, .F. ) ;
#113269=DIRECTION ( 'NONE',  ( 1.000000000000000000, 0.000000000000000000, -0.000000000000000000 ) ) ;
#113274=ORIENTED_EDGE ( 'NONE', *, *, #57442, .F. ) ;
#113283=DIRECTION ( 'NONE',  ( -1.000000000000000000, -0.000000000000000000, -0.000000000000000000 ) ) ;
#113285=DIRECTION ( 'NONE',  ( 0.000000000000000000, 0.000000000000000000, -1.000000000000000000 ) ) ;
#113290=ORIENTED_EDGE ( 'NONE', *, *, #237892, .T. ) ;
#113302=CARTESIAN_POINT ( 'NONE',  ( 18.40000000000000213, -9.499999999988840926, -73.99936209718019597 ) ) ;
#113305=AXIS2_PLACEMENT_3D ( 'NONE', #203283, #32385, #190153 ) ;
#113306=ORIENTED_EDGE ( 'NONE', *, *, #200155, .F. ) ;
#113330=EDGE_CURVE ( 'NONE', #128673, #62762, #137898, .T. ) ;
#113354=CARTESIAN_POINT ( 'NONE',  ( -18.50000000000000000, 11.65000000001115232, -79.15000000000004832 ) ) ;
#113373=CARTESIAN_POINT ( 'NONE',  ( 18.39999999999999858, -9.499999999988844479, -107.1001893912220879 ) ) ;
#113380=CARTESIAN_POINT ( 'NONE',  ( 18.49505832270840955, -9.438028062771737225, -74.19847317489390548 ) ) ;
#113386=CARTESIAN_POINT ( 'NONE',  ( -20.94999999999999929, 5.900000000011162093, -90.28090023534366537 ) ) ;
#113390=CARTESIAN_POINT ( 'NONE',  ( -21.14999999999999858, 6.540656951712397138, -67.00000000000004263 ) ) ;
#113433=CARTESIAN_POINT ( 'NONE',  ( 23.15000000000000213, -9.499999999988844479, -90.60603087734760663 ) ) ;
#113453=CARTESIAN_POINT ( 'NONE',  ( 23.14999999999999503, 11.65000000001116298, -79.15000000000004832 ) ) ;
#113460=DIRECTION ( 'NONE',  ( -1.000000000000000000, -0.000000000000000000, -0.000000000000000000 ) ) ;
#113462=CIRCLE ( 'NONE', #205019, 0.6000000000000033085 ) ;
#113477=AXIS2_PLACEMENT_3D ( 'NONE', #42576, #219933, #58275 ) ;
#113501=CARTESIAN_POINT ( 'NONE',  ( -23.25000000000000000, 1.115600667400684642E-11, -102.6000000000000512 ) ) ;
#113562=CARTESIAN_POINT ( 'NONE',  ( -21.45000000000000284, 7.708578643773852157, -88.15000000000004832 ) ) ;
#113565=DIRECTION ( 'NONE',  ( 0.000000000000000000, 1.000000000000000000, 0.000000000000000000 ) ) ;
#113566=ADVANCED_FACE ( 'NONE', ( #234722 ), #56053, .T. ) ;
#113583=EDGE_CURVE ( 'NONE', #201185, #235613, #229692, .T. ) ;
#113660=VECTOR ( 'NONE', #230055, 1000.000000000000000 ) ;
#113664=DIRECTION ( 'NONE',  ( 0.000000000000000000, 1.000000000000000000, 0.000000000000000000 ) ) ;
#113672=ORIENTED_EDGE ( 'NONE', *, *, #139362, .F. ) ;
#113725=LINE ( 'NONE', #38067, #8440 ) ;
#113730=CARTESIAN_POINT ( 'NONE',  ( 20.94999999999999574, -1.261786168553869603, -75.08649896354552311 ) ) ;
#113732=AXIS2_PLACEMENT_3D ( 'NONE', #3186, #181852, #26649 ) ;
#113749=ORIENTED_EDGE ( 'NONE', *, *, #72571, .F. ) ;
#113768=DIRECTION ( 'NONE',  ( 1.000000000000000000, -0.000000000000000000, -0.000000000000000000 ) ) ;
#113771=ORIENTED_EDGE ( 'NONE', *, *, #32502, .F. ) ;
#113789=DIRECTION ( 'NONE',  ( -3.265361837132813093E-16, 1.000000000000000000, 0.000000000000000000 ) ) ;
#113795=EDGE_LOOP ( 'NONE', ( #20685, #77893, #16276, #130508 ) ) ;
#113814=ORIENTED_EDGE ( 'NONE', *, *, #175517, .F. ) ;
#113817=DIRECTION ( 'NONE',  ( 0.000000000000000000, 0.000000000000000000, -1.000000000000000000 ) ) ;
#113834=AXIS2_PLACEMENT_3D ( 'NONE', #14469, #36611, #74455 ) ;
#113848=DIRECTION ( 'NONE',  ( 0.000000000000000000, 0.000000000000000000, -1.000000000000000000 ) ) ;
#113861=CARTESIAN_POINT ( 'NONE',  ( 22.00356870068402770, -5.670589261373817377E-12, -59.74575763823897034 ) ) ;
#113878=VERTEX_POINT ( 'NONE', #96159 ) ;
#113881=EDGE_LOOP ( 'NONE', ( #124603, #9157, #191703 ) ) ;
#113925=CIRCLE ( 'NONE', #230654, 0.1000000000000028644 ) ;
#113935=CARTESIAN_POINT ( 'NONE',  ( 21.05000000000000071, 1.115600667400684642E-11, -100.5000000000000426 ) ) ;
#113954=CARTESIAN_POINT ( 'NONE',  ( -18.47079683080345092, -9.471664105233751130, -74.10886054099226783 ) ) ;
#113968=VERTEX_POINT ( 'NONE', #233153 ) ;
#113981=ORIENTED_EDGE ( 'NONE', *, *, #166526, .F. ) ;
#113993=CIRCLE ( 'NONE', #213972, 0.1000000000000000472 ) ;
#113999=CARTESIAN_POINT ( 'NONE',  ( -20.54999999999999716, 1.115600667400684642E-11, -100.5000000000000426 ) ) ;
#114017=AXIS2_PLACEMENT_3D ( 'NONE', #152467, #250253, #96291 ) ;
#114067=EDGE_CURVE ( 'NONE', #187820, #221706, #13398, .T. ) ;
#114089=CIRCLE ( 'NONE', #193223, 2.000000000000002665 ) ;
#114110=SPHERICAL_SURFACE ( 'NONE', #75143, 0.1000000000000000056 ) ;
#114130=VERTEX_POINT ( 'NONE', #59581 ) ;
#114137=DIRECTION ( 'NONE',  ( 0.000000000000000000, 0.000000000000000000, 1.000000000000000000 ) ) ;
#114161=DIRECTION ( 'NONE',  ( 0.000000000000000000, 1.000000000000000000, 0.000000000000000000 ) ) ;
#114171=DIRECTION ( 'NONE',  ( 0.000000000000000000, -1.000000000000000000, 0.000000000000000000 ) ) ;
#114206=AXIS2_PLACEMENT_3D ( 'NONE', #67206, #86747, #25527 ) ;
#114244=DIRECTION ( 'NONE',  ( 0.000000000000000000, 0.000000000000000000, -1.000000000000000000 ) ) ;
#114254=DIRECTION ( 'NONE',  ( -1.000000000000000000, -2.952720810173289112E-16, 0.000000000000000000 ) ) ;
#114302=DIRECTION ( 'NONE',  ( 0.000000000000000000, 0.1350103645451876666, -0.9908441862701600211 ) ) ;
#114310=DIRECTION ( 'NONE',  ( 0.000000000000000000, -0.8068669527896844551, -0.5907332058517525963 ) ) ;
#114349=DIRECTION ( 'NONE',  ( 1.000000000000000000, -3.965082230804126670E-15, 0.000000000000000000 ) ) ;
#114351=EDGE_LOOP ( 'NONE', ( #214238, #84784, #39214, #240609, #143797 ) ) ;
#114386=CIRCLE ( 'NONE', #214342, 0.1000000000000053069 ) ;
#114408=CARTESIAN_POINT ( 'NONE',  ( -21.05000000000000071, 1.250000000011155299, -75.00000000000004263 ) ) ;
#114426=VECTOR ( 'NONE', #63014, 1000.000000000000000 ) ;
#114428=DIRECTION ( 'NONE',  ( -1.000000000000000000, 0.000000000000000000, -0.000000000000000000 ) ) ;
#114443=CARTESIAN_POINT ( 'NONE',  ( 18.49999999999999645, 1.866714910068465239, -78.75267524628205251 ) ) ;
#114462=ADVANCED_FACE ( 'NONE', ( #174170 ), #250882, .T. ) ;
#114486=TOROIDAL_SURFACE ( 'NONE', #52110, 0.2000000000000000111, 0.1000000000000000056 ) ;
#114487=CARTESIAN_POINT ( 'NONE',  ( 20.97468175916167965, 10.62526516438217783, -79.25476143541247609 ) ) ;
#114496=LINE ( 'NONE', #76640, #62709 ) ;
#114500=VERTEX_POINT ( 'NONE', #220935 ) ;
#114537=LINE ( 'NONE', #213628, #113142 ) ;
#114564=CARTESIAN_POINT ( 'NONE',  ( 20.85000000000000142, 6.933893972137497030, -104.2856458343736250 ) ) ;
#114574=DIRECTION ( 'NONE',  ( -1.000000000000000000, 0.000000000000000000, 0.000000000000000000 ) ) ;
#114591=CARTESIAN_POINT ( 'NONE',  ( 18.43473516226068298, -9.494942282747077300, -74.04589868334953451 ) ) ;
#114617=EDGE_LOOP ( 'NONE', ( #169561, #138401, #217336, #17426 ) ) ;
#114654=CARTESIAN_POINT ( 'NONE',  ( 18.43630871534874416, -9.679800874791798293, -107.1606320679841247 ) ) ;
#114655=VERTEX_POINT ( 'NONE', #83428 ) ;
#114660=CARTESIAN_POINT ( 'NONE',  ( 18.44364597020194552, -9.490487317151101720, -74.05797788968389739 ) ) ;
#114675=DIRECTION ( 'NONE',  ( 0.000000000000000000, 2.168404344970946942E-15, 1.000000000000000000 ) ) ;
#114690=CIRCLE ( 'NONE', #10465, 0.1000000000000028644 ) ;
#114705=TOROIDAL_SURFACE ( 'NONE', #77098, 11.65000000000000036, 0.1000000000000000056 ) ;
#114761=DIRECTION ( 'NONE',  ( 0.000000000000000000, 3.552713678800407449E-15, -1.000000000000000000 ) ) ;
#114771=PRODUCT_CONTEXT ( 'NONE', #70691, 'mechanical' ) ;
#114804=ADVANCED_FACE ( 'NONE', ( #183843 ), #149878, .F. ) ;
#114853=ORIENTED_EDGE ( 'NONE', *, *, #110095, .F. ) ;
#114907=CARTESIAN_POINT ( 'NONE',  ( 18.59999999999999432, -1.261786168553869603, -75.08649896354552311 ) ) ;
#114966=ORIENTED_EDGE ( 'NONE', *, *, #177181, .F. ) ;
#114970=ORIENTED_EDGE ( 'NONE', *, *, #110658, .F. ) ;
#114977=ORIENTED_EDGE ( 'NONE', *, *, #209871, .T. ) ;
#114979=DIRECTION ( 'NONE',  ( 1.000000000000000000, 0.000000000000000000, 0.000000000000000000 ) ) ;
#115009=CARTESIAN_POINT ( 'NONE',  ( -23.25000000000000000, 1.115600667400684642E-11, -67.00000000000004263 ) ) ;
#115023=DIRECTION ( 'NONE',  ( 0.000000000000000000, 0.000000000000000000, -1.000000000000000000 ) ) ;
#115094=DIRECTION ( 'NONE',  ( 0.000000000000000000, 0.000000000000000000, -1.000000000000000000 ) ) ;
#115120=ADVANCED_FACE ( 'NONE', ( #231339 ), #184615, .T. ) ;
#115134=AXIS2_PLACEMENT_3D ( 'NONE', #79048, #239446, #119501 ) ;
#115137=DIRECTION ( 'NONE',  ( 0.000000000000000000, 0.000000000000000000, 1.000000000000000000 ) ) ;
#115143=ORIENTED_EDGE ( 'NONE', *, *, #213360, .T. ) ;
#115152=CARTESIAN_POINT ( 'NONE',  ( 18.59999999999999432, 1.637172712981537659, -78.58215336547205254 ) ) ;
#115174=EDGE_CURVE ( 'NONE', #39555, #58451, #251241, .T. ) ;
#115191=DIRECTION ( 'NONE',  ( -1.000000000000000000, -0.000000000000000000, -0.000000000000000000 ) ) ;
#115197=CARTESIAN_POINT ( 'NONE',  ( 21.14999999999999858, 6.540656951712400691, -67.00000000000004263 ) ) ;
#115199=ORIENTED_EDGE ( 'NONE', *, *, #10680, .F. ) ;
#115242=DIRECTION ( 'NONE',  ( -1.000000000000000000, -1.836970198721029934E-16, -3.186635328391151676E-31 ) ) ;
#115244=VERTEX_POINT ( 'NONE', #237738 ) ;
#115269=ADVANCED_FACE ( 'NONE', ( #154391 ), #253437, .F. ) ;
#115270=ORIENTED_EDGE ( 'NONE', *, *, #25644, .T. ) ;
#115281=DIRECTION ( 'NONE',  ( 0.000000000000000000, 0.3738317757009345654, 0.9274965247785492695 ) ) ;
#115295=DIRECTION ( 'NONE',  ( 0.000000000000000000, 0.000000000000000000, -1.000000000000000000 ) ) ;
#115296=VERTEX_POINT ( 'NONE', #177792 ) ;
#115309=CARTESIAN_POINT ( 'NONE',  ( -20.85000000000000142, -1.835859311432481045, -112.0044391687985694 ) ) ;
#115312=DIRECTION ( 'NONE',  ( 0.000000000000000000, 0.000000000000000000, -1.000000000000000000 ) ) ;
#115343=EDGE_CURVE ( 'NONE', #38092, #104152, #64011, .T. ) ;
#115348=ADVANCED_FACE ( 'NONE', ( #220744 ), #394, .F. ) ;
#115359=PLANE ( 'NONE',  #128552 ) ;
#115382=SPHERICAL_SURFACE ( 'NONE', #58784, 0.1000000000000000056 ) ;
#115467=CARTESIAN_POINT ( 'NONE',  ( -18.59999999999999787, 11.75000000001115197, -79.15000000000004832 ) ) ;
#115475=EDGE_CURVE ( 'NONE', #136961, #47997, #209759, .T. ) ;
#115494=CARTESIAN_POINT ( 'NONE',  ( -18.55121869061588669, 10.32747123227773045, -106.0774032850249853 ) ) ;
#115509=CIRCLE ( 'NONE', #111429, 0.1000000000000028644 ) ;
#115510=CARTESIAN_POINT ( 'NONE',  ( -23.15000000000000213, 1.115600667400684642E-11, -67.00000000000004263 ) ) ;
#115531=ORIENTED_EDGE ( 'NONE', *, *, #31674, .F. ) ;
#115543=ADVANCED_FACE ( 'NONE', ( #68091 ), #105903, .T. ) ;
#115546=ORIENTED_EDGE ( 'NONE', *, *, #198361, .F. ) ;
#115550=CIRCLE ( 'NONE', #244723, 0.09999999999999917288 ) ;
#115559=EDGE_CURVE ( 'NONE', #147057, #219071, #84818, .T. ) ;
#115573=ORIENTED_EDGE ( 'NONE', *, *, #21439, .F. ) ;
#115642=CARTESIAN_POINT ( 'NONE',  ( 20.04142135623731136, 11.75000000001116263, -91.65000000000004832 ) ) ;
#115693=CARTESIAN_POINT ( 'NONE',  ( 20.95392731769792150, 8.883061479199918509, -75.52222797957135469 ) ) ;
#115702=DIRECTION ( 'NONE',  ( 0.000000000000000000, 0.000000000000000000, 1.000000000000000000 ) ) ;
#115712=CIRCLE ( 'NONE', #119826, 0.2000000000000057288 ) ;
#115748=VECTOR ( 'NONE', #237758, 1000.000000000000000 ) ;
#115753=DIRECTION ( 'NONE',  ( 1.000000000000000000, -0.000000000000000000, 0.000000000000000000 ) ) ;
#115771=CARTESIAN_POINT ( 'NONE',  ( 20.95512840106819752, 10.62384869378447583, -79.20247922079923342 ) ) ;
#115775=DIRECTION ( 'NONE',  ( 0.000000000000000000, 0.000000000000000000, -1.000000000000000000 ) ) ;
#115778=DIRECTION ( 'NONE',  ( 1.000000000000000000, -0.000000000000000000, -0.000000000000000000 ) ) ;
#115814=ORIENTED_EDGE ( 'NONE', *, *, #45170, .F. ) ;
#115839=DIRECTION ( 'NONE',  ( 0.000000000000000000, 0.000000000000000000, -1.000000000000000000 ) ) ;
#115891=ORIENTED_EDGE ( 'NONE', *, *, #193695, .F. ) ;
#115892=VECTOR ( 'NONE', #82363, 1000.000000000000000 ) ;
#115926=ORIENTED_EDGE ( 'NONE', *, *, #251336, .T. ) ;
#115937=AXIS2_PLACEMENT_3D ( 'NONE', #99932, #81644, #221178 ) ;
#115964=VECTOR ( 'NONE', #166905, 1000.000000000000227 ) ;
#115971=AXIS2_PLACEMENT_3D ( 'NONE', #26273, #126647, #87500 ) ;
#115989=EDGE_CURVE ( 'NONE', #135773, #177869, #250272, .T. ) ;
#116016=CIRCLE ( 'NONE', #49359, 0.2000000000000000944 ) ;
#116038=DIRECTION ( 'NONE',  ( -1.000000000000000000, -0.000000000000000000, -0.000000000000000000 ) ) ;
#116042=EDGE_CURVE ( 'NONE', #232478, #81812, #180169, .T. ) ;
#116044=VECTOR ( 'NONE', #238811, 1000.000000000000000 ) ;
#116047=CIRCLE ( 'NONE', #3585, 4.149999999999999467 ) ;
#116072=DIRECTION ( 'NONE',  ( 0.000000000000000000, 0.000000000000000000, -1.000000000000000000 ) ) ;
#116078=FACE_OUTER_BOUND ( 'NONE', #250131, .T. ) ;
#116119=DIRECTION ( 'NONE',  ( 1.000000000000000000, 0.000000000000000000, 0.000000000000000000 ) ) ;
#116125=DIRECTION ( 'NONE',  ( 1.000000000000000000, 0.000000000000000000, 0.000000000000000000 ) ) ;
#116133=CARTESIAN_POINT ( 'NONE',  ( 18.59999999999998721, 6.933893972137497030, -104.2856458343736250 ) ) ;
#116135=AXIS2_PLACEMENT_3D ( 'NONE', #193709, #42031, #133718 ) ;
#116189=ORIENTED_EDGE ( 'NONE', *, *, #137200, .T. ) ;
#116194=CARTESIAN_POINT ( 'NONE',  ( 18.39999999999999858, -9.599999999988845900, -107.1001893912220879 ) ) ;
#116214=CIRCLE ( 'NONE', #158556, 0.09999999999999996392 ) ;
#116217=DIRECTION ( 'NONE',  ( 0.000000000000000000, 0.8660254037844385966, -0.5000000000000003331 ) ) ;
#116218=CIRCLE ( 'NONE', #20542, 11.80000000000000426 ) ;
#116229=ORIENTED_EDGE ( 'NONE', *, *, #139362, .T. ) ;
#116231=AXIS2_PLACEMENT_3D ( 'NONE', #15696, #155208, #56043 ) ;
#116235=AXIS2_PLACEMENT_3D ( 'NONE', #51071, #5542, #224604 ) ;
#116244=ORIENTED_EDGE ( 'NONE', *, *, #151524, .T. ) ;
#116267=AXIS2_PLACEMENT_3D ( 'NONE', #174525, #31146, #253986 ) ;
#116268=DIRECTION ( 'NONE',  ( 0.000000000000000000, 0.000000000000000000, 1.000000000000000000 ) ) ;
#116273=ORIENTED_EDGE ( 'NONE', *, *, #87094, .F. ) ;
#116368=CARTESIAN_POINT ( 'NONE',  ( 19.97071067811864609, 11.72071067812981404, -91.65000000000004832 ) ) ;
#116388=DIRECTION ( 'NONE',  ( 1.000000000000000000, 0.000000000000000000, 0.000000000000000000 ) ) ;
#116427=( BOUNDED_SURFACE ( )  B_SPLINE_SURFACE ( 3, 2, ( 
 ( #11140, #47672, #48971 ),
 ( #51511, #150649, #72413 ),
 ( #110225, #28163, #148083 ),
 ( #108940, #30730, #149389 ),
 ( #89369, #32006, #8574 ),
 ( #166394, #225023, #88072 ),
 ( #249748, #245905, #107661 ),
 ( #127235, #227606, #68549 ),
 ( #12442, #146762, #91950 ),
 ( #189772, #188483, #171526 ),
 ( #46392, #206771, #230177 ),
 ( #226305, #125931, #128519 ) ),
 .UNSPECIFIED., .F., .F., .F. ) 
 B_SPLINE_SURFACE_WITH_KNOTS ( ( 4, 2, 2, 2, 2, 4 ),
 ( 3, 3 ),
 ( 3.174653483277205090, 3.943930578431714018, 4.713207673586222946, 5.482484768740731873, 5.867123316317986337, 6.251761863895240801 ),
 ( 0.000000000000000000, 1.000000000000000000 ),
 .UNSPECIFIED. ) 
 GEOMETRIC_REPRESENTATION_ITEM ( )  RATIONAL_B_SPLINE_SURFACE ( (
 ( 1.000000000000000000, 0.8659465255642401216, 1.000000000000000000),
 ( 1.000000000000000000, 0.8648614068488887918, 1.000000000000000000),
 ( 1.000000000000000000, 0.8489031841323232408, 1.000000000000000000),
 ( 1.000000000000000000, 0.7927507630162343721, 1.000000000000000000),
 ( 1.000000000000000000, 0.7523013859014273663, 1.000000000000000000),
 ( 1.000000000000000000, 0.6616226951191639394, 1.000000000000000000),
 ( 1.000000000000000000, 0.6112214368725455982, 1.000000000000000000),
 ( 1.000000000000000000, 0.5507684314497544031, 1.000000000000000000),
 ( 1.000000000000000000, 0.5333267243152143289, 1.000000000000000000),
 ( 1.000000000000000000, 0.5084565446480221462, 1.000000000000000000),
 ( 1.000000000000000000, 0.5010722703450330995, 1.000000000000000000),
 ( 1.000000000000000000, 0.5001234037138393429, 1.000000000000000000) ) ) 
 REPRESENTATION_ITEM ( '' )  SURFACE ( )  );
#116504=EDGE_CURVE ( 'NONE', #75223, #136961, #151498, .T. ) ;
#116541=CARTESIAN_POINT ( 'NONE',  ( -18.51991288638526001, -9.392436789662124141, -74.14326640395924528 ) ) ;
#116560=AXIS2_PLACEMENT_3D ( 'NONE', #199236, #124830, #222609 ) ;
#116580=CARTESIAN_POINT ( 'NONE',  ( -18.59999999999999787, 1.115600667400684642E-11, -100.5000000000000426 ) ) ;
#116581=CYLINDRICAL_SURFACE ( 'NONE', #215586, 0.09999999999999939493 ) ;
#116604=LINE ( 'NONE', #117878, #101896 ) ;
#116607=CARTESIAN_POINT ( 'NONE',  ( -18.59999999999999787, 9.250000000011157297, -79.25000000000004263 ) ) ;
#116608=ORIENTED_EDGE ( 'NONE', *, *, #215991, .T. ) ;
#116612=ADVANCED_FACE ( 'NONE', ( #120752 ), #238973, .F. ) ;
#116633=EDGE_CURVE ( 'NONE', #73311, #203104, #55568, .T. ) ;
#116641=CARTESIAN_POINT ( 'NONE',  ( -18.59999999999999787, 11.65000000001115232, -88.35000000000003695 ) ) ;
#116656=LINE ( 'NONE', #196195, #33343 ) ;
#116664=VERTEX_POINT ( 'NONE', #168880 ) ;
#116667=CARTESIAN_POINT ( 'NONE',  ( -22.59999999999999787, 0.1008583691098682150, -55.25043287651065782 ) ) ;
#116707=AXIS2_PLACEMENT_3D ( 'NONE', #143863, #219545, #4349 ) ;
#116751=CARTESIAN_POINT ( 'NONE',  ( 18.59999999999997655, 1.115600667400684642E-11, -100.5000000000000426 ) ) ;
#116760=VERTEX_POINT ( 'NONE', #184532 ) ;
#116767=EDGE_CURVE ( 'NONE', #118463, #94180, #247069, .T. ) ;
#116769=EDGE_CURVE ( 'NONE', #181023, #68571, #163948, .T. ) ;
#116807=FACE_OUTER_BOUND ( 'NONE', #184163, .T. ) ;
#116836=DIRECTION ( 'NONE',  ( -0.000000000000000000, -0.000000000000000000, -1.000000000000000000 ) ) ;
#116837=CARTESIAN_POINT ( 'NONE',  ( -21.09316766718153247, 0.03926340232583033080, -60.62984668752533679 ) ) ;
#116842=DIRECTION ( 'NONE',  ( 1.000000000000000000, -0.000000000000000000, -0.000000000000000000 ) ) ;
#116851=CIRCLE ( 'NONE', #183496, 0.09999999999999761857 ) ;
#116875=CARTESIAN_POINT ( 'NONE',  ( 20.94999999999999574, -1.736257131586239844, -78.56865232901753870 ) ) ;
#116925=CARTESIAN_POINT ( 'NONE',  ( 19.75857864376269291, 11.75000000001116263, -91.85000000000005116 ) ) ;
#116944=EDGE_CURVE ( 'NONE', #127382, #179546, #14316, .T. ) ;
#116948=EDGE_CURVE ( 'NONE', #139104, #108958, #223041, .T. ) ;
#117018=ORIENTED_EDGE ( 'NONE', *, *, #4722, .T. ) ;
#117028=EDGE_CURVE ( 'NONE', #211866, #16002, #196110, .T. ) ;
#117059=CARTESIAN_POINT ( 'NONE',  ( 21.09793522318426540, 10.72462451022393282, -79.23929087097731383 ) ) ;
#117083=EDGE_CURVE ( 'NONE', #163525, #206950, #135059, .T. ) ;
#117102=EDGE_LOOP ( 'NONE', ( #202380, #54076, #163173, #24712 ) ) ;
#117143=ORIENTED_EDGE ( 'NONE', *, *, #41904, .F. ) ;
#117145=CIRCLE ( 'NONE', #108756, 11.80000000000000249 ) ;
#117156=CARTESIAN_POINT ( 'NONE',  ( -21.14999999999999858, -11.74999999998884448, -67.00000000000004263 ) ) ;
#117162=CARTESIAN_POINT ( 'NONE',  ( 18.49999999999998579, -9.321008403350155902, -74.23593824907788985 ) ) ;
#117183=ORIENTED_EDGE ( 'NONE', *, *, #223331, .T. ) ;
#117190=FACE_OUTER_BOUND ( 'NONE', #170046, .T. ) ;
#117192=FACE_OUTER_BOUND ( 'NONE', #159769, .T. ) ;
#117215=AXIS2_PLACEMENT_3D ( 'NONE', #71292, #70010, #230330 ) ;
#117233=DIRECTION ( 'NONE',  ( 0.000000000000000000, 0.000000000000000000, -1.000000000000000000 ) ) ;
#117249=( BOUNDED_SURFACE ( )  B_SPLINE_SURFACE ( 3, 2, ( 
 ( #145881, #224137, #187610 ),
 ( #24695, #87182, #127621 ),
 ( #183743, #166778, #246285 ),
 ( #45511, #207165, #108060 ),
 ( #168074, #62515, #142036 ),
 ( #221552, #23415, #102891 ) ),
 .UNSPECIFIED., .F., .F., .T. ) 
 B_SPLINE_SURFACE_WITH_KNOTS ( ( 4, 2, 4 ),
 ( 3, 3 ),
 ( 6.719893378901017553E-05, 0.0002757154632485590319, 0.0004842319927081078341 ),
 ( 0.000000000000000000, 1.000000000000000000 ),
 .UNSPECIFIED. ) 
 GEOMETRIC_REPRESENTATION_ITEM ( )  RATIONAL_B_SPLINE_SURFACE ( (
 ( 1.000000000000000000, 0.7250110520819756932, 1.000000000000000000),
 ( 1.000000000000000000, 0.7277932058357919898, 1.000000000000000000),
 ( 1.000000000000000000, 0.7278452872619233238, 1.000000000000000000),
 ( 1.000000000000000000, 0.7221445671547584988, 1.000000000000000000),
 ( 1.000000000000000000, 0.7163662143780743508, 1.000000000000000000),
 ( 1.000000000000000000, 0.7071067811865475727, 1.000000000000000000) ) ) 
 REPRESENTATION_ITEM ( '' )  SURFACE ( )  );
#117264=DIRECTION ( 'NONE',  ( 0.000000000000000000, -0.6728971962616697722, -0.7397360091702875895 ) ) ;
#117297=CARTESIAN_POINT ( 'NONE',  ( -23.25000000000000000, 1.115650265596050101E-11, -62.95000000000004547 ) ) ;
#117330=ORIENTED_EDGE ( 'NONE', *, *, #91509, .T. ) ;
#117356=VECTOR ( 'NONE', #184114, 1000.000000000000000 ) ;
#117372=ADVANCED_FACE ( 'NONE', ( #33884 ), #121760, .T. ) ;
#117385=VERTEX_POINT ( 'NONE', #218869 ) ;
#117417=CARTESIAN_POINT ( 'NONE',  ( 20.12500000000000000, 9.750000000011153745, -88.25000000000005684 ) ) ;
#117422=AXIS2_PLACEMENT_3D ( 'NONE', #99621, #179220, #202608 ) ;
#117435=AXIS2_PLACEMENT_3D ( 'NONE', #231835, #188836, #227969 ) ;
#117451=ORIENTED_EDGE ( 'NONE', *, *, #87049, .T. ) ;
#117457=FACE_OUTER_BOUND ( 'NONE', #148145, .T. ) ;
#117459=DIRECTION ( 'NONE',  ( 1.000000000000000000, 0.000000000000000000, 0.000000000000000000 ) ) ;
#117482=CARTESIAN_POINT ( 'NONE',  ( -18.59999999999999787, 11.65000000001115232, -79.15000000000003411 ) ) ;
#117485=EDGE_CURVE ( 'NONE', #239872, #104152, #67509, .T. ) ;
#117488=ORIENTED_EDGE ( 'NONE', *, *, #190780, .F. ) ;
#117508=LINE ( 'NONE', #83478, #166316 ) ;
#117513=ORIENTED_EDGE ( 'NONE', *, *, #94114, .F. ) ;
#117557=PLANE ( 'NONE',  #240739 ) ;
#117558=DIRECTION ( 'NONE',  ( -0.000000000000000000, 1.000000000000000000, -0.000000000000000000 ) ) ;
#117572=EDGE_CURVE ( 'NONE', #137421, #121769, #133363, .T. ) ;
#117583=VECTOR ( 'NONE', #59917, 1000.000000000000000 ) ;
#117584=AXIS2_PLACEMENT_3D ( 'NONE', #118831, #60105, #19727 ) ;
#117595=VECTOR ( 'NONE', #191073, 1000.000000000000000 ) ;
#117616=ORIENTED_EDGE ( 'NONE', *, *, #8448, .F. ) ;
#117622=ORIENTED_EDGE ( 'NONE', *, *, #201271, .F. ) ;
#117623=ADVANCED_FACE ( 'NONE', ( #175614 ), #230441, .F. ) ;
#117629=DIRECTION ( 'NONE',  ( 0.000000000000000000, 0.01562499999998609446, -0.9998779222360101304 ) ) ;
#117632=DIRECTION ( 'NONE',  ( -1.000000000000000000, -0.000000000000000000, -0.000000000000000000 ) ) ;
#117660=DIRECTION ( 'NONE',  ( -1.000000000000000000, -2.952720810173289112E-16, 0.000000000000000000 ) ) ;
#117681=DIRECTION ( 'NONE',  ( 1.000000000000000000, 0.000000000000000000, 0.000000000000000000 ) ) ;
#117687=DIRECTION ( 'NONE',  ( -1.000000000000000000, -0.000000000000000000, 0.000000000000000000 ) ) ;
#117738=LINE ( 'NONE', #180287, #238545 ) ;
#117756=CARTESIAN_POINT ( 'NONE',  ( -23.25000000000000000, -9.682403433465239573, -107.1568433774128408 ) ) ;
#117765=CIRCLE ( 'NONE', #151101, 0.1000000000000028644 ) ;
#117766=CARTESIAN_POINT ( 'NONE',  ( 23.25000000000000000, 11.75000000001116263, -88.35000000000003695 ) ) ;
#117838=CARTESIAN_POINT ( 'NONE',  ( 18.49999999999999645, 1.115600667400684642E-11, -100.5000000000000426 ) ) ;
#117850=DIRECTION ( 'NONE',  ( 2.952720810173289112E-16, -1.000000000000000000, 0.000000000000000000 ) ) ;
#117878=CARTESIAN_POINT ( 'NONE',  ( -18.59999999999999787, 9.250000000011157297, -88.25000000000005684 ) ) ;
#117879=ORIENTED_EDGE ( 'NONE', *, *, #145854, .F. ) ;
#117898=CARTESIAN_POINT ( 'NONE',  ( -21.05000000000000071, -1.835341550213255957, -78.55515129256302487 ) ) ;
#117910=ADVANCED_FACE ( 'NONE', ( #5921 ), #47616, .T. ) ;
#117911=DIRECTION ( 'NONE',  ( 1.000000000000000000, 0.000000000000000000, 0.000000000000000000 ) ) ;
#117917=AXIS2_PLACEMENT_3D ( 'NONE', #4586, #147972, #5868 ) ;
#117966=ADVANCED_FACE ( 'NONE', ( #237709 ), #203717, .F. ) ;
#118044=VECTOR ( 'NONE', #52038, 1000.000000000000000 ) ;
#118067=CARTESIAN_POINT ( 'NONE',  ( -18.52643265882458579, 10.31973158071402530, -106.0505334713354983 ) ) ;
#118071=DIRECTION ( 'NONE',  ( 0.000000000000000000, 1.000000000000000000, 0.000000000000000000 ) ) ;
#118078=AXIS2_PLACEMENT_3D ( 'NONE', #206870, #28268, #247262 ) ;
#118089=DIRECTION ( 'NONE',  ( 1.000000000000000000, 0.000000000000000000, 0.000000000000000000 ) ) ;
#118102=ORIENTED_EDGE ( 'NONE', *, *, #23220, .T. ) ;
#118138=ORIENTED_EDGE ( 'NONE', *, *, #35954, .F. ) ;
#118147=EDGE_CURVE ( 'NONE', #100973, #161687, #16466, .T. ) ;
#118148=ORIENTED_EDGE ( 'NONE', *, *, #56740, .T. ) ;
#118177=VERTEX_POINT ( 'NONE', #129314 ) ;
#118180=CYLINDRICAL_SURFACE ( 'NONE', #185159, 0.09999999999999781286 ) ;
#118196=DIRECTION ( 'NONE',  ( -1.000000000000000000, 0.000000000000000000, 0.000000000000000000 ) ) ;
#118206=CARTESIAN_POINT ( 'NONE',  ( 20.94999999999999574, 1.750000000011155743, -78.66951155790169992 ) ) ;
#118283=CYLINDRICAL_SURFACE ( 'NONE', #125028, 0.09999999999999939493 ) ;
#118285=EDGE_CURVE ( 'NONE', #181023, #202644, #49936, .T. ) ;
#118330=AXIS2_PLACEMENT_3D ( 'NONE', #246102, #50429, #49169 ) ;
#118342=CARTESIAN_POINT ( 'NONE',  ( -18.59999999999999787, -9.480686695267820596, -107.4411151687578894 ) ) ;
#118350=CARTESIAN_POINT ( 'NONE',  ( 21.08804281139606474, 10.62183430185231892, -79.34999996737887784 ) ) ;
#118383=VERTEX_POINT ( 'NONE', #226234 ) ;
#118452=DIRECTION ( 'NONE',  ( 0.000000000000000000, 0.9876197685951252359, -0.1568667991644863424 ) ) ;
#118463=VERTEX_POINT ( 'NONE', #30665 ) ;
#118490=AXIS2_PLACEMENT_3D ( 'NONE', #5169, #29928, #148571 ) ;
#118502=VECTOR ( 'NONE', #171817, 1000.000000000000000 ) ;
#118503=DIRECTION ( 'NONE',  ( -0.000000000000000000, -0.000000000000000000, 1.000000000000000000 ) ) ;
#118513=VECTOR ( 'NONE', #145579, 1000.000000000000000 ) ;
#118514=EDGE_LOOP ( 'NONE', ( #181292, #154711, #152226, #54013 ) ) ;
#118527=CARTESIAN_POINT ( 'NONE',  ( 18.47135592147652972, -9.471088613254535105, -107.1835949398435019 ) ) ;
#118554=EDGE_LOOP ( 'NONE', ( #169726, #8026, #47390, #174481 ) ) ;
#118571=CARTESIAN_POINT ( 'NONE',  ( -21.14999999999999858, 1.115600667400684642E-11, -67.00000000000004263 ) ) ;
#118579=CARTESIAN_POINT ( 'NONE',  ( -22.49533356619860669, 11.65000000631534149, -66.93487741967732063 ) ) ;
#118583=CARTESIAN_POINT ( 'NONE',  ( -23.15000000000000213, -11.48912529306489994, -97.40000000000004832 ) ) ;
#118592=ORIENTED_EDGE ( 'NONE', *, *, #246647, .T. ) ;
#118613=ADVANCED_FACE ( 'NONE', ( #96988 ), #176589, .F. ) ;
#118624=CARTESIAN_POINT ( 'NONE',  ( 23.24999999999999289, 11.65000000001116298, -79.15000000000004832 ) ) ;
#118666=DIRECTION ( 'NONE',  ( 1.000000000000000000, 1.875376730785737719E-16, 0.000000000000000000 ) ) ;
#118671=CARTESIAN_POINT ( 'NONE',  ( -21.07928932188134041, 1.115600667400684642E-11, -67.00000000000004263 ) ) ;
#118674=CARTESIAN_POINT ( 'NONE',  ( 23.24999999999999289, 11.75000000001116263, -55.25000000000004974 ) ) ;
#118701=AXIS2_PLACEMENT_3D ( 'NONE', #14231, #168192, #112036 ) ;
#118732=EDGE_CURVE ( 'NONE', #222218, #219071, #103424, .T. ) ;
#118737=DIRECTION ( 'NONE',  ( 0.000000000000000000, 0.000000000000000000, -1.000000000000000000 ) ) ;
#118740=CARTESIAN_POINT ( 'NONE',  ( -21.05000000000000071, -1.851028230129704522, -78.65391326942254580 ) ) ;
#118741=ORIENTED_EDGE ( 'NONE', *, *, #107034, .F. ) ;
#118754=AXIS2_PLACEMENT_3D ( 'NONE', #234418, #216138, #192751 ) ;
#118773=DIRECTION ( 'NONE',  ( 1.000000000000000000, -0.000000000000000000, -0.000000000000000000 ) ) ;
#118785=ORIENTED_EDGE ( 'NONE', *, *, #90257, .F. ) ;
#118788=ADVANCED_FACE ( 'NONE', ( #65604 ), #21372, .T. ) ;
#118790=DIRECTION ( 'NONE',  ( 0.000000000000000000, 1.776356839400310418E-15, -1.000000000000000000 ) ) ;
#118813=AXIS2_PLACEMENT_3D ( 'NONE', #122215, #201738, #63501 ) ;
#118816=DIRECTION ( 'NONE',  ( 0.000000000000000000, 1.000000000000000000, 1.265107689135680095E-16 ) ) ;
#118825=ORIENTED_EDGE ( 'NONE', *, *, #211687, .F. ) ;
#118831=CARTESIAN_POINT ( 'NONE',  ( -21.14999999999999858, -0.09999999998884338825, -55.35042919245524473 ) ) ;
#118836=AXIS2_PLACEMENT_3D ( 'NONE', #180882, #244681, #26965 ) ;
#118919=LINE ( 'NONE', #58895, #13637 ) ;
#118951=EDGE_CURVE ( 'NONE', #211036, #237980, #113725, .T. ) ;
#118969=CARTESIAN_POINT ( 'NONE',  ( -23.25000000000000000, 7.021664781911246322, -104.3335654018973315 ) ) ;
#118974=DIRECTION ( 'NONE',  ( 0.000000000000000000, 0.000000000000000000, -1.000000000000000000 ) ) ;
#118992=DIRECTION ( 'NONE',  ( 0.000000000000000000, 8.673617379883787770E-15, -1.000000000000000000 ) ) ;
#119016=DIRECTION ( 'NONE',  ( 0.000000000000000000, 0.000000000000000000, -1.000000000000000000 ) ) ;
#119019=CARTESIAN_POINT ( 'NONE',  ( 18.59999999999998721, 6.846123162363745074, -104.2377262668499043 ) ) ;
#119041=ORIENTED_EDGE ( 'NONE', *, *, #13614, .F. ) ;
#119047=CARTESIAN_POINT ( 'NONE',  ( -22.39999999999999858, 1.115600667400684642E-11, -59.20922040162664501 ) ) ;
#119051=EDGE_CURVE ( 'NONE', #174644, #40125, #195722, .T. ) ;
#119069=DIRECTION ( 'NONE',  ( -0.000000000000000000, 0.1350103645451876666, 0.9908441862701600211 ) ) ;
#119076=AXIS2_PLACEMENT_3D ( 'NONE', #4184, #202399, #19929 ) ;
#119084=DIRECTION ( 'NONE',  ( 1.000000000000000000, -0.000000000000000000, -0.000000000000000000 ) ) ;
#119102=DIRECTION ( 'NONE',  ( 0.000000000000000000, 0.000000000000000000, -1.000000000000000000 ) ) ;
#119110=CARTESIAN_POINT ( 'NONE',  ( -18.46946985241261530, -9.509317228700416180, -73.98666256549968523 ) ) ;
#119113=EDGE_LOOP ( 'NONE', ( #99606, #37157, #236352, #111990, #169230 ) ) ;
#119133=ORIENTED_EDGE ( 'NONE', *, *, #104438, .F. ) ;
#119146=CYLINDRICAL_SURFACE ( 'NONE', #25998, 0.1000000000000000472 ) ;
#119167=CARTESIAN_POINT ( 'NONE',  ( -18.50000000000000000, -1.162701749926853712, -75.10000000000003695 ) ) ;
#119173=ORIENTED_EDGE ( 'NONE', *, *, #197227, .F. ) ;
#119176=CARTESIAN_POINT ( 'NONE',  ( -20.54999999999999716, 2.000000000011154189, -79.72462192276213955 ) ) ;
#119194=LINE ( 'NONE', #219552, #162017 ) ;
#119204=DIRECTION ( 'NONE',  ( 1.000000000000000000, -0.000000000000000000, -0.000000000000000000 ) ) ;
#119208=VERTEX_POINT ( 'NONE', #168313 ) ;
#119209=DIRECTION ( 'NONE',  ( 0.000000000000000000, 1.000000000000000000, 0.000000000000000000 ) ) ;
#119213=CIRCLE ( 'NONE', #169324, 0.1000000000000028644 ) ;
#119229=CARTESIAN_POINT ( 'NONE',  ( 21.14999999999999503, -11.74999999998883560, -55.25000000000004974 ) ) ;
#119247=CARTESIAN_POINT ( 'NONE',  ( -20.54999999999999716, 1.115600667400684642E-11, -100.5000000000000426 ) ) ;
#119284=AXIS2_PLACEMENT_3D ( 'NONE', #200987, #43201, #4062 ) ;
#119333=ORIENTED_EDGE ( 'NONE', *, *, #217117, .T. ) ;
#119336=ORIENTED_EDGE ( 'NONE', *, *, #204273, .T. ) ;
#119337=ADVANCED_FACE ( 'NONE', ( #192973 ), #78133, .F. ) ;
#119345=ORIENTED_EDGE ( 'NONE', *, *, #223539, .T. ) ;
#119364=DIRECTION ( 'NONE',  ( -0.000000000000000000, 0.000000000000000000, 1.000000000000000000 ) ) ;
#119386=ORIENTED_EDGE ( 'NONE', *, *, #99914, .F. ) ;
#119415=EDGE_LOOP ( 'NONE', ( #93759, #26581, #19976, #167840 ) ) ;
#119437=B_SPLINE_CURVE_WITH_KNOTS ( 'NONE', 3,
 ( #66874, #125560, #146386, #65585, #26476, #105971 ),
 .UNSPECIFIED., .F., .F.,
 ( 4, 2, 4 ),
 ( 0.000000000000000000, 0.0001891491689349542970, 0.0003782983378699085941 ),
 .UNSPECIFIED. ) ;
#119443=ORIENTED_EDGE ( 'NONE', *, *, #243245, .F. ) ;
#119452=EDGE_CURVE ( 'NONE', #6741, #242523, #179509, .T. ) ;
#119488=DIRECTION ( 'NONE',  ( -0.000000000000000000, -0.000000000000000000, 1.000000000000000000 ) ) ;
#119501=DIRECTION ( 'NONE',  ( 0.000000000000000000, 5.204170427930272346E-14, -1.000000000000000000 ) ) ;
#119502=AXIS2_PLACEMENT_3D ( 'NONE', #9914, #129852, #222866 ) ;
#119523=EDGE_LOOP ( 'NONE', ( #94953, #218738, #52408, #193160, #182290, #158458, #87588, #95332 ) ) ;
#119572=CARTESIAN_POINT ( 'NONE',  ( 20.94999999999999574, -11.64999999998883595, -70.00000000000004263 ) ) ;
#119595=DIRECTION ( 'NONE',  ( 0.000000000000000000, 1.000000000000000000, 0.000000000000000000 ) ) ;
#119599=VECTOR ( 'NONE', #214765, 1000.000000000000114 ) ;
#119603=CIRCLE ( 'NONE', #7134, 0.5000000000000004441 ) ;
#119604=ORIENTED_EDGE ( 'NONE', *, *, #76734, .T. ) ;
#119627=CARTESIAN_POINT ( 'NONE',  ( -18.58735405345342784, -9.566478620325442606, -107.3227146462660357 ) ) ;
#119633=VECTOR ( 'NONE', #212587, 1000.000000000000000 ) ;
#119639=ORIENTED_EDGE ( 'NONE', *, *, #112968, .F. ) ;
#119658=EDGE_CURVE ( 'NONE', #200601, #175862, #12929, .T. ) ;
#119662=CARTESIAN_POINT ( 'NONE',  ( -18.59999999999999787, -1.835859311432484375, -112.0044391687985694 ) ) ;
#119755=CARTESIAN_POINT ( 'NONE',  ( -20.99142135623731065, 11.60000000001115161, -93.57179676972452853 ) ) ;
#119770=VERTEX_POINT ( 'NONE', #219916 ) ;
#119809=ORIENTED_EDGE ( 'NONE', *, *, #217999, .T. ) ;
#119826=AXIS2_PLACEMENT_3D ( 'NONE', #32026, #72431, #108955 ) ;
#119842=CYLINDRICAL_SURFACE ( 'NONE', #174756, 0.5000000000000004441 ) ;
#119889=CARTESIAN_POINT ( 'NONE',  ( 21.40925344232283223, 0.09895018863080314031, -60.34148114060958790 ) ) ;
#119905=ORIENTED_EDGE ( 'NONE', *, *, #65709, .F. ) ;
#119906=AXIS2_PLACEMENT_3D ( 'NONE', #248083, #228540, #149011 ) ;
#119916=ORIENTED_EDGE ( 'NONE', *, *, #200115, .F. ) ;
#119919=LINE ( 'NONE', #256771, #6494 ) ;
#119920=DIRECTION ( 'NONE',  ( 0.000000000000000000, -0.8700118002898321601, 0.4930308989875230030 ) ) ;
#119989=EDGE_CURVE ( 'NONE', #179663, #58814, #52798, .T. ) ;
#120000=ORIENTED_EDGE ( 'NONE', *, *, #195409, .T. ) ;
#120025=DIRECTION ( 'NONE',  ( -1.000000000000000000, -1.836970198721029934E-16, 0.000000000000000000 ) ) ;
#120026=AXIS2_PLACEMENT_3D ( 'NONE', #51533, #170284, #210644 ) ;
#120034=EDGE_CURVE ( 'NONE', #146995, #13313, #17366, .T. ) ;
#120038=CYLINDRICAL_SURFACE ( 'NONE', #186291, 0.09999999999999892308 ) ;
#120049=CARTESIAN_POINT ( 'NONE',  ( 21.04999999999999716, 0.01471785653530480707, -60.65527659590978260 ) ) ;
#120052=CARTESIAN_POINT ( 'NONE',  ( 18.39999999999999858, -9.499999999988842703, -74.03206939669971121 ) ) ;
#120134=ORIENTED_EDGE ( 'NONE', *, *, #12557, .F. ) ;
#120195=ORIENTED_EDGE ( 'NONE', *, *, #86162, .F. ) ;
#120202=FACE_OUTER_BOUND ( 'NONE', #193192, .T. ) ;
#120239=ORIENTED_EDGE ( 'NONE', *, *, #4588, .F. ) ;
#120250=ORIENTED_EDGE ( 'NONE', *, *, #92253, .F. ) ;
#120271=CARTESIAN_POINT ( 'NONE',  ( 18.49505816908823874, -9.437872553199980530, -107.2776572016709480 ) ) ;
#120300=EDGE_LOOP ( 'NONE', ( #204947, #124612, #251248 ) ) ;
#120321=VECTOR ( 'NONE', #57347, 1000.000000000000000 ) ;
#120329=CARTESIAN_POINT ( 'NONE',  ( 21.14999999999999503, -11.64999999998883595, -69.90000000000004832 ) ) ;
#120362=VERTEX_POINT ( 'NONE', #157781 ) ;
#120408=VERTEX_POINT ( 'NONE', #152622 ) ;
#120431=ORIENTED_EDGE ( 'NONE', *, *, #93916, .T. ) ;
#120441=DIRECTION ( 'NONE',  ( 0.000000000000000000, 0.9908441862701596881, -0.1350103645451904977 ) ) ;
#120446=DIRECTION ( 'NONE',  ( 0.000000000000000000, -0.000000000000000000, -1.000000000000000000 ) ) ;
#120459=VECTOR ( 'NONE', #35935, 1000.000000000000000 ) ;
#120484=ORIENTED_EDGE ( 'NONE', *, *, #134131, .F. ) ;
#120521=EDGE_CURVE ( 'NONE', #194521, #114130, #46557, .T. ) ;
#120524=CARTESIAN_POINT ( 'NONE',  ( -21.05000000000000071, 1.115600667400684642E-11, -88.70000000000004547 ) ) ;
#120564=DIRECTION ( 'NONE',  ( 0.000000000000000000, -1.000000000000000000, 0.000000000000000000 ) ) ;
#120615=ORIENTED_EDGE ( 'NONE', *, *, #118285, .T. ) ;
#120627=ORIENTED_EDGE ( 'NONE', *, *, #149898, .T. ) ;
#120632=DIRECTION ( 'NONE',  ( 1.000000000000000000, 3.265361837132813093E-16, -0.000000000000000000 ) ) ;
#120664=DIRECTION ( 'NONE',  ( 1.000000000000000000, 0.000000000000000000, 0.000000000000000000 ) ) ;
#120704=EDGE_CURVE ( 'NONE', #129546, #223130, #42659, .T. ) ;
#120711=EDGE_CURVE ( 'NONE', #217161, #257895, #248830, .T. ) ;
#120722=CARTESIAN_POINT ( 'NONE',  ( 18.49999999999998934, 10.29288807859941457, -105.9580020160122018 ) ) ;
#120752=FACE_OUTER_BOUND ( 'NONE', #86814, .T. ) ;
#120763=DIRECTION ( 'NONE',  ( 0.000000000000000000, 0.008583690987128220901, 0.9999631594459055250 ) ) ;
#120784=DIRECTION ( 'NONE',  ( 1.000000000000000000, -0.000000000000000000, -0.000000000000000000 ) ) ;
#120817=VERTEX_POINT ( 'NONE', #114443 ) ;
#120828=EDGE_LOOP ( 'NONE', ( #30337, #201936, #51804, #95369, #223052 ) ) ;
#120832=ORIENTED_EDGE ( 'NONE', *, *, #79950, .F. ) ;
#120837=CARTESIAN_POINT ( 'NONE',  ( -22.39999999999999858, 1.115600667400684642E-11, -55.35042919245524473 ) ) ;
#120855=DIRECTION ( 'NONE',  ( 0.000000000000000000, 0.000000000000000000, 1.000000000000000000 ) ) ;
#120857=ORIENTED_EDGE ( 'NONE', *, *, #54484, .F. ) ;
#120868=CARTESIAN_POINT ( 'NONE',  ( -18.59999999999999787, 11.75000000001115552, -100.5000000000000426 ) ) ;
#120878=EDGE_CURVE ( 'NONE', #244178, #179546, #80037, .T. ) ;
#120895=AXIS2_PLACEMENT_3D ( 'NONE', #240107, #161870, #41924 ) ;
#120916=ADVANCED_FACE ( 'NONE', ( #182123 ), #142598, .F. ) ;
#120940=CARTESIAN_POINT ( 'NONE',  ( 21.05000000000000071, 1.115600667400684642E-11, -104.6000000000000512 ) ) ;
#120982=LINE ( 'NONE', #139203, #12460 ) ;
#120984=EDGE_CURVE ( 'NONE', #183920, #211645, #125984, .T. ) ;
#121010=CARTESIAN_POINT ( 'NONE',  ( -23.15000000000000213, 11.65000000001115588, -67.00000000000004263 ) ) ;
#121016=CARTESIAN_POINT ( 'NONE',  ( 21.04999999999999716, 6.304455821958818262, -67.02103547654014903 ) ) ;
#121069=ORIENTED_EDGE ( 'NONE', *, *, #207716, .F. ) ;
#121086=CARTESIAN_POINT ( 'NONE',  ( -18.59999999999999787, 1.261786168576181755, -75.08649896354552311 ) ) ;
#121093=CARTESIAN_POINT ( 'NONE',  ( -18.59999999999999787, -1.835859311432481045, -112.0044391687985694 ) ) ;
#121153=EDGE_CURVE ( 'NONE', #254405, #170816, #26112, .T. ) ;
#121159=ORIENTED_EDGE ( 'NONE', *, *, #55702, .F. ) ;
#121203=VERTEX_POINT ( 'NONE', #176692 ) ;
#121261=CARTESIAN_POINT ( 'NONE',  ( 21.14999999999999503, -11.74999999998883560, -69.90000000000004832 ) ) ;
#121345=CARTESIAN_POINT ( 'NONE',  ( 21.05000000000000071, 8.776282895303632259, -79.15000000000004832 ) ) ;
#121346=ORIENTED_EDGE ( 'NONE', *, *, #253111, .T. ) ;
#121372=EDGE_CURVE ( 'NONE', #86923, #127210, #197143, .T. ) ;
#121429=ORIENTED_EDGE ( 'NONE', *, *, #201878, .F. ) ;
#121430=CIRCLE ( 'NONE', #142236, 0.1000000000000028644 ) ;
#121460=DIRECTION ( 'NONE',  ( 1.000000000000000000, 0.000000000000000000, 0.000000000000000000 ) ) ;
#121465=CARTESIAN_POINT ( 'NONE',  ( -20.92356734117541706, 10.31973158071402175, -106.0505334713354841 ) ) ;
#121471=CARTESIAN_POINT ( 'NONE',  ( -20.94999999999999929, -1.249999999988843369, -75.00000000000004263 ) ) ;
#121526=DIRECTION ( 'NONE',  ( 1.000000000000000000, -0.000000000000000000, -0.000000000000000000 ) ) ;
#121530=CIRCLE ( 'NONE', #79776, 7.900000000000003908 ) ;
#121550=EDGE_CURVE ( 'NONE', #149698, #146995, #138498, .T. ) ;
#121563=ORIENTED_EDGE ( 'NONE', *, *, #43180, .F. ) ;
#121568=CARTESIAN_POINT ( 'NONE',  ( 20.94999999999999929, 11.65000000001115943, -93.71613433702195550 ) ) ;
#121575=EDGE_CURVE ( 'NONE', #63408, #224607, #217974, .T. ) ;
#121649=EDGE_CURVE ( 'NONE', #111810, #188971, #122152, .T. ) ;
#121684=ADVANCED_FACE ( 'NONE', ( #178033 ), #97343, .T. ) ;
#121731=DIRECTION ( 'NONE',  ( -1.000000000000000000, -0.000000000000000000, -0.000000000000000000 ) ) ;
#121733=DIRECTION ( 'NONE',  ( -1.000000000000000000, 0.000000000000000000, 0.000000000000000000 ) ) ;
#121748=EDGE_CURVE ( 'NONE', #54519, #205409, #14006, .T. ) ;
#121760=( BOUNDED_SURFACE ( )  B_SPLINE_SURFACE ( 3, 2, ( 
 ( #113373, #174682, #192916 ),
 ( #177226, #237177, #93797 ),
 ( #213751, #35159, #114654 ),
 ( #194220, #254146, #75553 ),
 ( #155099, #234596, #44104 ),
 ( #164058, #181064, #158943 ),
 ( #118527, #203169, #101455 ),
 ( #102763, #238451, #61092 ),
 ( #222721, #81904, #182344 ),
 ( #3680, #104045, #199338 ) ),
 .UNSPECIFIED., .F., .F., .F. ) 
 B_SPLINE_SURFACE_WITH_KNOTS ( ( 4, 2, 2, 2, 4 ),
 ( 3, 3 ),
 ( 0.0001701955120502369480, 0.0002247052511886141093, 0.0002792149903269912706, 0.0003882344686037456473, 0.0006062734251572542924 ),
 ( 0.000000000000000000, 1.000000000000000000 ),
 .UNSPECIFIED. ) 
 GEOMETRIC_REPRESENTATION_ITEM ( )  RATIONAL_B_SPLINE_SURFACE ( (
 ( 1.000000000000000000, 0.2966190024561626837, 1.000000000000000000),
 ( 1.000000000000000000, 0.2964522492704476098, 1.000000000000000000),
 ( 1.000000000000000000, 0.3059923531893983806, 1.000000000000000000),
 ( 1.000000000000000000, 0.3355751146934523033, 1.000000000000000000),
 ( 1.000000000000000000, 0.3550672384964473349, 1.000000000000000000),
 ( 1.000000000000000000, 0.4157034672179019674, 1.000000000000000000),
 ( 1.000000000000000000, 0.4588031877652369306, 1.000000000000000000),
 ( 1.000000000000000000, 0.5771441759665676408, 1.000000000000000000),
 ( 1.000000000000000000, 0.6469377121768183914, 1.000000000000000000),
 ( 1.000000000000000000, 0.7071067811865376918, 1.000000000000000000) ) ) 
 REPRESENTATION_ITEM ( '' )  SURFACE ( )  );
#121769=VERTEX_POINT ( 'NONE', #104853 ) ;
#121789=EDGE_CURVE ( 'NONE', #64899, #184752, #103587, .T. ) ;
#121792=CARTESIAN_POINT ( 'NONE',  ( 20.95443524775735256, 8.878554263883966513, -75.53372227560019780 ) ) ;
#121800=EDGE_CURVE ( 'NONE', #140759, #159539, #93090, .T. ) ;
#121811=ORIENTED_EDGE ( 'NONE', *, *, #233913, .F. ) ;
#121820=DIRECTION ( 'NONE',  ( -0.000000000000000000, 1.000000000000000000, -0.000000000000000000 ) ) ;
#121845=DIRECTION ( 'NONE',  ( 0.000000000000000000, 0.000000000000000000, 1.000000000000000000 ) ) ;
#121876=DIRECTION ( 'NONE',  ( -0.000000000000000000, -0.000000000000000000, 1.000000000000000000 ) ) ;
#121880=CIRCLE ( 'NONE', #221793, 0.1000000000000028644 ) ;
#121930=CARTESIAN_POINT ( 'NONE',  ( 22.45305468355010348, -0.1008583690885486023, -55.25043287651032387 ) ) ;
#121936=SPHERICAL_SURFACE ( 'NONE', #52690, 0.1000000000000000056 ) ;
#121963=EDGE_LOOP ( 'NONE', ( #175429, #7866, #108689, #215476 ) ) ;
#121968=ADVANCED_FACE ( 'NONE', ( #133451 ), #172632, .F. ) ;
#121977=CARTESIAN_POINT ( 'NONE',  ( 18.39999999999999858, -9.599999999988845900, -107.2001893912220964 ) ) ;
#121992=DIRECTION ( 'NONE',  ( 0.000000000000000000, 0.000000000000000000, -1.000000000000000000 ) ) ;
#121998=CARTESIAN_POINT ( 'NONE',  ( -21.05000000000000071, 1.162701749949165642, -75.00000000000004263 ) ) ;
#122086=ORIENTED_EDGE ( 'NONE', *, *, #121575, .F. ) ;
#122088=( NAMED_UNIT ( * ) SI_UNIT ( $, .STERADIAN. ) SOLID_ANGLE_UNIT ( ) );
#122106=LINE ( 'NONE', #102498, #179194 ) ;
#122113=ORIENTED_EDGE ( 'NONE', *, *, #78524, .T. ) ;
#122140=CARTESIAN_POINT ( 'NONE',  ( 22.50000000000000000, 11.64957080755595520, -66.90000000000004832 ) ) ;
#122152=CIRCLE ( 'NONE', #138848, 7.900000000000000355 ) ;
#122165=ORIENTED_EDGE ( 'NONE', *, *, #39991, .F. ) ;
#122173=VECTOR ( 'NONE', #17343, 1000.000000000000227 ) ;
#122175=B_SPLINE_CURVE_WITH_KNOTS ( 'NONE', 3,
 ( #73392, #152933, #232457, #253266, #74685, #49935, #129489, #12129, #52492, #233731 ),
 .UNSPECIFIED., .F., .F.,
 ( 4, 3, 3, 4 ),
 ( 0.000000000000000000, 0.0002000000000002884074, 0.001000000000045112589, 0.001967863649472103085 ),
 .UNSPECIFIED. ) ;
#122186=AXIS2_PLACEMENT_3D ( 'NONE', #241176, #138183, #62525 ) ;
#122215=CARTESIAN_POINT ( 'NONE',  ( 20.94999999999999929, 1.115600667400684642E-11, -67.00000000000004263 ) ) ;
#122217=ORIENTED_EDGE ( 'NONE', *, *, #174890, .T. ) ;
#122218=CARTESIAN_POINT ( 'NONE',  ( -20.64999999999999858, -8.663551401858001100, -90.97589888193274987 ) ) ;
#122247=AXIS2_PLACEMENT_3D ( 'NONE', #109473, #14264, #189032 ) ;
#122261=ORIENTED_EDGE ( 'NONE', *, *, #197530, .F. ) ;
#122273=CARTESIAN_POINT ( 'NONE',  ( 18.58719872626880232, -9.566644397587486637, -107.3224781963970571 ) ) ;
#122293=ORIENTED_EDGE ( 'NONE', *, *, #14471, .F. ) ;
#122315=CARTESIAN_POINT ( 'NONE',  ( 21.05000000000000071, 1.115600667400684642E-11, -100.5000000000000426 ) ) ;
#122327=CARTESIAN_POINT ( 'NONE',  ( 21.05000000000000071, 5.000000000011153745, -88.09473398108696074 ) ) ;
#122341=EDGE_LOOP ( 'NONE', ( #69431, #243034, #202172, #56835 ) ) ;
#122383=DIRECTION ( 'NONE',  ( 1.000000000000000000, -0.000000000000000000, -0.000000000000000000 ) ) ;
#122398=EDGE_CURVE ( 'NONE', #135773, #150875, #105912, .T. ) ;
#122417=DIRECTION ( 'NONE',  ( -0.000000000000000000, 1.000000000000000000, -0.000000000000000000 ) ) ;
#122418=ORIENTED_EDGE ( 'NONE', *, *, #167268, .T. ) ;
#122426=EDGE_CURVE ( 'NONE', #219071, #201185, #126789, .T. ) ;
#122429=ORIENTED_EDGE ( 'NONE', *, *, #95490, .T. ) ;
#122433=DIRECTION ( 'NONE',  ( -1.000000000000000000, 0.000000000000000000, 0.000000000000000000 ) ) ;
#122438=CARTESIAN_POINT ( 'NONE',  ( 22.01447462590973458, 0.09903700007069084210, -59.73619979877013719 ) ) ;
#122459=CARTESIAN_POINT ( 'NONE',  ( 20.94999999999999574, 11.62071067812981795, -93.63158334765908819 ) ) ;
#122480=DIRECTION ( 'NONE',  ( -0.000000000000000000, -1.000000000000000000, 6.308085367188393199E-16 ) ) ;
#122491=VECTOR ( 'NONE', #213946, 1000.000000000000000 ) ;
#122500=CARTESIAN_POINT ( 'NONE',  ( 20.94999999999999574, 6.400000000011158541, -76.93042463006162279 ) ) ;
#122543=DIRECTION ( 'NONE',  ( 0.000000000000000000, 0.000000000000000000, -1.000000000000000000 ) ) ;
#122595=CARTESIAN_POINT ( 'NONE',  ( 20.94999999999999929, 14.05000000001115623, -94.98630492923912527 ) ) ;
#122606=VECTOR ( 'NONE', #97337, 1000.000000000000000 ) ;
#122607=ORIENTED_EDGE ( 'NONE', *, *, #199004, .T. ) ;
#122616=ORIENTED_EDGE ( 'NONE', *, *, #208445, .T. ) ;
#122625=CARTESIAN_POINT ( 'NONE',  ( -20.85000000000000142, 6.846123162363745074, -104.2377262668499043 ) ) ;
#122626=ORIENTED_EDGE ( 'NONE', *, *, #116948, .T. ) ;
#122664=ORIENTED_EDGE ( 'NONE', *, *, #142246, .F. ) ;
#122667=ORIENTED_EDGE ( 'NONE', *, *, #37225, .F. ) ;
#122675=ORIENTED_EDGE ( 'NONE', *, *, #11084, .F. ) ;
#122685=ORIENTED_EDGE ( 'NONE', *, *, #31914, .F. ) ;
#122718=FACE_OUTER_BOUND ( 'NONE', #31008, .T. ) ;
#122728=ORIENTED_EDGE ( 'NONE', *, *, #104546, .T. ) ;
#122745=AXIS2_PLACEMENT_3D ( 'NONE', #207595, #210156, #87607 ) ;
#122760=CARTESIAN_POINT ( 'NONE',  ( -21.05000000000000071, -0.09999996528894432302, -60.52244781750656699 ) ) ;
#122775=AXIS2_PLACEMENT_3D ( 'NONE', #93723, #173318, #211108 ) ;
#122781=DIRECTION ( 'NONE',  ( 0.000000000000000000, 2.664535259100315349E-15, -1.000000000000000000 ) ) ;
#122783=DIRECTION ( 'NONE',  ( 0.000000000000000000, -1.000000000000000000, 0.000000000000000000 ) ) ;
#122785=AXIS2_PLACEMENT_3D ( 'NONE', #124517, #145343, #8421 ) ;
#122814=ADVANCED_FACE ( 'NONE', ( #256572 ), #153738, .T. ) ;
#122815=LINE ( 'NONE', #47087, #52654 ) ;
#122868=ORIENTED_EDGE ( 'NONE', *, *, #140521, .T. ) ;
#122869=DIRECTION ( 'NONE',  ( 0.000000000000000000, 0.5000000000000078826, -0.8660254037844340447 ) ) ;
#122881=CARTESIAN_POINT ( 'NONE',  ( 18.59999999999999076, 1.750000000011155743, -78.66951155790169992 ) ) ;
#122920=ORIENTED_EDGE ( 'NONE', *, *, #208124, .T. ) ;
#122924=CIRCLE ( 'NONE', #81192, 12.77499999999999503 ) ;
#122933=ORIENTED_EDGE ( 'NONE', *, *, #12921, .F. ) ;
#122950=AXIS2_PLACEMENT_3D ( 'NONE', #23828, #242837, #244116 ) ;
#122967=DIRECTION ( 'NONE',  ( 0.000000000000000000, 0.000000000000000000, -1.000000000000000000 ) ) ;
#123013=CYLINDRICAL_SURFACE ( 'NONE', #234394, 0.09999999999999804878 ) ;
#123054=VERTEX_POINT ( 'NONE', #129633 ) ;
#123062=EDGE_CURVE ( 'NONE', #102833, #210821, #243106, .T. ) ;
#123063=DIRECTION ( 'NONE',  ( 0.000000000000000000, -6.308085367188393199E-16, -1.000000000000000000 ) ) ;
#123078=FACE_OUTER_BOUND ( 'NONE', #51931, .T. ) ;
#123083=ORIENTED_EDGE ( 'NONE', *, *, #158026, .F. ) ;
#123086=DIRECTION ( 'NONE',  ( 1.000000000000000000, 0.000000000000000000, 0.000000000000000000 ) ) ;
#123090=DIRECTION ( 'NONE',  ( 0.000000000000000000, 0.000000000000000000, 1.000000000000000000 ) ) ;
#123126=EDGE_CURVE ( 'NONE', #15594, #108958, #168148, .T. ) ;
#123162=AXIS2_PLACEMENT_3D ( 'NONE', #170798, #95051, #174650 ) ;
#123165=DIRECTION ( 'NONE',  ( 1.000000000000000000, -0.000000000000000000, -0.000000000000000000 ) ) ;
#123178=CARTESIAN_POINT ( 'NONE',  ( 21.05193202509564898, 10.72393601970834354, -79.17253460332581483 ) ) ;
#123191=CARTESIAN_POINT ( 'NONE',  ( -20.94999999999999929, 1.835341550235569663, -78.55515129256303908 ) ) ;
#123198=CYLINDRICAL_SURFACE ( 'NONE', #233791, 0.09999999999999939493 ) ;
#123206=CARTESIAN_POINT ( 'NONE',  ( 22.59999999999999787, 0.04781839071596413748, -55.24997758095282308 ) ) ;
#123211=LINE ( 'NONE', #198892, #202545 ) ;
#123250=DIRECTION ( 'NONE',  ( 0.000000000000000000, 1.000000000000000000, 0.000000000000000000 ) ) ;
#123272=DIRECTION ( 'NONE',  ( 0.000000000000000000, 1.224646799142015331E-16, 1.000000000000000000 ) ) ;
#123278=ORIENTED_EDGE ( 'NONE', *, *, #205397, .F. ) ;
#123294=( BOUNDED_SURFACE ( )  B_SPLINE_SURFACE ( 3, 2, ( 
 ( #47225, #227158, #126781 ),
 ( #128072, #45959, #125497 ),
 ( #184176, #26417, #48524 ),
 ( #206326, #66813, #105905 ),
 ( #188050, #165935, #107212 ),
 ( #88921, #186773, #8127 ) ),
 .UNSPECIFIED., .F., .F., .F. ) 
 B_SPLINE_SURFACE_WITH_KNOTS ( ( 4, 2, 4 ),
 ( 3, 3 ),
 ( 1.570796326794895448, 2.356194490192343505, 3.141592653589791784 ),
 ( 0.000000000000000000, 1.000000000000000000 ),
 .UNSPECIFIED. ) 
 GEOMETRIC_REPRESENTATION_ITEM ( )  RATIONAL_B_SPLINE_SURFACE ( (
 ( 1.000000000000000000, 0.7071067811865352493, 1.000000000000000000),
 ( 1.000000000000000000, 0.6611148371780189992, 1.000000000000000000),
 ( 1.000000000000000000, 0.6092287576694327411, 1.000000000000000000),
 ( 1.000000000000000000, 0.5278258667059284592, 1.000000000000000000),
 ( 1.000000000000000000, 0.4993418825333061917, 1.000000000000000000),
 ( 1.000000000000000000, 0.4999999999999960587, 1.000000000000000000) ) ) 
 REPRESENTATION_ITEM ( '' )  SURFACE ( )  );
#123317=ORIENTED_EDGE ( 'NONE', *, *, #19455, .T. ) ;
#123332=DIRECTION ( 'NONE',  ( 0.000000000000000000, 0.000000000000000000, -1.000000000000000000 ) ) ;
#123346=CARTESIAN_POINT ( 'NONE',  ( 21.04999999999999716, 10.68430915749624077, -74.52669679032690908 ) ) ;
#123372=ORIENTED_EDGE ( 'NONE', *, *, #167462, .F. ) ;
#123390=ORIENTED_EDGE ( 'NONE', *, *, #27988, .F. ) ;
#123399=ORIENTED_EDGE ( 'NONE', *, *, #208768, .F. ) ;
#123409=CARTESIAN_POINT ( 'NONE',  ( -21.05000000000000071, -11.64999999998884306, -97.50000000000004263 ) ) ;
#123423=ADVANCED_FACE ( 'NONE', ( #53649 ), #130611, .T. ) ;
#123428=DIRECTION ( 'NONE',  ( 1.000000000000000000, 0.000000000000000000, 0.000000000000000000 ) ) ;
#123449=CARTESIAN_POINT ( 'NONE',  ( 21.14999999999999858, -0.09999999998884338825, -60.45934304829879835 ) ) ;
#123465=CARTESIAN_POINT ( 'NONE',  ( -18.43707690579160641, -9.682403433465239573, -107.1568433774128266 ) ) ;
#123466=CARTESIAN_POINT ( 'NONE',  ( -21.00023020733438273, 6.390869245278866018, -67.00000000000004263 ) ) ;
#123468=DIRECTION ( 'NONE',  ( 0.000000000000000000, 0.000000000000000000, 1.000000000000000000 ) ) ;
#123480=DIRECTION ( 'NONE',  ( -6.938893903907222067E-15, 1.000000000000000000, 0.000000000000000000 ) ) ;
#123495=EDGE_CURVE ( 'NONE', #224755, #198610, #159927, .T. ) ;
#123539=CARTESIAN_POINT ( 'NONE',  ( 21.05000000000000071, 1.115600667400684642E-11, -100.5000000000000426 ) ) ;
#123566=CARTESIAN_POINT ( 'NONE',  ( -18.58671080940899856, -9.406932858815459042, -74.12415446490474835 ) ) ;
#123588=VERTEX_POINT ( 'NONE', #114907 ) ;
#123593=CARTESIAN_POINT ( 'NONE',  ( 20.94999999999999929, 5.500000000011153745, -88.09473398108696074 ) ) ;
#123633=CIRCLE ( 'NONE', #86180, 0.09999999999999761857 ) ;
#123654=CARTESIAN_POINT ( 'NONE',  ( 21.07928932188134397, 0.09889514566555242248, -60.67148334360673800 ) ) ;
#123657=LINE ( 'NONE', #64944, #221931 ) ;
#123679=CARTESIAN_POINT ( 'NONE',  ( 22.41477678272288188, 0.0008238657741001866345, -55.35041471548464642 ) ) ;
#123688=ORIENTED_EDGE ( 'NONE', *, *, #160313, .T. ) ;
#123689=ORIENTED_EDGE ( 'NONE', *, *, #50112, .F. ) ;
#123697=DIRECTION ( 'NONE',  ( -1.000000000000000000, -0.000000000000000000, -0.000000000000000000 ) ) ;
#123703=CARTESIAN_POINT ( 'NONE',  ( -22.59999985501179154, 11.74986979301414181, -66.93440133020057203 ) ) ;
#123748=AXIS2_PLACEMENT_3D ( 'NONE', #190275, #11645, #205970 ) ;
#123776=CYLINDRICAL_SURFACE ( 'NONE', #148941, 2.000000000000001776 ) ;
#123878=ORIENTED_EDGE ( 'NONE', *, *, #176764, .F. ) ;
#123886=CARTESIAN_POINT ( 'NONE',  ( -18.59999999999999787, 7.120270961708750512, -104.1595630418393768 ) ) ;
#123901=VERTEX_POINT ( 'NONE', #59726 ) ;
#123904=CARTESIAN_POINT ( 'NONE',  ( -18.50000000000000000, 1.115600667400684642E-11, -100.5000000000000426 ) ) ;
#123914=EDGE_CURVE ( 'NONE', #150331, #232336, #60116, .T. ) ;
#123926=ORIENTED_EDGE ( 'NONE', *, *, #137109, .T. ) ;
#123949=ORIENTED_EDGE ( 'NONE', *, *, #251012, .T. ) ;
#123971=AXIS2_PLACEMENT_3D ( 'NONE', #168443, #208803, #75717 ) ;
#123980=ORIENTED_EDGE ( 'NONE', *, *, #231751, .F. ) ;
#124000=AXIS2_PLACEMENT_3D ( 'NONE', #166654, #145754, #83195 ) ;
#124004=VECTOR ( 'NONE', #190967, 1000.000000000000000 ) ;
#124032=CARTESIAN_POINT ( 'NONE',  ( -21.04999999999999716, 0.09843750001115433856, -60.70076908991315889 ) ) ;
#124036=DIRECTION ( 'NONE',  ( 0.000000000000000000, -1.000000000000000000, 0.000000000000000000 ) ) ;
#124038=AXIS2_PLACEMENT_3D ( 'NONE', #62422, #143218, #102793 ) ;
#124047=AXIS2_PLACEMENT_3D ( 'NONE', #85702, #62338, #226513 ) ;
#124067=CARTESIAN_POINT ( 'NONE',  ( 23.24999999999999645, -3.899999999988843502, -100.5000000000000426 ) ) ;
#124089=EDGE_CURVE ( 'NONE', #202644, #47237, #50430, .T. ) ;
#124094=PLANE ( 'NONE',  #115971 ) ;
#124123=FACE_OUTER_BOUND ( 'NONE', #132368, .T. ) ;
#124134=DIRECTION ( 'NONE',  ( -0.000000000000000000, -0.000000000000000000, 1.000000000000000000 ) ) ;
#124136=CARTESIAN_POINT ( 'NONE',  ( -20.54999999999999716, 1.115600667400684642E-11, -100.5000000000000426 ) ) ;
#124138=CARTESIAN_POINT ( 'NONE',  ( -22.50000000000000000, 0.1000000000111554016, -55.35042919245524473 ) ) ;
#124143=DIRECTION ( 'NONE',  ( -0.000000000000000000, 0.000000000000000000, 1.000000000000000000 ) ) ;
#124231=ORIENTED_EDGE ( 'NONE', *, *, #11543, .T. ) ;
#124246=CARTESIAN_POINT ( 'NONE',  ( 20.94999999999999929, 1.115600667400684642E-11, -100.5000000000000426 ) ) ;
#124265=EDGE_LOOP ( 'NONE', ( #131896, #136362 ) ) ;
#124269=ORIENTED_EDGE ( 'NONE', *, *, #194850, .F. ) ;
#124272=DIRECTION ( 'NONE',  ( 1.000000000000000000, 0.000000000000000000, -0.000000000000000000 ) ) ;
#124295=AXIS2_PLACEMENT_3D ( 'NONE', #95267, #52267, #233516 ) ;
#124312=LINE ( 'NONE', #25225, #154751 ) ;
#124337=CIRCLE ( 'NONE', #70379, 4.049999999999998934 ) ;
#124344=CARTESIAN_POINT ( 'NONE',  ( 21.30000000000002558, 1.115600667400684642E-11, -62.95000000000004547 ) ) ;
#124369=DIRECTION ( 'NONE',  ( 0.000000000000000000, -1.000000000000000000, -0.000000000000000000 ) ) ;
#124383=FACE_OUTER_BOUND ( 'NONE', #208542, .T. ) ;
#124421=AXIS2_PLACEMENT_3D ( 'NONE', #236468, #173985, #134780 ) ;
#124423=EDGE_LOOP ( 'NONE', ( #72824, #123390, #186518, #179345 ) ) ;
#124485=VERTEX_POINT ( 'NONE', #187119 ) ;
#124516=AXIS2_PLACEMENT_3D ( 'NONE', #241250, #222940, #183825 ) ;
#124517=CARTESIAN_POINT ( 'NONE',  ( -20.85000000000000142, 7.021664781911246322, -104.3335654018973315 ) ) ;
#124518=AXIS2_PLACEMENT_3D ( 'NONE', #151728, #233812, #69606 ) ;
#124603=ORIENTED_EDGE ( 'NONE', *, *, #57969, .F. ) ;
#124612=ORIENTED_EDGE ( 'NONE', *, *, #18927, .T. ) ;
#124622=VERTEX_POINT ( 'NONE', #130976 ) ;
#124630=AXIS2_PLACEMENT_3D ( 'NONE', #226395, #162610, #127323 ) ;
#124635=VECTOR ( 'NONE', #82998, 1000.000000000000000 ) ;
#124673=ORIENTED_EDGE ( 'NONE', *, *, #8485, .T. ) ;
#124690=CARTESIAN_POINT ( 'NONE',  ( 21.53699400380797613, 6.787711793200763566, -66.99999999998171063 ) ) ;
#124722=CIRCLE ( 'NONE', #12312, 0.09999999999999939493 ) ;
#124742=EDGE_CURVE ( 'NONE', #163227, #155361, #73192, .T. ) ;
#124754=FACE_OUTER_BOUND ( 'NONE', #66230, .T. ) ;
#124772=EDGE_CURVE ( 'NONE', #235613, #85481, #60479, .T. ) ;
#124783=DIRECTION ( 'NONE',  ( -0.000000000000000000, -1.000000000000000000, 6.308085367188393199E-16 ) ) ;
#124815=VERTEX_POINT ( 'NONE', #7848 ) ;
#124830=DIRECTION ( 'NONE',  ( 7.304098846218134667E-16, -1.000000000000000000, 0.000000000000000000 ) ) ;
#124849=ORIENTED_EDGE ( 'NONE', *, *, #84945, .T. ) ;
#124862=ORIENTED_EDGE ( 'NONE', *, *, #96205, .F. ) ;
#124899=DIRECTION ( 'NONE',  ( 1.000000000000000000, 0.000000000000000000, 0.000000000000000000 ) ) ;
#124941=ORIENTED_EDGE ( 'NONE', *, *, #50060, .T. ) ;
#124980=DIRECTION ( 'NONE',  ( 1.000000000000000000, -0.000000000000000000, 0.000000000000000000 ) ) ;
#124989=ORIENTED_EDGE ( 'NONE', *, *, #25505, .T. ) ;
#124999=ORIENTED_EDGE ( 'NONE', *, *, #41414, .F. ) ;
#125025=CARTESIAN_POINT ( 'NONE',  ( 23.24999999999999645, 1.115600667400684642E-11, -67.00000000000004263 ) ) ;
#125028=AXIS2_PLACEMENT_3D ( 'NONE', #157439, #236934, #58279 ) ;
#125055=ADVANCED_FACE ( 'NONE', ( #206867 ), #166488, .F. ) ;
#125086=CARTESIAN_POINT ( 'NONE',  ( 21.05000000000000071, 11.65000000001116298, -79.15000000000004832 ) ) ;
#125108=CARTESIAN_POINT ( 'NONE',  ( 23.24999999999999289, 11.75000000001116263, -67.10000000000005116 ) ) ;
#125145=AXIS2_PLACEMENT_3D ( 'NONE', #12747, #154823, #231780 ) ;
#125173=CARTESIAN_POINT ( 'NONE',  ( 20.85000000000000142, 11.75000000001115907, -93.71613433702195550 ) ) ;
#125193=EDGE_LOOP ( 'NONE', ( #110370, #122626, #36867, #78118 ) ) ;
#125260=DIRECTION ( 'NONE',  ( 1.000000000000000000, 0.000000000000000000, 0.000000000000000000 ) ) ;
#125298=EDGE_CURVE ( 'NONE', #248700, #198075, #110744, .T. ) ;
#125314=DIRECTION ( 'NONE',  ( 1.000000000000000000, -0.000000000000000000, -0.000000000000000000 ) ) ;
#125342=CARTESIAN_POINT ( 'NONE',  ( 21.05000000000000071, 4.850467289730772791, -79.03426740900172831 ) ) ;
#125360=ORIENTED_EDGE ( 'NONE', *, *, #69114, .T. ) ;
#125370=DIRECTION ( 'NONE',  ( 0.000000000000000000, 0.8660254037844482555, 0.4999999999999837907 ) ) ;
#125371=CIRCLE ( 'NONE', #12963, 0.1000000000000000472 ) ;
#125377=EDGE_CURVE ( 'NONE', #108958, #153327, #65137, .T. ) ;
#125462=DIRECTION ( 'NONE',  ( -1.000000000000000000, 0.000000000000000000, 0.000000000000000000 ) ) ;
#125475=CARTESIAN_POINT ( 'NONE',  ( 20.94999999999999929, 8.776282895303632259, -79.15000000000004832 ) ) ;
#125485=ADVANCED_FACE ( 'NONE', ( #245321 ), #6877, .T. ) ;
#125497=CARTESIAN_POINT ( 'NONE',  ( -21.14999999893415250, 11.75000000001115197, -73.84449534352643241 ) ) ;
#125498=EDGE_CURVE ( 'NONE', #31603, #201851, #122815, .T. ) ;
#125509=AXIS2_PLACEMENT_3D ( 'NONE', #138994, #218548, #39968 ) ;
#125517=CARTESIAN_POINT ( 'NONE',  ( -20.00857864376270001, 9.150000000011157653, -88.15000000000004832 ) ) ;
#125542=ORIENTED_EDGE ( 'NONE', *, *, #99914, .T. ) ;
#125560=CARTESIAN_POINT ( 'NONE',  ( -21.05000000000000071, 0.03363273534480391153, -60.74118280531856584 ) ) ;
#125649=VERTEX_POINT ( 'NONE', #139471 ) ;
#125650=CARTESIAN_POINT ( 'NONE',  ( 21.09096482362047809, 6.363544365415554793, -66.96055172122596844 ) ) ;
#125659=DIRECTION ( 'NONE',  ( -2.952720810173288619E-16, 1.000000000000000000, 0.000000000000000000 ) ) ;
#125666=ADVANCED_FACE ( 'NONE', ( #156521 ), #31852, .T. ) ;
#125667=CIRCLE ( 'NONE', #113205, 4.299999999999956302 ) ;
#125673=DIRECTION ( 'NONE',  ( -0.7070776581708965169, -0.7071359030027827286, -0.000000000000000000 ) ) ;
#125711=ORIENTED_EDGE ( 'NONE', *, *, #51727, .F. ) ;
#125715=FACE_OUTER_BOUND ( 'NONE', #109721, .T. ) ;
#125730=ORIENTED_EDGE ( 'NONE', *, *, #9887, .T. ) ;
#125740=ORIENTED_EDGE ( 'NONE', *, *, #167585, .T. ) ;
#125745=AXIS2_PLACEMENT_3D ( 'NONE', #113354, #151206, #35140 ) ;
#125754=AXIS2_PLACEMENT_3D ( 'NONE', #183698, #165417, #164137 ) ;
#125778=ORIENTED_EDGE ( 'NONE', *, *, #66430, .F. ) ;
#125788=ORIENTED_EDGE ( 'NONE', *, *, #236314, .T. ) ;
#125795=DIRECTION ( 'NONE',  ( -1.000000000000000000, 0.000000000000000000, 0.000000000000000000 ) ) ;
#125803=ADVANCED_FACE ( 'NONE', ( #202034 ), #107013, .T. ) ;
#125825=DIRECTION ( 'NONE',  ( 0.000000000000000000, -0.9999631594459056361, -0.008583690987124413183 ) ) ;
#125888=CARTESIAN_POINT ( 'NONE',  ( 23.14999999999999858, 1.115600667400684642E-11, -100.5000000000000426 ) ) ;
#125929=CARTESIAN_POINT ( 'NONE',  ( 23.14999999999998437, -11.74999999998884448, -67.00000000000004263 ) ) ;
#125931=CARTESIAN_POINT ( 'NONE',  ( 20.96937028524355640, 10.62446937163783289, -74.49142610116966523 ) ) ;
#125949=CIRCLE ( 'NONE', #76068, 0.09999999999999939493 ) ;
#125968=ORIENTED_EDGE ( 'NONE', *, *, #138253, .T. ) ;
#125984=LINE ( 'NONE', #47720, #230102 ) ;
#125987=FACE_OUTER_BOUND ( 'NONE', #225901, .T. ) ;
#126010=CYLINDRICAL_SURFACE ( 'NONE', #166182, 0.09999999999999781286 ) ;
#126027=DIRECTION ( 'NONE',  ( 0.000000000000000000, -1.000000000000000000, 0.000000000000000000 ) ) ;
#126061=DIRECTION ( 'NONE',  ( 0.000000000000000000, -1.000000000000000000, 0.000000000000000000 ) ) ;
#126072=AXIS2_PLACEMENT_3D ( 'NONE', #195510, #16860, #235879 ) ;
#126087=ORIENTED_EDGE ( 'NONE', *, *, #186030, .T. ) ;
#126133=DIRECTION ( 'NONE',  ( 0.000000000000000000, -1.000000000000000000, 0.000000000000000000 ) ) ;
#126136=CIRCLE ( 'NONE', #242678, 0.09999999999999949207 ) ;
#126139=CARTESIAN_POINT ( 'NONE',  ( 20.95512820512820440, 8.876151316299271343, -79.15000000000004832 ) ) ;
#126147=ORIENTED_EDGE ( 'NONE', *, *, #101516, .F. ) ;
#126160=AXIS2_PLACEMENT_3D ( 'NONE', #36286, #255254, #156244 ) ;
#126188=ADVANCED_FACE ( 'NONE', ( #90423, #170024, #184391 ), #111293, .F. ) ;
#126242=EDGE_CURVE ( 'NONE', #159539, #87242, #150434, .T. ) ;
#126272=TOROIDAL_SURFACE ( 'NONE', #5451, 0.2000000000000000111, 0.1000000000000000056 ) ;
#126304=AXIS2_PLACEMENT_3D ( 'NONE', #24185, #125825, #103674 ) ;
#126320=PRODUCT ( 'Injection Molded Chain Links 3', 'Injection Molded Chain Links 3', '', ( #114771 ) ) ;
#126366=CIRCLE ( 'NONE', #246972, 11.89999999999999858 ) ;
#126379=CARTESIAN_POINT ( 'NONE',  ( -20.94999999999999929, 1.115600667400684642E-11, -88.70000000000004547 ) ) ;
#126396=DIRECTION ( 'NONE',  ( 0.000000000000000000, 0.000000000000000000, -1.000000000000000000 ) ) ;
#126423=FACE_OUTER_BOUND ( 'NONE', #78817, .T. ) ;
#126431=TOROIDAL_SURFACE ( 'NONE', #14014, 12.97499999999999609, 0.1000000000000000056 ) ;
#126441=CARTESIAN_POINT ( 'NONE',  ( 21.05000000000000071, 11.75000000001115907, -93.48519422934610645 ) ) ;
#126446=ORIENTED_EDGE ( 'NONE', *, *, #223844, .F. ) ;
#126475=EDGE_LOOP ( 'NONE', ( #154184, #27463, #120857, #108200 ) ) ;
#126479=CARTESIAN_POINT ( 'NONE',  ( -20.54999999999999716, 1.115600667400684642E-11, -100.5000000000000426 ) ) ;
#126489=ADVANCED_FACE ( 'NONE', ( #246626 ), #227063, .F. ) ;
#126494=DIRECTION ( 'NONE',  ( 1.000000000000000000, 0.000000000000000000, 0.000000000000000000 ) ) ;
#126498=CARTESIAN_POINT ( 'NONE',  ( 18.59999999999999432, -1.637172712959223952, -78.58215336547205254 ) ) ;
#126522=DIRECTION ( 'NONE',  ( 0.000000000000000000, -1.000000000000000000, 0.000000000000000000 ) ) ;
#126540=CARTESIAN_POINT ( 'NONE',  ( -21.05000000000000071, 5.900000000011102586, -77.21909976465646253 ) ) ;
#126563=DIRECTION ( 'NONE',  ( 1.000000000000000000, -0.000000000000000000, -0.000000000000000000 ) ) ;
#126578=CIRCLE ( 'NONE', #5741, 0.1000000000000028644 ) ;
#126592=FACE_OUTER_BOUND ( 'NONE', #169959, .T. ) ;
#126608=ORIENTED_EDGE ( 'NONE', *, *, #89537, .T. ) ;
#126614=CIRCLE ( 'NONE', #134777, 0.09999999999999939493 ) ;
#126647=DIRECTION ( 'NONE',  ( 0.000000000000000000, -1.000000000000000000, -1.897661533703519897E-16 ) ) ;
#126649=DIRECTION ( 'NONE',  ( 1.000000000000000000, 0.000000000000000000, 0.000000000000000000 ) ) ;
#126661=CARTESIAN_POINT ( 'NONE',  ( -20.94999999999999929, 1.115600667400684642E-11, -100.5000000000000426 ) ) ;
#126676=( BOUNDED_CURVE ( )  B_SPLINE_CURVE ( 3, ( #108123, #187677, #9017, #228075 ),
 .UNSPECIFIED., .F., .T. ) 
 B_SPLINE_CURVE_WITH_KNOTS ( ( 4, 4 ),
 ( 3.141592653589791784, 4.712388980384688786 ),
 .UNSPECIFIED. ) 
 CURVE ( )  GEOMETRIC_REPRESENTATION_ITEM ( )  RATIONAL_B_SPLINE_CURVE ( ( 1.000000000000000000, 0.8047378541243649375, 0.8047378541243649375, 1.000000000000000000 ) ) 
 REPRESENTATION_ITEM ( '' )  );
#126712=TOROIDAL_SURFACE ( 'NONE', #109943, 0.2000000000000000111, 0.1000000000000000056 ) ;
#126722=ORIENTED_EDGE ( 'NONE', *, *, #233429, .F. ) ;
#126737=CARTESIAN_POINT ( 'NONE',  ( -20.64999999999999858, 2.000000000011154189, -87.27537807723794572 ) ) ;
#126738=DIRECTION ( 'NONE',  ( 0.000000000000000000, 0.000000000000000000, 1.000000000000000000 ) ) ;
#126763=DIRECTION ( 'NONE',  ( -0.000000000000000000, 1.000000000000000000, 1.734723475976807292E-15 ) ) ;
#126767=FACE_OUTER_BOUND ( 'NONE', #212186, .T. ) ;
#126779=DIRECTION ( 'NONE',  ( -1.000000000000000000, 0.000000000000000000, 0.000000000000000000 ) ) ;
#126781=CARTESIAN_POINT ( 'NONE',  ( -21.14999999999999858, 11.75000000001115197, -73.78386566297820082 ) ) ;
#126789=CIRCLE ( 'NONE', #147451, 0.5000000000000013323 ) ;
#126791=DIRECTION ( 'NONE',  ( 1.000000000000000000, 0.000000000000000000, 0.000000000000000000 ) ) ;
#126808=VERTEX_POINT ( 'NONE', #143372 ) ;
#126849=CARTESIAN_POINT ( 'NONE',  ( -20.94999999999999929, -1.362429037182149694, -108.3888812479212476 ) ) ;
#126875=ORIENTED_EDGE ( 'NONE', *, *, #10864, .T. ) ;
#126876=CIRCLE ( 'NONE', #14482, 0.09999999999999939493 ) ;
#126900=DIRECTION ( 'NONE',  ( -0.7071067811865475727, -0.7071067811865475727, 0.000000000000000000 ) ) ;
#126909=EDGE_CURVE ( 'NONE', #150821, #147343, #257826, .T. ) ;
#126956=DIRECTION ( 'NONE',  ( 0.000000000000000000, 0.000000000000000000, -1.000000000000000000 ) ) ;
#126990=CIRCLE ( 'NONE', #218536, 0.2000000000000057288 ) ;
#127021=CYLINDRICAL_SURFACE ( 'NONE', #43880, 0.1000000000000028644 ) ;
#127030=EDGE_CURVE ( 'NONE', #245368, #39159, #152396, .T. ) ;
#127031=CIRCLE ( 'NONE', #181220, 0.1000000000000028644 ) ;
#127045=ORIENTED_EDGE ( 'NONE', *, *, #2110, .T. ) ;
#127079=CARTESIAN_POINT ( 'NONE',  ( -21.05000000000000071, 6.257814610492678398, -66.90220970869081896 ) ) ;
#127102=CARTESIAN_POINT ( 'NONE',  ( -20.94999999999999929, 1.835341550235567887, -78.55515129256303908 ) ) ;
#127121=DIRECTION ( 'NONE',  ( 0.000000000000000000, -6.308085367188393199E-16, -1.000000000000000000 ) ) ;
#127122=ADVANCED_FACE ( 'NONE', ( #21844, #55789 ), #135350, .T. ) ;
#127178=ORIENTED_EDGE ( 'NONE', *, *, #227454, .T. ) ;
#127186=CARTESIAN_POINT ( 'NONE',  ( 18.59999999999999076, 1.835341550235567887, -78.65515129256301918 ) ) ;
#127200=CARTESIAN_POINT ( 'NONE',  ( 18.49999999999999289, 10.49142135624846617, -91.75000000000005684 ) ) ;
#127202=CARTESIAN_POINT ( 'NONE',  ( -20.54999999999999716, 2.500000000011154633, -87.27537807723794572 ) ) ;
#127210=VERTEX_POINT ( 'NONE', #243444 ) ;
#127223=LINE ( 'NONE', #48958, #71343 ) ;
#127235=CARTESIAN_POINT ( 'NONE',  ( 20.51284917709620359, 10.31088662285602275, -74.67247318559205382 ) ) ;
#127251=CARTESIAN_POINT ( 'NONE',  ( 22.00356870142806187, 7.254242362486740703, -67.00000000000004263 ) ) ;
#127265=TOROIDAL_SURFACE ( 'NONE', #14857, 12.77500000000000036, 0.1000000000000000056 ) ;
#127297=ADVANCED_FACE ( 'NONE', ( #153382 ), #112340, .T. ) ;
#127323=DIRECTION ( 'NONE',  ( 0.000000000000000000, 0.000000000000000000, -1.000000000000000000 ) ) ;
#127382=VERTEX_POINT ( 'NONE', #143717 ) ;
#127396=CIRCLE ( 'NONE', #52560, 0.09999999999999939493 ) ;
#127400=DIRECTION ( 'NONE',  ( -1.000000000000000000, 0.000000000000000000, 0.000000000000000000 ) ) ;
#127408=CARTESIAN_POINT ( 'NONE',  ( -21.55000000000000426, 7.708578643773852157, -88.15000000000004832 ) ) ;
#127420=ORIENTED_EDGE ( 'NONE', *, *, #17544, .F. ) ;
#127441=DIRECTION ( 'NONE',  ( 0.000000000000000000, 0.000000000000000000, 1.000000000000000000 ) ) ;
#127444=CIRCLE ( 'NONE', #73503, 0.5000000000000004441 ) ;
#127478=DIRECTION ( 'NONE',  ( -0.000000000000000000, -0.000000000000000000, -1.000000000000000000 ) ) ;
#127502=ORIENTED_EDGE ( 'NONE', *, *, #120034, .T. ) ;
#127607=ADVANCED_FACE ( 'NONE', ( #148876 ), #153000, .T. ) ;
#127617=ORIENTED_EDGE ( 'NONE', *, *, #75278, .F. ) ;
#127618=VERTEX_POINT ( 'NONE', #25092 ) ;
#127621=CARTESIAN_POINT ( 'NONE',  ( 20.95595624212412744, 10.62389120310530544, -74.62963291412694389 ) ) ;
#127623=CARTESIAN_POINT ( 'NONE',  ( 18.49999999999999289, 10.20857864377385127, -88.35000000000003695 ) ) ;
#127641=CIRCLE ( 'NONE', #219199, 0.09999999999999939493 ) ;
#127672=CARTESIAN_POINT ( 'NONE',  ( -22.00356870068980442, 1.356251047821719177E-11, -59.74575763824462626 ) ) ;
#127706=ORIENTED_EDGE ( 'NONE', *, *, #94036, .F. ) ;
#127724=ORIENTED_EDGE ( 'NONE', *, *, #254983, .F. ) ;
#127741=AXIS2_PLACEMENT_3D ( 'NONE', #112740, #210556, #71064 ) ;
#127742=CARTESIAN_POINT ( 'NONE',  ( 20.85000000106584750, 11.75000000001115907, -93.65550465647376654 ) ) ;
#127776=CARTESIAN_POINT ( 'NONE',  ( -18.59999994787167310, -9.523637689750348301, -107.3824495347726753 ) ) ;
#127784=ADVANCED_FACE ( 'NONE', ( #182567 ), #120038, .T. ) ;
#127795=VERTEX_POINT ( 'NONE', #239963 ) ;
#127796=DIRECTION ( 'NONE',  ( 2.342056488767301376E-15, -0.1350103645451904977, -0.9908441862701596881 ) ) ;
#127834=FACE_OUTER_BOUND ( 'NONE', #65598, .T. ) ;
#127841=CARTESIAN_POINT ( 'NONE',  ( -21.04999999999999361, 6.307425219576558995, -67.01681986838568150 ) ) ;
#127880=LINE ( 'NONE', #48331, #220762 ) ;
#127902=ORIENTED_EDGE ( 'NONE', *, *, #123495, .F. ) ;
#127912=ORIENTED_EDGE ( 'NONE', *, *, #69114, .F. ) ;
#127929=ORIENTED_EDGE ( 'NONE', *, *, #232990, .T. ) ;
#127950=CIRCLE ( 'NONE', #98667, 0.09999999999999741040 ) ;
#127954=DIRECTION ( 'NONE',  ( 0.000000000000000000, 0.000000000000000000, 1.000000000000000000 ) ) ;
#127956=EDGE_LOOP ( 'NONE', ( #97077, #129383, #9961, #86317 ) ) ;
#128024=AXIS2_PLACEMENT_3D ( 'NONE', #42326, #121876, #61891 ) ;
#128025=DIRECTION ( 'NONE',  ( 1.000000000000000000, 0.000000000000000000, -0.000000000000000000 ) ) ;
#128030=CARTESIAN_POINT ( 'NONE',  ( -20.94999999999999929, 7.021664781911246322, -104.3335654018973315 ) ) ;
#128055=CARTESIAN_POINT ( 'NONE',  ( 18.49713797159842343, -9.446482327567830239, -74.07145812161023457 ) ) ;
#128072=CARTESIAN_POINT ( 'NONE',  ( -21.05000000000000071, 11.63687328911505325, -73.82175921332471091 ) ) ;
#128078=ORIENTED_EDGE ( 'NONE', *, *, #139030, .F. ) ;
#128099=DIRECTION ( 'NONE',  ( 1.000000000000000000, 0.000000000000000000, 0.000000000000000000 ) ) ;
#128108=VERTEX_POINT ( 'NONE', #18023 ) ;
#128147=AXIS2_PLACEMENT_3D ( 'NONE', #161045, #163612, #27984 ) ;
#128228=ORIENTED_EDGE ( 'NONE', *, *, #243027, .F. ) ;
#128262=CARTESIAN_POINT ( 'NONE',  ( 22.49999999999999645, 11.64987090377453960, -66.91748010912705524 ) ) ;
#128277=CIRCLE ( 'NONE', #124000, 12.87499999999999822 ) ;
#128280=DIRECTION ( 'NONE',  ( -1.000000000000000000, 0.000000000000000000, 0.000000000000000000 ) ) ;
#128292=AXIS2_PLACEMENT_3D ( 'NONE', #40959, #200008, #21392 ) ;
#128296=CARTESIAN_POINT ( 'NONE',  ( 20.89878130938411616, 10.32747123227773045, -106.0774032850249711 ) ) ;
#128319=EDGE_CURVE ( 'NONE', #138090, #75643, #98943, .T. ) ;
#128330=ORIENTED_EDGE ( 'NONE', *, *, #94742, .F. ) ;
#128360=ORIENTED_EDGE ( 'NONE', *, *, #61619, .F. ) ;
#128373=CARTESIAN_POINT ( 'NONE',  ( -21.07928932188134041, 6.328516656409859387, -66.90110485434540522 ) ) ;
#128393=CARTESIAN_POINT ( 'NONE',  ( -23.25000000000000000, 11.75000000001115552, -67.00000000000004263 ) ) ;
#128397=CARTESIAN_POINT ( 'NONE',  ( 23.24999999999999289, 6.650000000011155876, -79.15000000000004832 ) ) ;
#128402=CARTESIAN_POINT ( 'NONE',  ( 22.50927854361889402, -0.1008580735143571466, -55.25043287397313208 ) ) ;
#128429=CARTESIAN_POINT ( 'NONE',  ( -21.07928932188134041, 6.328516656404449492, -66.90110485434564680 ) ) ;
#128519=CARTESIAN_POINT ( 'NONE',  ( 20.97250901189795513, 10.62456803371303593, -74.66454571696704079 ) ) ;
#128552=AXIS2_PLACEMENT_3D ( 'NONE', #97038, #77491, #20131 ) ;
#128596=CARTESIAN_POINT ( 'NONE',  ( -20.54999999999999716, 1.115600667400684642E-11, -98.50000000000004263 ) ) ;
#128599=EDGE_CURVE ( 'NONE', #163852, #246766, #235051, .T. ) ;
#128657=CARTESIAN_POINT ( 'NONE',  ( -21.05000000000000071, -1.162701749926853712, -75.10000000000003695 ) ) ;
#128673=VERTEX_POINT ( 'NONE', #130959 ) ;
#128732=DIRECTION ( 'NONE',  ( 1.000000000000000000, 0.000000000000000000, -0.000000000000000000 ) ) ;
#128747=AXIS2_PLACEMENT_3D ( 'NONE', #18077, #19375, #79319 ) ;
#128769=ADVANCED_FACE ( 'NONE', ( #154417 ), #136065, .F. ) ;
#128801=PLANE ( 'NONE',  #8213 ) ;
#128811=ORIENTED_EDGE ( 'NONE', *, *, #152703, .T. ) ;
#128812=CARTESIAN_POINT ( 'NONE',  ( 20.95512820512820440, 10.62384868372303615, -79.15000000000004832 ) ) ;
#128838=EDGE_LOOP ( 'NONE', ( #172246, #173144, #99231, #111581 ) ) ;
#128840=ORIENTED_EDGE ( 'NONE', *, *, #90539, .T. ) ;
#128868=CARTESIAN_POINT ( 'NONE',  ( -21.05000000000000071, 1.835341550235567887, -78.55515129256302487 ) ) ;
#128879=DIRECTION ( 'NONE',  ( -1.000000000000000000, 0.000000000000000000, 0.000000000000000000 ) ) ;
#128924=CARTESIAN_POINT ( 'NONE',  ( -20.94999999999999929, -11.29603075032412640, -97.45210084033617193 ) ) ;
#128927=CARTESIAN_POINT ( 'NONE',  ( -21.04386569057651357, 11.75000000001136513, -93.64283735177980361 ) ) ;
#128943=DIRECTION ( 'NONE',  ( 0.000000000000000000, -1.000000000000000000, 0.000000000000000000 ) ) ;
#128964=FACE_OUTER_BOUND ( 'NONE', #18798, .T. ) ;
#128970=DIRECTION ( 'NONE',  ( 0.000000000000000000, 0.000000000000000000, 1.000000000000000000 ) ) ;
#128976=ADVANCED_FACE ( 'NONE', ( #206351 ), #66835, .F. ) ;
#128982=ORIENTED_EDGE ( 'NONE', *, *, #162737, .T. ) ;
#128996=CARTESIAN_POINT ( 'NONE',  ( -21.14999999999999858, -11.64999999998884483, -67.00000000000004263 ) ) ;
#129000=DIRECTION ( 'NONE',  ( 1.000000000000000000, -0.000000000000000000, -0.000000000000000000 ) ) ;
#129005=LINE ( 'NONE', #225498, #199871 ) ;
#129024=DIRECTION ( 'NONE',  ( 1.000000000000000000, -0.000000000000000000, -0.000000000000000000 ) ) ;
#129028=CYLINDRICAL_SURFACE ( 'NONE', #70056, 0.1000000000000028644 ) ;
#129037=CIRCLE ( 'NONE', #62394, 1.899999999999999023 ) ;
#129057=CARTESIAN_POINT ( 'NONE',  ( -18.46919391072059113, -9.670724388266654259, -107.1738035317995070 ) ) ;
#129119=CARTESIAN_POINT ( 'NONE',  ( 19.90621891164687440, 11.75000000001116263, -91.82844527787746358 ) ) ;
#129134=EDGE_CURVE ( 'NONE', #86852, #197986, #175902, .T. ) ;
#129165=ADVANCED_FACE ( 'NONE', ( #117190 ), #51078, .T. ) ;
#129189=TOROIDAL_SURFACE ( 'NONE', #16776, 6.258578643762700899, 0.1000000000000000056 ) ;
#129204=AXIS2_PLACEMENT_3D ( 'NONE', #11035, #89271, #48868 ) ;
#129231=DIRECTION ( 'NONE',  ( -1.000000000000000000, 0.000000000000000000, 0.000000000000000000 ) ) ;
#129269=ORIENTED_EDGE ( 'NONE', *, *, #58039, .T. ) ;
#129282=DIRECTION ( 'NONE',  ( 0.000000000000000000, -1.000000000000000000, -0.000000000000000000 ) ) ;
#129289=CARTESIAN_POINT ( 'NONE',  ( -22.39999999999999503, 7.790779598384560245, -66.90000000000004832 ) ) ;
#129301=CARTESIAN_POINT ( 'NONE',  ( -23.15000000000000213, 1.115600667400684642E-11, -100.5000000000000426 ) ) ;
#129313=ORIENTED_EDGE ( 'NONE', *, *, #136652, .T. ) ;
#129314=CARTESIAN_POINT ( 'NONE',  ( 21.14999999999999858, 6.540656951712400691, -67.00000000000004263 ) ) ;
#129339=CIRCLE ( 'NONE', #158419, 0.09999999999999939493 ) ;
#129354=EDGE_LOOP ( 'NONE', ( #94814, #109311, #202508, #91375, #156940 ) ) ;
#129368=ORIENTED_EDGE ( 'NONE', *, *, #107610, .F. ) ;
#129383=ORIENTED_EDGE ( 'NONE', *, *, #171683, .F. ) ;
#129395=AXIS2_PLACEMENT_3D ( 'NONE', #56195, #135743, #91495 ) ;
#129402=( BOUNDED_SURFACE ( )  B_SPLINE_SURFACE ( 3, 2, ( 
 ( #55135, #134688, #33090 ),
 ( #112588, #113861, #16077 ),
 ( #95577, #193419, #156873 ),
 ( #155598, #56438, #77290 ) ),
 .UNSPECIFIED., .F., .F., .T. ) 
 B_SPLINE_SURFACE_WITH_KNOTS ( ( 4, 4 ),
 ( 3, 3 ),
 ( -5.204170427930421283E-18, 0.001979672783031532438 ),
 ( 0.000000000000000000, 1.000000000000000000 ),
 .UNSPECIFIED. ) 
 GEOMETRIC_REPRESENTATION_ITEM ( )  RATIONAL_B_SPLINE_SURFACE ( (
 ( 1.000000000000000000, 0.7103081912008367693, 1.000000000000000000),
 ( 1.000000000000000000, 0.7104998333558518731, 1.000000000000000000),
 ( 1.000000000000000000, 0.7107238315755336489, 1.000000000000000000),
 ( 1.000000000000000000, 0.7110073749539377319, 1.000000000000000000) ) ) 
 REPRESENTATION_ITEM ( '' )  SURFACE ( )  );
#129442=ADVANCED_FACE ( 'NONE', ( #107883 ), #28448, .F. ) ;
#129470=FACE_OUTER_BOUND ( 'NONE', #69957, .T. ) ;
#129474=ORIENTED_EDGE ( 'NONE', *, *, #159279, .F. ) ;
#129489=CARTESIAN_POINT ( 'NONE',  ( 21.76363531954645936, 7.012936547882880234, -66.90099812570059612 ) ) ;
#129495=CARTESIAN_POINT ( 'NONE',  ( 21.05000000000000071, 4.813084112160680661, -78.94151775652387926 ) ) ;
#129498=DIRECTION ( 'NONE',  ( 0.000000000000000000, -0.000000000000000000, -1.000000000000000000 ) ) ;
#129517=ORIENTED_EDGE ( 'NONE', *, *, #170723, .F. ) ;
#129546=VERTEX_POINT ( 'NONE', #37355 ) ;
#129551=DIRECTION ( 'NONE',  ( 0.000000000000000000, 0.000000000000000000, -1.000000000000000000 ) ) ;
#129552=VERTEX_POINT ( 'NONE', #116875 ) ;
#129582=DIRECTION ( 'NONE',  ( -1.000000000000000000, -0.000000000000000000, -0.000000000000000000 ) ) ;
#129602=EDGE_LOOP ( 'NONE', ( #43431, #45659, #143669 ) ) ;
#129615=CARTESIAN_POINT ( 'NONE',  ( -21.05000000000000071, 1.115600667400684642E-11, -71.29999999999999716 ) ) ;
#129633=CARTESIAN_POINT ( 'NONE',  ( 18.49999999999999645, -1.162701749926855266, -75.10000000000003695 ) ) ;
#129646=CARTESIAN_POINT ( 'NONE',  ( -21.05000000000000071, 6.478078221105993961, -67.09999993530584561 ) ) ;
#129659=ORIENTED_EDGE ( 'NONE', *, *, #67340, .T. ) ;
#129677=CARTESIAN_POINT ( 'NONE',  ( -23.25000000000000000, -1.164121893230052995, -108.4148480855716485 ) ) ;
#129681=CARTESIAN_POINT ( 'NONE',  ( 18.55121869061587958, 10.32747123227773400, -106.0774032850249711 ) ) ;
#129689=ORIENTED_EDGE ( 'NONE', *, *, #143398, .F. ) ;
#129694=ADVANCED_FACE ( 'NONE', ( #140264 ), #184537, .F. ) ;
#129703=CIRCLE ( 'NONE', #225534, 0.1000000000000028644 ) ;
#129753=CARTESIAN_POINT ( 'NONE',  ( -23.15000000000000213, 1.115625160336667635E-11, -102.5000000000000426 ) ) ;
#129765=AXIS2_PLACEMENT_3D ( 'NONE', #71120, #154525, #231472 ) ;
#129786=CARTESIAN_POINT ( 'NONE',  ( 22.50000000000000000, 1.115600667400684642E-11, -67.00000000000004263 ) ) ;
#129809=CARTESIAN_POINT ( 'NONE',  ( -20.64999999999999858, 2.400000000011155432, -87.27537807723794572 ) ) ;
#129835=DIRECTION ( 'NONE',  ( -1.000000000000000000, 0.000000000000000000, 0.000000000000000000 ) ) ;
#129852=DIRECTION ( 'NONE',  ( -1.000000000000000000, 0.000000000000000000, 0.000000000000000000 ) ) ;
#129865=ORIENTED_EDGE ( 'NONE', *, *, #238838, .F. ) ;
#129867=AXIS2_PLACEMENT_3D ( 'NONE', #66945, #209029, #166085 ) ;
#129883=EDGE_CURVE ( 'NONE', #250167, #232336, #199282, .T. ) ;
#129890=ORIENTED_EDGE ( 'NONE', *, *, #233429, .T. ) ;
#129913=DIRECTION ( 'NONE',  ( -0.000000000000000000, 0.000000000000000000, -1.000000000000000000 ) ) ;
#129928=VERTEX_POINT ( 'NONE', #214384 ) ;
#129948=CYLINDRICAL_SURFACE ( 'NONE', #23007, 0.09999999999999892308 ) ;
#130008=ORIENTED_EDGE ( 'NONE', *, *, #38589, .F. ) ;
#130026=VERTEX_POINT ( 'NONE', #102110 ) ;
#130073=CARTESIAN_POINT ( 'NONE',  ( -22.59999970745345976, -0.009356377315832288197, -55.24948679233083482 ) ) ;
#130078=DIRECTION ( 'NONE',  ( -0.000000000000000000, 0.000000000000000000, -1.000000000000000000 ) ) ;
#130091=DIRECTION ( 'NONE',  ( 0.000000000000000000, -1.000000000000000000, 0.000000000000000000 ) ) ;
#130114=ORIENTED_EDGE ( 'NONE', *, *, #223931, .F. ) ;
#130125=FACE_OUTER_BOUND ( 'NONE', #200118, .T. ) ;
#130127=DIRECTION ( 'NONE',  ( 1.000000000000000000, -0.000000000000000000, -0.000000000000000000 ) ) ;
#130149=CYLINDRICAL_SURFACE ( 'NONE', #248995, 7.900000000000003908 ) ;
#130176=DIRECTION ( 'NONE',  ( 1.000000000000000000, 0.000000000000000000, 0.000000000000000000 ) ) ;
#130177=VECTOR ( 'NONE', #51785, 1000.000000000000114 ) ;
#130185=FACE_OUTER_BOUND ( 'NONE', #62872, .T. ) ;
#130197=DIRECTION ( 'NONE',  ( 0.000000000000000000, 0.1350103645451904977, -0.9908441862701596881 ) ) ;
#130207=CARTESIAN_POINT ( 'NONE',  ( -20.64999999999999858, 7.250000000011155521, -88.15000000000004832 ) ) ;
#130209=CIRCLE ( 'NONE', #205031, 0.1000000000000028644 ) ;
#130212=DIRECTION ( 'NONE',  ( -0.7071067811865388020, 0.7071067811865561215, 0.000000000000000000 ) ) ;
#130218=AXIS2_PLACEMENT_3D ( 'NONE', #15582, #255390, #37710 ) ;
#130222=DIRECTION ( 'NONE',  ( 1.000000000000000000, 0.000000000000000000, 0.000000000000000000 ) ) ;
#130232=DIRECTION ( 'NONE',  ( 1.000000000000000000, 2.952720810173289112E-16, -0.000000000000000000 ) ) ;
#130246=CARTESIAN_POINT ( 'NONE',  ( -23.15000000000000213, -9.499999999988846255, -90.60603087734760663 ) ) ;
#130278=DIRECTION ( 'NONE',  ( 0.000000000000000000, 1.000000000000000000, 0.000000000000000000 ) ) ;
#130288=CARTESIAN_POINT ( 'NONE',  ( -21.05000000000000071, -1.835341550213255957, -78.55515129256302487 ) ) ;
#130292=ORIENTED_EDGE ( 'NONE', *, *, #39287, .T. ) ;
#130310=EDGE_LOOP ( 'NONE', ( #216823, #226598, #17036, #74029 ) ) ;
#130311=EDGE_CURVE ( 'NONE', #246680, #188088, #162060, .T. ) ;
#130321=DIRECTION ( 'NONE',  ( -1.000000000000000000, 0.000000000000000000, 0.000000000000000000 ) ) ;
#130329=TOROIDAL_SURFACE ( 'NONE', #17904, 2.100000000000002309, 0.1000000000000000056 ) ;
#130342=CARTESIAN_POINT ( 'NONE',  ( 23.24999999999999289, 11.65000000001116298, -67.00000000000004263 ) ) ;
#130348=EDGE_LOOP ( 'NONE', ( #126147, #254253, #179099, #38133 ) ) ;
#130349=ORIENTED_EDGE ( 'NONE', *, *, #13391, .T. ) ;
#130361=AXIS2_PLACEMENT_3D ( 'NONE', #167393, #85220, #126956 ) ;
#130389=CARTESIAN_POINT ( 'NONE',  ( -20.54999999999999716, 7.250000000011155521, -79.25000000000004263 ) ) ;
#130431=CIRCLE ( 'NONE', #17991, 11.80000000000000426 ) ;
#130448=AXIS2_PLACEMENT_3D ( 'NONE', #248972, #144706, #85998 ) ;
#130454=CARTESIAN_POINT ( 'NONE',  ( 19.75857864376268935, 11.65000000001115943, -91.85000000000003695 ) ) ;
#130463=ORIENTED_EDGE ( 'NONE', *, *, #143398, .T. ) ;
#130469=ORIENTED_EDGE ( 'NONE', *, *, #84945, .F. ) ;
#130481=ORIENTED_EDGE ( 'NONE', *, *, #209262, .T. ) ;
#130501=DIRECTION ( 'NONE',  ( 0.000000000000000000, 0.000000000000000000, -1.000000000000000000 ) ) ;
#130508=ORIENTED_EDGE ( 'NONE', *, *, #145662, .F. ) ;
#130561=ORIENTED_EDGE ( 'NONE', *, *, #43524, .T. ) ;
#130576=ADVANCED_FACE ( 'NONE', ( #246486 ), #103932, .F. ) ;
#130604=PLANE ( 'NONE',  #122745 ) ;
#130611=CYLINDRICAL_SURFACE ( 'NONE', #243274, 0.1000000000000028644 ) ;
#130614=CYLINDRICAL_SURFACE ( 'NONE', #37651, 0.1000000000000006162 ) ;
#130618=VECTOR ( 'NONE', #68461, 999.9999999999998863 ) ;
#130648=DIRECTION ( 'NONE',  ( 1.000000000000000000, -0.000000000000000000, -0.000000000000000000 ) ) ;
#130661=ORIENTED_EDGE ( 'NONE', *, *, #90539, .F. ) ;
#130671=B_SPLINE_CURVE_WITH_KNOTS ( 'NONE', 3,
 ( #63339, #142863, #159913, #81598, #162476, #221131, #257638, #20399, #222395, #43800 ),
 .UNSPECIFIED., .F., .F.,
 ( 4, 3, 3, 4 ),
 ( 7.757919228897728493E-18, 0.0002000000000002884074, 0.001000000000045107602, 0.001967863649472132576 ),
 .UNSPECIFIED. ) ;
#130677=AXIS2_PLACEMENT_3D ( 'NONE', #205894, #130197, #32437 ) ;
#130764=CARTESIAN_POINT ( 'NONE',  ( -23.25000000000000000, -8.999999999988844479, -90.60603087734760663 ) ) ;
#130772=CARTESIAN_POINT ( 'NONE',  ( 21.09787244211732826, 8.775370707348422172, -79.23925338431750731 ) ) ;
#130778=CARTESIAN_POINT ( 'NONE',  ( 21.04999999999999716, -0.03753606327451285835, -60.66772772606437059 ) ) ;
#130783=VERTEX_POINT ( 'NONE', #141940 ) ;
#130800=CYLINDRICAL_SURFACE ( 'NONE', #55981, 0.1000000000000028644 ) ;
#130832=AXIS2_PLACEMENT_3D ( 'NONE', #254747, #55274, #197379 ) ;
#130846=CARTESIAN_POINT ( 'NONE',  ( 18.60000000000000142, -9.399999999988782662, -74.29725975966333351 ) ) ;
#130867=AXIS2_PLACEMENT_3D ( 'NONE', #179626, #3524, #158791 ) ;
#130886=ADVANCED_FACE ( 'NONE', ( #40318 ), #119842, .F. ) ;
#130939=AXIS2_PLACEMENT_3D ( 'NONE', #133316, #197123, #56321 ) ;
#130946=CARTESIAN_POINT ( 'NONE',  ( 21.05000000000000071, 1.115600667400684642E-11, -100.5000000000000426 ) ) ;
#130959=CARTESIAN_POINT ( 'NONE',  ( -18.50000000000000000, 7.120270961708746960, -104.1595630418393768 ) ) ;
#130970=ORIENTED_EDGE ( 'NONE', *, *, #143841, .T. ) ;
#130971=CARTESIAN_POINT ( 'NONE',  ( 22.49999999999999645, 0.04562336060750230710, -55.34949566145051847 ) ) ;
#130976=CARTESIAN_POINT ( 'NONE',  ( 18.39999999999999858, -9.682403433465241349, -107.1568433774128408 ) ) ;
#130982=VECTOR ( 'NONE', #226023, 1000.000000000000000 ) ;
#131025=DIRECTION ( 'NONE',  ( 0.000000000000000000, 0.1350103645451876666, -0.9908441862701600211 ) ) ;
#131037=ADVANCED_FACE ( 'NONE', ( #16256 ), #37102, .F. ) ;
#131054=DIRECTION ( 'NONE',  ( -0.000000000000000000, 1.000000000000000000, -0.000000000000000000 ) ) ;
#131057=VERTEX_POINT ( 'NONE', #112764 ) ;
#131062=VECTOR ( 'NONE', #138289, 1000.000000000000000 ) ;
#131068=AXIS2_PLACEMENT_3D ( 'NONE', #55762, #135322, #115775 ) ;
#131091=ORIENTED_EDGE ( 'NONE', *, *, #144208, .T. ) ;
#131098=CARTESIAN_POINT ( 'NONE',  ( -23.25000000000000000, 1.910280373842930812, -87.86863214480109718 ) ) ;
#131104=CARTESIAN_POINT ( 'NONE',  ( 20.12500000000000000, 9.750000000011153745, -75.11177128211431864 ) ) ;
#131116=CARTESIAN_POINT ( 'NONE',  ( -20.54999999999999716, 1.115600667400684642E-11, -87.62500000000005684 ) ) ;
#131124=EDGE_CURVE ( 'NONE', #179546, #212939, #62472, .T. ) ;
#131146=ORIENTED_EDGE ( 'NONE', *, *, #155150, .F. ) ;
#131156=CARTESIAN_POINT ( 'NONE',  ( 20.94999999999999929, 1.115600667400684642E-11, -97.60000000000005116 ) ) ;
#131161=DIRECTION ( 'NONE',  ( 0.000000000000000000, 0.000000000000000000, 1.000000000000000000 ) ) ;
#131172=DIRECTION ( 'NONE',  ( 0.000000000000000000, 0.000000000000000000, -1.000000000000000000 ) ) ;
#131209=AXIS2_PLACEMENT_3D ( 'NONE', #53946, #151796, #154380 ) ;
#131249=AXIS2_PLACEMENT_3D ( 'NONE', #177167, #237110, #19346 ) ;
#131261=TOROIDAL_SURFACE ( 'NONE', #102018, 7.800000000000000711, 0.1000000000000000056 ) ;
#131282=LINE ( 'NONE', #234222, #2649 ) ;
#131291=ORIENTED_EDGE ( 'NONE', *, *, #215702, .T. ) ;
#131327=VERTEX_POINT ( 'NONE', #27820 ) ;
#131357=ORIENTED_EDGE ( 'NONE', *, *, #50112, .T. ) ;
#131452=AXIS2_PLACEMENT_3D ( 'NONE', #14491, #213947, #256870 ) ;
#131465=CARTESIAN_POINT ( 'NONE',  ( 23.24999999999999645, 1.115600667400684642E-11, -67.00000000000004263 ) ) ;
#131488=ORIENTED_EDGE ( 'NONE', *, *, #240118, .F. ) ;
#131510=CARTESIAN_POINT ( 'NONE',  ( -22.39999999999999503, 1.115541036281197940E-11, -59.20922040162664501 ) ) ;
#131523=CARTESIAN_POINT ( 'NONE',  ( 20.94999999999999574, 5.900000000011102586, -77.21909976465646253 ) ) ;
#131531=DIRECTION ( 'NONE',  ( -4.408576920032448588E-17, 0.1350103645451876666, 0.9908441862701600211 ) ) ;
#131542=AXIS2_PLACEMENT_3D ( 'NONE', #89981, #192954, #134237 ) ;
#131570=PLANE ( 'NONE',  #122775 ) ;
#131577=CARTESIAN_POINT ( 'NONE',  ( -23.25000000000000000, 1.115600667400684642E-11, -67.00000000000004263 ) ) ;
#131582=FACE_OUTER_BOUND ( 'NONE', #233719, .T. ) ;
#131591=DIRECTION ( 'NONE',  ( 0.000000000000000000, 0.000000000000000000, -1.000000000000000000 ) ) ;
#131612=DIRECTION ( 'NONE',  ( 0.000000000000000000, 0.000000000000000000, -1.000000000000000000 ) ) ;
#131622=ORIENTED_EDGE ( 'NONE', *, *, #42636, .T. ) ;
#131641=ORIENTED_EDGE ( 'NONE', *, *, #255068, .F. ) ;
#131665=LINE ( 'NONE', #70452, #67994 ) ;
#131666=CARTESIAN_POINT ( 'NONE',  ( -18.59999999999999787, 1.835341550235567887, -78.55515129256302487 ) ) ;
#131680=CARTESIAN_POINT ( 'NONE',  ( 20.04142135391667168, 11.75000000001116263, -91.70250686562992826 ) ) ;
#131683=FACE_OUTER_BOUND ( 'NONE', #253230, .T. ) ;
#131709=DIRECTION ( 'NONE',  ( 1.000000000000000000, 0.000000000000000000, 0.000000000000000000 ) ) ;
#131711=CARTESIAN_POINT ( 'NONE',  ( -23.15000000000000213, 1.115600667400684642E-11, -100.5000000000000426 ) ) ;
#131716=CYLINDRICAL_SURFACE ( 'NONE', #227088, 0.09999999999999939493 ) ;
#131739=EDGE_CURVE ( 'NONE', #190057, #96187, #25240, .T. ) ;
#131760=EDGE_CURVE ( 'NONE', #142448, #87242, #100206, .T. ) ;
#131774=FACE_OUTER_BOUND ( 'NONE', #110224, .T. ) ;
#131787=VERTEX_POINT ( 'NONE', #133019 ) ;
#131799=EDGE_LOOP ( 'NONE', ( #27332, #122086, #140308, #50870 ) ) ;
#131819=CARTESIAN_POINT ( 'NONE',  ( 18.49999999999998934, 6.450000000011156587, -77.01702717044007329 ) ) ;
#131836=ORIENTED_EDGE ( 'NONE', *, *, #42073, .F. ) ;
#131874=ORIENTED_EDGE ( 'NONE', *, *, #93257, .F. ) ;
#131884=EDGE_CURVE ( 'NONE', #66775, #194152, #23361, .T. ) ;
#131887=AXIS2_PLACEMENT_3D ( 'NONE', #211193, #191666, #173405 ) ;
#131896=ORIENTED_EDGE ( 'NONE', *, *, #244932, .T. ) ;
#131898=CARTESIAN_POINT ( 'NONE',  ( -18.49999999999999289, -9.419084502802128611, -107.3299078070254069 ) ) ;
#131993=ORIENTED_EDGE ( 'NONE', *, *, #58508, .T. ) ;
#132033=ORIENTED_EDGE ( 'NONE', *, *, #63569, .F. ) ;
#132114=CARTESIAN_POINT ( 'NONE',  ( 22.59999999999999432, 11.74956712350054744, -66.89914163090132604 ) ) ;
#132132=CARTESIAN_POINT ( 'NONE',  ( -18.59999999999999787, 1.115600667400684642E-11, -100.5000000000000426 ) ) ;
#132182=CARTESIAN_POINT ( 'NONE',  ( 18.59999999999999787, -11.74999999998883737, -91.85000000000003695 ) ) ;
#132188=FACE_OUTER_BOUND ( 'NONE', #165263, .T. ) ;
#132204=AXIS2_PLACEMENT_3D ( 'NONE', #103125, #203533, #181420 ) ;
#132230=CARTESIAN_POINT ( 'NONE',  ( 20.85000000000000142, -1.851617760457748618, -112.1031897196037050 ) ) ;
#132243=CARTESIAN_POINT ( 'NONE',  ( -18.43473496883415663, -9.494952410988144464, -74.04587157222827898 ) ) ;
#132278=DIRECTION ( 'NONE',  ( 2.952720810173289112E-16, -1.000000000000000000, 0.000000000000000000 ) ) ;
#132307=EDGE_CURVE ( 'NONE', #75643, #13417, #249635, .T. ) ;
#132313=DIRECTION ( 'NONE',  ( 1.836970198721029934E-16, -1.000000000000000000, -0.000000000000000000 ) ) ;
#132319=EDGE_CURVE ( 'NONE', #4212, #13417, #142108, .T. ) ;
#132335=ORIENTED_EDGE ( 'NONE', *, *, #10680, .T. ) ;
#132349=CARTESIAN_POINT ( 'NONE',  ( -23.15000000000000213, 1.115600667400684642E-11, -100.5000000000000426 ) ) ;
#132368=EDGE_LOOP ( 'NONE', ( #18424, #124941, #203205, #124989, #114966, #168545, #3057 ) ) ;
#132394=CARTESIAN_POINT ( 'NONE',  ( 20.95512820512820440, 8.876151316299271343, -75.55862899514100661 ) ) ;
#132442=CARTESIAN_POINT ( 'NONE',  ( 21.14999999999999858, 8.786607556611267356, -79.25000000000004263 ) ) ;
#132444=DIRECTION ( 'NONE',  ( -7.304098846218134667E-16, -1.000000000000000000, 0.000000000000000000 ) ) ;
#132458=CARTESIAN_POINT ( 'NONE',  ( 20.94999999999999929, 6.550000000011156231, -79.15000000000004832 ) ) ;
#132461=CARTESIAN_POINT ( 'NONE',  ( -18.50000000000000000, -1.135018845899022466, -108.2169768834323662 ) ) ;
#132515=ORIENTED_EDGE ( 'NONE', *, *, #139916, .T. ) ;
#132546=MECHANICAL_DESIGN_GEOMETRIC_PRESENTATION_REPRESENTATION('',(#190849),#32634);
#132550=VERTEX_POINT ( 'NONE', #155618 ) ;
#132554=DIRECTION ( 'NONE',  ( 0.000000000000000000, -8.881784197001266523E-15, 1.000000000000000000 ) ) ;
#132573=CARTESIAN_POINT ( 'NONE',  ( 20.95512820512820440, 8.876151316299271343, -75.55862899514100661 ) ) ;
#132579=ORIENTED_EDGE ( 'NONE', *, *, #243414, .T. ) ;
#132598=DIRECTION ( 'NONE',  ( 1.000000000000000000, 0.000000000000000000, 0.000000000000000000 ) ) ;
#132605=FACE_OUTER_BOUND ( 'NONE', #72995, .T. ) ;
#132610=CARTESIAN_POINT ( 'NONE',  ( -18.39999999999999858, -9.599999999988849453, -107.1001893912220879 ) ) ;
#132645=AXIS2_PLACEMENT_3D ( 'NONE', #255226, #33718, #211031 ) ;
#132648=DIRECTION ( 'NONE',  ( 1.000000000000000000, 0.000000000000000000, 0.000000000000000000 ) ) ;
#132673=EDGE_LOOP ( 'NONE', ( #224702, #149059, #65819, #240911 ) ) ;
#132700=EDGE_CURVE ( 'NONE', #246051, #254405, #107148, .T. ) ;
#132732=EDGE_CURVE ( 'NONE', #3545, #88741, #46589, .T. ) ;
#132759=AXIS2_PLACEMENT_3D ( 'NONE', #244205, #61738, #184247 ) ;
#132839=AXIS2_PLACEMENT_3D ( 'NONE', #181790, #47395, #125659 ) ;
#132870=CARTESIAN_POINT ( 'NONE',  ( -20.54999999999999716, 1.115600667400684642E-11, -102.4000000000000483 ) ) ;
#132880=CARTESIAN_POINT ( 'NONE',  ( 18.48536876927986228, -9.463527249856182877, -74.04861826508293632 ) ) ;
#132898=EDGE_CURVE ( 'NONE', #202477, #246051, #34182, .T. ) ;
#132907=AXIS2_PLACEMENT_3D ( 'NONE', #71526, #15394, #152353 ) ;
#132955=LINE ( 'NONE', #170837, #48374 ) ;
#133006=DIRECTION ( 'NONE',  ( 0.7071067811865475727, -0.7071067811865475727, 0.000000000000000000 ) ) ;
#133019=CARTESIAN_POINT ( 'NONE',  ( -23.25000000000000000, 1.910280373842936141, -79.63136785519898808 ) ) ;
#133050=DIRECTION ( 'NONE',  ( 1.000000000000000000, 0.000000000000000000, 0.000000000000000000 ) ) ;
#133058=LINE ( 'NONE', #212597, #238561 ) ;
#133094=AXIS2_PLACEMENT_3D ( 'NONE', #55746, #194038, #153665 ) ;
#133119=DIRECTION ( 'NONE',  ( 0.000000000000000000, -0.000000000000000000, -1.000000000000000000 ) ) ;
#133130=FACE_OUTER_BOUND ( 'NONE', #145059, .T. ) ;
#133216=VERTEX_POINT ( 'NONE', #130246 ) ;
#133218=CYLINDRICAL_SURFACE ( 'NONE', #100779, 4.049999999999998046 ) ;
#133231=CARTESIAN_POINT ( 'NONE',  ( -18.59999999999999787, -1.637172712959223952, -78.58215336547205254 ) ) ;
#133243=AXIS2_PLACEMENT_3D ( 'NONE', #226956, #10486, #131709 ) ;
#133253=VERTEX_POINT ( 'NONE', #48150 ) ;
#133316=CARTESIAN_POINT ( 'NONE',  ( -18.59999999999999787, 9.350000000011156942, -79.15000000000003411 ) ) ;
#133344=DIRECTION ( 'NONE',  ( 0.000000000000000000, -0.4930308989875248349, -0.8700118002898312719 ) ) ;
#133348=DIRECTION ( 'NONE',  ( 0.000000000000000000, 0.000000000000000000, -1.000000000000000000 ) ) ;
#133363=CIRCLE ( 'NONE', #145816, 0.09999999999999910349 ) ;
#133406=EDGE_LOOP ( 'NONE', ( #144386, #82372, #85463, #55960 ) ) ;
#133408=DIRECTION ( 'NONE',  ( -2.557131231893036985E-16, 0.8660254037844384856, -0.5000000000000002220 ) ) ;
#133451=FACE_OUTER_BOUND ( 'NONE', #72254, .T. ) ;
#133468=EDGE_LOOP ( 'NONE', ( #213703, #148319, #169844, #90428, #107329, #23179 ) ) ;
#133477=CARTESIAN_POINT ( 'NONE',  ( 18.59999999999999076, 11.75000000001115907, -91.85000000000003695 ) ) ;
#133601=CARTESIAN_POINT ( 'NONE',  ( -20.85000000000000142, -1.164121893230052995, -108.2148480855716457 ) ) ;
#133610=DIRECTION ( 'NONE',  ( 1.000000000000000000, 0.000000000000000000, -0.000000000000000000 ) ) ;
#133618=EDGE_LOOP ( 'NONE', ( #230248, #141903, #64221, #77874 ) ) ;
#133620=EDGE_LOOP ( 'NONE', ( #29056, #109660, #50763, #240582 ) ) ;
#133636=DIRECTION ( 'NONE',  ( 1.000000000000000000, 0.000000000000000000, 0.000000000000000000 ) ) ;
#133653=DIRECTION ( 'NONE',  ( 0.000000000000000000, -0.8660254037844384856, 0.5000000000000002220 ) ) ;
#133658=EDGE_CURVE ( 'NONE', #113044, #224195, #147118, .T. ) ;
#133668=ORIENTED_EDGE ( 'NONE', *, *, #222561, .F. ) ;
#133690=CARTESIAN_POINT ( 'NONE',  ( 21.14999999999999503, -11.64999999998883595, -55.25000000000004974 ) ) ;
#133696=DIRECTION ( 'NONE',  ( 0.000000000000000000, 0.000000000000000000, -1.000000000000000000 ) ) ;
#133700=VERTEX_POINT ( 'NONE', #13859 ) ;
#133718=DIRECTION ( 'NONE',  ( 0.000000000000000000, 0.000000000000000000, 1.000000000000000000 ) ) ;
#133721=SPHERICAL_SURFACE ( 'NONE', #81189, 0.1000000000000000056 ) ;
#133739=CARTESIAN_POINT ( 'NONE',  ( 23.14999999999998437, 11.75000000001115552, -67.00000000000004263 ) ) ;
#133742=ADVANCED_FACE ( 'NONE', ( #158522 ), #126272, .T. ) ;
#133763=VECTOR ( 'NONE', #39747, 1000.000000000000000 ) ;
#133769=DIRECTION ( 'NONE',  ( 2.940209281316622495E-16, -1.000000000000000000, -5.880418562633244990E-15 ) ) ;
#133796=CIRCLE ( 'NONE', #8916, 0.1000000000000029060 ) ;
#133809=ORIENTED_EDGE ( 'NONE', *, *, #215991, .F. ) ;
#133851=EDGE_LOOP ( 'NONE', ( #57551, #31695, #162668, #173446 ) ) ;
#133867=DIRECTION ( 'NONE',  ( 0.000000000000000000, 0.000000000000000000, -1.000000000000000000 ) ) ;
#133914=DIRECTION ( 'NONE',  ( 0.000000000000000000, 0.000000000000000000, -1.000000000000000000 ) ) ;
#133974=AXIS2_PLACEMENT_3D ( 'NONE', #115309, #74937, #192297 ) ;
#134012=DIRECTION ( 'NONE',  ( 0.000000000000000000, 0.4999999999999949485, -0.8660254037844415942 ) ) ;
#134013=B_SPLINE_CURVE_WITH_KNOTS ( 'NONE', 3,
 ( #4531, #5807, #164907, #50085, #202744, #206598, #108777 ),
 .UNSPECIFIED., .F., .F.,
 ( 4, 3, 4 ),
 ( 0.000000000000000000, 3.357501770814783759E-05, 5.199112466349758733E-05 ),
 .UNSPECIFIED. ) ;
#134036=ORIENTED_EDGE ( 'NONE', *, *, #175460, .T. ) ;
#134051=CARTESIAN_POINT ( 'NONE',  ( 23.14999999999999858, -3.999999999988843147, -100.5000000000000426 ) ) ;
#134063=CARTESIAN_POINT ( 'NONE',  ( -21.14999999999999858, 11.75000000001115552, -73.72613063605923855 ) ) ;
#134077=VERTEX_POINT ( 'NONE', #20964 ) ;
#134131=EDGE_CURVE ( 'NONE', #241878, #225548, #217824, .T. ) ;
#134133=AXIS2_PLACEMENT_3D ( 'NONE', #240027, #200886, #255680 ) ;
#134144=CARTESIAN_POINT ( 'NONE',  ( 23.24999999999999645, 5.000000000011153745, -88.09473398108696074 ) ) ;
#134163=FACE_OUTER_BOUND ( 'NONE', #224047, .T. ) ;
#134186=VERTEX_POINT ( 'NONE', #65188 ) ;
#134191=ORIENTED_EDGE ( 'NONE', *, *, #66866, .T. ) ;
#134222=EDGE_CURVE ( 'NONE', #87571, #86852, #159785, .T. ) ;
#134237=DIRECTION ( 'NONE',  ( 0.000000000000000000, 0.000000000000000000, -1.000000000000000000 ) ) ;
#134238=CIRCLE ( 'NONE', #151016, 3.999999999999999112 ) ;
#134259=ORIENTED_EDGE ( 'NONE', *, *, #174488, .F. ) ;
#134260=ORIENTED_EDGE ( 'NONE', *, *, #58752, .F. ) ;
#134297=DIRECTION ( 'NONE',  ( 0.000000000000000000, 0.000000000000000000, -1.000000000000000000 ) ) ;
#134319=DIRECTION ( 'NONE',  ( 1.000000000000000000, 3.265361837132813093E-16, -0.000000000000000000 ) ) ;
#134322=DIRECTION ( 'NONE',  ( 0.000000000000000000, -0.000000000000000000, 1.000000000000000000 ) ) ;
#134338=LINE ( 'NONE', #16997, #185331 ) ;
#134374=ORIENTED_EDGE ( 'NONE', *, *, #29199, .T. ) ;
#134383=EDGE_LOOP ( 'NONE', ( #163660, #50753, #214889, #205899 ) ) ;
#134387=ORIENTED_EDGE ( 'NONE', *, *, #22705, .T. ) ;
#134391=ORIENTED_EDGE ( 'NONE', *, *, #117028, .T. ) ;
#134400=DIRECTION ( 'NONE',  ( 0.000000000000000000, 0.9654727137038715545, -0.2605042016806676242 ) ) ;
#134402=EDGE_CURVE ( 'NONE', #52066, #24624, #230117, .T. ) ;
#134412=CARTESIAN_POINT ( 'NONE',  ( 21.05000000000000071, 11.65000000001115943, -67.10000000000005116 ) ) ;
#134486=AXIS2_PLACEMENT_3D ( 'NONE', #56046, #153944, #15700 ) ;
#134489=CIRCLE ( 'NONE', #105435, 11.65000000000000036 ) ;
#134501=EDGE_LOOP ( 'NONE', ( #50432, #26682, #94245, #256180 ) ) ;
#134618=AXIS2_PLACEMENT_3D ( 'NONE', #117898, #119204, #198726 ) ;
#134644=ORIENTED_EDGE ( 'NONE', *, *, #60463, .T. ) ;
#134686=VECTOR ( 'NONE', #43692, 1000.000000000000000 ) ;
#134688=CARTESIAN_POINT ( 'NONE',  ( 22.47007471830798053, 1.116269474027924959E-11, -59.27928934807359695 ) ) ;
#134690=DIRECTION ( 'NONE',  ( 0.000000000000000000, 0.000000000000000000, -1.000000000000000000 ) ) ;
#134703=DIRECTION ( 'NONE',  ( -1.836970198721029934E-16, 1.000000000000000000, 0.000000000000000000 ) ) ;
#134711=VERTEX_POINT ( 'NONE', #45319 ) ;
#134713=EDGE_CURVE ( 'NONE', #23868, #210308, #101068, .T. ) ;
#134720=CIRCLE ( 'NONE', #247148, 2.000000000000001776 ) ;
#134724=ORIENTED_EDGE ( 'NONE', *, *, #83007, .T. ) ;
#134777=AXIS2_PLACEMENT_3D ( 'NONE', #230714, #225535, #149902 ) ;
#134780=DIRECTION ( 'NONE',  ( 1.000000000000000000, 0.000000000000000000, 0.000000000000000000 ) ) ;
#134836=EDGE_LOOP ( 'NONE', ( #65309, #199298 ) ) ;
#134924=CYLINDRICAL_SURFACE ( 'NONE', #120026, 0.09999999999999939493 ) ;
#134930=EDGE_CURVE ( 'NONE', #44654, #176730, #9544, .T. ) ;
#134945=CARTESIAN_POINT ( 'NONE',  ( 18.59999999999999432, 1.162701749949165642, -75.10000000000003695 ) ) ;
#134965=AXIS2_PLACEMENT_3D ( 'NONE', #146730, #108910, #149355 ) ;
#135003=CYLINDRICAL_SURFACE ( 'NONE', #251378, 0.1000000000000028644 ) ;
#135023=AXIS2_PLACEMENT_3D ( 'NONE', #185683, #223503, #8341 ) ;
#135041=CARTESIAN_POINT ( 'NONE',  ( -18.55807992284872299, 10.32898536001801304, -106.0826683222765041 ) ) ;
#135059=CIRCLE ( 'NONE', #30885, 11.74999999999999645 ) ;
#135063=EDGE_CURVE ( 'NONE', #233091, #155368, #26313, .T. ) ;
#135075=CARTESIAN_POINT ( 'NONE',  ( 22.39999999999999858, 7.790779598384538929, -66.90000000000004832 ) ) ;
#135077=CARTESIAN_POINT ( 'NONE',  ( 23.15000000000000213, -8.999999999988842703, -90.60603087734760663 ) ) ;
#135080=CARTESIAN_POINT ( 'NONE',  ( -21.37071067811865532, 8.070710678129811910, -88.15000000000004832 ) ) ;
#135082=EDGE_CURVE ( 'NONE', #95981, #203190, #148866, .T. ) ;
#135130=ADVANCED_FACE ( 'NONE', ( #89261 ), #73047, .T. ) ;
#135143=AXIS2_PLACEMENT_3D ( 'NONE', #174933, #176180, #112346 ) ;
#135146=VECTOR ( 'NONE', #156682, 1000.000000000000000 ) ;
#135149=FACE_OUTER_BOUND ( 'NONE', #22235, .T. ) ;
#135160=DIRECTION ( 'NONE',  ( 0.000000000000000000, 0.000000000000000000, 1.000000000000000000 ) ) ;
#135186=VERTEX_POINT ( 'NONE', #150541 ) ;
#135202=CIRCLE ( 'NONE', #197935, 11.74999999999999645 ) ;
#135206=EDGE_CURVE ( 'NONE', #2322, #224755, #232659, .T. ) ;
#135234=CARTESIAN_POINT ( 'NONE',  ( 20.95289811251229750, 8.893168004469750088, -75.50180949391855734 ) ) ;
#135272=AXIS2_PLACEMENT_3D ( 'NONE', #41263, #219859, #137744 ) ;
#135279=CARTESIAN_POINT ( 'NONE',  ( -21.05000000000000071, 11.60000000001115517, -93.57179676972454274 ) ) ;
#135293=AXIS2_PLACEMENT_3D ( 'NONE', #179416, #728, #255017 ) ;
#135322=DIRECTION ( 'NONE',  ( 1.000000000000000000, 0.000000000000000000, -0.000000000000000000 ) ) ;
#135327=ORIENTED_EDGE ( 'NONE', *, *, #50824, .T. ) ;
#135333=VECTOR ( 'NONE', #127478, 1000.000000000000000 ) ;
#135340=LINE ( 'NONE', #134063, #99278 ) ;
#135350=PLANE ( 'NONE',  #33082 ) ;
#135387=CIRCLE ( 'NONE', #172872, 0.1000000000000000472 ) ;
#135399=CARTESIAN_POINT ( 'NONE',  ( -18.59999999999999787, 11.65000000001115232, -79.15000000000004832 ) ) ;
#135414=CARTESIAN_POINT ( 'NONE',  ( -20.54999999999999716, 7.150000000011155876, -79.25000000000004263 ) ) ;
#135420=CARTESIAN_POINT ( 'NONE',  ( 18.42595409746875745, -9.499999812554055012, -73.99936235174590138 ) ) ;
#135546=LINE ( 'NONE', #113433, #217191 ) ;
#135586=CARTESIAN_POINT ( 'NONE',  ( 21.05000000000000071, 1.115600667400684642E-11, -67.00000000000004263 ) ) ;
#135592=EDGE_CURVE ( 'NONE', #73858, #257895, #84890, .T. ) ;
#135600=CARTESIAN_POINT ( 'NONE',  ( 23.15000000000000213, -11.74999999998883560, -79.15000000000004832 ) ) ;
#135601=CIRCLE ( 'NONE', #64695, 0.6000000000000033085 ) ;
#135612=ORIENTED_EDGE ( 'NONE', *, *, #110, .F. ) ;
#135621=EDGE_CURVE ( 'NONE', #217587, #68571, #39165, .T. ) ;
#135657=FACE_OUTER_BOUND ( 'NONE', #185927, .T. ) ;
#135706=DIRECTION ( 'NONE',  ( 0.000000000000000000, 0.000000000000000000, 1.000000000000000000 ) ) ;
#135743=DIRECTION ( 'NONE',  ( 1.000000000000000000, 0.000000000000000000, 0.000000000000000000 ) ) ;
#135746=FACE_OUTER_BOUND ( 'NONE', #207545, .T. ) ;
#135773=VERTEX_POINT ( 'NONE', #83159 ) ;
#135778=SURFACE_STYLE_USAGE ( .BOTH. , #180066 ) ;
#135788=VERTEX_POINT ( 'NONE', #203147 ) ;
#135798=DIRECTION ( 'NONE',  ( 5.421010862427554711E-16, -1.000000000000000000, -3.252606517456533024E-15 ) ) ;
#135801=CIRCLE ( 'NONE', #202459, 0.09999999999999982514 ) ;
#135826=AXIS2_PLACEMENT_3D ( 'NONE', #223104, #82287, #161883 ) ;
#135848=DIRECTION ( 'NONE',  ( 1.000000000000000000, -0.000000000000000000, -0.000000000000000000 ) ) ;
#135881=CARTESIAN_POINT ( 'NONE',  ( 23.25000000000000000, -11.74999999998883560, -79.15000000000004832 ) ) ;
#135913=ORIENTED_EDGE ( 'NONE', *, *, #99180, .F. ) ;
#135950=AXIS2_PLACEMENT_3D ( 'NONE', #118571, #40339, #37754 ) ;
#135990=TOROIDAL_SURFACE ( 'NONE', #73676, 0.4000000000000012990, 0.1000000000000000056 ) ;
#136015=CARTESIAN_POINT ( 'NONE',  ( 21.09316766718127667, 6.370153312485569153, -66.96073659768534014 ) ) ;
#136048=ORIENTED_EDGE ( 'NONE', *, *, #5093, .F. ) ;
#136065=SPHERICAL_SURFACE ( 'NONE', #74438, 0.1000000000000000056 ) ;
#136090=CIRCLE ( 'NONE', #32094, 11.70000000000000284 ) ;
#136092=ADVANCED_FACE ( 'NONE', ( #181232 ), #239915, .F. ) ;
#136097=DIRECTION ( 'NONE',  ( 1.000000000000000000, 0.000000000000000000, 0.000000000000000000 ) ) ;
#136100=CARTESIAN_POINT ( 'NONE',  ( 21.05000000000000071, 10.72371710471867701, -67.00000000000004263 ) ) ;
#136131=ADVANCED_FACE ( 'NONE', ( #20885 ), #160154, .T. ) ;
#136170=CARTESIAN_POINT ( 'NONE',  ( -22.59999999999999787, 1.115600667400684642E-11, -67.00000000000004263 ) ) ;
#136184=CARTESIAN_POINT ( 'NONE',  ( 21.05000000000000071, 1.115600667400684642E-11, -67.00000000000004263 ) ) ;
#136286=AXIS2_PLACEMENT_3D ( 'NONE', #40867, #222008, #21301 ) ;
#136336=ORIENTED_EDGE ( 'NONE', *, *, #99441, .T. ) ;
#136362=ORIENTED_EDGE ( 'NONE', *, *, #80950, .T. ) ;
#136366=VECTOR ( 'NONE', #223086, 1000.000000000000000 ) ;
#136370=DIRECTION ( 'NONE',  ( -0.000000000000000000, -0.000000000000000000, -1.000000000000000000 ) ) ;
#136376=ORIENTED_EDGE ( 'NONE', *, *, #93452, .T. ) ;
#136399=EDGE_CURVE ( 'NONE', #18995, #230047, #193466, .T. ) ;
#136419=CARTESIAN_POINT ( 'NONE',  ( 20.84999999999998721, 11.75000000001115552, -100.5000000000000426 ) ) ;
#136450=DIRECTION ( 'NONE',  ( 0.000000000000000000, 1.000000000000000000, -0.000000000000000000 ) ) ;
#136458=DIRECTION ( 'NONE',  ( 1.000000000000000000, 0.000000000000000000, 0.000000000000000000 ) ) ;
#136530=FACE_OUTER_BOUND ( 'NONE', #52911, .T. ) ;
#136541=ORIENTED_EDGE ( 'NONE', *, *, #165084, .F. ) ;
#136615=EDGE_LOOP ( 'NONE', ( #207009, #112050, #197071, #67624 ) ) ;
#136652=EDGE_CURVE ( 'NONE', #238381, #208354, #166499, .T. ) ;
#136662=AXIS2_PLACEMENT_3D ( 'NONE', #167291, #246784, #22635 ) ;
#136699=EDGE_CURVE ( 'NONE', #100102, #78058, #110411, .T. ) ;
#136712=EDGE_CURVE ( 'NONE', #135186, #109568, #139617, .T. ) ;
#136714=DIRECTION ( 'NONE',  ( -0.000000000000000000, 1.000000000000000000, 2.891205793294679805E-16 ) ) ;
#136718=DIRECTION ( 'NONE',  ( 0.000000000000000000, 0.5000000000000014433, -0.8660254037844378194 ) ) ;
#136720=CARTESIAN_POINT ( 'NONE',  ( 18.50000000000000000, -9.499999999988842703, -55.25000000000004974 ) ) ;
#136723=EDGE_LOOP ( 'NONE', ( #166138, #63641, #70021, #20088 ) ) ;
#136724=ADVANCED_FACE ( 'NONE', ( #163907 ), #131261, .T. ) ;
#136725=DIRECTION ( 'NONE',  ( 0.000000000000000000, 1.000000000000000000, 0.000000000000000000 ) ) ;
#136773=ORIENTED_EDGE ( 'NONE', *, *, #191410, .F. ) ;
#136874=EDGE_LOOP ( 'NONE', ( #192541, #55608, #172379, #144321 ) ) ;
#136904=EDGE_LOOP ( 'NONE', ( #107526, #106603, #216284, #30366 ) ) ;
#136939=AXIS2_PLACEMENT_3D ( 'NONE', #50672, #192787, #36291 ) ;
#136961=VERTEX_POINT ( 'NONE', #223239 ) ;
#136997=CYLINDRICAL_SURFACE ( 'NONE', #197394, 0.09999999999999939493 ) ;
#137054=ORIENTED_EDGE ( 'NONE', *, *, #101715, .F. ) ;
#137109=EDGE_CURVE ( 'NONE', #89054, #58722, #56423, .T. ) ;
#137131=VECTOR ( 'NONE', #27993, 1000.000000000000000 ) ;
#137138=ORIENTED_EDGE ( 'NONE', *, *, #199859, .F. ) ;
#137171=EDGE_CURVE ( 'NONE', #147343, #231071, #243873, .T. ) ;
#137189=EDGE_LOOP ( 'NONE', ( #157117, #150316, #161495, #180770, #156801, #34481, #245995, #56473, #48392, #105605, #52666, #146314, #70928, #40526 ) ) ;
#137200=EDGE_CURVE ( 'NONE', #206950, #374, #156598, .T. ) ;
#137228=DIRECTION ( 'NONE',  ( 1.000000000000000000, 0.000000000000000000, 0.000000000000000000 ) ) ;
#137242=DIRECTION ( 'NONE',  ( 0.000000000000000000, 0.000000000000000000, -1.000000000000000000 ) ) ;
#137254=CYLINDRICAL_SURFACE ( 'NONE', #204458, 0.1000000000000028644 ) ;
#137292=EDGE_CURVE ( 'NONE', #98112, #85621, #160713, .T. ) ;
#137327=AXIS2_PLACEMENT_3D ( 'NONE', #113228, #93669, #130212 ) ;
#137337=LINE ( 'NONE', #232631, #19252 ) ;
#137341=ORIENTED_EDGE ( 'NONE', *, *, #129883, .F. ) ;
#137355=CYLINDRICAL_SURFACE ( 'NONE', #124421, 0.09999999999999939493 ) ;
#137365=CARTESIAN_POINT ( 'NONE',  ( -18.50000000000000355, -9.399999999988814636, -74.29725975966334772 ) ) ;
#137366=DIRECTION ( 'NONE',  ( 0.000000000000000000, -0.6728971962616697722, 0.7397360091702875895 ) ) ;
#137371=ORIENTED_EDGE ( 'NONE', *, *, #178984, .F. ) ;
#137421=VERTEX_POINT ( 'NONE', #66444 ) ;
#137430=DIRECTION ( 'NONE',  ( 1.000000000000000000, -7.304098846218135653E-16, -2.111765289898286048E-31 ) ) ;
#137446=DIRECTION ( 'NONE',  ( 0.000000000000000000, 0.000000000000000000, 1.000000000000000000 ) ) ;
#137448=AXIS2_PLACEMENT_3D ( 'NONE', #81648, #240772, #62133 ) ;
#137453=CARTESIAN_POINT ( 'NONE',  ( -18.50000000000000000, 9.250000000011157297, -88.35000000000003695 ) ) ;
#137454=ORIENTED_EDGE ( 'NONE', *, *, #166842, .T. ) ;
#137469=DIRECTION ( 'NONE',  ( 0.000000000000000000, 0.000000000000000000, -1.000000000000000000 ) ) ;
#137476=DIRECTION ( 'NONE',  ( -3.469446951953612296E-14, -0.9908441862701596881, -0.1350103645451904977 ) ) ;
#137479=SPHERICAL_SURFACE ( 'NONE', #16869, 0.1000000000000000056 ) ;
#137489=EDGE_CURVE ( 'NONE', #238715, #150205, #6459, .T. ) ;
#137497=SPHERICAL_SURFACE ( 'NONE', #180305, 0.1000000000000000056 ) ;
#137501=ADVANCED_FACE ( 'NONE', ( #14196, #11619, #50695 ), #112001, .F. ) ;
#137509=DIRECTION ( 'NONE',  ( 0.000000000000000000, 0.000000000000000000, -1.000000000000000000 ) ) ;
#137525=CIRCLE ( 'NONE', #233432, 0.09999999999999939493 ) ;
#137545=CARTESIAN_POINT ( 'NONE',  ( 23.24999999999999289, 6.650000000011155876, -88.15000000000004832 ) ) ;
#137562=VERTEX_POINT ( 'NONE', #175828 ) ;
#137570=EDGE_CURVE ( 'NONE', #220040, #26378, #121880, .T. ) ;
#137585=AXIS2_PLACEMENT_3D ( 'NONE', #157739, #133006, #112167 ) ;
#137594=ADVANCED_FACE ( 'NONE', ( #252763 ), #74180, .T. ) ;
#137595=CARTESIAN_POINT ( 'NONE',  ( -23.15000000000000213, 1.115600667400684642E-11, -100.5000000000000426 ) ) ;
#137639=EDGE_CURVE ( 'NONE', #205612, #230995, #125949, .T. ) ;
#137642=ORIENTED_EDGE ( 'NONE', *, *, #170940, .F. ) ;
#137644=DIRECTION ( 'NONE',  ( 0.000000000000000000, -1.000000000000000000, 0.000000000000000000 ) ) ;
#137650=FACE_OUTER_BOUND ( 'NONE', #193200, .T. ) ;
#137658=CARTESIAN_POINT ( 'NONE',  ( -21.14999999999999858, 1.115600667400684642E-11, -60.45934304829880546 ) ) ;
#137662=FACE_OUTER_BOUND ( 'NONE', #215861, .T. ) ;
#137671=EDGE_CURVE ( 'NONE', #140349, #143381, #63595, .T. ) ;
#137675=DIRECTION ( 'NONE',  ( 0.000000000000000000, 0.000000000000000000, -1.000000000000000000 ) ) ;
#137711=ORIENTED_EDGE ( 'NONE', *, *, #216471, .F. ) ;
#137744=DIRECTION ( 'NONE',  ( 0.000000000000000000, 0.000000000000000000, 1.000000000000000000 ) ) ;
#137748=DIRECTION ( 'NONE',  ( 1.000000000000000000, -0.000000000000000000, -0.000000000000000000 ) ) ;
#137753=CARTESIAN_POINT ( 'NONE',  ( -21.14999999999999858, 11.65000000001115588, -67.10000000000005116 ) ) ;
#137771=CARTESIAN_POINT ( 'NONE',  ( -18.39999999999999858, -9.519327731081281385, -73.97297637655937308 ) ) ;
#137777=VERTEX_POINT ( 'NONE', #24463 ) ;
#137784=CARTESIAN_POINT ( 'NONE',  ( -18.50000000000000000, 9.150000000011157653, -55.25000000000004974 ) ) ;
#137786=CARTESIAN_POINT ( 'NONE',  ( -18.59999999999999787, -1.687074390080403941, -54.18542703345839584 ) ) ;
#137836=CYLINDRICAL_SURFACE ( 'NONE', #235644, 0.1000000000000028644 ) ;
#137874=CIRCLE ( 'NONE', #92097, 0.1000000000000002692 ) ;
#137876=CARTESIAN_POINT ( 'NONE',  ( 21.06089410995816635, 10.72529553213474429, -79.20238073104307830 ) ) ;
#137896=ORIENTED_EDGE ( 'NONE', *, *, #39429, .T. ) ;
#137898=CIRCLE ( 'NONE', #71307, 0.2000000000000057288 ) ;
#137902=EDGE_CURVE ( 'NONE', #249989, #170195, #50387, .T. ) ;
#137959=CARTESIAN_POINT ( 'NONE',  ( 18.59999999999999076, 11.65000000001115943, -100.5000000000000426 ) ) ;
#137973=EDGE_CURVE ( 'NONE', #219130, #60211, #117765, .T. ) ;
#138011=DIRECTION ( 'NONE',  ( 1.000000000000000000, -0.000000000000000000, -0.000000000000000000 ) ) ;
#138041=ORIENTED_EDGE ( 'NONE', *, *, #140449, .F. ) ;
#138090=VERTEX_POINT ( 'NONE', #77656 ) ;
#138141=CYLINDRICAL_SURFACE ( 'NONE', #67149, 0.09999999999999939493 ) ;
#138173=LINE ( 'NONE', #216440, #19576 ) ;
#138183=DIRECTION ( 'NONE',  ( 0.000000000000000000, 0.2605042016806672911, -0.9654727137038716656 ) ) ;
#138190=LINE ( 'NONE', #157828, #110216 ) ;
#138253=EDGE_CURVE ( 'NONE', #203104, #94857, #63239, .T. ) ;
#138269=AXIS2_PLACEMENT_3D ( 'NONE', #217097, #175454, #157179 ) ;
#138278=DIRECTION ( 'NONE',  ( 7.304098846218134667E-16, 1.000000000000000000, -0.000000000000000000 ) ) ;
#138289=DIRECTION ( 'NONE',  ( -1.000000000000000000, -7.304098846218135653E-16, 4.607487905232624742E-31 ) ) ;
#138320=DIRECTION ( 'NONE',  ( 2.840903330521633255E-16, -0.8700118002898322711, 0.4930308989875231696 ) ) ;
#138334=( NAMED_UNIT ( * ) PLANE_ANGLE_UNIT ( ) SI_UNIT ( $, .RADIAN. ) );
#138340=CARTESIAN_POINT ( 'NONE',  ( 20.94999999999999929, -11.48912529306489994, -97.50000000000004263 ) ) ;
#138369=ORIENTED_EDGE ( 'NONE', *, *, #118732, .T. ) ;
#138381=CARTESIAN_POINT ( 'NONE',  ( 18.58685178364169843, -9.406733083793096029, -74.12442046908778082 ) ) ;
#138384=CIRCLE ( 'NONE', #71967, 0.1000000000000028644 ) ;
#138385=ORIENTED_EDGE ( 'NONE', *, *, #227286, .T. ) ;
#138389=CARTESIAN_POINT ( 'NONE',  ( 18.59999999999999432, -1.162701749926853712, -75.10000000000003695 ) ) ;
#138394=CARTESIAN_POINT ( 'NONE',  ( -20.87600722750343252, 10.33112638556969465, -106.0901228926975080 ) ) ;
#138401=ORIENTED_EDGE ( 'NONE', *, *, #28189, .T. ) ;
#138404=AXIS2_PLACEMENT_3D ( 'NONE', #229379, #32488, #15472 ) ;
#138428=AXIS2_PLACEMENT_3D ( 'NONE', #2967, #180341, #181634 ) ;
#138464=CARTESIAN_POINT ( 'NONE',  ( 18.59999999999999076, 1.115600667400684642E-11, -100.5000000000000426 ) ) ;
#138490=ORIENTED_EDGE ( 'NONE', *, *, #198361, .T. ) ;
#138498=LINE ( 'NONE', #141107, #142963 ) ;
#138499=ORIENTED_EDGE ( 'NONE', *, *, #209354, .F. ) ;
#138509=DIRECTION ( 'NONE',  ( -1.000000000000000000, -0.000000000000000000, -0.000000000000000000 ) ) ;
#138516=DIRECTION ( 'NONE',  ( 1.000000000000000000, 0.000000000000000000, -0.000000000000000000 ) ) ;
#138535=CARTESIAN_POINT ( 'NONE',  ( 20.12500000000000000, 9.750000000011153745, -75.11177128211431864 ) ) ;
#138538=FACE_OUTER_BOUND ( 'NONE', #168657, .T. ) ;
#138539=ORIENTED_EDGE ( 'NONE', *, *, #108273, .F. ) ;
#138545=AXIS2_PLACEMENT_3D ( 'NONE', #248732, #90927, #147042 ) ;
#138547=ORIENTED_EDGE ( 'NONE', *, *, #65652, .F. ) ;
#138550=VERTEX_POINT ( 'NONE', #168197 ) ;
#138616=AXIS2_PLACEMENT_3D ( 'NONE', #26998, #143044, #43964 ) ;
#138620=ORIENTED_EDGE ( 'NONE', *, *, #243569, .T. ) ;
#138655=ADVANCED_FACE ( 'NONE', ( #255331 ), #15521, .F. ) ;
#138701=CARTESIAN_POINT ( 'NONE',  ( -21.14999999999999858, 11.75000000001115552, -67.10000000000005116 ) ) ;
#138711=CARTESIAN_POINT ( 'NONE',  ( -21.14999999999999858, 11.65000000001115588, -67.00000000000004263 ) ) ;
#138719=ORIENTED_EDGE ( 'NONE', *, *, #255650, .F. ) ;
#138752=LINE ( 'NONE', #81353, #106974 ) ;
#138783=ORIENTED_EDGE ( 'NONE', *, *, #49027, .F. ) ;
#138803=ADVANCED_FACE ( 'NONE', ( #242226 ), #197970, .F. ) ;
#138842=ORIENTED_EDGE ( 'NONE', *, *, #76682, .F. ) ;
#138845=DIRECTION ( 'NONE',  ( 0.000000000000000000, 0.000000000000000000, 1.000000000000000000 ) ) ;
#138848=AXIS2_PLACEMENT_3D ( 'NONE', #116751, #120632, #197566 ) ;
#138870=AXIS2_PLACEMENT_3D ( 'NONE', #38199, #134690, #214256 ) ;
#138873=CARTESIAN_POINT ( 'NONE',  ( -18.50000324121759121, 10.29307482169070553, -105.9586421466940749 ) ) ;
#138877=DIRECTION ( 'NONE',  ( 0.000000000000000000, 0.000000000000000000, -1.000000000000000000 ) ) ;
#138885=EDGE_CURVE ( 'NONE', #39159, #93529, #222332, .T. ) ;
#138907=DIRECTION ( 'NONE',  ( 1.000000000000000000, -0.000000000000000000, -0.000000000000000000 ) ) ;
#138967=CARTESIAN_POINT ( 'NONE',  ( -20.64999999999999858, 7.250000000011155521, -79.35000000000005116 ) ) ;
#138974=AXIS2_PLACEMENT_3D ( 'NONE', #47222, #186770, #126779 ) ;
#138985=DIRECTION ( 'NONE',  ( -0.000000000000000000, 0.8660254037844411501, 0.4999999999999956701 ) ) ;
#138994=CARTESIAN_POINT ( 'NONE',  ( -20.64999999999999858, -8.999999999988844479, -90.60603087734760663 ) ) ;
#139030=EDGE_CURVE ( 'NONE', #202405, #19842, #55346, .T. ) ;
#139035=AXIS2_PLACEMENT_3D ( 'NONE', #126737, #206279, #204967 ) ;
#139058=FACE_OUTER_BOUND ( 'NONE', #151764, .T. ) ;
#139096=DIRECTION ( 'NONE',  ( -1.000000000000000000, -3.265361837132813093E-16, 0.000000000000000000 ) ) ;
#139101=AXIS2_PLACEMENT_3D ( 'NONE', #55489, #120664, #77631 ) ;
#139104=VERTEX_POINT ( 'NONE', #174308 ) ;
#139143=AXIS2_PLACEMENT_3D ( 'NONE', #77735, #236819, #58167 ) ;
#139203=CARTESIAN_POINT ( 'NONE',  ( -21.05000000000000071, -1.162701749926853712, -75.00000000000004263 ) ) ;
#139219=DIRECTION ( 'NONE',  ( -3.440080580676165868E-14, -0.1298341882520124002, -0.9915357197604841577 ) ) ;
#139304=CARTESIAN_POINT ( 'NONE',  ( 23.14999999999999503, 11.65000000001116298, -93.58519422934611498 ) ) ;
#139359=CARTESIAN_POINT ( 'NONE',  ( 22.48508240969612615, 0.04627641452807085970, -55.34998926842647649 ) ) ;
#139361=EDGE_CURVE ( 'NONE', #250224, #91092, #230349, .T. ) ;
#139362=EDGE_CURVE ( 'NONE', #242093, #154034, #55528, .T. ) ;
#139385=CARTESIAN_POINT ( 'NONE',  ( 20.94999999999999929, -1.164121893230052995, -108.4148480855716485 ) ) ;
#139402=CARTESIAN_POINT ( 'NONE',  ( 21.17356465864818915, 0.09891124102502621418, -60.57719687375832507 ) ) ;
#139418=CARTESIAN_POINT ( 'NONE',  ( 20.94999999999999929, 11.65000000001115943, -93.71613433702195550 ) ) ;
#139422=EDGE_CURVE ( 'NONE', #95768, #197421, #109726, .T. ) ;
#139438=EDGE_CURVE ( 'NONE', #198825, #63545, #242825, .T. ) ;
#139471=CARTESIAN_POINT ( 'NONE',  ( -21.14999999999999858, 1.115600667400684642E-11, -60.45934304829880546 ) ) ;
#139472=CARTESIAN_POINT ( 'NONE',  ( -20.54999999999999716, -8.999999999988846255, -76.89396912265249284 ) ) ;
#139489=CIRCLE ( 'NONE', #256138, 0.1000000000000028644 ) ;
#139491=VECTOR ( 'NONE', #55847, 1000.000000000000000 ) ;
#139545=DIRECTION ( 'NONE',  ( 1.000000000000000000, 0.000000000000000000, 0.000000000000000000 ) ) ;
#139550=CIRCLE ( 'NONE', #60443, 0.1999999999999987899 ) ;
#139617=CIRCLE ( 'NONE', #118813, 12.97499999999999964 ) ;
#139641=ORIENTED_EDGE ( 'NONE', *, *, #14390, .F. ) ;
#139679=EDGE_CURVE ( 'NONE', #202894, #66864, #188852, .T. ) ;
#139716=CARTESIAN_POINT ( 'NONE',  ( -20.64999999999999858, 1.115600667400684642E-11, -67.00000000000004263 ) ) ;
#139731=VECTOR ( 'NONE', #10793, 1000.000000000000000 ) ;
#139770=VECTOR ( 'NONE', #93696, 1000.000000000000000 ) ;
#139809=CIRCLE ( 'NONE', #256264, 0.09999999999999939493 ) ;
#139857=AXIS2_PLACEMENT_3D ( 'NONE', #64539, #181928, #1984 ) ;
#139872=AXIS2_PLACEMENT_3D ( 'NONE', #8572, #166392, #167663 ) ;
#139875=DIRECTION ( 'NONE',  ( 0.000000000000000000, 0.000000000000000000, 1.000000000000000000 ) ) ;
#139899=DIRECTION ( 'NONE',  ( -1.000000000000000000, 0.000000000000000000, 0.000000000000000000 ) ) ;
#139916=EDGE_CURVE ( 'NONE', #156656, #161687, #27675, .T. ) ;
#139920=CARTESIAN_POINT ( 'NONE',  ( 21.05000000000000071, 5.850000000011105428, -77.13249722427802624 ) ) ;
#139937=ORIENTED_EDGE ( 'NONE', *, *, #231932, .F. ) ;
#139948=EDGE_CURVE ( 'NONE', #31603, #104861, #143230, .T. ) ;
#139979=AXIS2_PLACEMENT_3D ( 'NONE', #5254, #185209, #86072 ) ;
#139985=DIRECTION ( 'NONE',  ( 0.000000000000000000, 0.000000000000000000, -1.000000000000000000 ) ) ;
#139992=DIRECTION ( 'NONE',  ( 1.000000000000000000, 0.000000000000000000, 0.000000000000000000 ) ) ;
#140038=DIRECTION ( 'NONE',  ( 0.000000000000000000, -0.000000000000000000, -1.000000000000000000 ) ) ;
#140051=ADVANCED_FACE ( 'NONE', ( #14515 ), #212699, .F. ) ;
#140058=CARTESIAN_POINT ( 'NONE',  ( 21.04999999999999361, 6.344359042054570352, -66.98514436510659209 ) ) ;
#140077=EDGE_CURVE ( 'NONE', #196163, #77148, #230988, .T. ) ;
#140080=DIRECTION ( 'NONE',  ( 1.000000000000000000, 2.952720810173289112E-16, -0.000000000000000000 ) ) ;
#140094=DIRECTION ( 'NONE',  ( -0.000000000000000000, 0.1350103645451876666, 0.9908441862701600211 ) ) ;
#140114=ADVANCED_FACE ( 'NONE', ( #15803 ), #136997, .T. ) ;
#140127=EDGE_LOOP ( 'NONE', ( #117143, #74151, #8177, #26922 ) ) ;
#140141=CIRCLE ( 'NONE', #56918, 0.09999999999999939493 ) ;
#140151=CARTESIAN_POINT ( 'NONE',  ( -18.50000000000000000, 1.115600667400684642E-11, -67.00000000000004263 ) ) ;
#140156=CIRCLE ( 'NONE', #173562, 0.1000000000000028644 ) ;
#140161=DIRECTION ( 'NONE',  ( 0.000000000000000000, 0.000000000000000000, -1.000000000000000000 ) ) ;
#140214=EDGE_CURVE ( 'NONE', #50987, #53620, #1321, .T. ) ;
#140215=DIRECTION ( 'NONE',  ( 0.000000000000000000, 0.000000000000000000, 1.000000000000000000 ) ) ;
#140226=CIRCLE ( 'NONE', #211002, 11.74999999999999645 ) ;
#140230=ADVANCED_FACE ( 'NONE', ( #174901 ), #23512, .T. ) ;
#140231=FACE_OUTER_BOUND ( 'NONE', #239250, .T. ) ;
#140233=DIRECTION ( 'NONE',  ( 1.000000000000000000, 2.952720810173289112E-16, -0.000000000000000000 ) ) ;
#140234=ORIENTED_EDGE ( 'NONE', *, *, #245037, .F. ) ;
#140264=FACE_OUTER_BOUND ( 'NONE', #218026, .T. ) ;
#140275=ORIENTED_EDGE ( 'NONE', *, *, #178934, .F. ) ;
#140276=ADVANCED_FACE ( 'NONE', ( #41780 ), #63885, .T. ) ;
#140297=VERTEX_POINT ( 'NONE', #182568 ) ;
#140305=DIRECTION ( 'NONE',  ( 0.000000000000000000, 0.8700118002898321601, -0.4930308989875230585 ) ) ;
#140306=ORIENTED_EDGE ( 'NONE', *, *, #219565, .T. ) ;
#140308=ORIENTED_EDGE ( 'NONE', *, *, #188559, .F. ) ;
#140321=DIRECTION ( 'NONE',  ( 0.000000000000000000, 0.4999999999999949485, -0.8660254037844415942 ) ) ;
#140327=CARTESIAN_POINT ( 'NONE',  ( -18.50000000000000000, 9.150000000011157653, -88.15000000000004832 ) ) ;
#140329=ORIENTED_EDGE ( 'NONE', *, *, #74520, .T. ) ;
#140342=ADVANCED_FACE ( 'NONE', ( #116807 ), #170744, .F. ) ;
#140345=FILL_AREA_STYLE_COLOUR ( '', #177438 ) ;
#140349=VERTEX_POINT ( 'NONE', #190264 ) ;
#140352=CARTESIAN_POINT ( 'NONE',  ( -21.44999999999999929, 7.350000000011155166, -88.15000000000004832 ) ) ;
#140378=ORIENTED_EDGE ( 'NONE', *, *, #89995, .T. ) ;
#140398=CARTESIAN_POINT ( 'NONE',  ( -20.64999999999999858, 4.350000000011156054, -88.15000000000004832 ) ) ;
#140432=ORIENTED_EDGE ( 'NONE', *, *, #170940, .T. ) ;
#140449=EDGE_CURVE ( 'NONE', #131787, #221121, #114386, .T. ) ;
#140462=CARTESIAN_POINT ( 'NONE',  ( -22.44366136229477249, 0.009341569497225223756, -55.35028144252613203 ) ) ;
#140478=DIRECTION ( 'NONE',  ( -0.000000000000000000, -0.000000000000000000, -1.000000000000000000 ) ) ;
#140491=ORIENTED_EDGE ( 'NONE', *, *, #84, .T. ) ;
#140498=DIRECTION ( 'NONE',  ( 0.000000000000000000, 0.4930308989875230585, 0.8700118002898322711 ) ) ;
#140506=ORIENTED_EDGE ( 'NONE', *, *, #209698, .T. ) ;
#140521=EDGE_CURVE ( 'NONE', #9696, #152504, #235191, .T. ) ;
#140531=CARTESIAN_POINT ( 'NONE',  ( 21.05000000000000071, 6.257814610487280937, -66.90220970869124528 ) ) ;
#140577=EDGE_LOOP ( 'NONE', ( #9353, #169396, #9448, #59809 ) ) ;
#140628=ADVANCED_FACE ( 'NONE', ( #106203 ), #93531, .T. ) ;
#140632=CARTESIAN_POINT ( 'NONE',  ( -21.59780538579341425, 6.847090529954407145, -66.90102133040205956 ) ) ;
#140635=DIRECTION ( 'NONE',  ( -1.000000000000000000, -0.000000000000000000, -0.000000000000000000 ) ) ;
#140674=DIRECTION ( 'NONE',  ( 0.000000000000000000, 0.000000000000000000, -1.000000000000000000 ) ) ;
#140684=CARTESIAN_POINT ( 'NONE',  ( -22.48660254037843487, 11.75000000001115730, -66.95000000000007390 ) ) ;
#140699=DIRECTION ( 'NONE',  ( 0.000000000000000000, 0.000000000000000000, -1.000000000000000000 ) ) ;
#140722=CARTESIAN_POINT ( 'NONE',  ( -18.50000000000000000, 1.115600667400684642E-11, -100.5000000000000426 ) ) ;
#140759=VERTEX_POINT ( 'NONE', #252145 ) ;
#140775=DIRECTION ( 'NONE',  ( 0.000000000000000000, 4.336808689942043768E-15, -1.000000000000000000 ) ) ;
#140783=AXIS2_PLACEMENT_3D ( 'NONE', #29075, #109837, #251929 ) ;
#140790=AXIS2_PLACEMENT_3D ( 'NONE', #123593, #107872, #127441 ) ;
#140811=CARTESIAN_POINT ( 'NONE',  ( -18.59999999999999787, -1.851028230129704522, -78.65391326942254580 ) ) ;
#140877=FACE_OUTER_BOUND ( 'NONE', #22159, .T. ) ;
#140891=VERTEX_POINT ( 'NONE', #158232 ) ;
#140906=ORIENTED_EDGE ( 'NONE', *, *, #115343, .T. ) ;
#140921=VERTEX_POINT ( 'NONE', #235167 ) ;
#140930=CIRCLE ( 'NONE', #45234, 7.900000000000003908 ) ;
#140933=CARTESIAN_POINT ( 'NONE',  ( 18.59999999999999076, 10.20857864377385127, -88.25000000000005684 ) ) ;
#140957=ADVANCED_FACE ( 'NONE', ( #126767 ), #202460, .T. ) ;
#140987=CYLINDRICAL_SURFACE ( 'NONE', #194585, 0.1000000000000028644 ) ;
#140991=CIRCLE ( 'NONE', #149368, 0.2000000000000057288 ) ;
#141035=DIRECTION ( 'NONE',  ( 0.000000000000000000, 1.000000000000000000, 0.000000000000000000 ) ) ;
#141055=EDGE_LOOP ( 'NONE', ( #117183, #28588, #138547, #53318 ) ) ;
#141066=AXIS2_PLACEMENT_3D ( 'NONE', #21719, #24300, #244597 ) ;
#141107=CARTESIAN_POINT ( 'NONE',  ( -23.24999999999999645, -9.599999999988845900, -107.2001893912220964 ) ) ;
#141111=CARTESIAN_POINT ( 'NONE',  ( 20.84999999999998721, -11.74999999998884448, -100.5000000000000426 ) ) ;
#141146=LINE ( 'NONE', #65443, #27259 ) ;
#141156=AXIS2_PLACEMENT_3D ( 'NONE', #87746, #206425, #167329 ) ;
#141221=EDGE_CURVE ( 'NONE', #118463, #177719, #47851, .T. ) ;
#141244=ORIENTED_EDGE ( 'NONE', *, *, #131884, .T. ) ;
#141258=DIRECTION ( 'NONE',  ( 0.000000000000000000, 0.000000000000000000, -1.000000000000000000 ) ) ;
#141287=ORIENTED_EDGE ( 'NONE', *, *, #22705, .F. ) ;
#141294=ADVANCED_FACE ( 'NONE', ( #135746 ), #197001, .T. ) ;
#141309=FACE_OUTER_BOUND ( 'NONE', #188347, .T. ) ;
#141339=AXIS2_PLACEMENT_3D ( 'NONE', #163745, #146710, #84138 ) ;
#141351=DIRECTION ( 'NONE',  ( 0.000000000000000000, -1.000000000000000000, 0.000000000000000000 ) ) ;
#141355=CARTESIAN_POINT ( 'NONE',  ( 20.94999999999999929, 1.115600667400684642E-11, -100.5000000000000426 ) ) ;
#141428=EDGE_LOOP ( 'NONE', ( #46521, #160175, #138783, #201399 ) ) ;
#141430=CARTESIAN_POINT ( 'NONE',  ( 19.75857864376268935, 11.65000000001115943, -91.75000000000005684 ) ) ;
#141434=LINE ( 'NONE', #179309, #63259 ) ;
#141453=AXIS2_PLACEMENT_3D ( 'NONE', #172818, #209319, #72408 ) ;
#141459=ORIENTED_EDGE ( 'NONE', *, *, #170655, .F. ) ;
#141478=CARTESIAN_POINT ( 'NONE',  ( 22.60000000000000142, 0.1008583691098682150, -55.25043287651065782 ) ) ;
#141515=AXIS2_PLACEMENT_3D ( 'NONE', #100202, #140635, #179788 ) ;
#141540=CARTESIAN_POINT ( 'NONE',  ( -22.50000000000000000, 0.1000000000111554016, -67.00000000000004263 ) ) ;
#141591=VECTOR ( 'NONE', #49081, 1000.000000000000114 ) ;
#141615=EDGE_CURVE ( 'NONE', #71443, #181843, #57169, .T. ) ;
#141632=ADVANCED_FACE ( 'NONE', ( #174634 ), #16807, .F. ) ;
#141636=ORIENTED_EDGE ( 'NONE', *, *, #166526, .T. ) ;
#141670=LINE ( 'NONE', #185938, #74051 ) ;
#141703=ORIENTED_EDGE ( 'NONE', *, *, #230460, .T. ) ;
#141747=CARTESIAN_POINT ( 'NONE',  ( -22.41119224318417125, 1.115600667400684642E-11, -55.35042919245524473 ) ) ;
#141789=ORIENTED_EDGE ( 'NONE', *, *, #234558, .F. ) ;
#141810=ORIENTED_EDGE ( 'NONE', *, *, #237917, .T. ) ;
#141825=EDGE_LOOP ( 'NONE', ( #129689, #180942, #212632, #22255 ) ) ;
#141851=DIRECTION ( 'NONE',  ( -1.000000000000000000, 0.000000000000000000, 0.000000000000000000 ) ) ;
#141860=PLANE ( 'NONE',  #140790 ) ;
#141869=EDGE_CURVE ( 'NONE', #15594, #67110, #244806, .T. ) ;
#141871=ORIENTED_EDGE ( 'NONE', *, *, #156808, .F. ) ;
#141903=ORIENTED_EDGE ( 'NONE', *, *, #141221, .T. ) ;
#141905=ORIENTED_EDGE ( 'NONE', *, *, #245246, .T. ) ;
#141910=PLANE ( 'NONE',  #194917 ) ;
#141913=CARTESIAN_POINT ( 'NONE',  ( 21.13614978966381841, 1.115600836807273770E-11, -60.50089529816626310 ) ) ;
#141918=ORIENTED_EDGE ( 'NONE', *, *, #49790, .T. ) ;
#141940=CARTESIAN_POINT ( 'NONE',  ( 21.05000000000000071, 1.115600667400684642E-11, -62.70000000000001705 ) ) ;
#141945=ADVANCED_FACE ( 'NONE', ( #89581 ), #8778, .F. ) ;
#141954=DIRECTION ( 'NONE',  ( 0.000000000000000000, 0.9875055080513743810, -0.1575844902526802316 ) ) ;
#141963=CARTESIAN_POINT ( 'NONE',  ( -22.59999999999999787, 11.74956712350054566, -66.89914163090132604 ) ) ;
#141964=ORIENTED_EDGE ( 'NONE', *, *, #38589, .T. ) ;
#141968=CARTESIAN_POINT ( 'NONE',  ( 18.39999999999999858, -9.499999999988842703, -107.4146583429697159 ) ) ;
#141973=VERTEX_POINT ( 'NONE', #210828 ) ;
#141991=AXIS2_PLACEMENT_3D ( 'NONE', #160445, #139545, #118737 ) ;
#141996=ADVANCED_FACE ( 'NONE', ( #167879 ), #27503, .T. ) ;
#142022=DIRECTION ( 'NONE',  ( 0.000000000000000000, 0.000000000000000000, -1.000000000000000000 ) ) ;
#142036=CARTESIAN_POINT ( 'NONE',  ( 20.95262331984766035, 10.50415726280100870, -74.56088832959336798 ) ) ;
#142064=CARTESIAN_POINT ( 'NONE',  ( -21.65000000000000213, 7.708578643773852157, -88.25000000000005684 ) ) ;
#142072=DIRECTION ( 'NONE',  ( 0.000000000000000000, 0.000000000000000000, 1.000000000000000000 ) ) ;
#142102=DIRECTION ( 'NONE',  ( 0.000000000000000000, 0.000000000000000000, -1.000000000000000000 ) ) ;
#142108=CIRCLE ( 'NONE', #192197, 11.75000000000000000 ) ;
#142152=ORIENTED_EDGE ( 'NONE', *, *, #20603, .F. ) ;
#142219=ORIENTED_EDGE ( 'NONE', *, *, #45261, .T. ) ;
#142220=LINE ( 'NONE', #159243, #96878 ) ;
#142236=AXIS2_PLACEMENT_3D ( 'NONE', #200039, #42252, #137469 ) ;
#142246=EDGE_CURVE ( 'NONE', #208340, #205048, #169332, .T. ) ;
#142267=DIRECTION ( 'NONE',  ( 0.000000000000000000, 0.000000000000000000, 1.000000000000000000 ) ) ;
#142272=CARTESIAN_POINT ( 'NONE',  ( -20.94999999999999929, 10.29270135741298731, -105.9573618871519756 ) ) ;
#142302=ADVANCED_FACE ( 'NONE', ( #233629 ), #34170, .T. ) ;
#142334=DIRECTION ( 'NONE',  ( -1.000000000000000000, 0.000000000000000000, 0.000000000000000000 ) ) ;
#142345=DIRECTION ( 'NONE',  ( -0.000000000000000000, 1.000000000000000000, 0.000000000000000000 ) ) ;
#142354=CARTESIAN_POINT ( 'NONE',  ( 18.42636655943171320, -9.496944315759472843, -107.1090805711555731 ) ) ;
#142365=ORIENTED_EDGE ( 'NONE', *, *, #25309, .F. ) ;
#142408=CARTESIAN_POINT ( 'NONE',  ( 23.14999999999999858, 1.115600667400684642E-11, -100.5000000000000426 ) ) ;
#142420=EDGE_LOOP ( 'NONE', ( #94590, #158974, #69709, #90714 ) ) ;
#142422=ADVANCED_FACE ( 'NONE', ( #176234 ), #57525, .F. ) ;
#142448=VERTEX_POINT ( 'NONE', #223028 ) ;
#142457=DIRECTION ( 'NONE',  ( 0.000000000000000000, 0.000000000000000000, 1.000000000000000000 ) ) ;
#142483=VERTEX_POINT ( 'NONE', #105630 ) ;
#142491=EDGE_LOOP ( 'NONE', ( #137896, #15768, #251200, #96891 ) ) ;
#142510=VECTOR ( 'NONE', #25943, 1000.000000000000000 ) ;
#142573=VERTEX_POINT ( 'NONE', #46947 ) ;
#142589=ORIENTED_EDGE ( 'NONE', *, *, #59346, .F. ) ;
#142598=TOROIDAL_SURFACE ( 'NONE', #59186, 1.900000000000002576, 0.1000000000000000056 ) ;
#142615=EDGE_CURVE ( 'NONE', #183920, #224594, #65415, .T. ) ;
#142616=CARTESIAN_POINT ( 'NONE',  ( -18.59999999999999787, -1.835859311432481045, -112.0044391687985694 ) ) ;
#142658=ORIENTED_EDGE ( 'NONE', *, *, #48641, .F. ) ;
#142670=CARTESIAN_POINT ( 'NONE',  ( 20.94999999999999574, 1.261786168576181755, -75.08649896354552311 ) ) ;
#142674=ORIENTED_EDGE ( 'NONE', *, *, #146159, .F. ) ;
#142676=CARTESIAN_POINT ( 'NONE',  ( -18.59999999999999787, 1.835341550235567887, -78.55515129256302487 ) ) ;
#142688=DIRECTION ( 'NONE',  ( 0.000000000000000000, -0.1350103645451876666, 0.9908441862701600211 ) ) ;
#142703=CYLINDRICAL_SURFACE ( 'NONE', #113732, 0.1000000000000028644 ) ;
#142725=EDGE_CURVE ( 'NONE', #89054, #183644, #119603, .T. ) ;
#142737=FACE_OUTER_BOUND ( 'NONE', #80034, .T. ) ;
#142741=DIRECTION ( 'NONE',  ( 0.000000000000000000, 0.000000000000000000, -1.000000000000000000 ) ) ;
#142745=CARTESIAN_POINT ( 'NONE',  ( 23.14999999999999858, 1.115600667400684642E-11, -100.5000000000000426 ) ) ;
#142762=DIRECTION ( 'NONE',  ( 0.000000000000000000, 0.000000000000000000, -1.000000000000000000 ) ) ;
#142764=CARTESIAN_POINT ( 'NONE',  ( 20.94999999999999929, -8.999999999988842703, -91.10603087734760663 ) ) ;
#142783=EDGE_LOOP ( 'NONE', ( #119809, #125778, #57798, #44967 ) ) ;
#142814=CIRCLE ( 'NONE', #138545, 11.70000000000000284 ) ;
#142849=DIRECTION ( 'NONE',  ( 0.000000000000000000, 0.000000000000000000, -1.000000000000000000 ) ) ;
#142863=CARTESIAN_POINT ( 'NONE',  ( -22.42357213249529124, 0.09908696401271366305, -59.32706761364011072 ) ) ;
#142875=AXIS2_PLACEMENT_3D ( 'NONE', #101752, #138320, #178802 ) ;
#142890=CARTESIAN_POINT ( 'NONE',  ( 18.49999999999999289, 10.20857864377385127, -55.25000000000004974 ) ) ;
#142961=CARTESIAN_POINT ( 'NONE',  ( 21.14999999999999503, 1.115600667400684642E-11, -67.00000000000004263 ) ) ;
#142963=VECTOR ( 'NONE', #42017, 1000.000000000000000 ) ;
#142967=EDGE_LOOP ( 'NONE', ( #170809, #181099, #137341, #69615 ) ) ;
#142988=EDGE_LOOP ( 'NONE', ( #185003, #231605, #85124, #23978 ) ) ;
#143027=EDGE_LOOP ( 'NONE', ( #113771, #245434, #75508, #244546, #136376, #246645, #22489, #189036, #240110, #154946 ) ) ;
#143029=CARTESIAN_POINT ( 'NONE',  ( 18.59999999999999076, 1.115600667400684642E-11, -100.5000000000000426 ) ) ;
#143035=( BOUNDED_SURFACE ( )  B_SPLINE_SURFACE ( 3, 2, ( 
 ( #227451, #168823, #245749 ),
 ( #50100, #26718, #129646 ),
 ( #48820, #146618, #244448 ),
 ( #104906, #30571, #46246 ),
 ( #185771, #226139, #205310 ),
 ( #128373, #209178, #127079 ) ),
 .UNSPECIFIED., .F., .F., .F. ) 
 B_SPLINE_SURFACE_WITH_KNOTS ( ( 4, 2, 4 ),
 ( 3, 3 ),
 ( 0.0001300404313046710908, 0.0003183318589266794407, 0.0005066232865486877636 ),
 ( 0.000000000000000000, 1.000000000000000000 ),
 .UNSPECIFIED. ) 
 GEOMETRIC_REPRESENTATION_ITEM ( )  RATIONAL_B_SPLINE_SURFACE ( (
 ( 1.000000000000000000, 0.7071067811865475727, 1.000000000000000000),
 ( 1.000000000000000000, 0.7625113560541593172, 1.000000000000000000),
 ( 1.000000000000000000, 0.8126073484686597848, 1.000000000000000000),
 ( 1.000000000000000000, 0.8923049332734360739, 1.000000000000000000),
 ( 1.000000000000000000, 0.9231914937768189722, 1.000000000000000000),
 ( 1.000000000000000000, 0.9238795325112911794, 1.000000000000000000) ) ) 
 REPRESENTATION_ITEM ( '' )  SURFACE ( )  );
#143044=DIRECTION ( 'NONE',  ( 1.000000000000000000, 0.000000000000000000, 0.000000000000000000 ) ) ;
#143060=CARTESIAN_POINT ( 'NONE',  ( 18.49999999999999645, -1.362429037182155023, -108.3888812479212476 ) ) ;
#143116=CARTESIAN_POINT ( 'NONE',  ( 20.94999999999999929, 5.500000000011153745, -79.40526601891313874 ) ) ;
#143123=CARTESIAN_POINT ( 'NONE',  ( 18.49999999999999289, 11.75000000001115907, -55.25000000000004974 ) ) ;
#143149=DIRECTION ( 'NONE',  ( 1.000000000000000000, 0.000000000000000000, 0.000000000000000000 ) ) ;
#143150=EDGE_CURVE ( 'NONE', #115296, #51379, #73814, .T. ) ;
#143153=DIRECTION ( 'NONE',  ( -1.000000000000000000, -2.952720810173289112E-16, 0.000000000000000000 ) ) ;
#143158=AXIS2_PLACEMENT_3D ( 'NONE', #27405, #106890, #136718 ) ;
#143194=CARTESIAN_POINT ( 'NONE',  ( -22.47071067811865319, 7.720074744509219933, -66.90090754529744288 ) ) ;
#143206=ORIENTED_EDGE ( 'NONE', *, *, #197530, .T. ) ;
#143211=ORIENTED_EDGE ( 'NONE', *, *, #22075, .F. ) ;
#143218=DIRECTION ( 'NONE',  ( -1.000000000000000000, 0.000000000000000000, 0.000000000000000000 ) ) ;
#143230=CIRCLE ( 'NONE', #30832, 0.1000000000000028644 ) ;
#143244=TOROIDAL_SURFACE ( 'NONE', #184947, 7.800000000000000711, 0.1000000000000000056 ) ;
#143245=CARTESIAN_POINT ( 'NONE',  ( -22.50014994444013539, 11.74971973190329955, -66.91691984328113563 ) ) ;
#143247=ORIENTED_EDGE ( 'NONE', *, *, #107012, .F. ) ;
#143263=DIRECTION ( 'NONE',  ( 1.000000000000000000, 0.000000000000000000, 0.000000000000000000 ) ) ;
#143275=CIRCLE ( 'NONE', #84982, 0.09999999999999939493 ) ;
#143342=AXIS2_PLACEMENT_3D ( 'NONE', #60793, #156092, #97329 ) ;
#143354=VECTOR ( 'NONE', #153847, 1000.000000000000000 ) ;
#143372=CARTESIAN_POINT ( 'NONE',  ( -20.64999999999999858, 1.115600667400684642E-11, -87.62500000000005684 ) ) ;
#143381=VERTEX_POINT ( 'NONE', #223681 ) ;
#143386=CIRCLE ( 'NONE', #72674, 0.09999999999999939493 ) ;
#143398=EDGE_CURVE ( 'NONE', #223063, #98112, #203145, .T. ) ;
#143417=DIRECTION ( 'NONE',  ( 1.000000000000000000, -0.000000000000000000, -0.000000000000000000 ) ) ;
#143437=CIRCLE ( 'NONE', #114206, 0.1000000000000004496 ) ;
#143452=DIRECTION ( 'NONE',  ( 0.000000000000000000, 1.000000000000000000, 0.000000000000000000 ) ) ;
#143491=ORIENTED_EDGE ( 'NONE', *, *, #145528, .F. ) ;
#143499=CARTESIAN_POINT ( 'NONE',  ( -18.59999999999999787, 7.021664781911246322, -104.3335654018973315 ) ) ;
#143503=DIRECTION ( 'NONE',  ( 1.000000000000000000, -0.000000000000000000, -0.000000000000000000 ) ) ;
#143507=CARTESIAN_POINT ( 'NONE',  ( 18.59999999999999076, 10.49142135624846439, -91.85000000000003695 ) ) ;
#143517=CIRCLE ( 'NONE', #6127, 0.1000000000000008937 ) ;
#143552=CARTESIAN_POINT ( 'NONE',  ( 20.95000000000000284, 11.60000000001116227, -93.57179676972454274 ) ) ;
#143563=VECTOR ( 'NONE', #4223, 1000.000000000000000 ) ;
#143581=VERTEX_POINT ( 'NONE', #69096 ) ;
#143584=CARTESIAN_POINT ( 'NONE',  ( -21.07928932188134397, 0.09889514566555071551, -60.67148334360674511 ) ) ;
#143601=CARTESIAN_POINT ( 'NONE',  ( 21.05000000000000071, 10.42338541492406279, -74.49205192387015018 ) ) ;
#143608=DIRECTION ( 'NONE',  ( -1.000000000000000000, 0.000000000000000000, 0.000000000000000000 ) ) ;
#143617=CIRCLE ( 'NONE', #118701, 2.000000000000001776 ) ;
#143630=ADVANCED_FACE ( 'NONE', ( #7834 ), #99265, .T. ) ;
#143654=CARTESIAN_POINT ( 'NONE',  ( 18.50000000000000000, -9.499999999988842703, -107.1001893912220879 ) ) ;
#143658=DIRECTION ( 'NONE',  ( 1.000000000000000000, -0.000000000000000000, -0.000000000000000000 ) ) ;
#143665=EDGE_CURVE ( 'NONE', #113007, #113044, #194984, .T. ) ;
#143669=ORIENTED_EDGE ( 'NONE', *, *, #54750, .F. ) ;
#143703=VERTEX_POINT ( 'NONE', #96321 ) ;
#143717=CARTESIAN_POINT ( 'NONE',  ( 18.49999999999999289, 6.846123162363745074, -104.2377262668499043 ) ) ;
#143723=CARTESIAN_POINT ( 'NONE',  ( -20.94999999999999929, -1.849153571964891274, -112.1059666197971012 ) ) ;
#143795=VERTEX_POINT ( 'NONE', #170801 ) ;
#143797=ORIENTED_EDGE ( 'NONE', *, *, #125298, .T. ) ;
#143809=FACE_OUTER_BOUND ( 'NONE', #78344, .T. ) ;
#143841=EDGE_CURVE ( 'NONE', #197693, #29779, #107648, .T. ) ;
#143854=ADVANCED_FACE ( 'NONE', ( #21952 ), #102729, .T. ) ;
#143863=CARTESIAN_POINT ( 'NONE',  ( -20.54999999999999716, 2.000000000011154189, -80.22462192276213955 ) ) ;
#143914=CARTESIAN_POINT ( 'NONE',  ( -20.54999999999999716, 1.940186915899009490, -79.82911921105336717 ) ) ;
#143919=DIRECTION ( 'NONE',  ( -1.000000000000000000, 0.000000000000000000, 0.000000000000000000 ) ) ;
#143924=CARTESIAN_POINT ( 'NONE',  ( 21.05000000000000426, 6.496686585778579826, -67.01465611851199355 ) ) ;
#143956=DIRECTION ( 'NONE',  ( 1.000000000000000000, -0.000000000000000000, -0.000000000000000000 ) ) ;
#143962=VERTEX_POINT ( 'NONE', #204413 ) ;
#144052=EDGE_LOOP ( 'NONE', ( #22580, #105408, #191009, #106483 ) ) ;
#144072=EDGE_CURVE ( 'NONE', #197421, #8169, #86218, .T. ) ;
#144134=AXIS2_PLACEMENT_3D ( 'NONE', #74948, #154494, #213141 ) ;
#144166=DIRECTION ( 'NONE',  ( -0.000000000000000000, 0.000000000000000000, -1.000000000000000000 ) ) ;
#144195=DIRECTION ( 'NONE',  ( -0.000000000000000000, -1.265107689135680095E-16, 1.000000000000000000 ) ) ;
#144208=EDGE_CURVE ( 'NONE', #77369, #89853, #127950, .T. ) ;
#144224=CARTESIAN_POINT ( 'NONE',  ( 22.47071067811865319, 7.720074744509197728, -66.90090754529744288 ) ) ;
#144277=CARTESIAN_POINT ( 'NONE',  ( -22.47071067811865674, 7.720074744509219045, -66.90090754529744288 ) ) ;
#144321=ORIENTED_EDGE ( 'NONE', *, *, #29759, .F. ) ;
#144335=CARTESIAN_POINT ( 'NONE',  ( -20.94999999999999929, 11.75000000001115552, -74.01480577065404987 ) ) ;
#144350=ORIENTED_EDGE ( 'NONE', *, *, #227821, .T. ) ;
#144367=ORIENTED_EDGE ( 'NONE', *, *, #227229, .F. ) ;
#144386=ORIENTED_EDGE ( 'NONE', *, *, #44638, .F. ) ;
#144398=AXIS2_PLACEMENT_3D ( 'NONE', #196533, #97403, #111886 ) ;
#144399=DIRECTION ( 'NONE',  ( 0.000000000000000000, -1.000000000000000000, -0.000000000000000000 ) ) ;
#144436=CIRCLE ( 'NONE', #69654, 0.2000000000000057288 ) ;
#144450=VERTEX_POINT ( 'NONE', #33231 ) ;
#144466=CARTESIAN_POINT ( 'NONE',  ( -23.25000000000000000, -11.64999999998884483, -67.00000000000004263 ) ) ;
#144484=CYLINDRICAL_SURFACE ( 'NONE', #60932, 7.900000000000003908 ) ;
#144489=DIRECTION ( 'NONE',  ( 0.000000000000000000, -1.000000000000000000, 0.000000000000000000 ) ) ;
#144499=EDGE_CURVE ( 'NONE', #39976, #249989, #94796, .T. ) ;
#144504=VERTEX_POINT ( 'NONE', #237811 ) ;
#144510=CARTESIAN_POINT ( 'NONE',  ( -23.25000000000000000, -8.999999999988846255, -76.89396912265249284 ) ) ;
#144522=EDGE_CURVE ( 'NONE', #248210, #223063, #98855, .T. ) ;
#144543=PLANE ( 'NONE',  #248720 ) ;
#144559=ADVANCED_FACE ( 'NONE', ( #78711 ), #116581, .T. ) ;
#144605=CARTESIAN_POINT ( 'NONE',  ( -23.15000000000000213, -11.48912529306489994, -97.50000000000004263 ) ) ;
#144609=ORIENTED_EDGE ( 'NONE', *, *, #63141, .T. ) ;
#144616=AXIS2_PLACEMENT_3D ( 'NONE', #186181, #49224, #208325 ) ;
#144636=VERTEX_POINT ( 'NONE', #39642 ) ;
#144657=CARTESIAN_POINT ( 'NONE',  ( 18.59999999999999076, 7.070967871809997973, -104.2465642218683541 ) ) ;
#144663=LINE ( 'NONE', #224205, #74537 ) ;
#144665=EDGE_CURVE ( 'NONE', #143795, #56745, #44924, .T. ) ;
#144670=VERTEX_POINT ( 'NONE', #126849 ) ;
#144706=DIRECTION ( 'NONE',  ( -4.408576920032448588E-17, 0.1350103645451876944, 0.9908441862701601321 ) ) ;
#144732=ORIENTED_EDGE ( 'NONE', *, *, #155352, .F. ) ;
#144734=ORIENTED_EDGE ( 'NONE', *, *, #49109, .T. ) ;
#144740=EDGE_LOOP ( 'NONE', ( #151617, #30836, #160798, #188276 ) ) ;
#144741=CARTESIAN_POINT ( 'NONE',  ( -18.41817142474039670, -9.498703066590936217, -107.1039654876371969 ) ) ;
#144753=DIRECTION ( 'NONE',  ( -1.000000000000000000, -2.952720810173289112E-16, 0.000000000000000000 ) ) ;
#144756=CARTESIAN_POINT ( 'NONE',  ( 20.94999999999999574, -11.64999999998883595, -69.90000000000004832 ) ) ;
#144792=EDGE_CURVE ( 'NONE', #245368, #93742, #7490, .T. ) ;
#144811=ADVANCED_FACE ( 'NONE', ( #92848 ), #49186, .T. ) ;
#144832=DIRECTION ( 'NONE',  ( 0.000000000000000000, 1.810617628050740656E-13, 1.000000000000000000 ) ) ;
#144838=AXIS2_PLACEMENT_3D ( 'NONE', #129809, #89395, #170277 ) ;
#144844=DIRECTION ( 'NONE',  ( 1.000000000000000000, -0.000000000000000000, 0.000000000000000000 ) ) ;
#144853=CYLINDRICAL_SURFACE ( 'NONE', #162519, 11.80000000000000426 ) ;
#144886=FACE_OUTER_BOUND ( 'NONE', #48484, .T. ) ;
#144891=DIRECTION ( 'NONE',  ( 1.000000000000000000, -0.000000000000000000, -0.000000000000000000 ) ) ;
#144893=FACE_OUTER_BOUND ( 'NONE', #159262, .T. ) ;
#144920=EDGE_LOOP ( 'NONE', ( #169004, #226643, #195126, #206040 ) ) ;
#144950=ADVANCED_FACE ( 'NONE', ( #35490 ), #117557, .F. ) ;
#144958=DIRECTION ( 'NONE',  ( 0.000000000000000000, 0.000000000000000000, -1.000000000000000000 ) ) ;
#144962=DIRECTION ( 'NONE',  ( 0.000000000000000000, 0.000000000000000000, -1.000000000000000000 ) ) ;
#145047=CARTESIAN_POINT ( 'NONE',  ( -18.39999999999999858, -9.399999999988850163, -55.25000000000004974 ) ) ;
#145056=AXIS2_PLACEMENT_3D ( 'NONE', #180185, #122783, #161912 ) ;
#145059=EDGE_LOOP ( 'NONE', ( #178420, #180248, #151165, #111023 ) ) ;
#145061=AXIS2_PLACEMENT_3D ( 'NONE', #22080, #40386, #235963 ) ;
#145114=DIRECTION ( 'NONE',  ( 0.000000000000000000, 0.4930308989875313852, 0.8700118002898274971 ) ) ;
#145140=CARTESIAN_POINT ( 'NONE',  ( 23.25000000000000000, -11.64999999998883595, -97.40000000000004832 ) ) ;
#145154=CARTESIAN_POINT ( 'NONE',  ( -21.44999999999999929, 7.250000000011155521, -79.35000000000005116 ) ) ;
#145171=VECTOR ( 'NONE', #124134, 1000.000000000000000 ) ;
#145173=LINE ( 'NONE', #6959, #12639 ) ;
#145196=ORIENTED_EDGE ( 'NONE', *, *, #150887, .F. ) ;
#145203=CARTESIAN_POINT ( 'NONE',  ( 21.05000000000000071, 6.441084688482579423, -67.01771943330844294 ) ) ;
#145225=CARTESIAN_POINT ( 'NONE',  ( -21.05000000000000071, 5.850000000011105428, -77.13249722427802624 ) ) ;
#145258=DIRECTION ( 'NONE',  ( 0.000000000000000000, 1.000000000000000000, 0.000000000000000000 ) ) ;
#145274=ORIENTED_EDGE ( 'NONE', *, *, #242915, .F. ) ;
#145293=EDGE_LOOP ( 'NONE', ( #149916, #55867, #226041, #180967 ) ) ;
#145340=EDGE_CURVE ( 'NONE', #154967, #49762, #66125, .T. ) ;
#145343=DIRECTION ( 'NONE',  ( -1.000000000000000000, 0.000000000000000000, 0.000000000000000000 ) ) ;
#145381=CARTESIAN_POINT ( 'NONE',  ( -20.54999999999999716, 2.000000000011154189, -87.27537807723794572 ) ) ;
#145391=ORIENTED_EDGE ( 'NONE', *, *, #113583, .T. ) ;
#145407=CARTESIAN_POINT ( 'NONE',  ( 20.94999999999999929, 5.850000000011105428, -77.13249722427802624 ) ) ;
#145411=DIRECTION ( 'NONE',  ( 1.000000000000000000, 0.000000000000000000, -0.000000000000000000 ) ) ;
#145444=ORIENTED_EDGE ( 'NONE', *, *, #54497, .F. ) ;
#145455=ADVANCED_FACE ( 'NONE', ( #148048 ), #156052, .T. ) ;
#145506=CARTESIAN_POINT ( 'NONE',  ( 20.95576188350343116, 10.60898054497455512, -74.61123372275433496 ) ) ;
#145517=CARTESIAN_POINT ( 'NONE',  ( 22.39999999999999858, 7.790779598384538041, -67.00000000000004263 ) ) ;
#145526=CARTESIAN_POINT ( 'NONE',  ( -20.94999999999999929, 11.70000000001115126, -93.74500185048142953 ) ) ;
#145528=EDGE_CURVE ( 'NONE', #40125, #120362, #116218, .T. ) ;
#145579=DIRECTION ( 'NONE',  ( -3.265361837132813093E-16, 1.000000000000000000, 0.000000000000000000 ) ) ;
#145588=AXIS2_PLACEMENT_3D ( 'NONE', #98009, #180161, #198421 ) ;
#145625=ORIENTED_EDGE ( 'NONE', *, *, #7311, .T. ) ;
#145626=VERTEX_POINT ( 'NONE', #71091 ) ;
#145662=EDGE_CURVE ( 'NONE', #174189, #68442, #119194, .T. ) ;
#145666=DIRECTION ( 'NONE',  ( 0.000000000000000000, 0.5000000000000078826, -0.8660254037844340447 ) ) ;
#145673=ORIENTED_EDGE ( 'NONE', *, *, #199509, .T. ) ;
#145689=DIRECTION ( 'NONE',  ( 0.000000000000000000, 0.000000000000000000, 1.000000000000000000 ) ) ;
#145694=ORIENTED_EDGE ( 'NONE', *, *, #239559, .T. ) ;
#145701=CARTESIAN_POINT ( 'NONE',  ( 21.05000000000000071, -11.64999999998883595, -67.00000000000004263 ) ) ;
#145710=AXIS2_PLACEMENT_3D ( 'NONE', #136184, #77500, #18835 ) ;
#145725=VECTOR ( 'NONE', #184313, 1000.000000000000227 ) ;
#145754=DIRECTION ( 'NONE',  ( 1.000000000000000000, 0.000000000000000000, 0.000000000000000000 ) ) ;
#145762=ORIENTED_EDGE ( 'NONE', *, *, #24055, .F. ) ;
#145769=AXIS2_PLACEMENT_3D ( 'NONE', #9209, #148737, #170910 ) ;
#145809=DIRECTION ( 'NONE',  ( -0.000000000000000000, 0.1350103645451626311, 0.9908441862701635738 ) ) ;
#145816=AXIS2_PLACEMENT_3D ( 'NONE', #46647, #148337, #49230 ) ;
#145837=CIRCLE ( 'NONE', #220685, 12.87499999999999822 ) ;
#145854=EDGE_CURVE ( 'NONE', #58814, #106717, #191240, .T. ) ;
#145861=CARTESIAN_POINT ( 'NONE',  ( -23.25000000000000000, -1.149570369564537842, -108.3159124845020074 ) ) ;
#145869=CYLINDRICAL_SURFACE ( 'NONE', #88882, 0.09999999999999939493 ) ;
#145880=EDGE_CURVE ( 'NONE', #24943, #236296, #4359, .T. ) ;
#145881=CARTESIAN_POINT ( 'NONE',  ( 21.05000000000000071, 10.72371710471868056, -74.66491356908764487 ) ) ;
#145896=ORIENTED_EDGE ( 'NONE', *, *, #149060, .T. ) ;
#145908=AXIS2_PLACEMENT_3D ( 'NONE', #69548, #192066, #13418 ) ;
#145927=DIRECTION ( 'NONE',  ( -1.000000000000000000, 0.000000000000000000, 0.000000000000000000 ) ) ;
#145929=TOROIDAL_SURFACE ( 'NONE', #200113, 0.2000000000000000111, 0.1000000000000000056 ) ;
#145989=AXIS2_PLACEMENT_3D ( 'NONE', #30971, #110466, #190014 ) ;
#145991=EDGE_CURVE ( 'NONE', #26378, #131057, #78929, .T. ) ;
#146009=ORIENTED_EDGE ( 'NONE', *, *, #177127, .T. ) ;
#146018=ORIENTED_EDGE ( 'NONE', *, *, #183317, .T. ) ;
#146079=AXIS2_PLACEMENT_3D ( 'NONE', #238276, #59616, #253990 ) ;
#146092=DIRECTION ( 'NONE',  ( 0.000000000000000000, 0.2605042016806672911, -0.9654727137038716656 ) ) ;
#146099=LINE ( 'NONE', #69163, #198645 ) ;
#146113=ORIENTED_EDGE ( 'NONE', *, *, #100078, .T. ) ;
#146123=ORIENTED_EDGE ( 'NONE', *, *, #140077, .F. ) ;
#146127=DIRECTION ( 'NONE',  ( 1.000000000000000000, -0.000000000000000000, -0.000000000000000000 ) ) ;
#146142=LINE ( 'NONE', #6632, #237525 ) ;
#146159=EDGE_CURVE ( 'NONE', #96642, #33467, #199796, .T. ) ;
#146200=DIRECTION ( 'NONE',  ( 0.000000000000000000, 0.000000000000000000, -1.000000000000000000 ) ) ;
#146216=DIRECTION ( 'NONE',  ( -1.000000000000000000, 0.000000000000000000, 0.000000000000000000 ) ) ;
#146228=DIRECTION ( 'NONE',  ( 0.000000000000000000, -1.000000000000000000, 0.000000000000000000 ) ) ;
#146254=AXIS2_PLACEMENT_3D ( 'NONE', #96445, #234701, #153933 ) ;
#146256=EDGE_CURVE ( 'NONE', #113968, #164187, #245572, .T. ) ;
#146279=CIRCLE ( 'NONE', #21413, 4.000000000000003553 ) ;
#146288=ORIENTED_EDGE ( 'NONE', *, *, #35833, .T. ) ;
#146314=ORIENTED_EDGE ( 'NONE', *, *, #251890, .T. ) ;
#146323=ORIENTED_EDGE ( 'NONE', *, *, #76682, .T. ) ;
#146342=TOROIDAL_SURFACE ( 'NONE', #200524, 12.97499999999999609, 0.1000000000000000056 ) ;
#146344=DIRECTION ( 'NONE',  ( -1.000000000000000000, 0.000000000000000000, 0.000000000000000000 ) ) ;
#146353=FACE_OUTER_BOUND ( 'NONE', #225847, .T. ) ;
#146358=ORIENTED_EDGE ( 'NONE', *, *, #137973, .T. ) ;
#146366=EDGE_LOOP ( 'NONE', ( #163273, #167265, #60091, #61242 ) ) ;
#146368=CIRCLE ( 'NONE', #154796, 0.09999999999999892308 ) ;
#146372=ORIENTED_EDGE ( 'NONE', *, *, #224227, .T. ) ;
#146386=CARTESIAN_POINT ( 'NONE',  ( -21.05000000000000426, -0.02103547652895406198, -60.69554417805237989 ) ) ;
#146388=DIRECTION ( 'NONE',  ( -1.000000000000000000, 0.000000000000000000, 0.000000000000000000 ) ) ;
#146413=EDGE_CURVE ( 'NONE', #80704, #149698, #249839, .T. ) ;
#146415=AXIS2_PLACEMENT_3D ( 'NONE', #213531, #75352, #221225 ) ;
#146445=VERTEX_POINT ( 'NONE', #208718 ) ;
#146454=VECTOR ( 'NONE', #103874, 1000.000000000000000 ) ;
#146501=CARTESIAN_POINT ( 'NONE',  ( -21.05000000000000071, -11.48912529306490349, -70.00000000000004263 ) ) ;
#146511=CARTESIAN_POINT ( 'NONE',  ( 22.59999985501178799, 11.74986979301414181, -66.93440133020047256 ) ) ;
#146515=CARTESIAN_POINT ( 'NONE',  ( -18.50000000000000000, 9.350000000011156942, -88.15000000000004832 ) ) ;
#146537=CARTESIAN_POINT ( 'NONE',  ( 20.91682497891422798, 10.32263460347359363, -106.0605957968672328 ) ) ;
#146543=CARTESIAN_POINT ( 'NONE',  ( 20.85000000000000142, 1.115600667400684642E-11, -100.5000000000000426 ) ) ;
#146566=ORIENTED_EDGE ( 'NONE', *, *, #171350, .T. ) ;
#146591=ORIENTED_EDGE ( 'NONE', *, *, #165346, .F. ) ;
#146618=CARTESIAN_POINT ( 'NONE',  ( -21.04999999999999716, 6.440770893673031239, -67.01759718700851920 ) ) ;
#146661=FACE_OUTER_BOUND ( 'NONE', #120828, .T. ) ;
#146710=DIRECTION ( 'NONE',  ( 0.000000000000000000, -0.000000000000000000, 1.000000000000000000 ) ) ;
#146728=CARTESIAN_POINT ( 'NONE',  ( 18.56308993302899069, 10.38069115533549969, -91.73922263893888385 ) ) ;
#146730=CARTESIAN_POINT ( 'NONE',  ( 18.49999999999998934, 6.650000000011155876, -79.35000000000005116 ) ) ;
#146746=ORIENTED_EDGE ( 'NONE', *, *, #135063, .T. ) ;
#146762=CARTESIAN_POINT ( 'NONE',  ( 20.50589344625181809, 10.48318793148705019, -74.57299497867310833 ) ) ;
#146806=AXIS2_PLACEMENT_3D ( 'NONE', #205005, #30265, #168524 ) ;
#146842=AXIS2_PLACEMENT_3D ( 'NONE', #151380, #129231, #230917 ) ;
#146850=DIRECTION ( 'NONE',  ( 0.000000000000000000, 0.1350103645451904977, 0.9908441862701596881 ) ) ;
#146857=EDGE_CURVE ( 'NONE', #223804, #13993, #50095, .T. ) ;
#146886=CYLINDRICAL_SURFACE ( 'NONE', #58601, 0.09999999999999939493 ) ;
#146892=DIRECTION ( 'NONE',  ( 0.000000000000000000, 0.000000000000000000, -1.000000000000000000 ) ) ;
#146919=DIRECTION ( 'NONE',  ( -1.000000000000000000, 7.304098846218135653E-16, 0.000000000000000000 ) ) ;
#146950=AXIS2_PLACEMENT_3D ( 'NONE', #71327, #110425, #111717 ) ;
#146986=AXIS2_PLACEMENT_3D ( 'NONE', #169999, #69583, #107399 ) ;
#146995=VERTEX_POINT ( 'NONE', #121977 ) ;
#147012=ORIENTED_EDGE ( 'NONE', *, *, #13614, .T. ) ;
#147035=EDGE_CURVE ( 'NONE', #201510, #138550, #187688, .T. ) ;
#147042=DIRECTION ( 'NONE',  ( 0.000000000000000000, 0.000000000000000000, -1.000000000000000000 ) ) ;
#147048=ADVANCED_FACE ( 'NONE', ( #173994 ), #191971, .F. ) ;
#147057=VERTEX_POINT ( 'NONE', #249640 ) ;
#147062=ORIENTED_EDGE ( 'NONE', *, *, #88382, .T. ) ;
#147063=FACE_OUTER_BOUND ( 'NONE', #50546, .T. ) ;
#147069=AXIS2_PLACEMENT_3D ( 'NONE', #22458, #117681, #137242 ) ;
#147081=FACE_OUTER_BOUND ( 'NONE', #244164, .T. ) ;
#147115=ORIENTED_EDGE ( 'NONE', *, *, #162849, .T. ) ;
#147118=CIRCLE ( 'NONE', #163696, 12.87499999999999822 ) ;
#147132=ORIENTED_EDGE ( 'NONE', *, *, #33415, .F. ) ;
#147144=EDGE_CURVE ( 'NONE', #23243, #83831, #33773, .T. ) ;
#147179=DIRECTION ( 'NONE',  ( 0.000000000000000000, 0.000000000000000000, -1.000000000000000000 ) ) ;
#147195=FACE_OUTER_BOUND ( 'NONE', #142783, .T. ) ;
#147196=DIRECTION ( 'NONE',  ( -1.000000000000000000, -3.265361837132813093E-16, 0.000000000000000000 ) ) ;
#147198=VECTOR ( 'NONE', #181525, 1000.000000000000000 ) ;
#147223=CARTESIAN_POINT ( 'NONE',  ( 20.94999999999999929, 4.813084112160684214, -88.55848224347622022 ) ) ;
#147229=SPHERICAL_SURFACE ( 'NONE', #14454, 0.1000000000000000056 ) ;
#147292=CIRCLE ( 'NONE', #34905, 0.09999999999999939493 ) ;
#147325=FACE_OUTER_BOUND ( 'NONE', #75544, .T. ) ;
#147327=CYLINDRICAL_SURFACE ( 'NONE', #35766, 0.09999999999999939493 ) ;
#147343=VERTEX_POINT ( 'NONE', #162997 ) ;
#147451=AXIS2_PLACEMENT_3D ( 'NONE', #36645, #217789, #15797 ) ;
#147531=CIRCLE ( 'NONE', #1761, 4.049999999999998046 ) ;
#147555=DIRECTION ( 'NONE',  ( 1.000000000000000000, 0.000000000000000000, 0.000000000000000000 ) ) ;
#147562=ORIENTED_EDGE ( 'NONE', *, *, #57969, .T. ) ;
#147585=ORIENTED_EDGE ( 'NONE', *, *, #162865, .F. ) ;
#147617=EDGE_CURVE ( 'NONE', #134077, #189474, #18998, .T. ) ;
#147641=AXIS2_PLACEMENT_3D ( 'NONE', #93380, #193778, #94666 ) ;
#147662=EDGE_LOOP ( 'NONE', ( #75156, #108883, #54901, #195112 ) ) ;
#147681=CARTESIAN_POINT ( 'NONE',  ( 21.14999999999999858, 1.115600667400684642E-11, -79.15000000000004832 ) ) ;
#147728=DIRECTION ( 'NONE',  ( 0.000000000000000000, 0.000000000000000000, -1.000000000000000000 ) ) ;
#147745=CARTESIAN_POINT ( 'NONE',  ( -21.55000000000000426, 7.750000000011159074, -88.15000000000004832 ) ) ;
#147754=ORIENTED_EDGE ( 'NONE', *, *, #210822, .F. ) ;
#147770=VECTOR ( 'NONE', #174376, 1000.000000000000000 ) ;
#147771=EDGE_CURVE ( 'NONE', #96642, #12745, #210727, .T. ) ;
#147789=DIRECTION ( 'NONE',  ( -1.000000000000000000, -0.000000000000000000, 0.000000000000000000 ) ) ;
#147798=DIRECTION ( 'NONE',  ( 1.000000000000000000, 0.000000000000000000, 0.000000000000000000 ) ) ;
#147803=ORIENTED_EDGE ( 'NONE', *, *, #16228, .T. ) ;
#147834=DIRECTION ( 'NONE',  ( 0.000000000000000000, 0.000000000000000000, 1.000000000000000000 ) ) ;
#147840=ORIENTED_EDGE ( 'NONE', *, *, #8817, .T. ) ;
#147859=ORIENTED_EDGE ( 'NONE', *, *, #195585, .F. ) ;
#147865=ORIENTED_EDGE ( 'NONE', *, *, #33963, .T. ) ;
#147911=CARTESIAN_POINT ( 'NONE',  ( 21.05000000000000071, 6.540656951712400691, -67.10000000000005116 ) ) ;
#147966=CARTESIAN_POINT ( 'NONE',  ( 18.58222699835054570, 10.33200063080772324, -106.0931674956643320 ) ) ;
#147972=DIRECTION ( 'NONE',  ( -1.000000000000000000, 0.000000000000000000, 0.000000000000000000 ) ) ;
#147982=CARTESIAN_POINT ( 'NONE',  ( -20.94999999999999929, -1.835341550213255957, -78.55515129256303908 ) ) ;
#147990=EDGE_CURVE ( 'NONE', #172095, #134186, #164937, .T. ) ;
#147991=DIRECTION ( 'NONE',  ( 0.000000000000000000, -2.428612866367527723E-14, -1.000000000000000000 ) ) ;
#147996=CARTESIAN_POINT ( 'NONE',  ( 21.05000000000000071, -9.399999999988844834, -90.60603087734760663 ) ) ;
#148005=DIRECTION ( 'NONE',  ( 1.000000000000000000, 0.000000000000000000, 0.000000000000000000 ) ) ;
#148029=DIRECTION ( 'NONE',  ( 1.000000000000000000, 0.000000000000000000, -0.000000000000000000 ) ) ;
#148041=CARTESIAN_POINT ( 'NONE',  ( -20.54999999999999716, 1.115624548013267999E-11, -98.60000000000005116 ) ) ;
#148048=FACE_OUTER_BOUND ( 'NONE', #9685, .T. ) ;
#148051=LINE ( 'NONE', #163766, #226548 ) ;
#148060=EDGE_LOOP ( 'NONE', ( #58314, #34444, #68737, #219441 ) ) ;
#148083=CARTESIAN_POINT ( 'NONE',  ( 20.52683494730037239, 8.980530818312608687, -75.50525272253725007 ) ) ;
#148117=CARTESIAN_POINT ( 'NONE',  ( -23.15000000000000213, -9.599999999988845900, -90.60603087734760663 ) ) ;
#148128=DIRECTION ( 'NONE',  ( 2.557131231893036985E-16, -0.8660254037844383745, 0.5000000000000003331 ) ) ;
#148145=EDGE_LOOP ( 'NONE', ( #14191, #20417, #32186, #158508 ) ) ;
#148155=DIRECTION ( 'NONE',  ( -0.000000000000000000, -0.000000000000000000, -1.000000000000000000 ) ) ;
#148189=CARTESIAN_POINT ( 'NONE',  ( -20.94999999999999929, 1.115600667400684642E-11, -100.5000000000000426 ) ) ;
#148202=DIRECTION ( 'NONE',  ( 1.000000000000000000, 0.000000000000000000, 0.000000000000000000 ) ) ;
#148205=ORIENTED_EDGE ( 'NONE', *, *, #19230, .F. ) ;
#148250=ADVANCED_FACE ( 'NONE', ( #248312 ), #143035, .T. ) ;
#148267=EDGE_CURVE ( 'NONE', #47237, #9696, #36148, .T. ) ;
#148308=LINE ( 'NONE', #109159, #10811 ) ;
#148319=ORIENTED_EDGE ( 'NONE', *, *, #15201, .T. ) ;
#148334=DIRECTION ( 'NONE',  ( 0.000000000000000000, -0.4930308989875248349, -0.8700118002898312719 ) ) ;
#148336=CARTESIAN_POINT ( 'NONE',  ( 21.05000000000000071, 8.776282895303632259, -75.48800072158441310 ) ) ;
#148337=DIRECTION ( 'NONE',  ( 0.000000000000000000, -0.8660254037844247188, 0.5000000000000245359 ) ) ;
#148342=ORIENTED_EDGE ( 'NONE', *, *, #58039, .F. ) ;
#148373=CARTESIAN_POINT ( 'NONE',  ( 23.15000000000000213, -11.48912529306489994, -97.50000000000004263 ) ) ;
#148374=ORIENTED_EDGE ( 'NONE', *, *, #27564, .F. ) ;
#148405=EDGE_CURVE ( 'NONE', #181843, #240894, #148572, .T. ) ;
#148411=ORIENTED_EDGE ( 'NONE', *, *, #129883, .T. ) ;
#148459=CARTESIAN_POINT ( 'NONE',  ( 18.49999999999999289, 10.49142135624846439, -91.85000000000003695 ) ) ;
#148472=CARTESIAN_POINT ( 'NONE',  ( -20.64999999999999858, -8.999999999988846255, -76.89396912265249284 ) ) ;
#148484=CIRCLE ( 'NONE', #36058, 0.1000000000000028644 ) ;
#148489=CARTESIAN_POINT ( 'NONE',  ( -20.99780126800925117, 11.60538868788787070, -93.58735257170555144 ) ) ;
#148500=EDGE_CURVE ( 'NONE', #201510, #71510, #103338, .T. ) ;
#148507=CARTESIAN_POINT ( 'NONE',  ( -23.15000000000000213, -11.64999999998884483, -67.00000000000004263 ) ) ;
#148514=B_SPLINE_CURVE_WITH_KNOTS ( 'NONE', 3,
 ( #48669, #89076, #70840, #130778, #205162, #30414, #225992, #47374 ),
 .UNSPECIFIED., .F., .F.,
 ( 4, 2, 2, 4 ),
 ( 0.000000000000000000, 0.0001881495939909140220, 0.0002822243909863799641, 0.0003762991879818459334 ),
 .UNSPECIFIED. ) ;
#148519=CARTESIAN_POINT ( 'NONE',  ( -22.00411653889206676, 0.09903810579716695872, -59.74655713235966914 ) ) ;
#148531=DIRECTION ( 'NONE',  ( 0.7071067811865474617, 0.7071067811865474617, -0.000000000000000000 ) ) ;
#148564=CARTESIAN_POINT ( 'NONE',  ( -20.94999999999999929, -1.835341550213257733, -78.55515129256303908 ) ) ;
#148571=DIRECTION ( 'NONE',  ( 0.000000000000000000, 0.8660254037844411501, 0.4999999999999956701 ) ) ;
#148572=CIRCLE ( 'NONE', #48593, 0.5000000000000004441 ) ;
#148578=DIRECTION ( 'NONE',  ( 0.000000000000000000, -0.9915357197604853789, 0.1298341882520022694 ) ) ;
#148631=CARTESIAN_POINT ( 'NONE',  ( -18.49999999999998579, -9.480686695267827702, -107.4411151687578752 ) ) ;
#148641=DIRECTION ( 'NONE',  ( -2.602085213965226419E-14, -0.000000000000000000, -1.000000000000000000 ) ) ;
#148665=FACE_OUTER_BOUND ( 'NONE', #129354, .T. ) ;
#148672=DIRECTION ( 'NONE',  ( 1.000000000000000000, -7.304098846218134667E-16, -4.217023435051625732E-16 ) ) ;
#148729=LINE ( 'NONE', #250381, #19314 ) ;
#148737=DIRECTION ( 'NONE',  ( 1.000000000000000000, -0.000000000000000000, 0.000000000000000000 ) ) ;
#148785=DIRECTION ( 'NONE',  ( 1.000000000000000000, 0.000000000000000000, 0.000000000000000000 ) ) ;
#148810=EDGE_CURVE ( 'NONE', #114130, #10085, #191286, .T. ) ;
#148822=ORIENTED_EDGE ( 'NONE', *, *, #25365, .T. ) ;
#148853=ADVANCED_FACE ( 'NONE', ( #15199 ), #153462, .F. ) ;
#148857=CARTESIAN_POINT ( 'NONE',  ( 21.05000000000000071, 1.115600667400684642E-11, -79.15000000000004832 ) ) ;
#148866=B_SPLINE_CURVE_WITH_KNOTS ( 'NONE', 3,
 ( #41184, #120722, #240639, #200234, #62017, #211800, #248347, #67141, #110117, #187113, #71021, #206653, #129681, #86671, #91843, #226174, #147966, #28046, #9727 ),
 .UNSPECIFIED., .F., .F.,
 ( 4, 3, 3, 3, 3, 3, 4 ),
 ( -2.000416914650301595E-06, 0.000000000000000000, 4.714008503747321038E-05, 9.979203887779781405E-05, 0.0001372215519229620922, 0.0001635031576221085176, 0.0001900083748504240578 ),
 .UNSPECIFIED. ) ;
#148876=FACE_OUTER_BOUND ( 'NONE', #201965, .T. ) ;
#148895=DIRECTION ( 'NONE',  ( 0.000000000000000000, -0.5000000000000078826, 0.8660254037844340447 ) ) ;
#148906=ORIENTED_EDGE ( 'NONE', *, *, #46695, .F. ) ;
#148940=SPHERICAL_SURFACE ( 'NONE', #227355, 0.1000000000000000056 ) ;
#148941=AXIS2_PLACEMENT_3D ( 'NONE', #65074, #200738, #221554 ) ;
#148944=AXIS2_PLACEMENT_3D ( 'NONE', #232057, #208644, #230774 ) ;
#148952=CARTESIAN_POINT ( 'NONE',  ( -21.05000000000000071, 1.115600667400684642E-11, -96.50000000000004263 ) ) ;
#148990=ORIENTED_EDGE ( 'NONE', *, *, #206020, .F. ) ;
#148992=PLANE ( 'NONE',  #58480 ) ;
#149011=DIRECTION ( 'NONE',  ( 0.000000000000000000, 1.734723475976757554E-14, -1.000000000000000000 ) ) ;
#149053=ORIENTED_EDGE ( 'NONE', *, *, #87763, .T. ) ;
#149059=ORIENTED_EDGE ( 'NONE', *, *, #220573, .F. ) ;
#149060=EDGE_CURVE ( 'NONE', #89853, #61020, #221072, .T. ) ;
#149077=CARTESIAN_POINT ( 'NONE',  ( 21.08804582317315379, 8.878166167103044515, -79.34999982940649943 ) ) ;
#149079=EDGE_LOOP ( 'NONE', ( #52363, #134724 ) ) ;
#149084=CYLINDRICAL_SURFACE ( 'NONE', #145908, 0.1000000000000028644 ) ;
#149089=AXIS2_PLACEMENT_3D ( 'NONE', #158393, #74997, #16304 ) ;
#149111=ORIENTED_EDGE ( 'NONE', *, *, #53736, .T. ) ;
#149153=CARTESIAN_POINT ( 'NONE',  ( 20.94999675878240808, 10.29307482169070909, -105.9586421466940749 ) ) ;
#149154=ORIENTED_EDGE ( 'NONE', *, *, #120034, .F. ) ;
#149169=TOROIDAL_SURFACE ( 'NONE', #82466, 0.2000000000000000111, 0.1000000000000000056 ) ;
#149190=AXIS2_PLACEMENT_3D ( 'NONE', #130764, #169946, #72095 ) ;
#149193=AXIS2_PLACEMENT_3D ( 'NONE', #206026, #109470, #209886 ) ;
#149230=ADVANCED_FACE ( 'NONE', ( #106252 ), #47568, .F. ) ;
#149234=ORIENTED_EDGE ( 'NONE', *, *, #173188, .F. ) ;
#149240=PLANE ( 'NONE',  #235723 ) ;
#149253=ORIENTED_EDGE ( 'NONE', *, *, #40974, .F. ) ;
#149259=CARTESIAN_POINT ( 'NONE',  ( -18.41799967126732795, -9.499999999988851584, -74.03206981325584479 ) ) ;
#149264=CARTESIAN_POINT ( 'NONE',  ( -18.59999999999999787, -1.162701749926853712, -75.10000000000003695 ) ) ;
#149289=ORIENTED_EDGE ( 'NONE', *, *, #142725, .F. ) ;
#149295=AXIS2_PLACEMENT_3D ( 'NONE', #224452, #125370, #103207 ) ;
#149309=VECTOR ( 'NONE', #150123, 1000.000000000000000 ) ;
#149318=ORIENTED_EDGE ( 'NONE', *, *, #31914, .T. ) ;
#149352=CARTESIAN_POINT ( 'NONE',  ( 18.49999999999999289, 10.25000000001115730, -91.65000000000003411 ) ) ;
#149355=DIRECTION ( 'NONE',  ( 0.000000000000000000, 0.000000000000000000, 1.000000000000000000 ) ) ;
#149367=ADVANCED_FACE ( 'NONE', ( #34478 ), #253148, .T. ) ;
#149368=AXIS2_PLACEMENT_3D ( 'NONE', #217032, #121820, #100906 ) ;
#149381=SPHERICAL_SURFACE ( 'NONE', #240385, 0.1000000000000000056 ) ;
#149389=CARTESIAN_POINT ( 'NONE',  ( 20.21494484322224849, 9.303170737879936425, -75.34026519177028547 ) ) ;
#149392=FACE_OUTER_BOUND ( 'NONE', #95002, .T. ) ;
#149488=ORIENTED_EDGE ( 'NONE', *, *, #8485, .F. ) ;
#149538=ORIENTED_EDGE ( 'NONE', *, *, #89592, .F. ) ;
#149547=FACE_OUTER_BOUND ( 'NONE', #180500, .T. ) ;
#149576=DIRECTION ( 'NONE',  ( -1.000000000000000000, 0.000000000000000000, 0.000000000000000000 ) ) ;
#149613=CIRCLE ( 'NONE', #12249, 0.09999999999999824307 ) ;
#149615=DIRECTION ( 'NONE',  ( 0.000000000000000000, 0.000000000000000000, -1.000000000000000000 ) ) ;
#149623=FACE_OUTER_BOUND ( 'NONE', #29551, .T. ) ;
#149624=DIRECTION ( 'NONE',  ( 1.000000000000000000, 0.000000000000000000, 0.000000000000000000 ) ) ;
#149634=VERTEX_POINT ( 'NONE', #246753 ) ;
#149636=EDGE_LOOP ( 'NONE', ( #11181, #40688, #163682, #130463, #25741, #10727, #80629, #237724, #126875, #222390, #149666 ) ) ;
#149645=DIRECTION ( 'NONE',  ( 0.000000000000000000, 0.000000000000000000, -1.000000000000000000 ) ) ;
#149656=ORIENTED_EDGE ( 'NONE', *, *, #204020, .T. ) ;
#149666=ORIENTED_EDGE ( 'NONE', *, *, #136712, .T. ) ;
#149696=FACE_OUTER_BOUND ( 'NONE', #225503, .T. ) ;
#149698=VERTEX_POINT ( 'NONE', #224624 ) ;
#149708=DIRECTION ( 'NONE',  ( 0.000000000000000000, 6.938893903907270030E-14, 1.000000000000000000 ) ) ;
#149753=DIRECTION ( 'NONE',  ( -0.000000000000000000, 0.000000000000000000, -1.000000000000000000 ) ) ;
#149769=ORIENTED_EDGE ( 'NONE', *, *, #185552, .T. ) ;
#149838=ORIENTED_EDGE ( 'NONE', *, *, #47232, .F. ) ;
#149878=PLANE ( 'NONE',  #192832 ) ;
#149898=EDGE_CURVE ( 'NONE', #150237, #242521, #78360, .T. ) ;
#149902=DIRECTION ( 'NONE',  ( -1.000000000000000000, -1.040834085586090568E-13, 0.000000000000000000 ) ) ;
#149911=EDGE_CURVE ( 'NONE', #197986, #131327, #86717, .T. ) ;
#149916=ORIENTED_EDGE ( 'NONE', *, *, #158669, .F. ) ;
#149944=ORIENTED_EDGE ( 'NONE', *, *, #236602, .T. ) ;
#150020=FACE_OUTER_BOUND ( 'NONE', #162543, .T. ) ;
#150036=ORIENTED_EDGE ( 'NONE', *, *, #151227, .F. ) ;
#150049=CIRCLE ( 'NONE', #16777, 11.74999999999999645 ) ;
#150074=EDGE_CURVE ( 'NONE', #13016, #254308, #107584, .T. ) ;
#150077=ORIENTED_EDGE ( 'NONE', *, *, #104102, .F. ) ;
#150103=DIRECTION ( 'NONE',  ( -1.000000000000000000, -0.000000000000000000, -0.000000000000000000 ) ) ;
#150109=AXIS2_PLACEMENT_3D ( 'NONE', #132610, #111759, #210857 ) ;
#150123=DIRECTION ( 'NONE',  ( 1.000000000000000000, -7.304098846218134667E-16, 4.607487905232622991E-31 ) ) ;
#150126=FACE_OUTER_BOUND ( 'NONE', #24885, .T. ) ;
#150171=EDGE_CURVE ( 'NONE', #55997, #175744, #44682, .T. ) ;
#150205=VERTEX_POINT ( 'NONE', #196744 ) ;
#150215=AXIS2_PLACEMENT_3D ( 'NONE', #207780, #151666, #30419 ) ;
#150220=ORIENTED_EDGE ( 'NONE', *, *, #232934, .F. ) ;
#150234=DIRECTION ( 'NONE',  ( 0.000000000000000000, 1.734723475976807292E-15, -1.000000000000000000 ) ) ;
#150237=VERTEX_POINT ( 'NONE', #98901 ) ;
#150241=CARTESIAN_POINT ( 'NONE',  ( -18.59999999999999787, -1.866714910046153308, -78.75267524628205251 ) ) ;
#150261=ORIENTED_EDGE ( 'NONE', *, *, #221935, .F. ) ;
#150290=CARTESIAN_POINT ( 'NONE',  ( 23.25000000000000000, -11.48912529306489994, -97.40000000000004832 ) ) ;
#150293=EDGE_CURVE ( 'NONE', #156376, #44654, #2381, .T. ) ;
#150298=ORIENTED_EDGE ( 'NONE', *, *, #224031, .F. ) ;
#150305=CYLINDRICAL_SURFACE ( 'NONE', #253726, 0.09999999999999939493 ) ;
#150316=ORIENTED_EDGE ( 'NONE', *, *, #193392, .T. ) ;
#150320=CARTESIAN_POINT ( 'NONE',  ( 21.05000000000000071, 5.500000000011153745, -79.40526601891313874 ) ) ;
#150321=AXIS2_PLACEMENT_3D ( 'NONE', #168330, #66617, #247817 ) ;
#150331=VERTEX_POINT ( 'NONE', #62382 ) ;
#150344=CARTESIAN_POINT ( 'NONE',  ( -20.64999999999999858, 2.000000000011154189, -87.67537807723795140 ) ) ;
#150352=DIRECTION ( 'NONE',  ( -1.000000000000000000, 0.000000000000000000, 0.000000000000000000 ) ) ;
#150353=CARTESIAN_POINT ( 'NONE',  ( 21.05000005001280172, 8.871279691782060439, -79.17794758824591383 ) ) ;
#150370=AXIS2_PLACEMENT_3D ( 'NONE', #68238, #129498, #150352 ) ;
#150383=CARTESIAN_POINT ( 'NONE',  ( -20.94999999999999929, -1.164121893230052995, -108.2148480855716457 ) ) ;
#150387=EDGE_CURVE ( 'NONE', #208354, #135788, #94730, .T. ) ;
#150393=VECTOR ( 'NONE', #43345, 1000.000000000000114 ) ;
#150397=DIRECTION ( 'NONE',  ( 0.000000000000000000, 0.000000000000000000, -1.000000000000000000 ) ) ;
#150406=TOROIDAL_SURFACE ( 'NONE', #191925, 0.4000000000000012990, 0.1000000000000000056 ) ;
#150415=ADVANCED_FACE ( 'NONE', ( #27137 ), #227865, .T. ) ;
#150431=DIRECTION ( 'NONE',  ( 1.000000000000000000, 0.000000000000000000, 0.000000000000000000 ) ) ;
#150434=LINE ( 'NONE', #212957, #227811 ) ;
#150437=EDGE_LOOP ( 'NONE', ( #149656, #203816, #119443 ) ) ;
#150444=DIRECTION ( 'NONE',  ( -0.000000000000000000, 0.7397360091702694929, 0.6728971962616898672 ) ) ;
#150449=DIRECTION ( 'NONE',  ( -1.000000000000000000, 0.000000000000000000, 0.000000000000000000 ) ) ;
#150457=ADVANCED_FACE ( 'NONE', ( #197396 ), #194542, .T. ) ;
#150459=DIRECTION ( 'NONE',  ( 0.000000000000000000, -0.9915357197604792727, 0.1298341882520475943 ) ) ;
#150463=VERTEX_POINT ( 'NONE', #175308 ) ;
#150465=DIRECTION ( 'NONE',  ( 0.000000000000000000, 0.000000000000000000, -1.000000000000000000 ) ) ;
#150504=ORIENTED_EDGE ( 'NONE', *, *, #208124, .F. ) ;
#150512=CARTESIAN_POINT ( 'NONE',  ( -21.05000000000000071, 1.115600667400684642E-11, -67.00000000000004263 ) ) ;
#150518=EDGE_CURVE ( 'NONE', #64899, #156656, #178152, .T. ) ;
#150541=CARTESIAN_POINT ( 'NONE',  ( 20.94999999999999929, 1.115600667400684642E-11, -79.97500000000005116 ) ) ;
#150577=CARTESIAN_POINT ( 'NONE',  ( -21.05000000000000071, 1.115600667400684642E-11, -67.00000000000004263 ) ) ;
#150636=AXIS2_PLACEMENT_3D ( 'NONE', #22138, #162934, #179925 ) ;
#150637=DIRECTION ( 'NONE',  ( 1.000000000000000000, 0.000000000000000000, 0.000000000000000000 ) ) ;
#150644=LINE ( 'NONE', #119229, #33177 ) ;
#150649=CARTESIAN_POINT ( 'NONE',  ( 20.75572585718219898, 8.882316728409760387, -75.49725839870761490 ) ) ;
#150663=ORIENTED_EDGE ( 'NONE', *, *, #144499, .T. ) ;
#150702=ORIENTED_EDGE ( 'NONE', *, *, #74996, .T. ) ;
#150705=EDGE_CURVE ( 'NONE', #135773, #111692, #103093, .T. ) ;
#150716=FACE_OUTER_BOUND ( 'NONE', #27530, .T. ) ;
#150760=DIRECTION ( 'NONE',  ( 0.000000000000000000, -1.000000000000000000, 0.000000000000000000 ) ) ;
#150764=DIRECTION ( 'NONE',  ( -1.000000000000000000, -0.000000000000000000, -0.000000000000000000 ) ) ;
#150772=ORIENTED_EDGE ( 'NONE', *, *, #169866, .F. ) ;
#150797=AXIS2_PLACEMENT_3D ( 'NONE', #110920, #48373, #249165 ) ;
#150812=CARTESIAN_POINT ( 'NONE',  ( -20.85000000000000142, 1.115600667400684642E-11, -100.5000000000000426 ) ) ;
#150821=VERTEX_POINT ( 'NONE', #47293 ) ;
#150874=LINE ( 'NONE', #251244, #100727 ) ;
#150875=VERTEX_POINT ( 'NONE', #150290 ) ;
#150881=AXIS2_PLACEMENT_3D ( 'NONE', #182637, #126494, #206036 ) ;
#150887=EDGE_CURVE ( 'NONE', #78259, #121203, #28526, .T. ) ;
#150913=SPHERICAL_SURFACE ( 'NONE', #211995, 0.1000000000000000056 ) ;
#150969=DIRECTION ( 'NONE',  ( 0.000000000000000000, 1.000000000000000000, -1.387778780781454006E-13 ) ) ;
#150970=ADVANCED_FACE ( 'NONE', ( #16019 ), #1549, .T. ) ;
#150993=ADVANCED_FACE ( 'NONE', ( #75969 ), #124094, .F. ) ;
#150998=EDGE_CURVE ( 'NONE', #94180, #94787, #95110, .T. ) ;
#151005=CARTESIAN_POINT ( 'NONE',  ( -20.64999999999999858, 7.150000000011155876, -88.15000000000004832 ) ) ;
#151016=AXIS2_PLACEMENT_3D ( 'NONE', #142408, #221920, #5439 ) ;
#151027=DIRECTION ( 'NONE',  ( -0.000000000000000000, 0.8660254037844502539, 0.4999999999999799605 ) ) ;
#151063=ADVANCED_FACE ( 'NONE', ( #225718 ), #223163, .T. ) ;
#151081=VECTOR ( 'NONE', #198765, 1000.000000000000000 ) ;
#151101=AXIS2_PLACEMENT_3D ( 'NONE', #72566, #234172, #32163 ) ;
#151105=CARTESIAN_POINT ( 'NONE',  ( 20.94999999999999929, 5.000000000011153745, -88.59473398108696074 ) ) ;
#151124=CARTESIAN_POINT ( 'NONE',  ( -23.25000000000000000, 11.75000000001115552, -55.25000000000004974 ) ) ;
#151165=ORIENTED_EDGE ( 'NONE', *, *, #61470, .F. ) ;
#151190=AXIS2_PLACEMENT_3D ( 'NONE', #134945, #15049, #12487 ) ;
#151206=DIRECTION ( 'NONE',  ( 1.000000000000000000, -7.304098846218133681E-16, -2.111765289898285610E-31 ) ) ;
#151209=EDGE_CURVE ( 'NONE', #70270, #4212, #86700, .T. ) ;
#151216=VERTEX_POINT ( 'NONE', #113501 ) ;
#151227=EDGE_CURVE ( 'NONE', #52970, #56430, #232678, .T. ) ;
#151234=CARTESIAN_POINT ( 'NONE',  ( -21.05000000000000071, -1.162701749926853712, -75.10000000000003695 ) ) ;
#151237=AXIS2_PLACEMENT_3D ( 'NONE', #8310, #207807, #9568 ) ;
#151243=CARTESIAN_POINT ( 'NONE',  ( 23.14999999999999858, 4.775700934590584090, -78.84876810404601599 ) ) ;
#151256=EDGE_LOOP ( 'NONE', ( #13674, #186267, #115199, #208636 ) ) ;
#151262=CARTESIAN_POINT ( 'NONE',  ( 19.87657994472042233, 11.75000000001092992, -91.76578812462598478 ) ) ;
#151267=AXIS2_PLACEMENT_3D ( 'NONE', #46045, #208978, #105999 ) ;
#151282=CIRCLE ( 'NONE', #134486, 4.049999999999998934 ) ;
#151372=DIRECTION ( 'NONE',  ( 0.000000000000000000, -1.000000000000000000, 0.000000000000000000 ) ) ;
#151376=ORIENTED_EDGE ( 'NONE', *, *, #237917, .F. ) ;
#151380=CARTESIAN_POINT ( 'NONE',  ( 21.30000000000002558, 1.115600667400684642E-11, -67.00000000000004263 ) ) ;
#151394=VECTOR ( 'NONE', #119364, 1000.000000000000000 ) ;
#151407=PLANE ( 'NONE',  #166423 ) ;
#151428=AXIS2_PLACEMENT_3D ( 'NONE', #122625, #161755, #163034 ) ;
#151451=ORIENTED_EDGE ( 'NONE', *, *, #78780, .T. ) ;
#151498=CIRCLE ( 'NONE', #43151, 11.65000000000000036 ) ;
#151503=ORIENTED_EDGE ( 'NONE', *, *, #233453, .F. ) ;
#151524=EDGE_CURVE ( 'NONE', #102379, #131057, #249246, .T. ) ;
#151543=EDGE_CURVE ( 'NONE', #144450, #10892, #70253, .T. ) ;
#151560=CARTESIAN_POINT ( 'NONE',  ( -18.59999999999999787, 11.75000000001115197, -74.01480577065404987 ) ) ;
#151589=ORIENTED_EDGE ( 'NONE', *, *, #151524, .F. ) ;
#151617=ORIENTED_EDGE ( 'NONE', *, *, #250035, .F. ) ;
#151656=ORIENTED_EDGE ( 'NONE', *, *, #201426, .T. ) ;
#151666=DIRECTION ( 'NONE',  ( 0.000000000000000000, -1.000000000000000000, 0.000000000000000000 ) ) ;
#151690=DIRECTION ( 'NONE',  ( 1.000000000000000000, -0.000000000000000000, -0.000000000000000000 ) ) ;
#151708=CARTESIAN_POINT ( 'NONE',  ( 22.48660254037843842, 11.65000000001115588, -66.95000000000003126 ) ) ;
#151728=CARTESIAN_POINT ( 'NONE',  ( 18.59999999999999787, -1.835341550213255957, -78.55515129256302487 ) ) ;
#151737=CARTESIAN_POINT ( 'NONE',  ( 21.00000000000000000, 9.750000000011153745, -88.15000000000004832 ) ) ;
#151748=CARTESIAN_POINT ( 'NONE',  ( -21.05000000000000071, -11.48912529306490349, -70.10000000000005116 ) ) ;
#151764=EDGE_LOOP ( 'NONE', ( #37971, #40896, #158676, #174199 ) ) ;
#151793=VECTOR ( 'NONE', #195425, 1000.000000000000000 ) ;
#151794=EDGE_LOOP ( 'NONE', ( #252482, #13279, #239061, #193074 ) ) ;
#151796=DIRECTION ( 'NONE',  ( 0.000000000000000000, -0.000000000000000000, -1.000000000000000000 ) ) ;
#151819=VERTEX_POINT ( 'NONE', #245659 ) ;
#151843=CARTESIAN_POINT ( 'NONE',  ( 22.50046968638275757, 0.04516984714972999138, -55.24995484552670888 ) ) ;
#151870=EDGE_CURVE ( 'NONE', #208853, #204053, #207920, .T. ) ;
#151904=CARTESIAN_POINT ( 'NONE',  ( -23.25000000000000000, 11.65000000001115588, -79.15000000000004832 ) ) ;
#151905=ORIENTED_EDGE ( 'NONE', *, *, #147990, .T. ) ;
#151951=DIRECTION ( 'NONE',  ( 0.000000000000000000, 0.7397360091702755991, -0.6728971962616832059 ) ) ;
#151973=VERTEX_POINT ( 'NONE', #78567 ) ;
#151979=DIRECTION ( 'NONE',  ( 1.000000000000000000, 0.000000000000000000, 0.000000000000000000 ) ) ;
#152008=DIRECTION ( 'NONE',  ( -1.000000000000000000, 0.000000000000000000, 0.000000000000000000 ) ) ;
#152015=ORIENTED_EDGE ( 'NONE', *, *, #237175, .T. ) ;
#152052=DIRECTION ( 'NONE',  ( 0.000000000000000000, -0.9908441862701596881, 0.1350103645451904977 ) ) ;
#152072=ADVANCED_FACE ( 'NONE', ( #257156 ), #27629, .F. ) ;
#152082=DIRECTION ( 'NONE',  ( 1.000000000000000000, 2.952720810173289112E-16, -0.000000000000000000 ) ) ;
#152087=DIRECTION ( 'NONE',  ( 0.000000000000000000, 0.000000000000000000, 1.000000000000000000 ) ) ;
#152143=CARTESIAN_POINT ( 'NONE',  ( 20.94999999999999929, -1.162701749926853712, -74.90000000000004832 ) ) ;
#152144=LINE ( 'NONE', #231673, #186357 ) ;
#152157=CARTESIAN_POINT ( 'NONE',  ( -18.50000000000000000, 3.912899247244609580, -78.48182297301100618 ) ) ;
#152185=CARTESIAN_POINT ( 'NONE',  ( 21.00000000000000000, 9.750000000011153745, -88.25000000000005684 ) ) ;
#152197=VERTEX_POINT ( 'NONE', #2872 ) ;
#152217=PLANE ( 'NONE',  #52034 ) ;
#152221=FACE_OUTER_BOUND ( 'NONE', #249258, .T. ) ;
#152226=ORIENTED_EDGE ( 'NONE', *, *, #170645, .F. ) ;
#152228=ORIENTED_EDGE ( 'NONE', *, *, #214597, .T. ) ;
#152247=CARTESIAN_POINT ( 'NONE',  ( -22.50047199487879368, 0.04490605193106571302, -55.24995258108270946 ) ) ;
#152306=ORIENTED_EDGE ( 'NONE', *, *, #169233, .F. ) ;
#152319=ADVANCED_FACE ( 'NONE', ( #150126 ), #208801, .T. ) ;
#152333=AXIS2_PLACEMENT_3D ( 'NONE', #52282, #229663, #211387 ) ;
#152336=AXIS2_PLACEMENT_3D ( 'NONE', #212793, #191965, #249355 ) ;
#152353=DIRECTION ( 'NONE',  ( 0.000000000000000000, 1.000000000000000000, 0.000000000000000000 ) ) ;
#152375=ADVANCED_FACE ( 'NONE', ( #71868 ), #151407, .T. ) ;
#152396=LINE ( 'NONE', #92379, #12210 ) ;
#152401=CARTESIAN_POINT ( 'NONE',  ( -21.05000000000000071, -11.29603075032412995, -70.04789915966391334 ) ) ;
#152434=CARTESIAN_POINT ( 'NONE',  ( 23.24999999999999289, 4.150000000011154988, -67.00000000000004263 ) ) ;
#152447=CARTESIAN_POINT ( 'NONE',  ( -23.25000000000000000, 6.933893972137497030, -104.2856458343736250 ) ) ;
#152453=CARTESIAN_POINT ( 'NONE',  ( 20.85000000000000142, 6.846123162363745074, -104.2377262668499043 ) ) ;
#152467=CARTESIAN_POINT ( 'NONE',  ( -22.39999999999999858, 0.1000000000111554016, -59.20922040162664501 ) ) ;
#152504=VERTEX_POINT ( 'NONE', #35332 ) ;
#152519=EDGE_CURVE ( 'NONE', #187777, #38637, #27323, .T. ) ;
#152531=ORIENTED_EDGE ( 'NONE', *, *, #219729, .F. ) ;
#152543=VERTEX_POINT ( 'NONE', #41730 ) ;
#152575=ORIENTED_EDGE ( 'NONE', *, *, #193660, .T. ) ;
#152613=DIRECTION ( 'NONE',  ( 0.000000000000000000, 0.000000000000000000, -1.000000000000000000 ) ) ;
#152614=CIRCLE ( 'NONE', #73502, 0.1000000000000028644 ) ;
#152622=CARTESIAN_POINT ( 'NONE',  ( 21.07928932188134397, 0.09889514566555242248, -60.67148334360673800 ) ) ;
#152629=CARTESIAN_POINT ( 'NONE',  ( 20.94999999999999929, -11.48912529306489994, -97.40000000000004832 ) ) ;
#152632=ADVANCED_FACE ( 'NONE', ( #82088 ), #79828, .F. ) ;
#152661=CARTESIAN_POINT ( 'NONE',  ( 23.15000000000000213, -11.64999999998884483, -67.00000000000004263 ) ) ;
#152678=EDGE_CURVE ( 'NONE', #231071, #250167, #251456, .T. ) ;
#152699=TOROIDAL_SURFACE ( 'NONE', #27800, 0.4000000000000009104, 0.1000000000000000056 ) ;
#152703=EDGE_CURVE ( 'NONE', #236288, #181403, #4235, .T. ) ;
#152712=DIRECTION ( 'NONE',  ( 0.000000000000000000, -1.000000000000000000, 0.000000000000000000 ) ) ;
#152760=DIRECTION ( 'NONE',  ( 2.952720810173289112E-16, -1.000000000000000000, 0.000000000000000000 ) ) ;
#152855=CIRCLE ( 'NONE', #11168, 11.70000000000000284 ) ;
#152871=LINE ( 'NONE', #56282, #24809 ) ;
#152876=AXIS2_PLACEMENT_3D ( 'NONE', #254271, #95217, #16985 ) ;
#152881=ORIENTED_EDGE ( 'NONE', *, *, #202136, .F. ) ;
#152882=ORIENTED_EDGE ( 'NONE', *, *, #21642, .T. ) ;
#152907=FACE_OUTER_BOUND ( 'NONE', #203425, .T. ) ;
#152933=CARTESIAN_POINT ( 'NONE',  ( 22.42357213249528769, 7.672932386371071445, -66.90091303599848516 ) ) ;
#152935=AXIS2_PLACEMENT_3D ( 'NONE', #21016, #97923, #100489 ) ;
#152992=DIRECTION ( 'NONE',  ( -1.000000000000000000, -0.000000000000000000, -0.000000000000000000 ) ) ;
#153000=TOROIDAL_SURFACE ( 'NONE', #77927, 2.100000000000002309, 0.1000000000000000056 ) ;
#153140=DIRECTION ( 'NONE',  ( 0.000000000000000000, 0.9999631594459056361, -0.008583690987128059571 ) ) ;
#153153=CARTESIAN_POINT ( 'NONE',  ( -20.15000000000000568, 9.291421356248463326, -79.25000000000004263 ) ) ;
#153158=DIRECTION ( 'NONE',  ( 0.000000000000000000, -0.9908441862701596881, 0.1350103645451904977 ) ) ;
#153266=VERTEX_POINT ( 'NONE', #98445 ) ;
#153271=DIRECTION ( 'NONE',  ( -1.000000000000000000, 0.000000000000000000, 0.000000000000000000 ) ) ;
#153288=DIRECTION ( 'NONE',  ( 0.000000000000000000, 1.000000000000000000, 0.000000000000000000 ) ) ;
#153295=CARTESIAN_POINT ( 'NONE',  ( 21.05000000000000071, -1.162701749926853712, -74.90000000000004832 ) ) ;
#153327=VERTEX_POINT ( 'NONE', #42376 ) ;
#153342=CARTESIAN_POINT ( 'NONE',  ( -20.54999999999999716, 9.350000000011156942, -79.25000000000004263 ) ) ;
#153350=EDGE_CURVE ( 'NONE', #223063, #203104, #229491, .T. ) ;
#153360=CARTESIAN_POINT ( 'NONE',  ( -20.54999999999999716, 9.350000000011156942, -88.15000000000004832 ) ) ;
#153364=AXIS2_PLACEMENT_3D ( 'NONE', #198776, #60545, #18858 ) ;
#153369=( BOUNDED_SURFACE ( )  B_SPLINE_SURFACE ( 3, 2, ( 
 ( #55486, #95920, #230304 ),
 ( #15125, #52948, #212050 ),
 ( #111645, #112937, #17667 ),
 ( #37268, #73838, #252423 ) ),
 .UNSPECIFIED., .F., .F., .T. ) 
 B_SPLINE_SURFACE_WITH_KNOTS ( ( 4, 4 ),
 ( 3, 3 ),
 ( 0.0002700421466196717673, 0.0004789321604330994782 ),
 ( 0.000000000000000000, 1.000000000000000000 ),
 .UNSPECIFIED. ) 
 GEOMETRIC_REPRESENTATION_ITEM ( )  RATIONAL_B_SPLINE_SURFACE ( (
 ( 1.000000000000000000, 0.7071067811865475727, 1.000000000000000000),
 ( 1.000000000000000000, 0.7163411249511767442, 1.000000000000000000),
 ( 1.000000000000000000, 0.7221957104841900676, 1.000000000000000000),
 ( 1.000000000000000000, 0.7250110520819876836, 1.000000000000000000) ) ) 
 REPRESENTATION_ITEM ( '' )  SURFACE ( )  );
#153377=CARTESIAN_POINT ( 'NONE',  ( -21.44999999999999929, 7.250000000011155521, -88.25000000000005684 ) ) ;
#153382=FACE_OUTER_BOUND ( 'NONE', #242708, .T. ) ;
#153384=ORIENTED_EDGE ( 'NONE', *, *, #193660, .F. ) ;
#153390=ORIENTED_EDGE ( 'NONE', *, *, #90164, .F. ) ;
#153400=CARTESIAN_POINT ( 'NONE',  ( -18.59999999999999787, 11.65000000001115232, -73.91480577065404134 ) ) ;
#153416=DIRECTION ( 'NONE',  ( 1.000000000000000000, 0.000000000000000000, -0.000000000000000000 ) ) ;
#153462=CYLINDRICAL_SURFACE ( 'NONE', #227841, 0.1000000000000028644 ) ;
#153463=ORIENTED_EDGE ( 'NONE', *, *, #101116, .T. ) ;
#153480=DIRECTION ( 'NONE',  ( 0.000000000000000000, 0.000000000000000000, -1.000000000000000000 ) ) ;
#153486=ORIENTED_EDGE ( 'NONE', *, *, #17538, .T. ) ;
#153513=CARTESIAN_POINT ( 'NONE',  ( 0.000000000000000000, 0.000000000000000000, 0.000000000000000000 ) ) ;
#153535=ORIENTED_EDGE ( 'NONE', *, *, #241203, .T. ) ;
#153544=DIRECTION ( 'NONE',  ( 0.000000000000000000, 1.000000000000000000, 0.000000000000000000 ) ) ;
#153546=VERTEX_POINT ( 'NONE', #181285 ) ;
#153572=DIRECTION ( 'NONE',  ( -1.000000000000000000, 0.000000000000000000, 0.000000000000000000 ) ) ;
#153578=EDGE_LOOP ( 'NONE', ( #234590, #162530, #256280, #8936 ) ) ;
#153591=EDGE_CURVE ( 'NONE', #56745, #246680, #254391, .T. ) ;
#153606=DIRECTION ( 'NONE',  ( 0.000000000000000000, 0.7397360091702777085, -0.6728971962616808744 ) ) ;
#153665=DIRECTION ( 'NONE',  ( 0.000000000000000000, 0.000000000000000000, -1.000000000000000000 ) ) ;
#153676=CARTESIAN_POINT ( 'NONE',  ( -20.99551997958347016, 11.75000000001097078, -93.65165913768963435 ) ) ;
#153697=ORIENTED_EDGE ( 'NONE', *, *, #211687, .T. ) ;
#153715=EDGE_LOOP ( 'NONE', ( #126608, #252384, #155978, #216814 ) ) ;
#153738=CYLINDRICAL_SURFACE ( 'NONE', #188757, 0.09999999999999939493 ) ;
#153838=CYLINDRICAL_SURFACE ( 'NONE', #148944, 0.1000000000000028644 ) ;
#153840=DIRECTION ( 'NONE',  ( 0.000000000000000000, 0.000000000000000000, -1.000000000000000000 ) ) ;
#153847=DIRECTION ( 'NONE',  ( -1.000000000000000000, -0.000000000000000000, -0.000000000000000000 ) ) ;
#153855=CARTESIAN_POINT ( 'NONE',  ( -23.25000000000000000, 1.115600667400684642E-11, -67.00000000000004263 ) ) ;
#153933=DIRECTION ( 'NONE',  ( 1.000000000000000000, 0.000000000000000000, 0.000000000000000000 ) ) ;
#153944=DIRECTION ( 'NONE',  ( 1.000000000000000000, 2.952720810173289112E-16, -0.000000000000000000 ) ) ;
#154034=VERTEX_POINT ( 'NONE', #199245 ) ;
#154059=ORIENTED_EDGE ( 'NONE', *, *, #178934, .T. ) ;
#154078=ORIENTED_EDGE ( 'NONE', *, *, #55122, .F. ) ;
#154079=CARTESIAN_POINT ( 'NONE',  ( -18.42637059832563651, -9.496945461878544492, -107.1090773097998721 ) ) ;
#154104=DIRECTION ( 'NONE',  ( -1.000000000000000000, -2.952720810173289112E-16, 0.000000000000000000 ) ) ;
#154117=ORIENTED_EDGE ( 'NONE', *, *, #205397, .T. ) ;
#154133=ORIENTED_EDGE ( 'NONE', *, *, #107424, .T. ) ;
#154140=ORIENTED_EDGE ( 'NONE', *, *, #13479, .T. ) ;
#154184=ORIENTED_EDGE ( 'NONE', *, *, #214867, .T. ) ;
#154194=EDGE_CURVE ( 'NONE', #31293, #68386, #200631, .T. ) ;
#154233=VECTOR ( 'NONE', #136714, 1000.000000000000000 ) ;
#154237=CARTESIAN_POINT ( 'NONE',  ( 21.05000000000000071, 1.162701749949165642, -74.90000000000004832 ) ) ;
#154277=CARTESIAN_POINT ( 'NONE',  ( 23.14999999999999858, 1.115600667400684642E-11, -104.5000000000000568 ) ) ;
#154292=CYLINDRICAL_SURFACE ( 'NONE', #70184, 0.1000000000000028644 ) ;
#154337=CARTESIAN_POINT ( 'NONE',  ( -20.85000000000000142, 10.33248238083635151, -106.0948465439132065 ) ) ;
#154380=DIRECTION ( 'NONE',  ( 1.000000000000000000, 0.000000000000000000, 0.000000000000000000 ) ) ;
#154391=FACE_OUTER_BOUND ( 'NONE', #173966, .T. ) ;
#154397=LINE ( 'NONE', #77367, #72383 ) ;
#154417=FACE_OUTER_BOUND ( 'NONE', #30809, .T. ) ;
#154425=ORIENTED_EDGE ( 'NONE', *, *, #42073, .T. ) ;
#154435=EDGE_LOOP ( 'NONE', ( #149488, #122616, #189334, #74258, #68691, #22191, #228757 ) ) ;
#154438=FACE_OUTER_BOUND ( 'NONE', #253786, .T. ) ;
#154494=DIRECTION ( 'NONE',  ( 0.000000000000000000, 0.8700118002898322711, -0.4930308989875231140 ) ) ;
#154507=AXIS2_PLACEMENT_3D ( 'NONE', #233454, #194331, #232162 ) ;
#154525=DIRECTION ( 'NONE',  ( -1.000000000000000000, -0.000000000000000000, 0.000000000000000000 ) ) ;
#154550=CARTESIAN_POINT ( 'NONE',  ( -18.59999999999999787, 7.021664781911246322, -104.3335654018973315 ) ) ;
#154561=EDGE_CURVE ( 'NONE', #196062, #214056, #16916, .T. ) ;
#154568=CARTESIAN_POINT ( 'NONE',  ( 20.94999999999999929, -1.835341550213257733, -78.55515129256302487 ) ) ;
#154605=DIRECTION ( 'NONE',  ( 0.000000000000000000, 0.000000000000000000, 1.000000000000000000 ) ) ;
#154622=ADVANCED_FACE ( 'NONE', ( #210617 ), #116427, .T. ) ;
#154629=DIRECTION ( 'NONE',  ( -0.000000000000000000, -0.1350103645451928291, -0.9908441862701594660 ) ) ;
#154640=VECTOR ( 'NONE', #118666, 1000.000000000000000 ) ;
#154641=FACE_OUTER_BOUND ( 'NONE', #234106, .T. ) ;
#154661=CARTESIAN_POINT ( 'NONE',  ( -18.53317502108577486, 10.32263460347359540, -106.0605957968672470 ) ) ;
#154665=AXIS2_PLACEMENT_3D ( 'NONE', #194316, #58607, #119920 ) ;
#154681=ORIENTED_EDGE ( 'NONE', *, *, #201402, .T. ) ;
#154684=EDGE_LOOP ( 'NONE', ( #33818, #173268, #146323, #138369 ) ) ;
#154696=AXIS2_PLACEMENT_3D ( 'NONE', #23452, #5099, #84626 ) ;
#154701=VERTEX_POINT ( 'NONE', #26877 ) ;
#154710=CARTESIAN_POINT ( 'NONE',  ( -21.11101077989000174, 0.01528526892543676310, -60.57631526527391941 ) ) ;
#154711=ORIENTED_EDGE ( 'NONE', *, *, #172877, .F. ) ;
#154737=CIRCLE ( 'NONE', #192158, 0.1000000000000028644 ) ;
#154751=VECTOR ( 'NONE', #104696, 1000.000000000000000 ) ;
#154778=ORIENTED_EDGE ( 'NONE', *, *, #10687, .T. ) ;
#154796=AXIS2_PLACEMENT_3D ( 'NONE', #207739, #126900, #29129 ) ;
#154823=DIRECTION ( 'NONE',  ( -1.000000000000000000, -0.000000000000000000, -0.000000000000000000 ) ) ;
#154832=ORIENTED_EDGE ( 'NONE', *, *, #240178, .F. ) ;
#154905=DIRECTION ( 'NONE',  ( 0.000000000000000000, 0.000000000000000000, -1.000000000000000000 ) ) ;
#154914=EDGE_CURVE ( 'NONE', #14603, #194502, #33878, .T. ) ;
#154929=CARTESIAN_POINT ( 'NONE',  ( 21.05000012384952868, 10.62872029888669978, -79.17797733003580163 ) ) ;
#154937=( BOUNDED_CURVE ( )  B_SPLINE_CURVE ( 3, ( #132394, #71156, #112830, #131104 ),
 .UNSPECIFIED., .F., .F. ) 
 B_SPLINE_CURVE_WITH_KNOTS ( ( 4, 4 ),
 ( 3.192897208853993085, 4.712388980384689674 ),
 .UNSPECIFIED. ) 
 CURVE ( )  GEOMETRIC_REPRESENTATION_ITEM ( )  RATIONAL_B_SPLINE_CURVE ( ( 1.000000000000000000, 0.8166740347213228279, 0.8166740347213228279, 1.000000000000000000 ) ) 
 REPRESENTATION_ITEM ( '' )  );
#154942=CARTESIAN_POINT ( 'NONE',  ( -23.15000000000000213, -11.64999999998884483, -97.40000000000004832 ) ) ;
#154943=DIRECTION ( 'NONE',  ( -1.000000000000000000, 0.000000000000000000, 0.000000000000000000 ) ) ;
#154945=VECTOR ( 'NONE', #7049, 1000.000000000000000 ) ;
#154946=ORIENTED_EDGE ( 'NONE', *, *, #175517, .T. ) ;
#154967=VERTEX_POINT ( 'NONE', #185616 ) ;
#155022=LINE ( 'NONE', #135414, #18493 ) ;
#155027=DIRECTION ( 'NONE',  ( 0.000000000000000000, 1.000000000000000000, 0.000000000000000000 ) ) ;
#155038=VERTEX_POINT ( 'NONE', #190785 ) ;
#155079=ORIENTED_EDGE ( 'NONE', *, *, #68831, .T. ) ;
#155089=DIRECTION ( 'NONE',  ( -1.000000000000000000, -0.000000000000000000, 0.000000000000000000 ) ) ;
#155098=LINE ( 'NONE', #234595, #5495 ) ;
#155099=CARTESIAN_POINT ( 'NONE',  ( 18.44206774312972641, -9.491027357528919239, -107.1262275046983206 ) ) ;
#155104=DIRECTION ( 'NONE',  ( 0.000000000000000000, 0.000000000000000000, -1.000000000000000000 ) ) ;
#155148=FACE_OUTER_BOUND ( 'NONE', #70712, .T. ) ;
#155150=EDGE_CURVE ( 'NONE', #129552, #238489, #17440, .T. ) ;
#155155=CARTESIAN_POINT ( 'NONE',  ( 20.46382478191414833, 10.59862044130854031, -74.67781446934550615 ) ) ;
#155203=DIRECTION ( 'NONE',  ( 0.000000000000000000, 0.000000000000000000, -1.000000000000000000 ) ) ;
#155208=DIRECTION ( 'NONE',  ( -0.000000000000000000, -1.000000000000000000, 0.000000000000000000 ) ) ;
#155229=DIRECTION ( 'NONE',  ( 0.000000000000000000, -1.000000000000000000, -2.891205793294679805E-16 ) ) ;
#155236=AXIS2_PLACEMENT_3D ( 'NONE', #45007, #60697, #221062 ) ;
#155252=EDGE_CURVE ( 'NONE', #187394, #231082, #219291, .T. ) ;
#155300=EDGE_CURVE ( 'NONE', #130026, #3373, #121530, .T. ) ;
#155320=ORIENTED_EDGE ( 'NONE', *, *, #215104, .T. ) ;
#155326=CARTESIAN_POINT ( 'NONE',  ( 21.07928932188134041, 0.09889514566578908039, -60.67148334360133788 ) ) ;
#155335=DIRECTION ( 'NONE',  ( 0.000000000000000000, 0.000000000000000000, -1.000000000000000000 ) ) ;
#155352=EDGE_CURVE ( 'NONE', #143703, #203901, #229823, .T. ) ;
#155361=VERTEX_POINT ( 'NONE', #65356 ) ;
#155368=VERTEX_POINT ( 'NONE', #124067 ) ;
#155375=CIRCLE ( 'NONE', #151267, 11.74999999999999645 ) ;
#155378=DIRECTION ( 'NONE',  ( -1.000000000000000000, -0.000000000000000000, 0.000000000000000000 ) ) ;
#155394=FILL_AREA_STYLE ('',( #75823 ) ) ;
#155410=EDGE_LOOP ( 'NONE', ( #117622, #138499, #107734, #228553, #158936 ) ) ;
#155427=AXIS2_PLACEMENT_3D ( 'NONE', #179379, #80215, #229405 ) ;
#155451=CIRCLE ( 'NONE', #126160, 0.09999999999999939493 ) ;
#155457=ORIENTED_EDGE ( 'NONE', *, *, #251890, .F. ) ;
#155525=DIRECTION ( 'NONE',  ( 0.000000000000000000, 0.000000000000000000, 1.000000000000000000 ) ) ;
#155555=ORIENTED_EDGE ( 'NONE', *, *, #22990, .F. ) ;
#155563=ORIENTED_EDGE ( 'NONE', *, *, #183702, .F. ) ;
#155584=AXIS2_PLACEMENT_3D ( 'NONE', #37018, #173986, #155688 ) ;
#155585=DIRECTION ( 'NONE',  ( 0.000000000000000000, 0.000000000000000000, -1.000000000000000000 ) ) ;
#155598=CARTESIAN_POINT ( 'NONE',  ( 21.00023020733503287, 1.115539681028482333E-11, -60.60913075473168021 ) ) ;
#155601=FACE_OUTER_BOUND ( 'NONE', #37218, .T. ) ;
#155618=CARTESIAN_POINT ( 'NONE',  ( -20.64999999999999858, -9.499999999988848032, -76.89396912265249284 ) ) ;
#155638=CARTESIAN_POINT ( 'NONE',  ( 20.94999999999999929, -11.29603075032412640, -97.45210084033617193 ) ) ;
#155645=LINE ( 'NONE', #173937, #252914 ) ;
#155688=DIRECTION ( 'NONE',  ( 1.000000000000000000, 0.000000000000000000, 0.000000000000000000 ) ) ;
#155694=EDGE_CURVE ( 'NONE', #127618, #132550, #184034, .T. ) ;
#155723=EDGE_CURVE ( 'NONE', #53634, #123588, #205851, .T. ) ;
#155724=DIRECTION ( 'NONE',  ( 0.000000000000000000, 5.329070518200686707E-15, 1.000000000000000000 ) ) ;
#155748=CARTESIAN_POINT ( 'NONE',  ( -23.15000000000000213, -8.999999999988844479, -90.60603087734760663 ) ) ;
#155768=ORIENTED_EDGE ( 'NONE', *, *, #17054, .T. ) ;
#155770=CARTESIAN_POINT ( 'NONE',  ( -21.65000000000000213, 7.750000000011155521, -79.35000000000005116 ) ) ;
#155781=VECTOR ( 'NONE', #23606, 1000.000000000000000 ) ;
#155788=EDGE_CURVE ( 'NONE', #189474, #61020, #79949, .T. ) ;
#155795=ORIENTED_EDGE ( 'NONE', *, *, #10687, .F. ) ;
#155799=DIRECTION ( 'NONE',  ( 0.000000000000000000, 1.000000000000000000, 0.000000000000000000 ) ) ;
#155821=CARTESIAN_POINT ( 'NONE',  ( -22.45305610364635740, -0.1008583690875579086, -55.25043287651066493 ) ) ;
#155829=AXIS2_PLACEMENT_3D ( 'NONE', #117482, #255651, #39248 ) ;
#155854=LINE ( 'NONE', #100937, #234048 ) ;
#155882=ORIENTED_EDGE ( 'NONE', *, *, #135621, .F. ) ;
#155899=LINE ( 'NONE', #51594, #214955 ) ;
#155907=AXIS2_PLACEMENT_3D ( 'NONE', #73173, #152712, #133119 ) ;
#155974=DIRECTION ( 'NONE',  ( 0.000000000000000000, 1.000000000000000000, 0.000000000000000000 ) ) ;
#155978=ORIENTED_EDGE ( 'NONE', *, *, #104546, .F. ) ;
#155983=ORIENTED_EDGE ( 'NONE', *, *, #243211, .T. ) ;
#156024=CYLINDRICAL_SURFACE ( 'NONE', #105484, 0.1000000000000000472 ) ;
#156052=( BOUNDED_SURFACE ( )  B_SPLINE_SURFACE ( 3, 2, ( 
 ( #166357, #149352, #245861 ),
 ( #223708, #8534, #228868 ),
 ( #50206, #67218, #184594 ),
 ( #146728, #88036, #226264 ),
 ( #5937, #85459, #247127 ),
 ( #47630, #127200, #107623 ) ),
 .UNSPECIFIED., .F., .F., .F. ) 
 B_SPLINE_SURFACE_WITH_KNOTS ( ( 4, 2, 4 ),
 ( 3, 3 ),
 ( 3.141592653589793116, 3.926990816987241395, 4.712388980384689674 ),
 ( 0.000000000000000000, 1.000000000000000000 ),
 .UNSPECIFIED. ) 
 GEOMETRIC_REPRESENTATION_ITEM ( )  RATIONAL_B_SPLINE_SURFACE ( (
 ( 1.000000000000000000, 0.9238795325112820755, 1.000000000000000000),
 ( 1.000000000000000000, 0.9240297172248476132, 1.000000000000000000),
 ( 1.000000000000000000, 0.9038128468032942120, 1.000000000000000000),
 ( 1.000000000000000000, 0.8282379607655763198, 1.000000000000000000),
 ( 1.000000000000000000, 0.7727932973486544288, 1.000000000000000000),
 ( 1.000000000000000000, 0.7071067811865475727, 1.000000000000000000) ) ) 
 REPRESENTATION_ITEM ( '' )  SURFACE ( )  );
#156071=DIRECTION ( 'NONE',  ( 0.000000000000000000, 0.000000000000000000, -1.000000000000000000 ) ) ;
#156075=ORIENTED_EDGE ( 'NONE', *, *, #1970, .T. ) ;
#156090=DIRECTION ( 'NONE',  ( 0.000000000000000000, 0.000000000000000000, -1.000000000000000000 ) ) ;
#156092=DIRECTION ( 'NONE',  ( 0.7070776581708965169, 0.000000000000000000, 0.7071359030027827286 ) ) ;
#156156=CARTESIAN_POINT ( 'NONE',  ( 23.25000000000000000, 6.550000000011156231, -79.35000000000005116 ) ) ;
#156180=FACE_OUTER_BOUND ( 'NONE', #180309, .T. ) ;
#156188=AXIS2_PLACEMENT_3D ( 'NONE', #242235, #126133, #225223 ) ;
#156210=CARTESIAN_POINT ( 'NONE',  ( 21.04999999999999716, 10.72371711693665652, -79.17623960113832027 ) ) ;
#156244=DIRECTION ( 'NONE',  ( 1.000000000000000000, 0.000000000000000000, 0.000000000000000000 ) ) ;
#156279=DIRECTION ( 'NONE',  ( -1.000000000000000000, 0.000000000000000000, 0.000000000000000000 ) ) ;
#156285=EDGE_LOOP ( 'NONE', ( #80526, #138490, #50185, #63996 ) ) ;
#156298=DIRECTION ( 'NONE',  ( 1.000000000000000000, -7.304098846218134667E-16, -4.217023435051626718E-16 ) ) ;
#156308=FACE_OUTER_BOUND ( 'NONE', #157621, .T. ) ;
#156310=LINE ( 'NONE', #117156, #151793 ) ;
#156313=DIRECTION ( 'NONE',  ( -1.000000000000000000, -0.000000000000000000, 0.000000000000000000 ) ) ;
#156317=CARTESIAN_POINT ( 'NONE',  ( 18.50000000000000355, -9.421456145484233602, -74.24198208401919885 ) ) ;
#156339=CARTESIAN_POINT ( 'NONE',  ( -18.59999999999999787, -1.835859311432481045, -112.0044391687985694 ) ) ;
#156361=CIRCLE ( 'NONE', #118754, 0.1000000000000002554 ) ;
#156376=VERTEX_POINT ( 'NONE', #202347 ) ;
#156387=ADVANCED_FACE ( 'NONE', ( #21177 ), #221882, .T. ) ;
#156389=CARTESIAN_POINT ( 'NONE',  ( 18.50000000000000000, -9.419209763398098900, -74.24776946275900968 ) ) ;
#156421=EDGE_CURVE ( 'NONE', #140349, #89932, #87515, .T. ) ;
#156494=DIRECTION ( 'NONE',  ( 0.000000000000000000, 0.000000000000000000, -1.000000000000000000 ) ) ;
#156521=FACE_OUTER_BOUND ( 'NONE', #81354, .T. ) ;
#156523=DIRECTION ( 'NONE',  ( 0.000000000000000000, 0.000000000000000000, -1.000000000000000000 ) ) ;
#156538=EDGE_LOOP ( 'NONE', ( #117488, #131357, #14453 ) ) ;
#156545=EDGE_CURVE ( 'NONE', #39695, #109372, #164227, .T. ) ;
#156598=LINE ( 'NONE', #236089, #35633 ) ;
#156633=AXIS2_PLACEMENT_3D ( 'NONE', #83150, #46610, #63626 ) ;
#156635=ORIENTED_EDGE ( 'NONE', *, *, #256631, .T. ) ;
#156655=EDGE_CURVE ( 'NONE', #3373, #36418, #15734, .T. ) ;
#156656=VERTEX_POINT ( 'NONE', #253021 ) ;
#156659=CARTESIAN_POINT ( 'NONE',  ( 23.24999999999999645, 1.115600667400684642E-11, -100.5000000000000426 ) ) ;
#156666=AXIS2_PLACEMENT_3D ( 'NONE', #92160, #128732, #251218 ) ;
#156673=DIRECTION ( 'NONE',  ( 9.044546369203339308E-15, -0.7397360091702694929, -0.6728971962616898672 ) ) ;
#156679=DIRECTION ( 'NONE',  ( 0.000000000000000000, -1.265107689135680095E-16, 1.000000000000000000 ) ) ;
#156682=DIRECTION ( 'NONE',  ( 1.000000000000000000, 0.000000000000000000, 0.000000000000000000 ) ) ;
#156694=CARTESIAN_POINT ( 'NONE',  ( 23.24999999999999645, -2.099999999988846344, -100.5000000000000426 ) ) ;
#156699=ORIENTED_EDGE ( 'NONE', *, *, #101950, .T. ) ;
#156715=EDGE_CURVE ( 'NONE', #13140, #24943, #138190, .T. ) ;
#156723=CARTESIAN_POINT ( 'NONE',  ( 18.60000000000000142, -9.321008403350125704, -74.23593824907794669 ) ) ;
#156731=VECTOR ( 'NONE', #206555, 1000.000000000000000 ) ;
#156735=CARTESIAN_POINT ( 'NONE',  ( -23.15000000000000213, 2.000000000011154189, -87.27537807723794572 ) ) ;
#156764=AXIS2_PLACEMENT_3D ( 'NONE', #159689, #222190, #179270 ) ;
#156767=ADVANCED_FACE ( 'NONE', ( #44263 ), #219025, .F. ) ;
#156779=DIRECTION ( 'NONE',  ( -0.000000000000000000, 0.01283462868039629209, -0.9999176327611372095 ) ) ;
#156801=ORIENTED_EDGE ( 'NONE', *, *, #249567, .T. ) ;
#156808=EDGE_CURVE ( 'NONE', #143581, #11117, #210201, .T. ) ;
#156822=CARTESIAN_POINT ( 'NONE',  ( -20.00857864376270001, 9.150000000011157653, -88.25000000000005684 ) ) ;
#156831=DIRECTION ( 'NONE',  ( 1.000000000000000000, -0.000000000000000000, -0.000000000000000000 ) ) ;
#156873=CARTESIAN_POINT ( 'NONE',  ( 21.53752568622135044, 0.09897446127761702628, -60.21319212545145660 ) ) ;
#156888=AXIS2_PLACEMENT_3D ( 'NONE', #25269, #202605, #140038 ) ;
#156891=CIRCLE ( 'NONE', #52780, 0.5000000000000004441 ) ;
#156894=ORIENTED_EDGE ( 'NONE', *, *, #106254, .F. ) ;
#156901=CIRCLE ( 'NONE', #165237, 0.1000000000000028644 ) ;
#156920=LINE ( 'NONE', #117756, #84819 ) ;
#156940=ORIENTED_EDGE ( 'NONE', *, *, #204020, .F. ) ;
#156955=EDGE_CURVE ( 'NONE', #44654, #202405, #226941, .T. ) ;
#157006=TOROIDAL_SURFACE ( 'NONE', #256891, 4.149999999999999467, 0.1000000000000000056 ) ;
#157065=CIRCLE ( 'NONE', #177911, 0.09999999999999939493 ) ;
#157099=EDGE_CURVE ( 'NONE', #13417, #52066, #216145, .T. ) ;
#157100=CARTESIAN_POINT ( 'NONE',  ( -22.50485643085240284, -0.07878633906603056680, -55.25020506082763916 ) ) ;
#157117=ORIENTED_EDGE ( 'NONE', *, *, #119452, .F. ) ;
#157161=ORIENTED_EDGE ( 'NONE', *, *, #54710, .T. ) ;
#157177=LINE ( 'NONE', #153342, #183171 ) ;
#157179=DIRECTION ( 'NONE',  ( 0.000000000000000000, 4.336808689941893885E-15, 1.000000000000000000 ) ) ;
#157208=CARTESIAN_POINT ( 'NONE',  ( 20.94999999999999574, -11.48912529306490349, -70.10000000000005116 ) ) ;
#157224=CARTESIAN_POINT ( 'NONE',  ( 23.14999999999998437, -4.049999999988842525, -67.00000000000004263 ) ) ;
#157227=CARTESIAN_POINT ( 'NONE',  ( -18.59117750673696889, 10.33248238083634796, -106.0948465439131922 ) ) ;
#157243=AXIS2_PLACEMENT_3D ( 'NONE', #48028, #108016, #68903 ) ;
#157261=DIRECTION ( 'NONE',  ( 1.000000000000000000, 2.952720810173289112E-16, -0.000000000000000000 ) ) ;
#157269=CARTESIAN_POINT ( 'NONE',  ( -21.05000000000000071, 11.65000000001115232, -67.10000000000005116 ) ) ;
#157343=EDGE_CURVE ( 'NONE', #172403, #40125, #55450, .T. ) ;
#157348=VERTEX_POINT ( 'NONE', #132461 ) ;
#157367=LINE ( 'NONE', #199027, #230466 ) ;
#157370=ORIENTED_EDGE ( 'NONE', *, *, #177048, .T. ) ;
#157423=ORIENTED_EDGE ( 'NONE', *, *, #58752, .T. ) ;
#157439=CARTESIAN_POINT ( 'NONE',  ( -20.95000000000000284, 11.65000000001115232, -93.48519422934610645 ) ) ;
#157444=EDGE_LOOP ( 'NONE', ( #244616, #112224, #199043, #132033, #197668, #58572, #29634, #16360, #111228, #71134, #92808, #253069, #172293, #42477, #154140, #54885, #34466, #90279, #97889, #177193, #194821, #61102, #252374, #69948, #106256 ) ) ;
#157481=ORIENTED_EDGE ( 'NONE', *, *, #25039, .F. ) ;
#157497=DIRECTION ( 'NONE',  ( -0.000000000000000000, 0.000000000000000000, -1.000000000000000000 ) ) ;
#157506=AXIS2_PLACEMENT_3D ( 'NONE', #156822, #78517, #116388 ) ;
#157524=AXIS2_PLACEMENT_3D ( 'NONE', #176912, #119488, #236847 ) ;
#157584=CIRCLE ( 'NONE', #145056, 0.1000000000000028644 ) ;
#157585=SPHERICAL_SURFACE ( 'NONE', #81218, 0.1000000000000000056 ) ;
#157595=AXIS2_PLACEMENT_3D ( 'NONE', #197997, #44076, #61056 ) ;
#157608=CARTESIAN_POINT ( 'NONE',  ( 18.41789779300687968, -9.499999999988844479, -74.03206966635994490 ) ) ;
#157620=CARTESIAN_POINT ( 'NONE',  ( -21.05000000000000071, 11.60000000001115517, -93.57179676972454274 ) ) ;
#157621=EDGE_LOOP ( 'NONE', ( #192957, #64199, #86088, #76565 ) ) ;
#157706=DIRECTION ( 'NONE',  ( 0.000000000000000000, 1.000000000000000000, 0.000000000000000000 ) ) ;
#157722=AXIS2_PLACEMENT_3D ( 'NONE', #202330, #27590, #181504 ) ;
#157727=FACE_OUTER_BOUND ( 'NONE', #246074, .T. ) ;
#157739=CARTESIAN_POINT ( 'NONE',  ( 18.49999999999998934, 10.25000000001115552, -91.75000000000005684 ) ) ;
#157747=TOROIDAL_SURFACE ( 'NONE', #45259, 11.90000000000000213, 0.1000000000000000056 ) ;
#157778=AXIS2_PLACEMENT_3D ( 'NONE', #100309, #80748, #142022 ) ;
#157781=CARTESIAN_POINT ( 'NONE',  ( -18.59999999999999787, 5.900000000011102586, -77.21909976465646253 ) ) ;
#157784=DIRECTION ( 'NONE',  ( 0.000000000000000000, 0.01562499999998609446, -0.9998779222360101304 ) ) ;
#157793=FACE_OUTER_BOUND ( 'NONE', #97620, .T. ) ;
#157806=LINE ( 'NONE', #179907, #117583 ) ;
#157811=DIRECTION ( 'NONE',  ( 0.000000000000000000, 1.000000000000000000, 0.000000000000000000 ) ) ;
#157814=DIRECTION ( 'NONE',  ( -1.000000000000000000, 0.000000000000000000, 0.000000000000000000 ) ) ;
#157827=EDGE_CURVE ( 'NONE', #113878, #242523, #101796, .T. ) ;
#157828=CARTESIAN_POINT ( 'NONE',  ( -21.55000000000000426, 7.708578643773852157, -88.25000000000005684 ) ) ;
#157833=AXIS2_PLACEMENT_3D ( 'NONE', #138389, #19776, #142267 ) ;
#157915=DIRECTION ( 'NONE',  ( -1.000000000000000000, -2.952720810173289112E-16, 0.000000000000000000 ) ) ;
#157918=VECTOR ( 'NONE', #87701, 1000.000000000000000 ) ;
#158002=VECTOR ( 'NONE', #61514, 1000.000000000000000 ) ;
#158024=ORIENTED_EDGE ( 'NONE', *, *, #218446, .F. ) ;
#158026=EDGE_CURVE ( 'NONE', #21107, #50892, #93815, .T. ) ;
#158037=DIRECTION ( 'NONE',  ( 0.000000000000000000, 0.008583690987128059571, -0.9999631594459056361 ) ) ;
#158061=ADVANCED_FACE ( 'NONE', ( #150020 ), #131716, .T. ) ;
#158067=FACE_OUTER_BOUND ( 'NONE', #53179, .T. ) ;
#158085=VECTOR ( 'NONE', #50319, 1000.000000000000000 ) ;
#158109=ORIENTED_EDGE ( 'NONE', *, *, #161241, .F. ) ;
#158120=DIRECTION ( 'NONE',  ( 0.000000000000000000, -1.000000000000000000, 0.000000000000000000 ) ) ;
#158145=ORIENTED_EDGE ( 'NONE', *, *, #131124, .T. ) ;
#158161=EDGE_CURVE ( 'NONE', #183644, #133216, #2221, .T. ) ;
#158169=ORIENTED_EDGE ( 'NONE', *, *, #25923, .T. ) ;
#158213=CARTESIAN_POINT ( 'NONE',  ( 20.94999999999999929, -8.999999999988842703, -91.00603087734759811 ) ) ;
#158232=CARTESIAN_POINT ( 'NONE',  ( 18.49999999999999289, 11.65000000001115588, -100.5000000000000426 ) ) ;
#158265=DIRECTION ( 'NONE',  ( 1.000000000000000000, 0.000000000000000000, 0.000000000000000000 ) ) ;
#158330=EDGE_CURVE ( 'NONE', #77390, #163525, #2672, .T. ) ;
#158334=CARTESIAN_POINT ( 'NONE',  ( 18.59999999999999076, 6.450000000011156587, -77.01702717044007329 ) ) ;
#158386=EDGE_CURVE ( 'NONE', #127210, #29232, #27410, .T. ) ;
#158391=LINE ( 'NONE', #57947, #42088 ) ;
#158393=CARTESIAN_POINT ( 'NONE',  ( 18.59999999999999076, 5.950000000011100632, -77.30570230503489881 ) ) ;
#158400=AXIS2_PLACEMENT_3D ( 'NONE', #46714, #149708, #150969 ) ;
#158419=AXIS2_PLACEMENT_3D ( 'NONE', #15999, #193336, #215448 ) ;
#158458=ORIENTED_EDGE ( 'NONE', *, *, #220846, .T. ) ;
#158469=ADVANCED_FACE ( 'NONE', ( #10401 ), #147327, .T. ) ;
#158508=ORIENTED_EDGE ( 'NONE', *, *, #151543, .F. ) ;
#158522=FACE_OUTER_BOUND ( 'NONE', #85434, .T. ) ;
#158535=CARTESIAN_POINT ( 'NONE',  ( 23.14999999999999858, 1.115600667400684642E-11, -100.5000000000000426 ) ) ;
#158556=AXIS2_PLACEMENT_3D ( 'NONE', #177004, #199101, #256435 ) ;
#158593=AXIS2_PLACEMENT_3D ( 'NONE', #229028, #203025, #47789 ) ;
#158607=AXIS2_PLACEMENT_3D ( 'NONE', #128868, #130127, #227955 ) ;
#158608=CIRCLE ( 'NONE', #357, 0.1999999999999987899 ) ;
#158661=AXIS2_PLACEMENT_3D ( 'NONE', #204175, #189761, #223735 ) ;
#158669=EDGE_CURVE ( 'NONE', #37535, #129928, #52479, .T. ) ;
#158676=ORIENTED_EDGE ( 'NONE', *, *, #46695, .T. ) ;
#158709=CARTESIAN_POINT ( 'NONE',  ( 22.39999999999999503, 7.790779598384535376, -67.00000000000004263 ) ) ;
#158759=ORIENTED_EDGE ( 'NONE', *, *, #175193, .T. ) ;
#158776=CARTESIAN_POINT ( 'NONE',  ( 21.09551895715237180, 10.62143732717995270, -79.23712466590011161 ) ) ;
#158782=EDGE_CURVE ( 'NONE', #202894, #172095, #148308, .T. ) ;
#158784=AXIS2_PLACEMENT_3D ( 'NONE', #164895, #26687, #65788 ) ;
#158791=DIRECTION ( 'NONE',  ( 0.000000000000000000, -0.000000000000000000, -1.000000000000000000 ) ) ;
#158834=ADVANCED_FACE ( 'NONE', ( #227833 ), #190003, .T. ) ;
#158901=AXIS2_PLACEMENT_3D ( 'NONE', #216117, #221242, #257765 ) ;
#158926=DIRECTION ( 'NONE',  ( 1.000000000000000000, 0.000000000000000000, 0.000000000000000000 ) ) ;
#158936=ORIENTED_EDGE ( 'NONE', *, *, #230352, .F. ) ;
#158943=CARTESIAN_POINT ( 'NONE',  ( 18.52326479938708559, -9.642364444904341525, -107.2147574134056924 ) ) ;
#158944=ORIENTED_EDGE ( 'NONE', *, *, #256332, .F. ) ;
#158974=ORIENTED_EDGE ( 'NONE', *, *, #145880, .T. ) ;
#158987=VERTEX_POINT ( 'NONE', #178161 ) ;
#159032=EDGE_CURVE ( 'NONE', #232478, #103372, #69447, .T. ) ;
#159040=FACE_OUTER_BOUND ( 'NONE', #133406, .T. ) ;
#159049=LINE ( 'NONE', #68930, #100025 ) ;
#159073=TOROIDAL_SURFACE ( 'NONE', #79897, 7.800000000000000711, 0.1000000000000000056 ) ;
#159092=CARTESIAN_POINT ( 'NONE',  ( -23.25000000000000000, 1.115600667400684642E-11, -100.5000000000000426 ) ) ;
#159102=EDGE_CURVE ( 'NONE', #31603, #247198, #140141, .T. ) ;
#159134=CARTESIAN_POINT ( 'NONE',  ( -20.85000000000000142, 7.021664781911246322, -104.3335654018973315 ) ) ;
#159210=DIRECTION ( 'NONE',  ( 0.000000000000000000, -1.000000000000000000, 0.000000000000000000 ) ) ;
#159243=CARTESIAN_POINT ( 'NONE',  ( 20.94999999999999929, -9.499999999988844479, -90.60603087734760663 ) ) ;
#159252=ORIENTED_EDGE ( 'NONE', *, *, #241203, .F. ) ;
#159259=DIRECTION ( 'NONE',  ( 1.000000000000000000, 0.000000000000000000, 0.000000000000000000 ) ) ;
#159262=EDGE_LOOP ( 'NONE', ( #148411, #102949, #213191, #255674, #228501 ) ) ;
#159279=EDGE_CURVE ( 'NONE', #132550, #102379, #37069, .T. ) ;
#159304=AXIS2_PLACEMENT_3D ( 'NONE', #151124, #113269, #230661 ) ;
#159332=EDGE_CURVE ( 'NONE', #115296, #164855, #152855, .T. ) ;
#159402=VECTOR ( 'NONE', #57626, 1000.000000000000000 ) ;
#159406=ORIENTED_EDGE ( 'NONE', *, *, #134402, .F. ) ;
#159434=CARTESIAN_POINT ( 'NONE',  ( 21.13461538461538325, 8.885417037985616773, -79.35000000000005116 ) ) ;
#159435=ORIENTED_EDGE ( 'NONE', *, *, #197409, .T. ) ;
#159481=AXIS2_PLACEMENT_3D ( 'NONE', #136170, #106040, #1813 ) ;
#159502=DIRECTION ( 'NONE',  ( 0.000000000000000000, 0.000000000000000000, 1.000000000000000000 ) ) ;
#159503=ORIENTED_EDGE ( 'NONE', *, *, #245246, .F. ) ;
#159504=EDGE_CURVE ( 'NONE', #191668, #167725, #119437, .T. ) ;
#159508=DIRECTION ( 'NONE',  ( 1.000000000000000000, -0.000000000000000000, -0.000000000000000000 ) ) ;
#159513=ORIENTED_EDGE ( 'NONE', *, *, #251993, .F. ) ;
#159539=VERTEX_POINT ( 'NONE', #113390 ) ;
#159541=ORIENTED_EDGE ( 'NONE', *, *, #45261, .F. ) ;
#159560=CARTESIAN_POINT ( 'NONE',  ( -22.50000000000000000, 11.64976291804307884, -66.91119002361310208 ) ) ;
#159564=DIRECTION ( 'NONE',  ( 1.000000000000000000, 0.000000000000000000, 0.000000000000000000 ) ) ;
#159571=CIRCLE ( 'NONE', #26487, 0.1000000000000028644 ) ;
#159579=VECTOR ( 'NONE', #257279, 1000.000000000000000 ) ;
#159635=CARTESIAN_POINT ( 'NONE',  ( 20.94999999999999574, 1.835341550235569663, -78.55515129256302487 ) ) ;
#159655=CARTESIAN_POINT ( 'NONE',  ( 21.07954763557417266, 6.329290990048654919, -66.93412408138154035 ) ) ;
#159660=ORIENTED_EDGE ( 'NONE', *, *, #99960, .T. ) ;
#159689=CARTESIAN_POINT ( 'NONE',  ( -20.54999999999999716, -8.999999999988846255, -76.89396912265249284 ) ) ;
#159698=ORIENTED_EDGE ( 'NONE', *, *, #150518, .F. ) ;
#159702=ADVANCED_FACE ( 'NONE', ( #1110 ), #36446, .F. ) ;
#159712=DIRECTION ( 'NONE',  ( 0.000000000000000000, 0.000000000000000000, 1.000000000000000000 ) ) ;
#159743=ORIENTED_EDGE ( 'NONE', *, *, #123126, .F. ) ;
#159747=ORIENTED_EDGE ( 'NONE', *, *, #47166, .F. ) ;
#159754=CARTESIAN_POINT ( 'NONE',  ( -20.85000000000000142, 10.33248238083634440, -106.0948465439131922 ) ) ;
#159769=EDGE_LOOP ( 'NONE', ( #65250, #149289, #123926, #96932 ) ) ;
#159785=CIRCLE ( 'NONE', #151428, 0.1000000000000002831 ) ;
#159814=CYLINDRICAL_SURFACE ( 'NONE', #238987, 11.74999999999999645 ) ;
#159821=CARTESIAN_POINT ( 'NONE',  ( -20.54999999999999716, 1.115600667400684642E-11, -100.5000000000000426 ) ) ;
#159852=AXIS2_PLACEMENT_3D ( 'NONE', #177332, #15684, #235970 ) ;
#159891=DIRECTION ( 'NONE',  ( 0.000000000000000000, 0.9915357197604882655, -0.1298341882519793711 ) ) ;
#159901=ORIENTED_EDGE ( 'NONE', *, *, #27712, .T. ) ;
#159913=CARTESIAN_POINT ( 'NONE',  ( -22.37643362114956957, 0.09908137369253962323, -59.37421000604164334 ) ) ;
#159917=CARTESIAN_POINT ( 'NONE',  ( 21.98333005346336932, 1.115600667400684642E-11, -59.62592467094338389 ) ) ;
#159926=CARTESIAN_POINT ( 'NONE',  ( 20.94999999999999574, 6.350000000011161383, -76.84382208968317229 ) ) ;
#159927=CIRCLE ( 'NONE', #155829, 0.1000000000000028644 ) ;
#159928=DIRECTION ( 'NONE',  ( -1.000000000000000000, 0.000000000000000000, 0.000000000000000000 ) ) ;
#159933=AXIS2_PLACEMENT_3D ( 'NONE', #97684, #15647, #233402 ) ;
#159980=ORIENTED_EDGE ( 'NONE', *, *, #228719, .F. ) ;
#160032=PRODUCT_DEFINITION ( 'UNKNOWN', '', #202882, #40142 ) ;
#160046=LINE ( 'NONE', #218687, #238780 ) ;
#160065=CARTESIAN_POINT ( 'NONE',  ( -22.48479450179659977, 0.04699158119804078271, -55.35000155374843445 ) ) ;
#160070=LINE ( 'NONE', #102602, #10059 ) ;
#160101=CARTESIAN_POINT ( 'NONE',  ( 21.05000000000000071, -8.999999999988842703, -90.60603087734760663 ) ) ;
#160105=DIRECTION ( 'NONE',  ( 0.000000000000000000, 0.000000000000000000, 1.000000000000000000 ) ) ;
#160106=CARTESIAN_POINT ( 'NONE',  ( -21.14999999999999503, 11.75000000001115197, -73.91914724595881125 ) ) ;
#160119=CARTESIAN_POINT ( 'NONE',  ( 23.14999999999999858, -2.099999999988846344, -100.5000000000000426 ) ) ;
#160140=DIRECTION ( 'NONE',  ( -1.000000000000000000, 0.000000000000000000, 0.000000000000000000 ) ) ;
#160154=TOROIDAL_SURFACE ( 'NONE', #1709, 0.2000000000000000111, 0.1000000000000000056 ) ;
#160175=ORIENTED_EDGE ( 'NONE', *, *, #231462, .F. ) ;
#160222=ORIENTED_EDGE ( 'NONE', *, *, #79583, .T. ) ;
#160240=DIRECTION ( 'NONE',  ( 1.000000000000000000, -0.000000000000000000, -0.000000000000000000 ) ) ;
#160250=EDGE_LOOP ( 'NONE', ( #149318, #31584, #241804, #159513 ) ) ;
#160267=CIRCLE ( 'NONE', #56162, 0.09999999999999971412 ) ;
#160297=ORIENTED_EDGE ( 'NONE', *, *, #167076, .F. ) ;
#160298=CYLINDRICAL_SURFACE ( 'NONE', #35501, 0.09999999999999939493 ) ;
#160302=CARTESIAN_POINT ( 'NONE',  ( 22.24259225415828567, 0.09906588346399246292, -59.50806212943462725 ) ) ;
#160313=EDGE_CURVE ( 'NONE', #110538, #187394, #40794, .T. ) ;
#160340=ORIENTED_EDGE ( 'NONE', *, *, #156715, .F. ) ;
#160372=ORIENTED_EDGE ( 'NONE', *, *, #36266, .T. ) ;
#160373=DIRECTION ( 'NONE',  ( 1.000000000000000000, 0.000000000000000000, 0.000000000000000000 ) ) ;
#160374=DIRECTION ( 'NONE',  ( 1.000000000000000000, 0.000000000000000000, 0.000000000000000000 ) ) ;
#160377=DIRECTION ( 'NONE',  ( 7.304098846218134667E-16, -1.000000000000000000, 0.000000000000000000 ) ) ;
#160414=ORIENTED_EDGE ( 'NONE', *, *, #98244, .T. ) ;
#160424=DIRECTION ( 'NONE',  ( 0.000000000000000000, 0.000000000000000000, -1.000000000000000000 ) ) ;
#160445=CARTESIAN_POINT ( 'NONE',  ( -21.05000000000000071, -11.64999999998884306, -97.40000000000004832 ) ) ;
#160446=CARTESIAN_POINT ( 'NONE',  ( 18.57071067811864040, 10.17928932189250091, -88.35000000000003695 ) ) ;
#160447=DIRECTION ( 'NONE',  ( 0.000000000000000000, 0.000000000000000000, -1.000000000000000000 ) ) ;
#160458=CARTESIAN_POINT ( 'NONE',  ( -18.59999999999999787, 11.65000000001115232, -55.25000000000004974 ) ) ;
#160486=AXIS2_PLACEMENT_3D ( 'NONE', #18407, #156673, #91848 ) ;
#160493=VERTEX_POINT ( 'NONE', #150320 ) ;
#160544=ORIENTED_EDGE ( 'NONE', *, *, #229683, .T. ) ;
#160560=CARTESIAN_POINT ( 'NONE',  ( -21.05000000000000071, 6.257814610487270279, -66.90220970869124528 ) ) ;
#160583=DIRECTION ( 'NONE',  ( 0.000000000000000000, -0.9893560106964500722, 0.1455152366551550613 ) ) ;
#160617=CARTESIAN_POINT ( 'NONE',  ( 23.15000000000000213, -9.499999999988848032, -76.89396912265249284 ) ) ;
#160623=ORIENTED_EDGE ( 'NONE', *, *, #156955, .T. ) ;
#160663=ORIENTED_EDGE ( 'NONE', *, *, #182778, .F. ) ;
#160674=CARTESIAN_POINT ( 'NONE',  ( 18.39999999999999858, -9.499999999988842703, -107.1001893912220879 ) ) ;
#160680=ORIENTED_EDGE ( 'NONE', *, *, #61126, .F. ) ;
#160713=CIRCLE ( 'NONE', #223021, 12.97499999999999964 ) ;
#160731=DIRECTION ( 'NONE',  ( 0.000000000000000000, 0.000000000000000000, 1.000000000000000000 ) ) ;
#160752=CARTESIAN_POINT ( 'NONE',  ( -23.15000000000000213, 1.115600667400684642E-11, -87.62500000000005684 ) ) ;
#160798=ORIENTED_EDGE ( 'NONE', *, *, #182513, .F. ) ;
#160817=ORIENTED_EDGE ( 'NONE', *, *, #213695, .F. ) ;
#160839=FACE_OUTER_BOUND ( 'NONE', #157444, .T. ) ;
#160846=CIRCLE ( 'NONE', #202517, 4.000000000000003553 ) ;
#160881=VECTOR ( 'NONE', #43758, 1000.000000000000000 ) ;
#160885=DIRECTION ( 'NONE',  ( 0.000000000000000000, -1.000000000000000000, 0.000000000000000000 ) ) ;
#160901=CYLINDRICAL_SURFACE ( 'NONE', #40843, 4.000000000000003553 ) ;
#160918=FACE_OUTER_BOUND ( 'NONE', #232776, .T. ) ;
#160919=ORIENTED_EDGE ( 'NONE', *, *, #39947, .T. ) ;
#160934=DIRECTION ( 'NONE',  ( 1.000000000000000000, -0.000000000000000000, -0.000000000000000000 ) ) ;
#160983=AXIS2_PLACEMENT_3D ( 'NONE', #54891, #157915, #152760 ) ;
#161015=FACE_OUTER_BOUND ( 'NONE', #99899, .T. ) ;
#161024=CARTESIAN_POINT ( 'NONE',  ( 21.07189867249812210, 10.72498027010430377, -79.21245144227678736 ) ) ;
#161045=CARTESIAN_POINT ( 'NONE',  ( -20.00857864376270001, 9.150000000011157653, -79.35000000000005116 ) ) ;
#161048=AXIS2_PLACEMENT_3D ( 'NONE', #233348, #75556, #195505 ) ;
#161051=CARTESIAN_POINT ( 'NONE',  ( 23.14999999999999858, 4.813084112160680661, -78.94151775652387926 ) ) ;
#161100=ORIENTED_EDGE ( 'NONE', *, *, #88382, .F. ) ;
#161155=CIRCLE ( 'NONE', #256955, 6.258578643762696458 ) ;
#161163=EDGE_LOOP ( 'NONE', ( #94037, #183257, #209550, #249511 ) ) ;
#161226=ADVANCED_FACE ( 'NONE', ( #59862 ), #26888, .T. ) ;
#161241=EDGE_CURVE ( 'NONE', #103372, #241878, #203616, .T. ) ;
#161269=DIRECTION ( 'NONE',  ( 0.000000000000000000, -1.776356839400277286E-15, -1.000000000000000000 ) ) ;
#161304=ORIENTED_EDGE ( 'NONE', *, *, #75920, .F. ) ;
#161323=DIRECTION ( 'NONE',  ( 0.000000000000000000, -0.4999999999999949485, 0.8660254037844415942 ) ) ;
#161335=ORIENTED_EDGE ( 'NONE', *, *, #255197, .T. ) ;
#161337=DIRECTION ( 'NONE',  ( 0.000000000000000000, 0.000000000000000000, -1.000000000000000000 ) ) ;
#161340=ORIENTED_EDGE ( 'NONE', *, *, #192803, .F. ) ;
#161379=EDGE_CURVE ( 'NONE', #195188, #155038, #103819, .T. ) ;
#161418=ORIENTED_EDGE ( 'NONE', *, *, #235263, .F. ) ;
#161432=ORIENTED_EDGE ( 'NONE', *, *, #21090, .F. ) ;
#161434=DIRECTION ( 'NONE',  ( 0.000000000000000000, 0.1568667991644863147, 0.9876197685951252359 ) ) ;
#161449=ORIENTED_EDGE ( 'NONE', *, *, #181365, .T. ) ;
#161455=FACE_OUTER_BOUND ( 'NONE', #95099, .T. ) ;
#161495=ORIENTED_EDGE ( 'NONE', *, *, #255243, .T. ) ;
#161506=CARTESIAN_POINT ( 'NONE',  ( 21.14999999999999858, 1.115600667400684642E-11, -60.45934304829879835 ) ) ;
#161567=AXIS2_PLACEMENT_3D ( 'NONE', #125517, #225864, #244163 ) ;
#161579=EDGE_CURVE ( 'NONE', #59101, #203487, #3892, .T. ) ;
#161612=CARTESIAN_POINT ( 'NONE',  ( -18.59999999999999787, 9.350000000011156942, -79.25000000000004263 ) ) ;
#161620=DIRECTION ( 'NONE',  ( 1.000000000000000000, 0.000000000000000000, 0.000000000000000000 ) ) ;
#161648=LINE ( 'NONE', #179921, #168200 ) ;
#161657=CARTESIAN_POINT ( 'NONE',  ( -23.15000000000000213, 1.910280373842930812, -87.86863214480109718 ) ) ;
#161687=VERTEX_POINT ( 'NONE', #127623 ) ;
#161706=VECTOR ( 'NONE', #223152, 1000.000000000000000 ) ;
#161728=CARTESIAN_POINT ( 'NONE',  ( 20.85000000000000142, -1.835859311432481045, -112.0044391687985694 ) ) ;
#161729=ORIENTED_EDGE ( 'NONE', *, *, #252200, .T. ) ;
#161755=DIRECTION ( 'NONE',  ( -0.000000000000000000, -0.4791956752371546169, -0.8777080977375152360 ) ) ;
#161758=EDGE_LOOP ( 'NONE', ( #154133, #134259, #98207, #240898 ) ) ;
#161816=ORIENTED_EDGE ( 'NONE', *, *, #210086, .T. ) ;
#161818=FACE_OUTER_BOUND ( 'NONE', #41738, .T. ) ;
#161832=ORIENTED_EDGE ( 'NONE', *, *, #159279, .T. ) ;
#161869=CARTESIAN_POINT ( 'NONE',  ( -20.89878130938411616, 10.32747123227773045, -106.0774032850249711 ) ) ;
#161870=DIRECTION ( 'NONE',  ( 0.000000000000000000, -0.9876197685951252359, -0.1568667991644863424 ) ) ;
#161883=DIRECTION ( 'NONE',  ( 0.000000000000000000, 0.000000000000000000, 1.000000000000000000 ) ) ;
#161888=CARTESIAN_POINT ( 'NONE',  ( -21.05000000000000071, 1.115600667400684642E-11, -67.00000000000004263 ) ) ;
#161895=DIRECTION ( 'NONE',  ( 1.000000000000000000, 0.000000000000000000, 0.000000000000000000 ) ) ;
#161912=DIRECTION ( 'NONE',  ( 0.000000000000000000, 0.000000000000000000, -1.000000000000000000 ) ) ;
#161950=ORIENTED_EDGE ( 'NONE', *, *, #61470, .T. ) ;
#161972=LINE ( 'NONE', #103235, #71942 ) ;
#161992=DIRECTION ( 'NONE',  ( -0.000000000000000000, 0.000000000000000000, -1.000000000000000000 ) ) ;
#162017=VECTOR ( 'NONE', #59168, 1000.000000000000000 ) ;
#162031=AXIS2_PLACEMENT_3D ( 'NONE', #244111, #167192, #229704 ) ;
#162060=CIRCLE ( 'NONE', #32912, 0.09999999999999939493 ) ;
#162148=DIRECTION ( 'NONE',  ( 1.000000000000000000, 0.000000000000000000, -0.000000000000000000 ) ) ;
#162181=EDGE_CURVE ( 'NONE', #37535, #250224, #28241, .T. ) ;
#162183=DIRECTION ( 'NONE',  ( 1.000000000000000000, 0.000000000000000000, 0.000000000000000000 ) ) ;
#162197=EDGE_CURVE ( 'NONE', #83997, #231898, #71625, .T. ) ;
#162214=ADVANCED_FACE ( 'NONE', ( #12519 ), #92025, .T. ) ;
#162218=CARTESIAN_POINT ( 'NONE',  ( 21.14999999999999503, -0.09999999998884338825, -55.35042919245524473 ) ) ;
#162231=DIRECTION ( 'NONE',  ( 0.000000000000000000, 0.000000000000000000, -1.000000000000000000 ) ) ;
#162281=DIRECTION ( 'NONE',  ( 0.000000000000000000, 0.000000000000000000, -1.000000000000000000 ) ) ;
#162283=DIRECTION ( 'NONE',  ( 0.000000000000000000, 0.000000000000000000, 1.000000000000000000 ) ) ;
#162291=DIRECTION ( 'NONE',  ( 1.000000000000000000, 0.000000000000000000, 0.000000000000000000 ) ) ;
#162314=CARTESIAN_POINT ( 'NONE',  ( 21.09696443733127325, 10.72400988392963228, -79.23477752704826571 ) ) ;
#162382=CYLINDRICAL_SURFACE ( 'NONE', #181927, 0.09999999999999939493 ) ;
#162387=ORIENTED_EDGE ( 'NONE', *, *, #27039, .F. ) ;
#162404=DIRECTION ( 'NONE',  ( -1.000000000000000000, 0.000000000000000000, 0.000000000000000000 ) ) ;
#162421=DIRECTION ( 'NONE',  ( -1.000000000000000000, -3.265361837132813093E-16, 0.000000000000000000 ) ) ;
#162442=AXIS2_PLACEMENT_3D ( 'NONE', #165102, #6011, #227627 ) ;
#162476=CARTESIAN_POINT ( 'NONE',  ( -22.14074124539699895, 0.09905289585522827900, -59.60992214895627939 ) ) ;
#162483=EDGE_CURVE ( 'NONE', #210308, #130026, #74651, .T. ) ;
#162484=CARTESIAN_POINT ( 'NONE',  ( -21.05000000000000071, 1.835341550235567887, -78.55515129256302487 ) ) ;
#162487=CARTESIAN_POINT ( 'NONE',  ( -20.85000000000000142, -11.74999999998884448, -100.5000000000000426 ) ) ;
#162510=( NAMED_UNIT ( * ) PLANE_ANGLE_UNIT ( ) SI_UNIT ( $, .RADIAN. ) );
#162519=AXIS2_PLACEMENT_3D ( 'NONE', #161888, #125314, #27532 ) ;
#162530=ORIENTED_EDGE ( 'NONE', *, *, #101950, .F. ) ;
#162533=ORIENTED_EDGE ( 'NONE', *, *, #14581, .T. ) ;
#162543=EDGE_LOOP ( 'NONE', ( #3695, #249572, #127706, #113814, #153384 ) ) ;
#162547=CARTESIAN_POINT ( 'NONE',  ( 21.00023020733438273, 6.390869245278871347, -67.00000000000004263 ) ) ;
#162582=ORIENTED_EDGE ( 'NONE', *, *, #43645, .T. ) ;
#162588=DIRECTION ( 'NONE',  ( 0.000000000000000000, 1.000000000000000000, 0.000000000000000000 ) ) ;
#162598=CARTESIAN_POINT ( 'NONE',  ( -18.59999999999999787, -1.263275465206102233, -108.4018646667464481 ) ) ;
#162610=DIRECTION ( 'NONE',  ( 0.000000000000000000, -1.000000000000000000, 0.000000000000000000 ) ) ;
#162636=EDGE_CURVE ( 'NONE', #102720, #82676, #15756, .T. ) ;
#162664=CIRCLE ( 'NONE', #146079, 0.1999999999999996503 ) ;
#162668=ORIENTED_EDGE ( 'NONE', *, *, #151209, .F. ) ;
#162737=EDGE_CURVE ( 'NONE', #224643, #218145, #237106, .T. ) ;
#162740=ORIENTED_EDGE ( 'NONE', *, *, #237408, .F. ) ;
#162765=ORIENTED_EDGE ( 'NONE', *, *, #158330, .T. ) ;
#162789=CARTESIAN_POINT ( 'NONE',  ( -21.17356465864818205, 6.422803126252873973, -66.90108875898617669 ) ) ;
#162817=LINE ( 'NONE', #205764, #191817 ) ;
#162826=ORIENTED_EDGE ( 'NONE', *, *, #243245, .T. ) ;
#162830=CARTESIAN_POINT ( 'NONE',  ( -21.05000000000000071, 1.115600667400684642E-11, -67.00000000000004263 ) ) ;
#162846=AXIS2_PLACEMENT_3D ( 'NONE', #148117, #244634, #28200 ) ;
#162849=EDGE_CURVE ( 'NONE', #100804, #220045, #44284, .T. ) ;
#162865=EDGE_CURVE ( 'NONE', #38016, #237011, #226749, .T. ) ;
#162896=AXIS2_PLACEMENT_3D ( 'NONE', #222479, #240790, #43873 ) ;
#162925=CARTESIAN_POINT ( 'NONE',  ( -18.42554971533677843, -9.497159669426592288, -74.03982691354869417 ) ) ;
#162934=DIRECTION ( 'NONE',  ( -1.000000000000000000, -2.952720810173289112E-16, 0.000000000000000000 ) ) ;
#162946=ORIENTED_EDGE ( 'NONE', *, *, #191884, .F. ) ;
#162957=LINE ( 'NONE', #61270, #220016 ) ;
#162961=CARTESIAN_POINT ( 'NONE',  ( -21.05000000000000071, 1.736257131608553550, -78.56865232901755292 ) ) ;
#162983=B_SPLINE_CURVE_WITH_KNOTS ( 'NONE', 3,
 ( #68894, #168017, #166725, #84534, #24647, #105392, #104127 ),
 .UNSPECIFIED., .F., .F.,
 ( 4, 3, 4 ),
 ( 0.000000000000000000, 0.0007844235214594269838, 0.001767853679404345069 ),
 .UNSPECIFIED. ) ;
#162997=CARTESIAN_POINT ( 'NONE',  ( 21.05000000000000071, 5.000000000011153745, -88.59473398108696074 ) ) ;
#163024=DIRECTION ( 'NONE',  ( 0.000000000000000000, 1.734723475976757554E-14, 1.000000000000000000 ) ) ;
#163034=DIRECTION ( 'NONE',  ( 0.000000000000000000, -0.8777080977375132376, 0.4791956752371582251 ) ) ;
#163111=AXIS2_PLACEMENT_3D ( 'NONE', #52801, #72403, #150637 ) ;
#163124=CYLINDRICAL_SURFACE ( 'NONE', #169143, 0.1000000000000028644 ) ;
#163156=DIRECTION ( 'NONE',  ( 1.000000000000000000, 0.000000000000000000, 0.000000000000000000 ) ) ;
#163173=ORIENTED_EDGE ( 'NONE', *, *, #20913, .F. ) ;
#163220=DIRECTION ( 'NONE',  ( 1.000000000000000000, 0.000000000000000000, -0.000000000000000000 ) ) ;
#163227=VERTEX_POINT ( 'NONE', #122218 ) ;
#163249=CYLINDRICAL_SURFACE ( 'NONE', #105333, 0.8750000000000007772 ) ;
#163273=ORIENTED_EDGE ( 'NONE', *, *, #173862, .T. ) ;
#163282=EDGE_CURVE ( 'NONE', #208732, #240643, #83313, .T. ) ;
#163298=EDGE_CURVE ( 'NONE', #72835, #60863, #252405, .T. ) ;
#163325=EDGE_CURVE ( 'NONE', #169137, #223322, #248571, .T. ) ;
#163350=ORIENTED_EDGE ( 'NONE', *, *, #4562, .F. ) ;
#163388=EDGE_LOOP ( 'NONE', ( #95755, #48222, #188934, #180340 ) ) ;
#163490=LINE ( 'NONE', #26565, #27226 ) ;
#163491=DIRECTION ( 'NONE',  ( 0.000000000000000000, 0.000000000000000000, -1.000000000000000000 ) ) ;
#163506=ADVANCED_FACE ( 'NONE', ( #154641 ), #58371, .F. ) ;
#163525=VERTEX_POINT ( 'NONE', #159754 ) ;
#163546=CARTESIAN_POINT ( 'NONE',  ( -21.05000000000000071, 1.115649653272650466E-11, -104.5000000000000568 ) ) ;
#163577=AXIS2_PLACEMENT_3D ( 'NONE', #162218, #185607, #26549 ) ;
#163612=DIRECTION ( 'NONE',  ( -0.000000000000000000, -2.891205793294679805E-16, 1.000000000000000000 ) ) ;
#163660=ORIENTED_EDGE ( 'NONE', *, *, #67626, .T. ) ;
#163681=CARTESIAN_POINT ( 'NONE',  ( 23.24999999999999645, 1.115600667400684642E-11, -100.5000000000000426 ) ) ;
#163682=ORIENTED_EDGE ( 'NONE', *, *, #144522, .T. ) ;
#163687=AXIS2_PLACEMENT_3D ( 'NONE', #219881, #257662, #199044 ) ;
#163696=AXIS2_PLACEMENT_3D ( 'NONE', #115510, #56793, #93378 ) ;
#163721=B_SPLINE_CURVE_WITH_KNOTS ( 'NONE', 3,
 ( #222539, #123465, #183444, #4767, #58325, #119627, #38803, #118342 ),
 .UNSPECIFIED., .F., .F.,
 ( 4, 2, 2, 4 ),
 ( 0.000000000000000000, 0.0001094981963948479494, 0.0002189963927896958987, 0.0004379927855793917975 ),
 .UNSPECIFIED. ) ;
#163724=ORIENTED_EDGE ( 'NONE', *, *, #258032, .F. ) ;
#163745=CARTESIAN_POINT ( 'NONE',  ( -21.14999999999999858, -11.64999999998884483, -67.00000000000004263 ) ) ;
#163759=ADVANCED_FACE ( 'NONE', ( #249575 ), #87886, .T. ) ;
#163760=CARTESIAN_POINT ( 'NONE',  ( 21.05000000000000071, 8.776282895303632259, -75.55862899514100661 ) ) ;
#163766=CARTESIAN_POINT ( 'NONE',  ( -20.05000000000000426, 9.250000000011157297, -79.35000000000005116 ) ) ;
#163799=CARTESIAN_POINT ( 'NONE',  ( -20.94999999999999929, 1.115600667400684642E-11, -67.00000000000004263 ) ) ;
#163808=CARTESIAN_POINT ( 'NONE',  ( 20.95420533658165141, 10.54586447477073285, -74.56750602069328693 ) ) ;
#163812=EDGE_CURVE ( 'NONE', #125649, #189474, #223019, .T. ) ;
#163852=VERTEX_POINT ( 'NONE', #74817 ) ;
#163867=CARTESIAN_POINT ( 'NONE',  ( 23.24999999999997513, 11.75000000001116263, -93.48519422934610645 ) ) ;
#163885=CARTESIAN_POINT ( 'NONE',  ( -22.39999999999999858, 7.790779598384559357, -67.00000000000004263 ) ) ;
#163897=CARTESIAN_POINT ( 'NONE',  ( -21.14999999999999858, 11.75000000001115552, -73.78386566297820082 ) ) ;
#163907=FACE_OUTER_BOUND ( 'NONE', #53372, .T. ) ;
#163920=CIRCLE ( 'NONE', #255454, 0.1000000000000028644 ) ;
#163948=CIRCLE ( 'NONE', #51481, 0.09999999999999693856 ) ;
#163989=DIRECTION ( 'NONE',  ( 1.000000000000000000, 0.000000000000000000, 0.000000000000000000 ) ) ;
#163994=LINE ( 'NONE', #143116, #68923 ) ;
#164000=ADVANCED_FACE ( 'NONE', ( #103306 ), #79416, .F. ) ;
#164058=CARTESIAN_POINT ( 'NONE',  ( 18.46163235739467368, -9.480150806907140293, -107.1576105398775240 ) ) ;
#164063=ORIENTED_EDGE ( 'NONE', *, *, #6017, .T. ) ;
#164093=VECTOR ( 'NONE', #26005, 1000.000000000000000 ) ;
#164095=ORIENTED_EDGE ( 'NONE', *, *, #106748, .T. ) ;
#164113=ADVANCED_FACE ( 'NONE', ( #252770 ), #50365, .F. ) ;
#164128=EDGE_LOOP ( 'NONE', ( #149111, #186462, #140306, #120431, #177799, #221453, #239054, #252351, #83093, #67654, #129890 ) ) ;
#164137=DIRECTION ( 'NONE',  ( 0.000000000000000000, -1.776356839400188145E-15, 1.000000000000000000 ) ) ;
#164180=CARTESIAN_POINT ( 'NONE',  ( 18.49999999999999289, 10.49142135624846439, -91.85000000000003695 ) ) ;
#164181=ADVANCED_FACE ( 'NONE', ( #220075 ), #16760, .F. ) ;
#164187=VERTEX_POINT ( 'NONE', #983 ) ;
#164227=CIRCLE ( 'NONE', #214104, 11.70000000000000284 ) ;
#164314=DIRECTION ( 'NONE',  ( 1.000000000000000000, -0.000000000000000000, -0.000000000000000000 ) ) ;
#164321=AXIS2_PLACEMENT_3D ( 'NONE', #113999, #193559, #96971 ) ;
#164356=CARTESIAN_POINT ( 'NONE',  ( -18.59999999999999787, -1.736705739456431807, -112.0174225876237699 ) ) ;
#164385=ORIENTED_EDGE ( 'NONE', *, *, #41904, .T. ) ;
#164410=ADVANCED_FACE ( 'NONE', ( #149547 ), #170423, .T. ) ;
#164419=CARTESIAN_POINT ( 'NONE',  ( -20.89192007715127986, 10.32898536001801304, -106.0826683222764899 ) ) ;
#164468=EDGE_CURVE ( 'NONE', #60368, #152543, #92263, .T. ) ;
#164507=DIRECTION ( 'NONE',  ( 0.000000000000000000, 0.000000000000000000, 1.000000000000000000 ) ) ;
#164521=DIRECTION ( 'NONE',  ( -1.000000000000000000, 0.000000000000000000, 0.000000000000000000 ) ) ;
#164588=DIRECTION ( 'NONE',  ( 0.000000000000000000, -0.1298341882520022694, -0.9915357197604853789 ) ) ;
#164618=CYLINDRICAL_SURFACE ( 'NONE', #108370, 0.1000000000000028644 ) ;
#164653=CARTESIAN_POINT ( 'NONE',  ( -18.50000000000000000, 9.350000000011156942, -79.15000000000003411 ) ) ;
#164811=DIRECTION ( 'NONE',  ( 0.000000000000000000, 0.000000000000000000, -1.000000000000000000 ) ) ;
#164834=ORIENTED_EDGE ( 'NONE', *, *, #144665, .F. ) ;
#164849=DIRECTION ( 'NONE',  ( 3.469446951953498700E-14, -0.7899159663865300551, -0.6132151058540831201 ) ) ;
#164851=CARTESIAN_POINT ( 'NONE',  ( 20.90851465518106167, 10.32532329027886320, -106.0699343018359997 ) ) ;
#164855=VERTEX_POINT ( 'NONE', #28875 ) ;
#164875=CARTESIAN_POINT ( 'NONE',  ( 21.05933563467872105, 10.72452471209247626, -79.19364774895599624 ) ) ;
#164879=DIRECTION ( 'NONE',  ( 0.000000000000000000, -1.000000000000000000, 0.000000000000000000 ) ) ;
#164895=CARTESIAN_POINT ( 'NONE',  ( -23.25000000000000000, 4.350000000011156054, -88.15000000000004832 ) ) ;
#164896=CARTESIAN_POINT ( 'NONE',  ( -23.15000000000000213, 11.65000000001115588, -93.48519422934610645 ) ) ;
#164907=CARTESIAN_POINT ( 'NONE',  ( 22.49806830649814060, 11.64988965485023620, -66.92253568367453909 ) ) ;
#164916=ORIENTED_EDGE ( 'NONE', *, *, #50824, .F. ) ;
#164937=CIRCLE ( 'NONE', #169073, 0.1000000000000028644 ) ;
#164962=CARTESIAN_POINT ( 'NONE',  ( 21.05000000000000071, -11.64999999998883595, -97.40000000000004832 ) ) ;
#164998=VECTOR ( 'NONE', #199283, 1000.000000000000000 ) ;
#165002=ADVANCED_FACE ( 'NONE', ( #131774 ), #171592, .F. ) ;
#165044=ORIENTED_EDGE ( 'NONE', *, *, #88853, .F. ) ;
#165054=VERTEX_POINT ( 'NONE', #170957 ) ;
#165058=PRESENTATION_STYLE_ASSIGNMENT (( #5959 ) ) ;
#165083=DIRECTION ( 'NONE',  ( -0.7071067811865475727, -0.7071067811865475727, -0.000000000000000000 ) ) ;
#165084=EDGE_CURVE ( 'NONE', #187409, #13140, #157806, .T. ) ;
#165102=CARTESIAN_POINT ( 'NONE',  ( -20.85000000000000142, -1.164121893230052995, -108.4148480855716485 ) ) ;
#165146=LINE ( 'NONE', #163867, #224573 ) ;
#165164=PLANE ( 'NONE',  #118836 ) ;
#165172=CARTESIAN_POINT ( 'NONE',  ( 18.39999999999999858, -9.499999999988842703, -107.1001893912220879 ) ) ;
#165193=FACE_OUTER_BOUND ( 'NONE', #174127, .T. ) ;
#165237=AXIS2_PLACEMENT_3D ( 'NONE', #94518, #253590, #73715 ) ;
#165263=EDGE_LOOP ( 'NONE', ( #163350, #116229, #76251, #4915 ) ) ;
#165266=DIRECTION ( 'NONE',  ( 0.000000000000000000, 1.000000000000000000, 0.000000000000000000 ) ) ;
#165295=ORIENTED_EDGE ( 'NONE', *, *, #79042, .T. ) ;
#165304=CONICAL_SURFACE ( 'NONE', #152876, 4.049999999999998046, 0.7853981633974604915 ) ;
#165323=ADVANCED_FACE ( 'NONE', ( #90214 ), #133218, .F. ) ;
#165346=EDGE_CURVE ( 'NONE', #221121, #247770, #92625, .T. ) ;
#165347=CARTESIAN_POINT ( 'NONE',  ( 20.94999999999999574, 10.47338541492405994, -74.57865446424858646 ) ) ;
#165350=CARTESIAN_POINT ( 'NONE',  ( -23.25000000000000000, -1.835859311432481045, -112.0044391687985694 ) ) ;
#165383=DIRECTION ( 'NONE',  ( 1.000000000000000000, 0.000000000000000000, -0.000000000000000000 ) ) ;
#165393=ORIENTED_EDGE ( 'NONE', *, *, #140214, .T. ) ;
#165394=CARTESIAN_POINT ( 'NONE',  ( 21.13461538461538325, 8.885417037985616773, -79.35000000000005116 ) ) ;
#165417=DIRECTION ( 'NONE',  ( 1.000000000000000000, 0.000000000000000000, 0.000000000000000000 ) ) ;
#165419=FACE_OUTER_BOUND ( 'NONE', #243162, .T. ) ;
#165517=DIRECTION ( 'NONE',  ( -0.7071067811865389130, 8.659560562355038861E-17, -0.7071067811865561215 ) ) ;
#165518=DIRECTION ( 'NONE',  ( -1.000000000000000000, 0.000000000000000000, 0.000000000000000000 ) ) ;
#165533=ORIENTED_EDGE ( 'NONE', *, *, #193182, .F. ) ;
#165541=CARTESIAN_POINT ( 'NONE',  ( 21.05000000000000071, 5.000000000011153745, -79.40526601891313874 ) ) ;
#165547=DIRECTION ( 'NONE',  ( -1.836970198721029934E-16, 1.000000000000000000, 0.000000000000000000 ) ) ;
#165554=CARTESIAN_POINT ( 'NONE',  ( -21.64999999999999858, 7.250000000011148416, -79.25000000000004263 ) ) ;
#165589=CARTESIAN_POINT ( 'NONE',  ( 20.94999999999999929, 11.65000000001116298, -93.71613433702195550 ) ) ;
#165626=CARTESIAN_POINT ( 'NONE',  ( -18.49372193242250972, -9.442484523346742264, -107.2647812600345816 ) ) ;
#165635=EDGE_LOOP ( 'NONE', ( #249113, #83034, #244066, #75227, #177810 ) ) ;
#165683=CARTESIAN_POINT ( 'NONE',  ( 23.24999999999999289, 6.450000000011156587, -88.15000000000004832 ) ) ;
#165804=VECTOR ( 'NONE', #243038, 1000.000000000000000 ) ;
#165893=DIRECTION ( 'NONE',  ( 0.000000000000000000, -0.000000000000000000, 1.000000000000000000 ) ) ;
#165913=ORIENTED_EDGE ( 'NONE', *, *, #93029, .F. ) ;
#165935=CARTESIAN_POINT ( 'NONE',  ( -20.94684162602228028, 11.75000000001115374, -73.84164399907105292 ) ) ;
#165957=ORIENTED_EDGE ( 'NONE', *, *, #35205, .F. ) ;
#165975=EDGE_LOOP ( 'NONE', ( #256148, #240664 ) ) ;
#166056=VECTOR ( 'NONE', #49376, 1000.000000000000000 ) ;
#166085=DIRECTION ( 'NONE',  ( 0.000000000000000000, 0.000000000000000000, -1.000000000000000000 ) ) ;
#166130=CARTESIAN_POINT ( 'NONE',  ( -21.64999999999999858, 7.250000000011148416, -88.15000000000004832 ) ) ;
#166137=CARTESIAN_POINT ( 'NONE',  ( 21.05000000000000071, -11.74999999998883560, -69.90000000000004832 ) ) ;
#166138=ORIENTED_EDGE ( 'NONE', *, *, #157827, .T. ) ;
#166174=CARTESIAN_POINT ( 'NONE',  ( 19.97071067811865674, 11.72071067812981759, -91.70857864376274904 ) ) ;
#166180=LINE ( 'NONE', #44919, #156731 ) ;
#166181=DIRECTION ( 'NONE',  ( 1.000000000000000000, 0.000000000000000000, 0.000000000000000000 ) ) ;
#166182=AXIS2_PLACEMENT_3D ( 'NONE', #243394, #64758, #3492 ) ;
#166219=CARTESIAN_POINT ( 'NONE',  ( 22.57856590037848932, -0.004128330053174996891, -55.24994153732460944 ) ) ;
#166241=ORIENTED_EDGE ( 'NONE', *, *, #182222, .T. ) ;
#166250=ORIENTED_EDGE ( 'NONE', *, *, #92089, .F. ) ;
#166307=DIRECTION ( 'NONE',  ( 0.000000000000000000, 1.897661533703519897E-16, -1.000000000000000000 ) ) ;
#166316=VECTOR ( 'NONE', #202179, 1000.000000000000000 ) ;
#166354=CARTESIAN_POINT ( 'NONE',  ( -21.05000000000000071, 1.115600667400684642E-11, -100.5000000000000426 ) ) ;
#166357=CARTESIAN_POINT ( 'NONE',  ( 18.52928932188133970, 10.27928932189250055, -91.65000000000004832 ) ) ;
#166362=DIRECTION ( 'NONE',  ( -1.000000000000000000, 0.000000000000000000, 0.000000000000000000 ) ) ;
#166368=CIRCLE ( 'NONE', #195584, 4.300000000000039790 ) ;
#166376=CIRCLE ( 'NONE', #66394, 0.1000000000000028644 ) ;
#166392=DIRECTION ( 'NONE',  ( 0.000000000000000000, 0.000000000000000000, -1.000000000000000000 ) ) ;
#166394=CARTESIAN_POINT ( 'NONE',  ( 20.22516295850462598, 9.899364295460458152, -74.91006571209143772 ) ) ;
#166407=ORIENTED_EDGE ( 'NONE', *, *, #196709, .F. ) ;
#166423=AXIS2_PLACEMENT_3D ( 'NONE', #230951, #172283, #211371 ) ;
#166451=CIRCLE ( 'NONE', #49881, 0.09999999999999939493 ) ;
#166488=PLANE ( 'NONE',  #102332 ) ;
#166499=LINE ( 'NONE', #205573, #239603 ) ;
#166526=EDGE_CURVE ( 'NONE', #209971, #56225, #75870, .T. ) ;
#166541=CARTESIAN_POINT ( 'NONE',  ( -21.44999999999999929, 7.250000000011155521, -88.15000000000004832 ) ) ;
#166566=EDGE_CURVE ( 'NONE', #13993, #236185, #229987, .T. ) ;
#166571=DIRECTION ( 'NONE',  ( -1.000000000000000000, 0.000000000000000000, 0.000000000000000000 ) ) ;
#166573=EDGE_CURVE ( 'NONE', #11117, #164187, #113462, .T. ) ;
#166635=EDGE_LOOP ( 'NONE', ( #141918, #247422, #128360, #249958 ) ) ;
#166654=CARTESIAN_POINT ( 'NONE',  ( 21.05000000000000071, 1.115600667400684642E-11, -67.00000000000004263 ) ) ;
#166664=EDGE_LOOP ( 'NONE', ( #47654, #147865, #230434 ) ) ;
#166675=VERTEX_POINT ( 'NONE', #165683 ) ;
#166685=DIRECTION ( 'NONE',  ( -1.000000000000000000, -1.836970198721029934E-16, 0.000000000000000000 ) ) ;
#166692=ORIENTED_EDGE ( 'NONE', *, *, #31674, .T. ) ;
#166705=CARTESIAN_POINT ( 'NONE',  ( 21.03675099975491136, 8.875180032795967122, -79.32554213677809685 ) ) ;
#166725=CARTESIAN_POINT ( 'NONE',  ( 21.51976009735019346, 6.910458441670357388, -67.00000000000004263 ) ) ;
#166764=CARTESIAN_POINT ( 'NONE',  ( -23.15000000000000213, 1.115600667400684642E-11, -67.00000000000004263 ) ) ;
#166776=CIRCLE ( 'NONE', #158400, 0.09999999999999939493 ) ;
#166778=CARTESIAN_POINT ( 'NONE',  ( 21.05000000000000071, 10.60832956796507531, -74.59168501329543233 ) ) ;
#166807=EDGE_CURVE ( 'NONE', #187777, #59145, #138384, .T. ) ;
#166825=DIRECTION ( 'NONE',  ( 0.000000000000000000, 0.000000000000000000, -1.000000000000000000 ) ) ;
#166842=EDGE_CURVE ( 'NONE', #45318, #31293, #13519, .T. ) ;
#166860=ORIENTED_EDGE ( 'NONE', *, *, #65183, .F. ) ;
#166874=CARTESIAN_POINT ( 'NONE',  ( -23.15000000000000213, 1.910280373842936141, -79.63136785519898808 ) ) ;
#166905=DIRECTION ( 'NONE',  ( -0.000000000000000000, -0.8700118002898321601, 0.4930308989875230030 ) ) ;
#166939=ORIENTED_EDGE ( 'NONE', *, *, #194246, .T. ) ;
#166956=AXIS2_PLACEMENT_3D ( 'NONE', #53305, #165893, #36325 ) ;
#166964=DIRECTION ( 'NONE',  ( 0.000000000000000000, 0.000000000000000000, -1.000000000000000000 ) ) ;
#166980=ORIENTED_EDGE ( 'NONE', *, *, #183820, .F. ) ;
#166998=CARTESIAN_POINT ( 'NONE',  ( 19.75857864376269291, 11.65000000001116476, -91.75000000000005684 ) ) ;
#167016=ORIENTED_EDGE ( 'NONE', *, *, #66852, .T. ) ;
#167031=CARTESIAN_POINT ( 'NONE',  ( -18.59999999999999787, 11.65000000001115232, -88.25000000000005684 ) ) ;
#167036=DIRECTION ( 'NONE',  ( -0.000000000000000000, -0.000000000000000000, 1.000000000000000000 ) ) ;
#167044=CARTESIAN_POINT ( 'NONE',  ( -20.85000000000000142, -1.835859311432481045, -112.1044391687985780 ) ) ;
#167058=CYLINDRICAL_SURFACE ( 'NONE', #61872, 0.09999999999999939493 ) ;
#167059=AXIS2_PLACEMENT_3D ( 'NONE', #76733, #196679, #40213 ) ;
#167061=EDGE_CURVE ( 'NONE', #217530, #183920, #172625, .T. ) ;
#167076=EDGE_CURVE ( 'NONE', #62297, #201338, #186205, .T. ) ;
#167088=CARTESIAN_POINT ( 'NONE',  ( 23.15000000000000213, -8.663551401857999323, -90.97589888193273566 ) ) ;
#167123=LINE ( 'NONE', #66712, #48411 ) ;
#167126=AXIS2_PLACEMENT_3D ( 'NONE', #32415, #108074, #111938 ) ;
#167139=EDGE_LOOP ( 'NONE', ( #48455, #7100, #8527, #51047 ) ) ;
#167164=ADVANCED_FACE ( 'NONE', ( #212198 ), #10134, .T. ) ;
#167179=CIRCLE ( 'NONE', #154696, 0.09999999999999939493 ) ;
#167192=DIRECTION ( 'NONE',  ( 0.000000000000000000, 0.000000000000000000, 1.000000000000000000 ) ) ;
#167240=CIRCLE ( 'NONE', #71556, 11.80000000000000426 ) ;
#167265=ORIENTED_EDGE ( 'NONE', *, *, #217282, .F. ) ;
#167268=EDGE_CURVE ( 'NONE', #247975, #214743, #68344, .T. ) ;
#167274=EDGE_LOOP ( 'NONE', ( #182066, #237197, #43393, #255998 ) ) ;
#167291=CARTESIAN_POINT ( 'NONE',  ( -21.05000000000000071, 11.65000000001115588, -93.48519422934610645 ) ) ;
#167310=DIRECTION ( 'NONE',  ( 1.000000000000000000, -0.000000000000000000, -0.000000000000000000 ) ) ;
#167329=DIRECTION ( 'NONE',  ( -1.000000000000000000, 0.000000000000000000, 0.000000000000000000 ) ) ;
#167381=EDGE_CURVE ( 'NONE', #179279, #129546, #255100, .T. ) ;
#167393=CARTESIAN_POINT ( 'NONE',  ( 20.84999999999999432, -1.164121893230052995, -108.4148480855716485 ) ) ;
#167439=CARTESIAN_POINT ( 'NONE',  ( 20.94999999999999929, 10.29270135741298731, -105.9573618871519756 ) ) ;
#167457=VECTOR ( 'NONE', #133408, 1000.000000000000114 ) ;
#167462=EDGE_CURVE ( 'NONE', #106375, #4212, #28125, .T. ) ;
#167473=EDGE_LOOP ( 'NONE', ( #116608, #87975, #22152, #250621 ) ) ;
#167481=CARTESIAN_POINT ( 'NONE',  ( 23.14999999999999503, 6.450000000011156587, -55.25000000000004974 ) ) ;
#167491=PLANE ( 'NONE',  #169372 ) ;
#167494=AXIS2_PLACEMENT_3D ( 'NONE', #131577, #129024, #50727 ) ;
#167500=CARTESIAN_POINT ( 'NONE',  ( -20.64999999999999858, 2.000000000011154189, -87.27537807723794572 ) ) ;
#167585=EDGE_CURVE ( 'NONE', #55890, #118463, #34470, .T. ) ;
#167597=ORIENTED_EDGE ( 'NONE', *, *, #17504, .T. ) ;
#167609=PLANE ( 'NONE',  #71850 ) ;
#167618=ORIENTED_EDGE ( 'NONE', *, *, #47881, .F. ) ;
#167637=ORIENTED_EDGE ( 'NONE', *, *, #39485, .F. ) ;
#167655=LINE ( 'NONE', #171517, #117595 ) ;
#167663=DIRECTION ( 'NONE',  ( -1.000000000000000000, 0.000000000000000000, 0.000000000000000000 ) ) ;
#167683=VECTOR ( 'NONE', #71597, 1000.000000000000000 ) ;
#167693=CARTESIAN_POINT ( 'NONE',  ( -23.25000000000000000, 1.115600667400684642E-11, -104.4000000000000483 ) ) ;
#167695=DIRECTION ( 'NONE',  ( -1.000000000000000000, 0.000000000000000000, 0.000000000000000000 ) ) ;
#167703=TOROIDAL_SURFACE ( 'NONE', #63615, 0.2000000000000000111, 0.1000000000000000056 ) ;
#167719=DIRECTION ( 'NONE',  ( 0.000000000000000000, 0.000000000000000000, -1.000000000000000000 ) ) ;
#167725=VERTEX_POINT ( 'NONE', #200982 ) ;
#167729=DIRECTION ( 'NONE',  ( 1.301042606982683418E-14, -0.8660254037844330455, 0.5000000000000096589 ) ) ;
#167767=ORIENTED_EDGE ( 'NONE', *, *, #158161, .F. ) ;
#167772=DIRECTION ( 'NONE',  ( 1.000000000000000000, -0.000000000000000000, -0.000000000000000000 ) ) ;
#167784=ADVANCED_FACE ( 'NONE', ( #187856 ), #238633, .F. ) ;
#167808=VECTOR ( 'NONE', #44133, 1000.000000000000000 ) ;
#167835=DIRECTION ( 'NONE',  ( 1.000000000000000000, 0.000000000000000000, -0.000000000000000000 ) ) ;
#167840=ORIENTED_EDGE ( 'NONE', *, *, #68491, .T. ) ;
#167843=ORIENTED_EDGE ( 'NONE', *, *, #14562, .T. ) ;
#167879=FACE_OUTER_BOUND ( 'NONE', #185597, .T. ) ;
#167884=AXIS2_PLACEMENT_3D ( 'NONE', #187932, #107092, #54494 ) ;
#167983=EDGE_CURVE ( 'NONE', #87673, #17147, #135546, .T. ) ;
#167992=ORIENTED_EDGE ( 'NONE', *, *, #27988, .T. ) ;
#167996=TOROIDAL_SURFACE ( 'NONE', #34901, 0.2000000000000000111, 0.1000000000000000056 ) ;
#168017=CARTESIAN_POINT ( 'NONE',  ( 21.33487959338958362, 6.725558151922348848, -67.00000000000004263 ) ) ;
#168026=FACE_OUTER_BOUND ( 'NONE', #80792, .T. ) ;
#168053=DIRECTION ( 'NONE',  ( 0.000000000000000000, 0.000000000000000000, -1.000000000000000000 ) ) ;
#168074=CARTESIAN_POINT ( 'NONE',  ( 21.05000000000000071, 10.48459288120634270, -74.45671357058543549 ) ) ;
#168124=CARTESIAN_POINT ( 'NONE',  ( -21.07016717457011268, 1.115057211061726283E-11, -60.67905916189913995 ) ) ;
#168143=CARTESIAN_POINT ( 'NONE',  ( 23.15000000000000213, -8.999999999988844479, -76.89396912265249284 ) ) ;
#168148=CIRCLE ( 'NONE', #251288, 0.09999999999999939493 ) ;
#168185=CARTESIAN_POINT ( 'NONE',  ( 20.94999999999999929, 11.63687328911539787, -93.67824078667517540 ) ) ;
#168192=DIRECTION ( 'NONE',  ( -1.000000000000000000, -0.000000000000000000, 0.000000000000000000 ) ) ;
#168197=CARTESIAN_POINT ( 'NONE',  ( -18.59999999999999787, -1.162701749926853712, -75.00000000000004263 ) ) ;
#168200=VECTOR ( 'NONE', #2529, 1000.000000000000000 ) ;
#168203=EDGE_CURVE ( 'NONE', #250167, #202762, #63260, .T. ) ;
#168218=CIRCLE ( 'NONE', #189024, 7.800000000000001599 ) ;
#168220=DIRECTION ( 'NONE',  ( 0.000000000000000000, 0.000000000000000000, -1.000000000000000000 ) ) ;
#168297=AXIS2_PLACEMENT_3D ( 'NONE', #84322, #243450, #62254 ) ;
#168306=CARTESIAN_POINT ( 'NONE',  ( 23.14999999999999858, 6.650000000011155876, -79.35000000000005116 ) ) ;
#168312=EDGE_LOOP ( 'NONE', ( #34734, #140906, #6186, #225436, #6415, #59507 ) ) ;
#168313=CARTESIAN_POINT ( 'NONE',  ( -20.54999999999999716, 7.150000000011155876, -88.15000000000004832 ) ) ;
#168315=SPHERICAL_SURFACE ( 'NONE', #133243, 0.1000000000000000056 ) ;
#168330=CARTESIAN_POINT ( 'NONE',  ( -21.14999999999999858, 11.65000000001115588, -67.10000000000005116 ) ) ;
#168364=DIRECTION ( 'NONE',  ( 0.000000000000000000, 9.769962616701369667E-15, 1.000000000000000000 ) ) ;
#168367=CARTESIAN_POINT ( 'NONE',  ( -21.05000000000000071, -0.09999999998884338825, -55.35000000000004405 ) ) ;
#168374=AXIS2_PLACEMENT_3D ( 'NONE', #246639, #227075, #47137 ) ;
#168434=VECTOR ( 'NONE', #99687, 1000.000000000000227 ) ;
#168443=CARTESIAN_POINT ( 'NONE',  ( -21.05000000000000071, 14.05000000001115623, -72.51369507076104526 ) ) ;
#168447=ORIENTED_EDGE ( 'NONE', *, *, #172877, .T. ) ;
#168456=VERTEX_POINT ( 'NONE', #50555 ) ;
#168464=TOROIDAL_SURFACE ( 'NONE', #230782, 0.2000000000000000111, 0.1000000000000000056 ) ;
#168465=CARTESIAN_POINT ( 'NONE',  ( 21.05000000000000071, 1.115623935689868526E-11, -98.60000000000005116 ) ) ;
#168470=ORIENTED_EDGE ( 'NONE', *, *, #167381, .F. ) ;
#168515=AXIS2_PLACEMENT_3D ( 'NONE', #210431, #232576, #150459 ) ;
#168524=DIRECTION ( 'NONE',  ( 0.000000000000000000, -0.8068669527896844551, -0.5907332058517525963 ) ) ;
#168527=ADVANCED_FACE ( 'NONE', ( #216061 ), #34454, .F. ) ;
#168545=ORIENTED_EDGE ( 'NONE', *, *, #41796, .T. ) ;
#168549=EDGE_LOOP ( 'NONE', ( #37704, #153535, #65038, #142219, #254260, #235539, #145673, #125730, #189602, #145625, #90274 ) ) ;
#168553=DIRECTION ( 'NONE',  ( 1.000000000000000000, -0.000000000000000000, -0.000000000000000000 ) ) ;
#168593=CARTESIAN_POINT ( 'NONE',  ( -20.64999999999999858, 1.115600667400684642E-11, -100.5000000000000426 ) ) ;
#168657=EDGE_LOOP ( 'NONE', ( #140234, #222881, #161100, #80377 ) ) ;
#168669=CARTESIAN_POINT ( 'NONE',  ( -21.93642651522410247, 7.327166239336959208, -67.00000000000004263 ) ) ;
#168674=CARTESIAN_POINT ( 'NONE',  ( 20.95512820512820440, 8.876151316299269567, -79.15000000000004832 ) ) ;
#168705=LINE ( 'NONE', #90388, #196995 ) ;
#168749=DIRECTION ( 'NONE',  ( 1.000000000000000000, 0.000000000000000000, 0.000000000000000000 ) ) ;
#168790=ORIENTED_EDGE ( 'NONE', *, *, #147144, .T. ) ;
#168823=CARTESIAN_POINT ( 'NONE',  ( -21.05000000000000071, 6.540656951712399803, -67.00000000000004263 ) ) ;
#168864=VERTEX_POINT ( 'NONE', #99636 ) ;
#168880=CARTESIAN_POINT ( 'NONE',  ( -20.64999999999999858, 2.500000000011156409, -80.22462192276213955 ) ) ;
#168939=CARTESIAN_POINT ( 'NONE',  ( -21.59142135623730852, 7.850000000011158718, -88.15000000000004832 ) ) ;
#168957=EDGE_LOOP ( 'NONE', ( #253049, #61203, #119905, #74437 ) ) ;
#168965=CARTESIAN_POINT ( 'NONE',  ( -20.64999999999999858, 2.400000000011155432, -80.22462192276213955 ) ) ;
#168988=AXIS2_PLACEMENT_3D ( 'NONE', #126479, #207322, #168220 ) ;
#168989=DIRECTION ( 'NONE',  ( 0.000000000000000000, 0.000000000000000000, -1.000000000000000000 ) ) ;
#169004=ORIENTED_EDGE ( 'NONE', *, *, #244060, .T. ) ;
#169018=DIRECTION ( 'NONE',  ( -1.000000000000000000, -0.000000000000000000, 0.000000000000000000 ) ) ;
#169073=AXIS2_PLACEMENT_3D ( 'NONE', #95946, #153416, #114244 ) ;
#169077=CARTESIAN_POINT ( 'NONE',  ( 21.03670563405601968, 10.62482368933940258, -79.32554688620919592 ) ) ;
#169084=DIRECTION ( 'NONE',  ( 1.000000000000000000, -7.304098846218133681E-16, 4.607487905232622991E-31 ) ) ;
#169100=AXIS2_PLACEMENT_3D ( 'NONE', #92172, #132598, #133867 ) ;
#169113=ORIENTED_EDGE ( 'NONE', *, *, #116504, .T. ) ;
#169120=ORIENTED_EDGE ( 'NONE', *, *, #231932, .T. ) ;
#169124=DIRECTION ( 'NONE',  ( 1.000000000000000000, 0.000000000000000000, 0.000000000000000000 ) ) ;
#169137=VERTEX_POINT ( 'NONE', #97581 ) ;
#169139=ORIENTED_EDGE ( 'NONE', *, *, #116769, .F. ) ;
#169143=AXIS2_PLACEMENT_3D ( 'NONE', #186531, #101812, #82246 ) ;
#169149=CARTESIAN_POINT ( 'NONE',  ( -20.54999999999999716, 2.500000000011156409, -80.22462192276213955 ) ) ;
#169197=EDGE_LOOP ( 'NONE', ( #61884, #52255, #13980, #186814, #238846, #210593, #230200 ) ) ;
#169230=ORIENTED_EDGE ( 'NONE', *, *, #172415, .F. ) ;
#169233=EDGE_CURVE ( 'NONE', #169584, #58451, #38705, .T. ) ;
#169262=ORIENTED_EDGE ( 'NONE', *, *, #183820, .T. ) ;
#169324=AXIS2_PLACEMENT_3D ( 'NONE', #152143, #29635, #213357 ) ;
#169332=CIRCLE ( 'NONE', #198510, 0.09999999999999736877 ) ;
#169372=AXIS2_PLACEMENT_3D ( 'NONE', #246991, #10966, #189611 ) ;
#169380=DIRECTION ( 'NONE',  ( -1.000000000000000000, 7.304098846218134667E-16, 2.111765289898285610E-31 ) ) ;
#169396=ORIENTED_EDGE ( 'NONE', *, *, #39287, .F. ) ;
#169413=ORIENTED_EDGE ( 'NONE', *, *, #222561, .T. ) ;
#169432=DIRECTION ( 'NONE',  ( 2.952720810173289112E-16, -1.000000000000000000, 0.000000000000000000 ) ) ;
#169466=CYLINDRICAL_SURFACE ( 'NONE', #130448, 0.1000000000000000472 ) ;
#169478=AXIS2_PLACEMENT_3D ( 'NONE', #103464, #241715, #46073 ) ;
#169491=ORIENTED_EDGE ( 'NONE', *, *, #91088, .F. ) ;
#169506=CARTESIAN_POINT ( 'NONE',  ( -18.50000000000000000, -9.421290279512154697, -107.3238821790262847 ) ) ;
#169537=EDGE_CURVE ( 'NONE', #96642, #198075, #257601, .T. ) ;
#169561=ORIENTED_EDGE ( 'NONE', *, *, #160313, .F. ) ;
#169574=ADVANCED_FACE ( 'NONE', ( #15221 ), #156024, .F. ) ;
#169584=VERTEX_POINT ( 'NONE', #184535 ) ;
#169611=DIRECTION ( 'NONE',  ( 1.000000000000000000, 0.000000000000000000, 0.000000000000000000 ) ) ;
#169621=LINE ( 'NONE', #49622, #249982 ) ;
#169648=ORIENTED_EDGE ( 'NONE', *, *, #96205, .T. ) ;
#169708=DIRECTION ( 'NONE',  ( 1.000000000000000000, 7.304098846218134667E-16, -0.000000000000000000 ) ) ;
#169726=ORIENTED_EDGE ( 'NONE', *, *, #97630, .F. ) ;
#169731=DIRECTION ( 'NONE',  ( -0.000000000000000000, -1.000000000000000000, 6.308085367188393199E-16 ) ) ;
#169735=CIRCLE ( 'NONE', #157243, 4.300000000000039790 ) ;
#169748=VECTOR ( 'NONE', #142688, 1000.000000000000114 ) ;
#169802=ORIENTED_EDGE ( 'NONE', *, *, #78780, .F. ) ;
#169818=CARTESIAN_POINT ( 'NONE',  ( -23.25000000000000000, 1.115600667400684642E-11, -67.00000000000004263 ) ) ;
#169825=ORIENTED_EDGE ( 'NONE', *, *, #103898, .T. ) ;
#169838=DIRECTION ( 'NONE',  ( 0.000000000000000000, -0.5000000000000014433, 0.8660254037844378194 ) ) ;
#169844=ORIENTED_EDGE ( 'NONE', *, *, #194850, .T. ) ;
#169863=AXIS2_PLACEMENT_3D ( 'NONE', #235236, #159564, #20060 ) ;
#169866=EDGE_CURVE ( 'NONE', #70706, #114500, #243240, .T. ) ;
#169905=AXIS2_PLACEMENT_3D ( 'NONE', #49729, #144962, #204935 ) ;
#169910=ORIENTED_EDGE ( 'NONE', *, *, #25505, .F. ) ;
#169946=DIRECTION ( 'NONE',  ( 1.000000000000000000, 0.000000000000000000, -0.000000000000000000 ) ) ;
#169948=CARTESIAN_POINT ( 'NONE',  ( -21.51976009735018991, 6.910458441670358276, -67.00000000000004263 ) ) ;
#169959=EDGE_LOOP ( 'NONE', ( #216780, #138719, #95362, #146123 ) ) ;
#169972=ADVANCED_FACE ( 'NONE', ( #14920 ), #37063, .T. ) ;
#169999=CARTESIAN_POINT ( 'NONE',  ( -20.54999999999999716, 7.250000000011155521, -88.25000000000005684 ) ) ;
#170000=FACE_OUTER_BOUND ( 'NONE', #92429, .T. ) ;
#170024=FACE_BOUND ( 'NONE', #55869, .T. ) ;
#170027=AXIS2_PLACEMENT_3D ( 'NONE', #183550, #21913, #163989 ) ;
#170046=EDGE_LOOP ( 'NONE', ( #256156, #224216, #108545, #250058 ) ) ;
#170124=ORIENTED_EDGE ( 'NONE', *, *, #159102, .T. ) ;
#170149=ORIENTED_EDGE ( 'NONE', *, *, #130311, .T. ) ;
#170163=AXIS2_PLACEMENT_3D ( 'NONE', #13529, #115191, #194753 ) ;
#170172=CARTESIAN_POINT ( 'NONE',  ( -21.09610168723073187, 6.378955715235938406, -66.96641049310854044 ) ) ;
#170195=VERTEX_POINT ( 'NONE', #9459 ) ;
#170218=DIRECTION ( 'NONE',  ( 1.000000000000000000, 0.000000000000000000, -0.000000000000000000 ) ) ;
#170252=DIRECTION ( 'NONE',  ( 0.000000000000000000, 0.000000000000000000, -1.000000000000000000 ) ) ;
#170256=DIRECTION ( 'NONE',  ( 0.000000000000000000, 0.000000000000000000, -1.000000000000000000 ) ) ;
#170269=ORIENTED_EDGE ( 'NONE', *, *, #41112, .T. ) ;
#170277=DIRECTION ( 'NONE',  ( 1.000000000000000000, 0.000000000000000000, 0.000000000000000000 ) ) ;
#170284=DIRECTION ( 'NONE',  ( -3.265361837132813093E-16, 1.000000000000000000, 0.000000000000000000 ) ) ;
#170297=ORIENTED_EDGE ( 'NONE', *, *, #108665, .F. ) ;
#170333=DIRECTION ( 'NONE',  ( 1.000000000000000000, 0.000000000000000000, -0.000000000000000000 ) ) ;
#170336=CARTESIAN_POINT ( 'NONE',  ( 21.05543885634738643, 8.775771046858691804, -79.18438447071473263 ) ) ;
#170356=EDGE_LOOP ( 'NONE', ( #14574, #214695, #158759, #21660 ) ) ;
#170357=ORIENTED_EDGE ( 'NONE', *, *, #245037, .T. ) ;
#170360=AXIS2_PLACEMENT_3D ( 'NONE', #82037, #258095, #79490 ) ;
#170367=CIRCLE ( 'NONE', #74690, 7.720710678118678061 ) ;
#170392=CARTESIAN_POINT ( 'NONE',  ( -20.64999999999999858, 4.350000000011156054, -79.35000000000005116 ) ) ;
#170410=LINE ( 'NONE', #208214, #64770 ) ;
#170423=CYLINDRICAL_SURFACE ( 'NONE', #112939, 0.1000000000000028644 ) ;
#170495=LINE ( 'NONE', #208298, #222542 ) ;
#170523=CARTESIAN_POINT ( 'NONE',  ( -23.25000000000000000, 11.75000000001115552, -55.25000000000004974 ) ) ;
#170533=CARTESIAN_POINT ( 'NONE',  ( 18.59999999999999787, 1.115600667400684642E-11, -67.00000000000004263 ) ) ;
#170546=AXIS2_PLACEMENT_3D ( 'NONE', #131819, #70600, #229645 ) ;
#170562=VECTOR ( 'NONE', #124980, 1000.000000000000000 ) ;
#170563=EDGE_LOOP ( 'NONE', ( #42917, #176241, #146009 ) ) ;
#170577=EDGE_LOOP ( 'NONE', ( #98913, #59821, #46598, #49574 ) ) ;
#170645=EDGE_CURVE ( 'NONE', #164855, #60863, #160267, .T. ) ;
#170655=EDGE_CURVE ( 'NONE', #96043, #233701, #193904, .T. ) ;
#170687=EDGE_CURVE ( 'NONE', #247975, #187820, #219476, .T. ) ;
#170702=ORIENTED_EDGE ( 'NONE', *, *, #38220, .F. ) ;
#170703=ORIENTED_EDGE ( 'NONE', *, *, #120711, .F. ) ;
#170704=AXIS2_PLACEMENT_3D ( 'NONE', #157208, #195042, #140161 ) ;
#170723=EDGE_CURVE ( 'NONE', #75742, #56430, #189463, .T. ) ;
#170735=DIRECTION ( 'NONE',  ( 0.000000000000000000, 0.000000000000000000, -1.000000000000000000 ) ) ;
#170744=SPHERICAL_SURFACE ( 'NONE', #247473, 0.1000000000000000056 ) ;
#170745=ORIENTED_EDGE ( 'NONE', *, *, #145340, .F. ) ;
#170747=DIRECTION ( 'NONE',  ( 0.000000000000000000, 4.440892098500631684E-15, -1.000000000000000000 ) ) ;
#170798=CARTESIAN_POINT ( 'NONE',  ( -23.15000000000000213, -8.999999999988844479, -90.60603087734760663 ) ) ;
#170801=CARTESIAN_POINT ( 'NONE',  ( -20.85000000000000142, -11.74999999998884448, -97.60000000000005116 ) ) ;
#170809=ORIENTED_EDGE ( 'NONE', *, *, #47159, .T. ) ;
#170813=EDGE_LOOP ( 'NONE', ( #218428, #67719, #213417, #119133 ) ) ;
#170816=VERTEX_POINT ( 'NONE', #222399 ) ;
#170837=CARTESIAN_POINT ( 'NONE',  ( 21.05000000000000071, -1.849084418615859926, -78.65601052144717187 ) ) ;
#170847=CYLINDRICAL_SURFACE ( 'NONE', #45427, 0.09999999999999939493 ) ;
#170899=DIRECTION ( 'NONE',  ( -1.000000000000000000, -7.304098846218133681E-16, 4.217023435051677994E-16 ) ) ;
#170910=DIRECTION ( 'NONE',  ( 0.000000000000000000, -1.214306433183730130E-13, 1.000000000000000000 ) ) ;
#170931=AXIS2_PLACEMENT_3D ( 'NONE', #91007, #186271, #29793 ) ;
#170940=EDGE_CURVE ( 'NONE', #80974, #225893, #139550, .T. ) ;
#170957=CARTESIAN_POINT ( 'NONE',  ( 18.59999999999999432, 1.162701749949165642, -75.00000000000004263 ) ) ;
#170981=ORIENTED_EDGE ( 'NONE', *, *, #85531, .T. ) ;
#170983=ADVANCED_FACE ( 'NONE', ( #228858 ), #227563, .T. ) ;
#170995=ORIENTED_EDGE ( 'NONE', *, *, #171593, .T. ) ;
#171030=CIRCLE ( 'NONE', #204272, 0.1000000000000028644 ) ;
#171060=EDGE_LOOP ( 'NONE', ( #112849, #70892, #23883, #177316, #124231 ) ) ;
#171061=EDGE_CURVE ( 'NONE', #198610, #80091, #239126, .T. ) ;
#171106=AXIS2_PLACEMENT_3D ( 'NONE', #125025, #207129, #8921 ) ;
#171129=ORIENTED_EDGE ( 'NONE', *, *, #182149, .F. ) ;
#171142=CARTESIAN_POINT ( 'NONE',  ( 23.24999999999999289, -4.149999999988843058, -67.00000000000004263 ) ) ;
#171282=AXIS2_PLACEMENT_3D ( 'NONE', #42934, #177343, #198146 ) ;
#171350=EDGE_CURVE ( 'NONE', #38707, #208826, #52460, .T. ) ;
#171357=CYLINDRICAL_SURFACE ( 'NONE', #204070, 0.09999999999999939493 ) ;
#171375=DIRECTION ( 'NONE',  ( 1.000000000000000000, 0.000000000000000000, 0.000000000000000000 ) ) ;
#171377=VECTOR ( 'NONE', #7140, 1000.000000000000000 ) ;
#171390=EDGE_LOOP ( 'NONE', ( #131091, #87061, #133809, #248485 ) ) ;
#171406=AXIS2_PLACEMENT_3D ( 'NONE', #72821, #171934, #48085 ) ;
#171407=LINE ( 'NONE', #215615, #109739 ) ;
#171418=CARTESIAN_POINT ( 'NONE',  ( 21.05000000000000071, 11.65000000001116298, -67.00000000000004263 ) ) ;
#171421=CARTESIAN_POINT ( 'NONE',  ( 22.40000000000010516, 1.020245298088821341E-11, -55.24956710754111811 ) ) ;
#171476=EDGE_LOOP ( 'NONE', ( #174918, #172373, #204933, #131836 ) ) ;
#171485=ORIENTED_EDGE ( 'NONE', *, *, #65152, .T. ) ;
#171492=DIRECTION ( 'NONE',  ( 1.000000000000000000, -0.000000000000000000, -0.000000000000000000 ) ) ;
#171502=ORIENTED_EDGE ( 'NONE', *, *, #229538, .F. ) ;
#171517=CARTESIAN_POINT ( 'NONE',  ( -18.50000000000000000, 11.75000000001115197, -88.35000000000003695 ) ) ;
#171518=FACE_OUTER_BOUND ( 'NONE', #120300, .T. ) ;
#171526=CARTESIAN_POINT ( 'NONE',  ( 20.74897398619109268, 10.59569302167756888, -74.67931145625556155 ) ) ;
#171585=FACE_OUTER_BOUND ( 'NONE', #34365, .T. ) ;
#171592=TOROIDAL_SURFACE ( 'NONE', #92440, 0.9750000000000019762, 0.1000000000000000056 ) ;
#171593=EDGE_CURVE ( 'NONE', #67110, #189061, #81631, .T. ) ;
#171598=ADVANCED_FACE ( 'NONE', ( #120202 ), #62759, .F. ) ;
#171600=EDGE_CURVE ( 'NONE', #258086, #124815, #40671, .T. ) ;
#171604=CARTESIAN_POINT ( 'NONE',  ( 21.05000000000000071, 8.776282895303632259, -79.15000000000004832 ) ) ;
#171620=ADVANCED_FACE ( 'NONE', ( #183986 ), #52626, .T. ) ;
#171664=CARTESIAN_POINT ( 'NONE',  ( 23.14999999999999503, 11.65000000001116298, -79.15000000000004832 ) ) ;
#171673=EDGE_CURVE ( 'NONE', #5531, #220045, #40014, .T. ) ;
#171683=EDGE_CURVE ( 'NONE', #129928, #37535, #106589, .T. ) ;
#171699=CARTESIAN_POINT ( 'NONE',  ( 23.25000000000000000, -11.64999999998884483, -67.00000000000004263 ) ) ;
#171746=EDGE_LOOP ( 'NONE', ( #75619, #147562, #212126 ) ) ;
#171751=DIRECTION ( 'NONE',  ( 1.000000000000000000, 0.000000000000000000, 0.000000000000000000 ) ) ;
#171753=DIRECTION ( 'NONE',  ( -2.561896900575096011E-15, -0.5907332058517279494, 0.8068669527897025517 ) ) ;
#171778=VERTEX_POINT ( 'NONE', #167031 ) ;
#171788=CARTESIAN_POINT ( 'NONE',  ( 20.94999999999999929, 1.115600667400684642E-11, -100.5000000000000426 ) ) ;
#171817=DIRECTION ( 'NONE',  ( 1.000000000000000000, -0.000000000000000000, -0.000000000000000000 ) ) ;
#171819=CARTESIAN_POINT ( 'NONE',  ( -22.50000000000094147, 0.1008583691097610646, -55.25043287651063650 ) ) ;
#171822=DIRECTION ( 'NONE',  ( 0.000000000000000000, 1.000000000000000000, -6.308085367188393199E-16 ) ) ;
#171845=SPHERICAL_SURFACE ( 'NONE', #98799, 0.1000000000000000056 ) ;
#171857=EDGE_CURVE ( 'NONE', #77148, #219131, #148729, .T. ) ;
#171897=AXIS2_PLACEMENT_3D ( 'NONE', #72729, #130091, #208379 ) ;
#171907=ORIENTED_EDGE ( 'NONE', *, *, #182099, .F. ) ;
#171934=DIRECTION ( 'NONE',  ( -1.000000000000000000, -0.000000000000000000, -0.000000000000000000 ) ) ;
#171937=CARTESIAN_POINT ( 'NONE',  ( -20.96428641294214046, 11.75000000001149481, -93.67489317794102988 ) ) ;
#171945=CARTESIAN_POINT ( 'NONE',  ( 21.14999999999999858, 1.115600667400684642E-11, -55.35042919245524473 ) ) ;
#171965=LINE ( 'NONE', #113227, #22466 ) ;
#171967=CARTESIAN_POINT ( 'NONE',  ( -21.53699400384661899, 1.514529946271319711E-11, -60.21228820675978000 ) ) ;
#171972=CARTESIAN_POINT ( 'NONE',  ( -18.59999999999999787, 9.150000000011157653, -55.25000000000004974 ) ) ;
#171989=CIRCLE ( 'NONE', #59467, 0.09999999999999939493 ) ;
#172028=( BOUNDED_SURFACE ( )  B_SPLINE_SURFACE ( 3, 2, ( 
 ( #144224, #47695, #145517 ),
 ( #106378, #127251, #42573 ),
 ( #242053, #124690, #85515 ),
 ( #105074, #24320, #162547 ) ),
 .UNSPECIFIED., .F., .F., .F. ) 
 B_SPLINE_SURFACE_WITH_KNOTS ( ( 4, 4 ),
 ( 3, 3 ),
 ( 0.04058434257139475337, 0.04256401539001600232 ),
 ( 0.000000000000000000, 1.000000000000000000 ),
 .UNSPECIFIED. ) 
 GEOMETRIC_REPRESENTATION_ITEM ( )  RATIONAL_B_SPLINE_SURFACE ( (
 ( 1.000000000000000000, 0.7103081912008297749, 1.000000000000000000),
 ( 1.000000000000000000, 0.7104998333555460066, 1.000000000000000000),
 ( 1.000000000000000000, 0.7107238315755025626, 1.000000000000000000),
 ( 1.000000000000000000, 0.7110073749539292942, 1.000000000000000000) ) ) 
 REPRESENTATION_ITEM ( '' )  SURFACE ( )  );
#172033=ORIENTED_EDGE ( 'NONE', *, *, #15350, .F. ) ;
#172036=CARTESIAN_POINT ( 'NONE',  ( 18.46082813848004989, -9.480749650896276748, -74.08437010271569534 ) ) ;
#172051=AXIS2_PLACEMENT_3D ( 'NONE', #236353, #35622, #56411 ) ;
#172065=AXIS2_PLACEMENT_3D ( 'NONE', #146515, #143956, #147834 ) ;
#172066=ORIENTED_EDGE ( 'NONE', *, *, #155300, .T. ) ;
#172095=VERTEX_POINT ( 'NONE', #200688 ) ;
#172098=DIRECTION ( 'NONE',  ( 0.000000000000000000, -1.000000000000000000, 0.000000000000000000 ) ) ;
#172112=AXIS2_PLACEMENT_3D ( 'NONE', #87801, #206491, #108677 ) ;
#172124=DIRECTION ( 'NONE',  ( 1.000000000000000000, -0.000000000000000000, -0.000000000000000000 ) ) ;
#172149=AXIS2_PLACEMENT_3D ( 'NONE', #86678, #188376, #123272 ) ;
#172159=FACE_OUTER_BOUND ( 'NONE', #134383, .T. ) ;
#172237=DIRECTION ( 'NONE',  ( -0.000000000000000000, -0.000000000000000000, 1.000000000000000000 ) ) ;
#172246=ORIENTED_EDGE ( 'NONE', *, *, #55565, .T. ) ;
#172250=CARTESIAN_POINT ( 'NONE',  ( 20.12500000000000000, 9.750000000011153745, -88.15000000000004832 ) ) ;
#172252=AXIS2_PLACEMENT_3D ( 'NONE', #125888, #26834, #202865 ) ;
#172283=DIRECTION ( 'NONE',  ( 0.000000000000000000, -0.5000000000000004441, -0.8660254037844384856 ) ) ;
#172293=ORIENTED_EDGE ( 'NONE', *, *, #25923, .F. ) ;
#172363=AXIS2_PLACEMENT_3D ( 'NONE', #152629, #16950, #211288 ) ;
#172365=DIRECTION ( 'NONE',  ( 0.000000000000000000, -0.9915357197604792727, 0.1298341882520473722 ) ) ;
#172373=ORIENTED_EDGE ( 'NONE', *, *, #163812, .F. ) ;
#172379=ORIENTED_EDGE ( 'NONE', *, *, #140521, .F. ) ;
#172389=AXIS2_PLACEMENT_3D ( 'NONE', #91781, #209148, #30544 ) ;
#172403=VERTEX_POINT ( 'NONE', #97378 ) ;
#172412=EDGE_CURVE ( 'NONE', #29232, #12856, #44630, .T. ) ;
#172415=EDGE_CURVE ( 'NONE', #197986, #36418, #61197, .T. ) ;
#172438=LINE ( 'NONE', #52428, #69184 ) ;
#172455=EDGE_CURVE ( 'NONE', #252694, #137777, #157065, .T. ) ;
#172461=CIRCLE ( 'NONE', #55668, 0.09999999999999892308 ) ;
#172468=AXIS2_PLACEMENT_3D ( 'NONE', #103321, #21268, #142457 ) ;
#172469=EDGE_LOOP ( 'NONE', ( #147840, #149538, #77541, #165957 ) ) ;
#172510=ORIENTED_EDGE ( 'NONE', *, *, #148500, .F. ) ;
#172561=CARTESIAN_POINT ( 'NONE',  ( -23.25000000000000000, 4.150000000011156764, -79.35000000000005116 ) ) ;
#172575=FACE_OUTER_BOUND ( 'NONE', #142491, .T. ) ;
#172618=LINE ( 'NONE', #154337, #23238 ) ;
#172625=CIRCLE ( 'NONE', #60120, 0.09999999999999867328 ) ;
#172632=PLANE ( 'NONE',  #193078 ) ;
#172682=CARTESIAN_POINT ( 'NONE',  ( 18.59999999999999787, -1.835859311432481045, -112.0044391687985694 ) ) ;
#172812=FACE_OUTER_BOUND ( 'NONE', #24316, .T. ) ;
#172815=AXIS2_PLACEMENT_3D ( 'NONE', #118674, #160377, #179927 ) ;
#172818=CARTESIAN_POINT ( 'NONE',  ( 21.05000000000000071, 5.000000000011153745, -79.40526601891313874 ) ) ;
#172872=AXIS2_PLACEMENT_3D ( 'NONE', #62253, #182208, #24436 ) ;
#172877=EDGE_CURVE ( 'NONE', #60863, #51379, #210649, .T. ) ;
#172888=DIRECTION ( 'NONE',  ( 1.000000000000000000, -0.000000000000000000, -0.000000000000000000 ) ) ;
#172926=ORIENTED_EDGE ( 'NONE', *, *, #178984, .T. ) ;
#172951=FACE_OUTER_BOUND ( 'NONE', #44418, .T. ) ;
#172970=EDGE_LOOP ( 'NONE', ( #17550, #230536, #43653, #209194 ) ) ;
#172979=EDGE_LOOP ( 'NONE', ( #238474, #125968, #60336, #190593 ) ) ;
#173000=EDGE_CURVE ( 'NONE', #24899, #113044, #39996, .T. ) ;
#173001=DIRECTION ( 'NONE',  ( 1.000000000000000000, 0.000000000000000000, 0.000000000000000000 ) ) ;
#173024=DIRECTION ( 'NONE',  ( 1.000000000000000000, -0.000000000000000000, -0.000000000000000000 ) ) ;
#173031=DIRECTION ( 'NONE',  ( 0.000000000000000000, 0.000000000000000000, 1.000000000000000000 ) ) ;
#173052=TOROIDAL_SURFACE ( 'NONE', #60567, 2.100000000000002309, 0.1000000000000000056 ) ;
#173054=DIRECTION ( 'NONE',  ( 0.000000000000000000, 0.000000000000000000, 1.000000000000000000 ) ) ;
#173069=ADVANCED_FACE ( 'NONE', ( #179816 ), #235960, .T. ) ;
#173095=DIRECTION ( 'NONE',  ( -3.265361837132813093E-16, 1.000000000000000000, 0.000000000000000000 ) ) ;
#173144=ORIENTED_EDGE ( 'NONE', *, *, #193337, .T. ) ;
#173188=EDGE_CURVE ( 'NONE', #168456, #201338, #127641, .T. ) ;
#173225=CARTESIAN_POINT ( 'NONE',  ( 21.30000000000002558, 1.115600667400684642E-11, -67.00000000000004263 ) ) ;
#173268=ORIENTED_EDGE ( 'NONE', *, *, #258032, .T. ) ;
#173285=CARTESIAN_POINT ( 'NONE',  ( 20.94999999999999929, -11.64999999998883595, -100.5000000000000284 ) ) ;
#173305=DIRECTION ( 'NONE',  ( 1.000000000000000000, 0.000000000000000000, 0.000000000000000000 ) ) ;
#173318=DIRECTION ( 'NONE',  ( 0.000000000000000000, -0.000000000000000000, 1.000000000000000000 ) ) ;
#173320=CIRCLE ( 'NONE', #81637, 0.1000000000000028644 ) ;
#173330=VERTEX_POINT ( 'NONE', #137771 ) ;
#173355=ORIENTED_EDGE ( 'NONE', *, *, #21090, .T. ) ;
#173365=CIRCLE ( 'NONE', #77604, 0.1000000000000028644 ) ;
#173379=ORIENTED_EDGE ( 'NONE', *, *, #59327, .T. ) ;
#173391=CARTESIAN_POINT ( 'NONE',  ( -22.39999999999999858, 11.75000000001115552, -66.90000000000004832 ) ) ;
#173400=FACE_OUTER_BOUND ( 'NONE', #58577, .T. ) ;
#173405=DIRECTION ( 'NONE',  ( 0.000000000000000000, 0.000000000000000000, -1.000000000000000000 ) ) ;
#173411=DIRECTION ( 'NONE',  ( -0.000000000000000000, 0.9274965247785350586, 0.3738317757009704811 ) ) ;
#173429=CARTESIAN_POINT ( 'NONE',  ( 18.59999999999999076, 6.650000000011155876, -88.25000000000005684 ) ) ;
#173439=CIRCLE ( 'NONE', #27672, 0.1000000000000028644 ) ;
#173446=ORIENTED_EDGE ( 'NONE', *, *, #1970, .F. ) ;
#173458=CARTESIAN_POINT ( 'NONE',  ( 20.95512820512820440, 10.62384868372303615, -74.66491356908764487 ) ) ;
#173509=CARTESIAN_POINT ( 'NONE',  ( 18.59999999999999432, -1.162701749926853712, -75.00000000000004263 ) ) ;
#173523=DIRECTION ( 'NONE',  ( -3.265361837132813586E-16, 1.000000000000000000, 0.000000000000000000 ) ) ;
#173540=AXIS2_PLACEMENT_3D ( 'NONE', #219821, #85412, #41225 ) ;
#173562=AXIS2_PLACEMENT_3D ( 'NONE', #205115, #162183, #241695 ) ;
#173586=VECTOR ( 'NONE', #61797, 1000.000000000000000 ) ;
#173594=LINE ( 'NONE', #117417, #122491 ) ;
#173617=DIRECTION ( 'NONE',  ( 0.000000000000000000, 0.5000000000000078826, -0.8660254037844340447 ) ) ;
#173629=CARTESIAN_POINT ( 'NONE',  ( 21.14999999999999858, 1.115486826172573664E-11, -60.45934304829879835 ) ) ;
#173642=CIRCLE ( 'NONE', #52752, 11.80000000000000426 ) ;
#173654=CARTESIAN_POINT ( 'NONE',  ( -18.47690164073607022, -9.464844538001083052, -107.2013809398361843 ) ) ;
#173658=VECTOR ( 'NONE', #251997, 1000.000000000000000 ) ;
#173696=ORIENTED_EDGE ( 'NONE', *, *, #43524, .F. ) ;
#173700=VERTEX_POINT ( 'NONE', #167044 ) ;
#173722=ORIENTED_EDGE ( 'NONE', *, *, #176930, .T. ) ;
#173728=CARTESIAN_POINT ( 'NONE',  ( 18.57071067811864040, 10.17928932189250091, -88.25000000000005684 ) ) ;
#173733=DIRECTION ( 'NONE',  ( 0.000000000000000000, 0.000000000000000000, -1.000000000000000000 ) ) ;
#173738=CARTESIAN_POINT ( 'NONE',  ( 20.94999999999999929, 6.846123162363745074, -104.2377262668499043 ) ) ;
#173742=VECTOR ( 'NONE', #12640, 1000.000000000000114 ) ;
#173862=EDGE_CURVE ( 'NONE', #127795, #106375, #115509, .T. ) ;
#173902=AXIS2_PLACEMENT_3D ( 'NONE', #41439, #182220, #160105 ) ;
#173905=ORIENTED_EDGE ( 'NONE', *, *, #137171, .F. ) ;
#173909=ORIENTED_EDGE ( 'NONE', *, *, #156808, .T. ) ;
#173919=ADVANCED_FACE ( 'NONE', ( #252950 ), #96433, .F. ) ;
#173925=DIRECTION ( 'NONE',  ( 1.000000000000000000, 0.000000000000000000, 0.000000000000000000 ) ) ;
#173932=EDGE_CURVE ( 'NONE', #53335, #176751, #227962, .T. ) ;
#173933=DIRECTION ( 'NONE',  ( 1.000000000000000000, 0.000000000000000000, 0.000000000000000000 ) ) ;
#173937=CARTESIAN_POINT ( 'NONE',  ( -20.64999999999999858, 7.250000000011155521, -79.25000000000004263 ) ) ;
#173956=CIRCLE ( 'NONE', #215583, 0.1000000000000004496 ) ;
#173966=EDGE_LOOP ( 'NONE', ( #188792, #75825, #147803, #67466 ) ) ;
#173983=AXIS2_PLACEMENT_3D ( 'NONE', #244535, #204121, #142849 ) ;
#173985=DIRECTION ( 'NONE',  ( -0.000000000000000000, 0.000000000000000000, 1.000000000000000000 ) ) ;
#173986=DIRECTION ( 'NONE',  ( 0.000000000000000000, -0.000000000000000000, 1.000000000000000000 ) ) ;
#173994=FACE_OUTER_BOUND ( 'NONE', #167274, .T. ) ;
#174028=FACE_OUTER_BOUND ( 'NONE', #119113, .T. ) ;
#174038=CARTESIAN_POINT ( 'NONE',  ( 18.59999999999999076, 6.650000000011155876, -88.35000000000003695 ) ) ;
#174063=FACE_OUTER_BOUND ( 'NONE', #111389, .T. ) ;
#174096=FACE_OUTER_BOUND ( 'NONE', #213379, .T. ) ;
#174124=CARTESIAN_POINT ( 'NONE',  ( -22.39999999999999858, -0.1008583690875579364, -55.25043287651065782 ) ) ;
#174127=EDGE_LOOP ( 'NONE', ( #241015, #216855, #102504, #239769 ) ) ;
#174128=DIRECTION ( 'NONE',  ( 0.000000000000000000, 1.000000000000000000, 0.000000000000000000 ) ) ;
#174137=DIRECTION ( 'NONE',  ( 0.000000000000000000, 0.000000000000000000, -1.000000000000000000 ) ) ;
#174148=CIRCLE ( 'NONE', #124047, 11.80000000000000426 ) ;
#174155=EDGE_CURVE ( 'NONE', #130783, #237011, #169735, .T. ) ;
#174170=FACE_OUTER_BOUND ( 'NONE', #238831, .T. ) ;
#174189=VERTEX_POINT ( 'NONE', #253921 ) ;
#174199=ORIENTED_EDGE ( 'NONE', *, *, #162181, .F. ) ;
#174201=CARTESIAN_POINT ( 'NONE',  ( 22.39999999999999858, 7.790779598384538929, -66.90000000000004832 ) ) ;
#174234=EDGE_LOOP ( 'NONE', ( #190898, #57575, #232361, #170995 ) ) ;
#174237=CARTESIAN_POINT ( 'NONE',  ( -18.57399277249657032, 10.33112638556969465, -106.0901228926975222 ) ) ;
#174241=EDGE_CURVE ( 'NONE', #4255, #85481, #232259, .T. ) ;
#174249=EDGE_CURVE ( 'NONE', #75011, #229956, #99119, .T. ) ;
#174287=CIRCLE ( 'NONE', #70223, 0.09999999999999781286 ) ;
#174288=( BOUNDED_SURFACE ( )  B_SPLINE_SURFACE ( 3, 2, ( 
 ( #69718, #188364, #231361 ),
 ( #149259, #50126, #52693 ),
 ( #132243, #74876, #119110 ),
 ( #56527, #213055, #34463 ),
 ( #113954, #255986, #37023 ),
 ( #233910, #116541, #177820 ),
 ( #193517, #194814, #99507 ),
 ( #137365, #16175, #14887 ) ),
 .UNSPECIFIED., .F., .F., .F. ) 
 B_SPLINE_SURFACE_WITH_KNOTS ( ( 4, 2, 2, 4 ),
 ( 3, 3 ),
 ( 0.0001723339234021445073, 0.0002782939632049938328, 0.0003842540030078432124, 0.0005961740826135418633 ),
 ( 0.000000000000000000, 1.000000000000000000 ),
 .UNSPECIFIED. ) 
 GEOMETRIC_REPRESENTATION_ITEM ( )  RATIONAL_B_SPLINE_SURFACE ( (
 ( 1.000000000000000000, 0.9504532311154628710, 1.000000000000000000),
 ( 1.000000000000000000, 0.9506023220710236865, 1.000000000000000000),
 ( 1.000000000000000000, 0.9395774818181227284, 1.000000000000000000),
 ( 1.000000000000000000, 0.9079328464647767882, 1.000000000000000000),
 ( 1.000000000000000000, 0.8875702416206470158, 1.000000000000000000),
 ( 1.000000000000000000, 0.8205919608038449997, 1.000000000000000000),
 ( 1.000000000000000000, 0.7666842783599741029, 1.000000000000000000),
 ( 1.000000000000000000, 0.7071067811864506503, 1.000000000000000000) ) ) 
 REPRESENTATION_ITEM ( '' )  SURFACE ( )  );
#174300=DIRECTION ( 'NONE',  ( 1.000000000000000000, -0.000000000000000000, -0.000000000000000000 ) ) ;
#174308=CARTESIAN_POINT ( 'NONE',  ( -20.94999999999999929, -11.64999999998884483, -70.00000000000004263 ) ) ;
#174331=DIRECTION ( 'NONE',  ( 1.000000000000000000, -0.000000000000000000, -0.000000000000000000 ) ) ;
#174332=ORIENTED_EDGE ( 'NONE', *, *, #217999, .F. ) ;
#174335=CIRCLE ( 'NONE', #149190, 0.6000000000000033085 ) ;
#174352=DIRECTION ( 'NONE',  ( 0.000000000000000000, 0.5000000000000078826, 0.8660254037844340447 ) ) ;
#174376=DIRECTION ( 'NONE',  ( 2.952720810173289112E-16, -1.000000000000000000, -0.000000000000000000 ) ) ;
#174379=CYLINDRICAL_SURFACE ( 'NONE', #233073, 0.09999999999999939493 ) ;
#174389=ORIENTED_EDGE ( 'NONE', *, *, #134713, .T. ) ;
#174391=( BOUNDED_SURFACE ( )  B_SPLINE_SURFACE ( 3, 2, ( 
 ( #143584, #124032, #206130 ),
 ( #105708, #23670, #243961 ),
 ( #82293, #203558, #24946 ),
 ( #181445, #2769, #241412 ),
 ( #104428, #65324, #122760 ),
 ( #224391, #183991, #7937 ) ),
 .UNSPECIFIED., .F., .F., .F. ) 
 B_SPLINE_SURFACE_WITH_KNOTS ( ( 4, 2, 4 ),
 ( 3, 3 ),
 ( 0.0001792624049599542341, 0.0003686986002124689049, 0.0005581347954649835486 ),
 ( 0.000000000000000000, 1.000000000000000000 ),
 .UNSPECIFIED. ) 
 GEOMETRIC_REPRESENTATION_ITEM ( )  RATIONAL_B_SPLINE_SURFACE ( (
 ( 1.000000000000000000, 0.9238795325112860723, 1.000000000000000000),
 ( 1.000000000000000000, 0.9229318695238166725, 1.000000000000000000),
 ( 1.000000000000000000, 0.8926288119231142737, 1.000000000000000000),
 ( 1.000000000000000000, 0.8123777807271115314, 1.000000000000000000),
 ( 1.000000000000000000, 0.7629087100931926102, 1.000000000000000000),
 ( 1.000000000000000000, 0.7071067811865475727, 1.000000000000000000) ) ) 
 REPRESENTATION_ITEM ( '' )  SURFACE ( )  );
#174407=EDGE_CURVE ( 'NONE', #163227, #126808, #3254, .T. ) ;
#174425=CARTESIAN_POINT ( 'NONE',  ( -21.14999999999999858, 11.65000000001115588, -67.10000000000005116 ) ) ;
#174452=DIRECTION ( 'NONE',  ( 0.000000000000000000, 0.000000000000000000, 1.000000000000000000 ) ) ;
#174481=ORIENTED_EDGE ( 'NONE', *, *, #167983, .T. ) ;
#174488=EDGE_CURVE ( 'NONE', #93529, #201917, #245931, .T. ) ;
#174513=B_SPLINE_CURVE_WITH_KNOTS ( 'NONE', 3,
 ( #24401, #201728, #41397, #3517, #924, #80457, #160065, #200453, #43938, #21821, #242132, #140462, #239584, #180893, #141747, #103888 ),
 .UNSPECIFIED., .F., .F.,
 ( 4, 3, 3, 3, 3, 4 ),
 ( 0.000000000000000000, 2.209075297430740031E-05, 5.594258369009624354E-05, 8.979524372342015197E-05, 0.0001236472815274586301, 0.0001574990747609555279 ),
 .UNSPECIFIED. ) ;
#174525=CARTESIAN_POINT ( 'NONE',  ( 20.94999999999999929, 1.115600667400684642E-11, -67.00000000000004263 ) ) ;
#174547=DIRECTION ( 'NONE',  ( -4.701977403289178058E-30, 1.734723475976807094E-14, -1.000000000000000000 ) ) ;
#174559=LINE ( 'NONE', #35031, #177636 ) ;
#174583=DIRECTION ( 'NONE',  ( -1.000000000000000000, -2.952720810173289112E-16, 0.000000000000000000 ) ) ;
#174610=ADVANCED_FACE ( 'NONE', ( #251037 ), #134924, .T. ) ;
#174634=FACE_OUTER_BOUND ( 'NONE', #237987, .T. ) ;
#174637=ORIENTED_EDGE ( 'NONE', *, *, #166807, .T. ) ;
#174642=EDGE_LOOP ( 'NONE', ( #157370, #253055, #201325, #252424 ) ) ;
#174644=VERTEX_POINT ( 'NONE', #69876 ) ;
#174650=DIRECTION ( 'NONE',  ( 0.000000000000000000, 0.000000000000000000, -1.000000000000000000 ) ) ;
#174682=CARTESIAN_POINT ( 'NONE',  ( 18.40000000000000568, -9.499999999988890664, -107.4221498493303955 ) ) ;
#174694=DIRECTION ( 'NONE',  ( 0.000000000000000000, 0.000000000000000000, -1.000000000000000000 ) ) ;
#174699=DIRECTION ( 'NONE',  ( 1.000000000000000000, -0.000000000000000000, -0.000000000000000000 ) ) ;
#174707=CYLINDRICAL_SURFACE ( 'NONE', #218054, 0.09999999999999939493 ) ;
#174738=DIRECTION ( 'NONE',  ( 1.000000000000000000, -0.000000000000000000, -0.000000000000000000 ) ) ;
#174741=DIRECTION ( 'NONE',  ( -5.603264701231743991E-32, 1.897661533703519897E-16, -1.000000000000000000 ) ) ;
#174756=AXIS2_PLACEMENT_3D ( 'NONE', #20736, #181094, #178538 ) ;
#174780=CARTESIAN_POINT ( 'NONE',  ( -20.64999999999999858, -8.999999999988844479, -90.60603087734760663 ) ) ;
#174808=CARTESIAN_POINT ( 'NONE',  ( -20.64999999999999858, -8.999999999988846255, -76.89396912265249284 ) ) ;
#174815=DIRECTION ( 'NONE',  ( -1.000000000000000000, 0.000000000000000000, 0.000000000000000000 ) ) ;
#174826=CIRCLE ( 'NONE', #145710, 11.65000000000000746 ) ;
#174833=AXIS2_PLACEMENT_3D ( 'NONE', #124136, #18912, #203658 ) ;
#174845=AXIS2_PLACEMENT_3D ( 'NONE', #42690, #24440, #25700 ) ;
#174890=EDGE_CURVE ( 'NONE', #242995, #249989, #219616, .T. ) ;
#174901=FACE_OUTER_BOUND ( 'NONE', #85811, .T. ) ;
#174903=ORIENTED_EDGE ( 'NONE', *, *, #32100, .F. ) ;
#174914=FACE_OUTER_BOUND ( 'NONE', #228670, .T. ) ;
#174918=ORIENTED_EDGE ( 'NONE', *, *, #147617, .T. ) ;
#174921=EDGE_CURVE ( 'NONE', #47997, #211866, #191111, .T. ) ;
#174933=CARTESIAN_POINT ( 'NONE',  ( 23.24999999999999645, 1.115600667400684642E-11, -100.5000000000000426 ) ) ;
#174974=( NAMED_UNIT ( * ) SI_UNIT ( $, .STERADIAN. ) SOLID_ANGLE_UNIT ( ) );
#174977=LINE ( 'NONE', #138340, #135146 ) ;
#174987=CIRCLE ( 'NONE', #79034, 0.09999999999999484301 ) ;
#175004=DIRECTION ( 'NONE',  ( 0.000000000000000000, 0.000000000000000000, -1.000000000000000000 ) ) ;
#175031=ORIENTED_EDGE ( 'NONE', *, *, #44922, .F. ) ;
#175035=LINE ( 'NONE', #32945, #111691 ) ;
#175072=ORIENTED_EDGE ( 'NONE', *, *, #206515, .T. ) ;
#175193=EDGE_CURVE ( 'NONE', #198825, #114655, #245315, .T. ) ;
#175220=CARTESIAN_POINT ( 'NONE',  ( 21.08134388332232234, 6.334680580529113314, -66.92418108249302122 ) ) ;
#175242=CARTESIAN_POINT ( 'NONE',  ( 20.94999999999999929, -9.399999999988846611, -76.89396912265249284 ) ) ;
#175244=CARTESIAN_POINT ( 'NONE',  ( -21.05000000000000071, 1.835341550235567887, -78.55515129256302487 ) ) ;
#175254=ORIENTED_EDGE ( 'NONE', *, *, #35354, .T. ) ;
#175282=CARTESIAN_POINT ( 'NONE',  ( -18.50000000000000000, -9.499999999988849808, -55.25000000000004974 ) ) ;
#175283=CARTESIAN_POINT ( 'NONE',  ( -20.54999999999999716, 2.400000000011155432, -90.60603087734760663 ) ) ;
#175287=ADVANCED_FACE ( 'NONE', ( #88776 ), #57023, .T. ) ;
#175289=ORIENTED_EDGE ( 'NONE', *, *, #214298, .T. ) ;
#175298=CARTESIAN_POINT ( 'NONE',  ( -22.50000000000000000, 11.64957080755595520, -66.90000000000004832 ) ) ;
#175308=CARTESIAN_POINT ( 'NONE',  ( 23.24999999999999289, 5.950000000011163692, -90.19429769496522908 ) ) ;
#175315=ORIENTED_EDGE ( 'NONE', *, *, #195020, .F. ) ;
#175327=CYLINDRICAL_SURFACE ( 'NONE', #210090, 0.1000000000000028644 ) ;
#175339=CARTESIAN_POINT ( 'NONE',  ( -23.25000000000000000, 1.115600667400684642E-11, -67.00000000000004263 ) ) ;
#175401=EDGE_CURVE ( 'NONE', #236185, #102720, #256473, .T. ) ;
#175424=DIRECTION ( 'NONE',  ( 0.000000000000000000, 0.8700118002898321601, -0.4930308989875230030 ) ) ;
#175429=ORIENTED_EDGE ( 'NONE', *, *, #145854, .T. ) ;
#175454=DIRECTION ( 'NONE',  ( 1.000000000000000000, -0.000000000000000000, 0.000000000000000000 ) ) ;
#175460=EDGE_CURVE ( 'NONE', #135788, #158987, #219974, .T. ) ;
#175463=CARTESIAN_POINT ( 'NONE',  ( -20.94999999999999929, 11.65000000001115232, -100.5000000000000426 ) ) ;
#175476=LINE ( 'NONE', #217119, #176712 ) ;
#175477=DIRECTION ( 'NONE',  ( 0.000000000000000000, 0.000000000000000000, -1.000000000000000000 ) ) ;
#175517=EDGE_CURVE ( 'NONE', #61798, #256256, #165146, .T. ) ;
#175539=AXIS2_PLACEMENT_3D ( 'NONE', #203928, #240492, #3141 ) ;
#175541=CIRCLE ( 'NONE', #63074, 0.09999999999999939493 ) ;
#175551=CARTESIAN_POINT ( 'NONE',  ( -21.11927991906891577, 0.009083679485028523307, -60.55150688150853711 ) ) ;
#175553=CARTESIAN_POINT ( 'NONE',  ( -21.05000000000000071, 1.835341550235567887, -78.55515129256302487 ) ) ;
#175554=DIRECTION ( 'NONE',  ( 0.000000000000000000, 0.000000000000000000, -1.000000000000000000 ) ) ;
#175609=ORIENTED_EDGE ( 'NONE', *, *, #119989, .T. ) ;
#175614=FACE_OUTER_BOUND ( 'NONE', #126475, .T. ) ;
#175631=CARTESIAN_POINT ( 'NONE',  ( 20.01093837587850288, 11.75000000001116263, -91.75439743459725150 ) ) ;
#175648=ADVANCED_FACE ( 'NONE', ( #150716 ), #51574, .T. ) ;
#175687=ORIENTED_EDGE ( 'NONE', *, *, #122426, .T. ) ;
#175688=VECTOR ( 'NONE', #129835, 1000.000000000000000 ) ;
#175727=CARTESIAN_POINT ( 'NONE',  ( -20.85000000000000142, 1.115600667400684642E-11, -100.5000000000000426 ) ) ;
#175728=AXIS2_PLACEMENT_3D ( 'NONE', #100988, #22817, #59305 ) ;
#175744=VERTEX_POINT ( 'NONE', #21494 ) ;
#175766=CARTESIAN_POINT ( 'NONE',  ( 21.05000000000000071, 10.72371710471867701, -79.15000000000004832 ) ) ;
#175815=AXIS2_PLACEMENT_3D ( 'NONE', #20922, #17063, #234808 ) ;
#175820=ORIENTED_EDGE ( 'NONE', *, *, #131739, .F. ) ;
#175828=CARTESIAN_POINT ( 'NONE',  ( 23.14999999999999858, 4.000000000011155521, -100.5000000000000426 ) ) ;
#175830=CARTESIAN_POINT ( 'NONE',  ( -22.39999999999999858, 0.1000000000111554016, -59.20922040162664501 ) ) ;
#175861=CIRCLE ( 'NONE', #96695, 0.1000000000000028644 ) ;
#175862=VERTEX_POINT ( 'NONE', #206532 ) ;
#175884=DIRECTION ( 'NONE',  ( 1.875376730785737719E-16, -1.000000000000000000, 0.000000000000000000 ) ) ;
#175902=LINE ( 'NONE', #70713, #74621 ) ;
#175905=DIRECTION ( 'NONE',  ( 0.000000000000000000, 0.000000000000000000, -1.000000000000000000 ) ) ;
#175921=EDGE_LOOP ( 'NONE', ( #167767, #32632, #255709, #229220 ) ) ;
#175954=ADVANCED_FACE ( 'NONE', ( #211689 ), #108075, .T. ) ;
#175958=DIRECTION ( 'NONE',  ( -0.000000000000000000, 1.000000000000000000, -1.224646799147352961E-16 ) ) ;
#176004=DIRECTION ( 'NONE',  ( 0.000000000000000000, 1.000000000000000000, 0.000000000000000000 ) ) ;
#176038=DIRECTION ( 'NONE',  ( 0.000000000000000000, 0.9998779222360102414, 0.01562499999996356907 ) ) ;
#176118=ORIENTED_EDGE ( 'NONE', *, *, #32100, .T. ) ;
#176119=CARTESIAN_POINT ( 'NONE',  ( -20.54999999999999716, 7.150000000011155876, -79.35000000000005116 ) ) ;
#176130=DIRECTION ( 'NONE',  ( 1.000000000000000000, 0.000000000000000000, 0.000000000000000000 ) ) ;
#176132=DIRECTION ( 'NONE',  ( 0.000000000000000000, -1.000000000000000000, 0.000000000000000000 ) ) ;
#176180=DIRECTION ( 'NONE',  ( 1.000000000000000000, 2.952720810173289112E-16, -0.000000000000000000 ) ) ;
#176207=EDGE_CURVE ( 'NONE', #78012, #89054, #145837, .T. ) ;
#176214=AXIS2_PLACEMENT_3D ( 'NONE', #164962, #84083, #8467 ) ;
#176234=FACE_OUTER_BOUND ( 'NONE', #78843, .T. ) ;
#176241=ORIENTED_EDGE ( 'NONE', *, *, #244313, .T. ) ;
#176247=CIRCLE ( 'NONE', #93017, 0.1000000000000002692 ) ;
#176249=LINE ( 'NONE', #60109, #60835 ) ;
#176267=ORIENTED_EDGE ( 'NONE', *, *, #224227, .F. ) ;
#176290=DIRECTION ( 'NONE',  ( 1.000000000000000000, -0.000000000000000000, -0.000000000000000000 ) ) ;
#176302=CIRCLE ( 'NONE', #63855, 0.1000000000000002831 ) ;
#176328=DIRECTION ( 'NONE',  ( 0.000000000000000000, -0.8777080977375132376, 0.4791956752371582251 ) ) ;
#176333=CARTESIAN_POINT ( 'NONE',  ( 20.94999999999999929, 1.115600667400684642E-11, -100.5000000000000426 ) ) ;
#176339=CIRCLE ( 'NONE', #43056, 12.87499999999999822 ) ;
#176385=FACE_OUTER_BOUND ( 'NONE', #168312, .T. ) ;
#176410=EDGE_LOOP ( 'NONE', ( #134260, #174389, #204428, #236732 ) ) ;
#176412=FACE_OUTER_BOUND ( 'NONE', #46914, .T. ) ;
#176484=ORIENTED_EDGE ( 'NONE', *, *, #110658, .T. ) ;
#176553=AXIS2_PLACEMENT_3D ( 'NONE', #131465, #211011, #230579 ) ;
#176559=EDGE_CURVE ( 'NONE', #45948, #206992, #63278, .T. ) ;
#176562=CARTESIAN_POINT ( 'NONE',  ( 20.85000000000000142, -1.835859311432481045, -112.0044391687985694 ) ) ;
#176571=CIRCLE ( 'NONE', #139101, 0.5000000000000004441 ) ;
#176589=CYLINDRICAL_SURFACE ( 'NONE', #24853, 0.1000000000000028644 ) ;
#176599=DIRECTION ( 'NONE',  ( 1.224646799147353207E-16, 1.000000000000000000, 0.000000000000000000 ) ) ;
#176643=EDGE_CURVE ( 'NONE', #96043, #14463, #104768, .T. ) ;
#176664=CARTESIAN_POINT ( 'NONE',  ( 23.14999999999999503, 6.550000000011156231, -79.35000000000005116 ) ) ;
#176689=CARTESIAN_POINT ( 'NONE',  ( -23.25000000000000000, 10.33248238083634440, -106.0948465439131922 ) ) ;
#176692=CARTESIAN_POINT ( 'NONE',  ( -21.05000000000000071, 1.162701749949165642, -74.90000000000004832 ) ) ;
#176695=B_SPLINE_CURVE_WITH_KNOTS ( 'NONE', 3,
 ( #106673, #204498, #85809, #166705, #64994, #165394 ),
 .UNSPECIFIED., .F., .F.,
 ( 4, 2, 4 ),
 ( 0.000000000000000000, 0.0001496588209255828787, 0.0002993176418511657574 ),
 .UNSPECIFIED. ) ;
#176712=VECTOR ( 'NONE', #219706, 1000.000000000000114 ) ;
#176728=DIRECTION ( 'NONE',  ( 0.000000000000000000, 0.000000000000000000, 1.000000000000000000 ) ) ;
#176730=VERTEX_POINT ( 'NONE', #23652 ) ;
#176735=EDGE_CURVE ( 'NONE', #230941, #163525, #5772, .T. ) ;
#176751=VERTEX_POINT ( 'NONE', #241393 ) ;
#176764=EDGE_CURVE ( 'NONE', #224755, #114130, #206105, .T. ) ;
#176778=LINE ( 'NONE', #22730, #96898 ) ;
#176812=FACE_OUTER_BOUND ( 'NONE', #150437, .T. ) ;
#176843=TOROIDAL_SURFACE ( 'NONE', #210158, 0.2000000000000000111, 0.1000000000000000056 ) ;
#176879=CARTESIAN_POINT ( 'NONE',  ( 21.05000000000000071, 6.650000000011155876, -79.15000000000004832 ) ) ;
#176900=CIRCLE ( 'NONE', #93476, 12.87499999999999822 ) ;
#176912=CARTESIAN_POINT ( 'NONE',  ( 20.94999999999999929, 8.776282895303628706, -75.55862899514100661 ) ) ;
#176929=DIRECTION ( 'NONE',  ( 0.000000000000000000, -0.01283462868041947667, -0.9999176327611367654 ) ) ;
#176930=EDGE_CURVE ( 'NONE', #82405, #58814, #76787, .T. ) ;
#176953=ADVANCED_FACE ( 'NONE', ( #172159 ), #251649, .F. ) ;
#176956=EDGE_LOOP ( 'NONE', ( #60514, #104575 ) ) ;
#176959=FACE_OUTER_BOUND ( 'NONE', #217597, .T. ) ;
#176982=CARTESIAN_POINT ( 'NONE',  ( -20.64999999999999858, 1.115600667400684642E-11, -100.5000000000000426 ) ) ;
#176996=ADVANCED_FACE ( 'NONE', ( #58562 ), #103419, .T. ) ;
#177004=CARTESIAN_POINT ( 'NONE',  ( 20.94999999999999929, 1.835341550235569663, -78.55515129256303908 ) ) ;
#177006=DIRECTION ( 'NONE',  ( 0.000000000000000000, 0.000000000000000000, -1.000000000000000000 ) ) ;
#177026=AXIS2_PLACEMENT_3D ( 'NONE', #139472, #20851, #140775 ) ;
#177048=EDGE_CURVE ( 'NONE', #233528, #152504, #46715, .T. ) ;
#177049=CARTESIAN_POINT ( 'NONE',  ( 21.00000000000000000, 9.750000000011153745, -88.25000000000005684 ) ) ;
#177125=DIRECTION ( 'NONE',  ( 0.000000000000000000, -1.000000000000000000, 0.000000000000000000 ) ) ;
#177127=EDGE_CURVE ( 'NONE', #115296, #129552, #9310, .T. ) ;
#177143=VECTOR ( 'NONE', #3759, 1000.000000000000000 ) ;
#177157=VERTEX_POINT ( 'NONE', #243636 ) ;
#177159=CARTESIAN_POINT ( 'NONE',  ( 18.51997666896878059, -9.392332131507778570, -74.14340618748370559 ) ) ;
#177167=CARTESIAN_POINT ( 'NONE',  ( 18.49999999999999289, 7.021664781911246322, -104.3335654018973315 ) ) ;
#177168=CARTESIAN_POINT ( 'NONE',  ( 18.39999999999999858, -9.399999999988843058, -55.25000000000004974 ) ) ;
#177181=EDGE_CURVE ( 'NONE', #16604, #61134, #176695, .T. ) ;
#177193=ORIENTED_EDGE ( 'NONE', *, *, #72059, .T. ) ;
#177204=ORIENTED_EDGE ( 'NONE', *, *, #256516, .T. ) ;
#177207=AXIS2_PLACEMENT_3D ( 'NONE', #28251, #226391, #243406 ) ;
#177226=CARTESIAN_POINT ( 'NONE',  ( 18.40916198585730967, -9.499999999988844479, -107.1001896318234543 ) ) ;
#177253=ADVANCED_FACE ( 'NONE', ( #252611 ), #171845, .T. ) ;
#177313=LINE ( 'NONE', #97705, #252521 ) ;
#177316=ORIENTED_EDGE ( 'NONE', *, *, #241478, .T. ) ;
#177332=CARTESIAN_POINT ( 'NONE',  ( -20.94999999999999929, 1.115600667400684642E-11, -67.00000000000004263 ) ) ;
#177343=DIRECTION ( 'NONE',  ( 1.000000000000000000, -0.000000000000000000, -0.000000000000000000 ) ) ;
#177357=VERTEX_POINT ( 'NONE', #80371 ) ;
#177373=CIRCLE ( 'NONE', #119076, 0.1000000000000028644 ) ;
#177375=DIRECTION ( 'NONE',  ( 0.000000000000000000, 1.000000000000000000, 0.000000000000000000 ) ) ;
#177391=CIRCLE ( 'NONE', #98028, 0.9750000000000036415 ) ;
#177422=ORIENTED_EDGE ( 'NONE', *, *, #105509, .F. ) ;
#177429=VECTOR ( 'NONE', #217159, 1000.000000000000000 ) ;
#177438=COLOUR_RGB ( '', 0.08235294, 0.09019608, 0.10196078) ;
#177514=DIRECTION ( 'NONE',  ( 0.000000000000000000, 0.000000000000000000, -1.000000000000000000 ) ) ;
#177531=DIRECTION ( 'NONE',  ( 0.000000000000000000, 0.000000000000000000, -1.000000000000000000 ) ) ;
#177541=ORIENTED_EDGE ( 'NONE', *, *, #29759, .T. ) ;
#177563=ORIENTED_EDGE ( 'NONE', *, *, #171593, .F. ) ;
#177627=ADVANCED_FACE ( 'NONE', ( #149392 ), #91953, .T. ) ;
#177636=VECTOR ( 'NONE', #229355, 1000.000000000000000 ) ;
#177679=DIRECTION ( 'NONE',  ( 0.000000000000000000, 0.000000000000000000, -1.000000000000000000 ) ) ;
#177680=DIRECTION ( 'NONE',  ( 1.000000000000000000, 0.000000000000000000, 0.000000000000000000 ) ) ;
#177702=DIRECTION ( 'NONE',  ( -0.000000000000000000, -2.891205793294679805E-16, 1.000000000000000000 ) ) ;
#177706=EDGE_CURVE ( 'NONE', #51884, #210178, #85954, .T. ) ;
#177707=DIRECTION ( 'NONE',  ( 1.000000000000000000, 0.000000000000000000, 0.000000000000000000 ) ) ;
#177719=VERTEX_POINT ( 'NONE', #180487 ) ;
#177746=ADVANCED_FACE ( 'NONE', ( #217021 ), #22719, .F. ) ;
#177770=ORIENTED_EDGE ( 'NONE', *, *, #233308, .F. ) ;
#177775=FACE_OUTER_BOUND ( 'NONE', #153715, .T. ) ;
#177792=CARTESIAN_POINT ( 'NONE',  ( 21.05000000000000071, -1.835341550213257733, -78.55515129256303908 ) ) ;
#177799=ORIENTED_EDGE ( 'NONE', *, *, #30699, .T. ) ;
#177810=ORIENTED_EDGE ( 'NONE', *, *, #254404, .F. ) ;
#177817=AXIS2_PLACEMENT_3D ( 'NONE', #65175, #239982, #80874 ) ;
#177820=CARTESIAN_POINT ( 'NONE',  ( -18.58693740092145319, -9.406432150241773371, -74.12481645650147755 ) ) ;
#177860=EDGE_CURVE ( 'NONE', #154701, #77148, #186521, .T. ) ;
#177869=VERTEX_POINT ( 'NONE', #23998 ) ;
#177873=DIRECTION ( 'NONE',  ( 1.000000000000000000, 0.000000000000000000, -0.000000000000000000 ) ) ;
#177896=CIRCLE ( 'NONE', #82168, 0.5000000000000004441 ) ;
#177911=AXIS2_PLACEMENT_3D ( 'NONE', #59537, #200374, #197791 ) ;
#177912=AXIS2_PLACEMENT_3D ( 'NONE', #140398, #243356, #64723 ) ;
#177925=EDGE_LOOP ( 'NONE', ( #105245, #64645, #125711, #38723, #39319, #21290, #220370, #103807, #242241, #137454, #25478, #225886 ) ) ;
#177937=PLANE ( 'NONE',  #73688 ) ;
#177956=CARTESIAN_POINT ( 'NONE',  ( 20.94999999999999929, 6.450000000011156587, -77.01702717044007329 ) ) ;
#177989=DIRECTION ( 'NONE',  ( 0.000000000000000000, -1.000000000000000000, 0.000000000000000000 ) ) ;
#178000=VECTOR ( 'NONE', #7619, 999.9999999999998863 ) ;
#178033=FACE_OUTER_BOUND ( 'NONE', #93659, .T. ) ;
#178038=VECTOR ( 'NONE', #102489, 1000.000000000000000 ) ;
#178057=ORIENTED_EDGE ( 'NONE', *, *, #233075, .T. ) ;
#178069=CARTESIAN_POINT ( 'NONE',  ( -23.15000000000000213, 1.115600667400684642E-11, -67.00000000000004263 ) ) ;
#178096=ORIENTED_EDGE ( 'NONE', *, *, #43789, .T. ) ;
#178102=LINE ( 'NONE', #95960, #222883 ) ;
#178134=EDGE_LOOP ( 'NONE', ( #106930, #214870, #141789, #168790 ) ) ;
#178152=CIRCLE ( 'NONE', #86516, 0.1000000000000028644 ) ;
#178161=CARTESIAN_POINT ( 'NONE',  ( -22.50000000000000000, 11.64957080755595520, -66.90000000000004832 ) ) ;
#178163=CARTESIAN_POINT ( 'NONE',  ( -22.59999999999999787, 0.1000000000111554016, -55.35042919245524473 ) ) ;
#178192=CLOSED_SHELL ( 'NONE', ( #74397, #72955, #150457, #33294, #125485, #143630, #243946, #129442, #38174, #33425, #98540, #14566, #67778, #63392, #255925, #87329, #149367, #120916, #141996, #28839, #208736, #205251, #226561, #249508, #65870, #58515, #209960, #26691, #115269, #169972, #181308, #211486, #5952, #249318, #181218, #95356, #1428, #140628, #143854, #116612, #17882, #238862, #158834, #210437, #73868, #207482, #211798, #130886, #34381, #177746, #38747, #12341, #8942, #231585, #128976, #1253, #6488, #2581, #137501, #73485, #195492, #127122, #240460, #245124, #252982, #156767, #126489, #144950, #91852, #249156, #126188, #231393, #15077, #194204, #180173, #136092, #80391, #212478, #173919, #25072, #114804, #181830, #17670, #140276, #205458, #253559, #141632, #170983, #165323, #59325, #159702, #52975, #182934, #152072, #181196, #203681, #104311, #69659, #223958, #108617, #92167, #164181, #108269, #32430, #149230, #79341, #40883, #52965, #41686, #176953, #118788, #228928, #239040, #181491, #33659, #150993, #183559, #81444, #75896, #16581, #190481, #129165, #31042, #254302, #217781, #216296, #13810, #192231, #9746, #46861, #21898, #35720, #253033, #29016, #121968, #175287, #152375, #240698, #254060, #88369, #253076, #56265, #215635, #100285, #125055, #102103, #108753, #101190, #119337, #69776, #22735, #199927, #20098, #232470, #179209, #48274, #18217, #240333, #141945, #189069, #79111, #205480, #39990, #33280, #9872, #32347, #239360, #117623, #129694, #131037, #115543, #70143, #142302, #123423, #186543, #246542, #141294, #12549, #12120, #217505, #11120, #93482, #67463, #115120, #2068, #201911, #38780, #150970, #13460, #37601, #76030, #51814, #64297, #251683, #158061, #210049, #96978, #241291, #147048, #223959, #167164, #32312, #164000, #162214, #81358, #196278, #73617, #29854, #58354, #36575, #45582, #21149, #82338, #140114, #150415, #66384, #200703, #69604, #58680, #217226, #75442, #43492, #81742, #95855, #253466, #83410, #145455, #13620, #103820, #248739, #48727, #46248, #113220, #63945, #125803, #234417, #196509, #20443, #177627, #11729, #198818, #130576, #237797, #28342, #253854, #127784, #230143, #216311, #181911, #30724, #220555, #154622, #196960, #183907, #161226, #86161, #95073, #12291, #102961, #70835, #256546, #23696, #92849, #37274, #7547, #18800, #95867, #25558, #50098, #109157, #246666, #192984, #234882, #213118, #52581, #25921, #174610, #3104, #163759, #113566, #165002, #191856, #15846, #35046, #148853, #75754, #49964, #202756, #80749, #106198, #216513, #208328, #106404, #43700, #50919, #62153, #99902, #94215, #127297, #96249, #144559, #87075, #104852, #121684, #36870, #52874, #32171, #182372, #71678, #136724, #11300, #25666, #29402, #114462, #96818, #140230, #133742, #181762, #152319, #195910, #255935, #112709, #106737, #125666, #191611, #64532, #179847, #19673, #128769, #91560, #56678, #185018, #76841, #140051, #169574, #248455, #255691, #115348, #27880, #32574, #58245, #71347, #25817, #49312, #108330, #227860, #117372, #243063, #40423, #118613, #201729, #184459, #199822, #97836, #138803, #233622, #58233, #171598, #197718, #136131, #20828, #14147, #200187, #75506, #74391, #110070, #62881, #164410, #37583, #140342, #185068, #86603, #193985, #54661, #224867, #197717, #195504, #56207, #117910, #75664, #202895, #167784, #173069, #163506, #122814, #117966, #77179, #178717, #182467, #53471, #188395, #127607, #168527, #235893, #21827, #92044, #96888, #164113, #245729, #238848, #235365, #11960, #109145, #194614, #70736, #206321, #312, #28712, #239394, #32359, #208316, #215382, #99852, #184154, #11940, #35078, #175954, #59695, #81918, #39578, #184182, #56749, #96382, #71957, #144811, #140957, #28250, #88885, #206281, #6911, #151063, #247123, #230379, #23625, #148250, #229648, #23121, #179855, #208527, #183005, #171620, #32010, #25657, #187031, #231225, #15755, #101797, #142422, #138655, #152632, #59354, #186258, #97619, #156387, #65244, #54441, #176996, #221310, #51417, #177253, #68023, #92706, #191372, #105223, #180681, #67873, #208299, #158469, #137594, #112661, #135130, #47009, #195602, #75244, #185179, #222810, #223774, #175648 ) ) ;
#178238=VERTEX_POINT ( 'NONE', #11506 ) ;
#178282=EDGE_CURVE ( 'NONE', #255102, #133253, #61224, .T. ) ;
#178284=ORIENTED_EDGE ( 'NONE', *, *, #70383, .T. ) ;
#178285=ORIENTED_EDGE ( 'NONE', *, *, #202136, .T. ) ;
#178346=VERTEX_POINT ( 'NONE', #33672 ) ;
#178362=CARTESIAN_POINT ( 'NONE',  ( -20.94999999999999929, 1.115600667400684642E-11, -100.5000000000000426 ) ) ;
#178365=CARTESIAN_POINT ( 'NONE',  ( 18.49999999999999289, 6.450000000011156587, -55.25000000000004974 ) ) ;
#178414=CIRCLE ( 'NONE', #65956, 0.09999999999999939493 ) ;
#178420=ORIENTED_EDGE ( 'NONE', *, *, #192803, .T. ) ;
#178515=ORIENTED_EDGE ( 'NONE', *, *, #105016, .T. ) ;
#178538=DIRECTION ( 'NONE',  ( 0.000000000000000000, 0.000000000000000000, 1.000000000000000000 ) ) ;
#178542=CARTESIAN_POINT ( 'NONE',  ( 22.49806830649814060, 0.07746431633666323036, -55.35011034516096373 ) ) ;
#178555=DIRECTION ( 'NONE',  ( 0.000000000000000000, 0.000000000000000000, -1.000000000000000000 ) ) ;
#178598=CARTESIAN_POINT ( 'NONE',  ( -23.25000000000000000, 1.115649040949250830E-11, -96.60000000000005116 ) ) ;
#178652=VECTOR ( 'NONE', #142345, 1000.000000000000000 ) ;
#178684=DIRECTION ( 'NONE',  ( 0.000000000000000000, 0.000000000000000000, 1.000000000000000000 ) ) ;
#178690=CARTESIAN_POINT ( 'NONE',  ( -21.14999999999999858, 1.115600667400684642E-11, -67.00000000000004263 ) ) ;
#178717=ADVANCED_FACE ( 'NONE', ( #12483 ), #194974, .T. ) ;
#178734=DIRECTION ( 'NONE',  ( -1.000000000000000000, 0.000000000000000000, 0.000000000000000000 ) ) ;
#178792=ORIENTED_EDGE ( 'NONE', *, *, #204477, .T. ) ;
#178802=DIRECTION ( 'NONE',  ( 0.000000000000000000, -0.4930308989875313852, -0.8700118002898274971 ) ) ;
#178840=CARTESIAN_POINT ( 'NONE',  ( 21.00000000000000000, 9.750000000011153745, -88.15000000000004832 ) ) ;
#178858=DIRECTION ( 'NONE',  ( 0.000000000000000000, 0.8660254037844411501, 0.4999999999999956701 ) ) ;
#178878=DIRECTION ( 'NONE',  ( 0.000000000000000000, 0.000000000000000000, 1.000000000000000000 ) ) ;
#178934=EDGE_CURVE ( 'NONE', #170816, #70703, #21471, .T. ) ;
#178965=VERTEX_POINT ( 'NONE', #207825 ) ;
#178984=EDGE_CURVE ( 'NONE', #75869, #15594, #46144, .T. ) ;
#179013=CARTESIAN_POINT ( 'NONE',  ( 23.14999999999998437, 1.115600667400684642E-11, -67.00000000000004263 ) ) ;
#179033=VERTEX_POINT ( 'NONE', #27905 ) ;
#179039=DIRECTION ( 'NONE',  ( -0.000000000000000000, -0.000000000000000000, 1.000000000000000000 ) ) ;
#179075=VECTOR ( 'NONE', #226757, 1000.000000000000000 ) ;
#179099=ORIENTED_EDGE ( 'NONE', *, *, #228398, .F. ) ;
#179104=CIRCLE ( 'NONE', #174845, 0.5000000000000013323 ) ;
#179145=CARTESIAN_POINT ( 'NONE',  ( -22.49436431346200038, 11.64995094766461392, -66.93309647027778908 ) ) ;
#179174=CARTESIAN_POINT ( 'NONE',  ( -18.50000000000000000, 11.65000000001115232, -79.25000000000004263 ) ) ;
#179194=VECTOR ( 'NONE', #202915, 1000.000000000000000 ) ;
#179209=ADVANCED_FACE ( 'NONE', ( #170000 ), #154292, .F. ) ;
#179220=DIRECTION ( 'NONE',  ( 0.000000000000000000, 1.000000000000000000, -1.224646799147353207E-16 ) ) ;
#179270=DIRECTION ( 'NONE',  ( 0.000000000000000000, 0.000000000000000000, 1.000000000000000000 ) ) ;
#179279=VERTEX_POINT ( 'NONE', #121568 ) ;
#179301=CYLINDRICAL_SURFACE ( 'NONE', #84522, 0.5000000000000004441 ) ;
#179309=CARTESIAN_POINT ( 'NONE',  ( 18.59999999999999076, 6.550000000011156231, -88.25000000000005684 ) ) ;
#179317=CARTESIAN_POINT ( 'NONE',  ( 21.05000000000000071, 10.72371710471867701, -79.16119029412749342 ) ) ;
#179336=CARTESIAN_POINT ( 'NONE',  ( 20.85000000000000142, 11.75000000001115907, -93.71613433702195550 ) ) ;
#179345=ORIENTED_EDGE ( 'NONE', *, *, #12485, .F. ) ;
#179359=ORIENTED_EDGE ( 'NONE', *, *, #55559, .T. ) ;
#179373=ORIENTED_EDGE ( 'NONE', *, *, #91088, .T. ) ;
#179379=CARTESIAN_POINT ( 'NONE',  ( -21.45000000000000284, 7.708578643773852157, -79.25000000000004263 ) ) ;
#179400=CARTESIAN_POINT ( 'NONE',  ( 23.14999999999999503, 11.65000000001116298, -55.25000000000004974 ) ) ;
#179404=ORIENTED_EDGE ( 'NONE', *, *, #24774, .F. ) ;
#179413=CARTESIAN_POINT ( 'NONE',  ( 20.94999999999999929, 5.500000000011153745, -88.09473398108696074 ) ) ;
#179416=CARTESIAN_POINT ( 'NONE',  ( -21.05000000000000071, -1.249999999988843369, -75.00000000000004263 ) ) ;
#179442=CARTESIAN_POINT ( 'NONE',  ( -21.05000000000000426, 11.60000000001115872, -73.92820323027559937 ) ) ;
#179509=CIRCLE ( 'NONE', #233671, 0.2000000000000057288 ) ;
#179546=VERTEX_POINT ( 'NONE', #90088 ) ;
#179575=EDGE_LOOP ( 'NONE', ( #75784, #70120, #123878, #31102 ) ) ;
#179612=CARTESIAN_POINT ( 'NONE',  ( 18.49999999999999289, 10.29270135741298731, -105.9573618871519756 ) ) ;
#179616=CARTESIAN_POINT ( 'NONE',  ( 23.14999999999999503, 11.75000000001116263, -55.25000000000004974 ) ) ;
#179620=AXIS2_PLACEMENT_3D ( 'NONE', #68367, #84011, #86609 ) ;
#179626=CARTESIAN_POINT ( 'NONE',  ( 18.49999999999998934, 6.550000000011156231, -88.25000000000005684 ) ) ;
#179628=CIRCLE ( 'NONE', #67184, 0.09999999999999939493 ) ;
#179663=VERTEX_POINT ( 'NONE', #165347 ) ;
#179689=CARTESIAN_POINT ( 'NONE',  ( 18.60000000000000142, -9.523946312306552642, -107.3820279953382624 ) ) ;
#179696=ORIENTED_EDGE ( 'NONE', *, *, #112399, .F. ) ;
#179732=ORIENTED_EDGE ( 'NONE', *, *, #219423, .F. ) ;
#179747=CARTESIAN_POINT ( 'NONE',  ( 23.15000000000000213, -8.999999999988842703, -90.60603087734760663 ) ) ;
#179787=ORIENTED_EDGE ( 'NONE', *, *, #14254, .F. ) ;
#179788=DIRECTION ( 'NONE',  ( 0.000000000000000000, -1.687538997430242044E-14, -1.000000000000000000 ) ) ;
#179789=AXIS2_PLACEMENT_3D ( 'NONE', #159635, #100889, #137476 ) ;
#179812=CARTESIAN_POINT ( 'NONE',  ( 22.40736611211992368, 1.115600667400684642E-11, -55.35042919245524473 ) ) ;
#179816=FACE_OUTER_BOUND ( 'NONE', #25937, .T. ) ;
#179822=AXIS2_PLACEMENT_3D ( 'NONE', #26207, #105695, #28812 ) ;
#179831=EDGE_LOOP ( 'NONE', ( #191742, #100650, #169802, #167618 ) ) ;
#179845=ORIENTED_EDGE ( 'NONE', *, *, #209904, .T. ) ;
#179847=ADVANCED_FACE ( 'NONE', ( #15270 ), #32965, .T. ) ;
#179855=ADVANCED_FACE ( 'NONE', ( #11414 ), #150913, .F. ) ;
#179864=CIRCLE ( 'NONE', #217416, 0.1000000000000028644 ) ;
#179870=CARTESIAN_POINT ( 'NONE',  ( 21.05000000000000071, 11.60000000001116227, -93.57179676972454274 ) ) ;
#179873=CARTESIAN_POINT ( 'NONE',  ( -18.59999999999999787, 11.65000000001115232, -74.01480577065404987 ) ) ;
#179877=CIRCLE ( 'NONE', #67426, 0.6000000000000033085 ) ;
#179891=DIRECTION ( 'NONE',  ( 0.000000000000000000, 0.000000000000000000, -1.000000000000000000 ) ) ;
#179899=CARTESIAN_POINT ( 'NONE',  ( -23.25000000000000000, 11.75000000001115552, -100.5000000000000426 ) ) ;
#179907=CARTESIAN_POINT ( 'NONE',  ( -21.55000000000000426, 7.750000000011155521, -79.35000000000005116 ) ) ;
#179921=CARTESIAN_POINT ( 'NONE',  ( -18.50000000000000355, -1.263275465206102233, -108.4018646667464481 ) ) ;
#179925=DIRECTION ( 'NONE',  ( 2.952720810173289112E-16, -1.000000000000000000, 0.000000000000000000 ) ) ;
#179927=DIRECTION ( 'NONE',  ( 1.000000000000000000, 7.304098846218134667E-16, 0.000000000000000000 ) ) ;
#179932=DIRECTION ( 'NONE',  ( 1.000000000000000000, -0.000000000000000000, -0.000000000000000000 ) ) ;
#179946=CYLINDRICAL_SURFACE ( 'NONE', #83350, 0.09999999999999781286 ) ;
#179978=DIRECTION ( 'NONE',  ( -0.000000000000000000, 0.8660254037844411501, 0.4999999999999956701 ) ) ;
#179983=CARTESIAN_POINT ( 'NONE',  ( 23.14999999999999858, 1.115600667400684642E-11, -79.87500000000004263 ) ) ;
#179985=CARTESIAN_POINT ( 'NONE',  ( 20.94999999999999929, 1.115600667400684642E-11, -100.5000000000000426 ) ) ;
#180017=DIRECTION ( 'NONE',  ( 1.000000000000000000, -0.000000000000000000, -0.000000000000000000 ) ) ;
#180023=DIRECTION ( 'NONE',  ( -0.7071067811865474617, -0.7071067811865474617, -0.000000000000000000 ) ) ;
#180034=CARTESIAN_POINT ( 'NONE',  ( -21.05000000000000071, 11.65000000001115232, -73.78386566297820082 ) ) ;
#180055=EDGE_LOOP ( 'NONE', ( #185845, #87218, #200588, #175315 ) ) ;
#180063=EDGE_CURVE ( 'NONE', #91092, #151216, #45384, .T. ) ;
#180066=SURFACE_SIDE_STYLE ('',( #60093 ) ) ;
#180083=AXIS2_PLACEMENT_3D ( 'NONE', #192813, #174583, #169432 ) ;
#180126=ORIENTED_EDGE ( 'NONE', *, *, #155723, .F. ) ;
#180128=AXIS2_PLACEMENT_3D ( 'NONE', #147996, #166307, #85406 ) ;
#180129=DIRECTION ( 'NONE',  ( 0.000000000000000000, -0.1455152366551522025, -0.9893560106964505163 ) ) ;
#180133=EDGE_LOOP ( 'NONE', ( #34441, #58816, #44154, #217677 ) ) ;
#180139=DIRECTION ( 'NONE',  ( -1.000000000000000000, -0.000000000000000000, -0.000000000000000000 ) ) ;
#180161=DIRECTION ( 'NONE',  ( 0.000000000000000000, 1.000000000000000000, -1.224646799147353207E-16 ) ) ;
#180169=CIRCLE ( 'NONE', #38878, 0.1000000000000028644 ) ;
#180173=ADVANCED_FACE ( 'NONE', ( #181711 ), #107299, .F. ) ;
#180185=CARTESIAN_POINT ( 'NONE',  ( -18.59999999999999787, 7.021664781911246322, -104.1335654018973287 ) ) ;
#180186=CARTESIAN_POINT ( 'NONE',  ( 21.14999999999999858, 11.65000000001116298, -79.15000000000004832 ) ) ;
#180248=ORIENTED_EDGE ( 'NONE', *, *, #90594, .T. ) ;
#180287=CARTESIAN_POINT ( 'NONE',  ( -23.15000000000000213, 4.250000000011156409, -79.25000000000004263 ) ) ;
#180305=AXIS2_PLACEMENT_3D ( 'NONE', #65363, #59218, #60536 ) ;
#180309=EDGE_LOOP ( 'NONE', ( #181251, #257205, #151589, #129474 ) ) ;
#180327=CIRCLE ( 'NONE', #246956, 12.87499999999999822 ) ;
#180340=ORIENTED_EDGE ( 'NONE', *, *, #50436, .F. ) ;
#180341=DIRECTION ( 'NONE',  ( -1.000000000000000000, 0.000000000000000000, 0.000000000000000000 ) ) ;
#180369=EDGE_LOOP ( 'NONE', ( #166860, #4797, #239157, #49211, #227149 ) ) ;
#180390=PLANE ( 'NONE',  #85430 ) ;
#180408=DIRECTION ( 'NONE',  ( 0.000000000000000000, 0.000000000000000000, 1.000000000000000000 ) ) ;
#180428=CARTESIAN_POINT ( 'NONE',  ( -23.25000000000000000, 1.115600667400684642E-11, -100.5000000000000426 ) ) ;
#180457=( BOUNDED_SURFACE ( )  B_SPLINE_SURFACE ( 3, 2, ( 
 ( #246859, #188191, #207770 ),
 ( #149077, #111215, #106049 ),
 ( #249457, #66948, #130772 ),
 ( #70834, #9535, #51206 ),
 ( #185617, #150353, #229882 ),
 ( #168674, #190786, #46091 ) ),
 .UNSPECIFIED., .F., .F., .F. ) 
 B_SPLINE_SURFACE_WITH_KNOTS ( ( 4, 2, 4 ),
 ( 3, 3 ),
 ( 0.0001381104793128061785, 0.0002947094729387644179, 0.0004513084665647226030 ),
 ( 0.000000000000000000, 1.000000000000000000 ),
 .UNSPECIFIED. ) 
 GEOMETRIC_REPRESENTATION_ITEM ( )  RATIONAL_B_SPLINE_SURFACE ( (
 ( 1.000000000000000000, 0.7071067811865494601, 1.000000000000000000),
 ( 1.000000000000000000, 0.6919563088099165427, 1.000000000000000000),
 ( 1.000000000000000000, 0.6959445945717444015, 1.000000000000000000),
 ( 1.000000000000000000, 0.7137882985313115380, 1.000000000000000000),
 ( 1.000000000000000000, 0.7257496306096496985, 1.000000000000000000),
 ( 1.000000000000000000, 0.7250110520819876836, 1.000000000000000000) ) ) 
 REPRESENTATION_ITEM ( '' )  SURFACE ( )  );
#180468=CIRCLE ( 'NONE', #101295, 4.000000000000003553 ) ;
#180480=AXIS2_PLACEMENT_3D ( 'NONE', #78682, #254724, #196090 ) ;
#180484=ORIENTED_EDGE ( 'NONE', *, *, #16576, .F. ) ;
#180487=CARTESIAN_POINT ( 'NONE',  ( -21.05000000000000071, 11.65000000001115232, -73.78386566297820082 ) ) ;
#180500=EDGE_LOOP ( 'NONE', ( #189573, #180126, #110865, #209847 ) ) ;
#180547=FACE_OUTER_BOUND ( 'NONE', #99161, .T. ) ;
#180551=LINE ( 'NONE', #59260, #168434 ) ;
#180580=CARTESIAN_POINT ( 'NONE',  ( 21.12769345151713196, 10.71928767695172624, -79.24748034619751991 ) ) ;
#180591=VECTOR ( 'NONE', #21764, 1000.000000000000000 ) ;
#180616=ORIENTED_EDGE ( 'NONE', *, *, #6017, .F. ) ;
#180660=LINE ( 'NONE', #102362, #257437 ) ;
#180665=EDGE_CURVE ( 'NONE', #18995, #82481, #71755, .T. ) ;
#180669=EDGE_LOOP ( 'NONE', ( #229438, #149253, #204126, #186167 ) ) ;
#180672=DIRECTION ( 'NONE',  ( 1.000000000000000000, 7.304098846218134667E-16, 0.000000000000000000 ) ) ;
#180681=ADVANCED_FACE ( 'NONE', ( #206109 ), #168315, .F. ) ;
#180691=FACE_OUTER_BOUND ( 'NONE', #106090, .T. ) ;
#180719=EDGE_CURVE ( 'NONE', #75223, #211866, #174987, .T. ) ;
#180770=ORIENTED_EDGE ( 'NONE', *, *, #162737, .F. ) ;
#180780=TOROIDAL_SURFACE ( 'NONE', #47475, 3.899999999999999467, 0.1000000000000000056 ) ;
#180792=FACE_OUTER_BOUND ( 'NONE', #122341, .T. ) ;
#180827=CARTESIAN_POINT ( 'NONE',  ( -20.64999999999999858, 1.115600667400684642E-11, -100.5000000000000426 ) ) ;
#180859=AXIS2_PLACEMENT_3D ( 'NONE', #137545, #97108, #177989 ) ;
#180869=ORIENTED_EDGE ( 'NONE', *, *, #73637, .F. ) ;
#180874=DIRECTION ( 'NONE',  ( 0.000000000000000000, 0.000000000000000000, -1.000000000000000000 ) ) ;
#180880=CARTESIAN_POINT ( 'NONE',  ( -20.64999999999999858, 1.925233644870967487, -87.76975646687391475 ) ) ;
#180882=CARTESIAN_POINT ( 'NONE',  ( 20.94999999999999929, -8.999999999988842703, -90.60603087734760663 ) ) ;
#180893=CARTESIAN_POINT ( 'NONE',  ( -22.42253884134832020, 0.001932351146464880492, -55.35039430265162252 ) ) ;
#180900=ORIENTED_EDGE ( 'NONE', *, *, #41796, .F. ) ;
#180921=DIRECTION ( 'NONE',  ( -0.000000000000000000, 1.000000000000000000, -0.000000000000000000 ) ) ;
#180942=ORIENTED_EDGE ( 'NONE', *, *, #153350, .T. ) ;
#180967=ORIENTED_EDGE ( 'NONE', *, *, #227998, .F. ) ;
#180968=DIRECTION ( 'NONE',  ( 0.000000000000000000, 0.000000000000000000, 1.000000000000000000 ) ) ;
#180979=ORIENTED_EDGE ( 'NONE', *, *, #150705, .T. ) ;
#180997=EDGE_CURVE ( 'NONE', #50892, #97606, #166776, .T. ) ;
#181016=DIRECTION ( 'NONE',  ( 0.000000000000000000, 0.000000000000000000, -1.000000000000000000 ) ) ;
#181023=VERTEX_POINT ( 'NONE', #188803 ) ;
#181032=AXIS2_PLACEMENT_3D ( 'NONE', #164896, #89198, #47491 ) ;
#181044=CARTESIAN_POINT ( 'NONE',  ( -23.15000000000000213, 11.75000000001115552, -55.25000000000004974 ) ) ;
#181054=CIRCLE ( 'NONE', #201696, 0.09999999999999939493 ) ;
#181064=CARTESIAN_POINT ( 'NONE',  ( 18.33996824403462611, -9.569639859420533412, -107.3190656375166725 ) ) ;
#181065=VERTEX_POINT ( 'NONE', #32333 ) ;
#181085=EDGE_LOOP ( 'NONE', ( #188631, #35267, #119173, #87792 ) ) ;
#181094=DIRECTION ( 'NONE',  ( -1.000000000000000000, 0.000000000000000000, 0.000000000000000000 ) ) ;
#181097=CARTESIAN_POINT ( 'NONE',  ( 22.43288208788031568, 0.004899854896538679595, -55.35034815628097249 ) ) ;
#181099=ORIENTED_EDGE ( 'NONE', *, *, #74557, .F. ) ;
#181183=EDGE_CURVE ( 'NONE', #140297, #76466, #200233, .T. ) ;
#181196=ADVANCED_FACE ( 'NONE', ( #76554 ), #113122, .F. ) ;
#181197=FACE_OUTER_BOUND ( 'NONE', #79610, .T. ) ;
#181218=ADVANCED_FACE ( 'NONE', ( #160918 ), #216808, .F. ) ;
#181219=ORIENTED_EDGE ( 'NONE', *, *, #30633, .T. ) ;
#181220=AXIS2_PLACEMENT_3D ( 'NONE', #170392, #92076, #88199 ) ;
#181231=ORIENTED_EDGE ( 'NONE', *, *, #6983, .F. ) ;
#181232=FACE_OUTER_BOUND ( 'NONE', #232677, .T. ) ;
#181239=EDGE_CURVE ( 'NONE', #17165, #187777, #66789, .T. ) ;
#181240=DIRECTION ( 'NONE',  ( -0.000000000000000000, 1.000000000000000000, 0.000000000000000000 ) ) ;
#181241=EDGE_CURVE ( 'NONE', #105777, #73858, #145173, .T. ) ;
#181251=ORIENTED_EDGE ( 'NONE', *, *, #47354, .T. ) ;
#181266=CARTESIAN_POINT ( 'NONE',  ( -18.59999999999999787, 9.250000000011157297, -79.35000000000005116 ) ) ;
#181284=EDGE_CURVE ( 'NONE', #168864, #68442, #116851, .T. ) ;
#181285=CARTESIAN_POINT ( 'NONE',  ( -18.50000000000000000, 10.29270135741298375, -105.9573618871519898 ) ) ;
#181291=DIRECTION ( 'NONE',  ( -1.000000000000000000, -0.000000000000000000, 0.000000000000000000 ) ) ;
#181292=ORIENTED_EDGE ( 'NONE', *, *, #143150, .T. ) ;
#181296=CARTESIAN_POINT ( 'NONE',  ( -20.64999999999999858, 7.150000000011155876, -79.25000000000004263 ) ) ;
#181308=ADVANCED_FACE ( 'NONE', ( #85175 ), #244276, .T. ) ;
#181330=ORIENTED_EDGE ( 'NONE', *, *, #100027, .T. ) ;
#181365=EDGE_CURVE ( 'NONE', #18615, #31646, #122175, .T. ) ;
#181403=VERTEX_POINT ( 'NONE', #9521 ) ;
#181408=DIRECTION ( 'NONE',  ( 0.000000000000000000, 0.9908441862701596881, 0.1350103645451904977 ) ) ;
#181420=DIRECTION ( 'NONE',  ( 0.000000000000000000, -1.000000000000000000, 0.000000000000000000 ) ) ;
#181422=CIRCLE ( 'NONE', #252296, 12.87499999999999822 ) ;
#181445=CARTESIAN_POINT ( 'NONE',  ( -21.11833042828136087, 0.007100509070459421791, -60.55435530614461470 ) ) ;
#181456=ORIENTED_EDGE ( 'NONE', *, *, #218641, .F. ) ;
#181486=EDGE_LOOP ( 'NONE', ( #215777, #154425, #122429, #46576 ) ) ;
#181491=ADVANCED_FACE ( 'NONE', ( #39402 ), #19827, .T. ) ;
#181504=DIRECTION ( 'NONE',  ( 0.000000000000000000, 0.000000000000000000, -1.000000000000000000 ) ) ;
#181508=CARTESIAN_POINT ( 'NONE',  ( 18.46905048506370406, -9.473744257371240707, -107.1759862922554731 ) ) ;
#181518=LINE ( 'NONE', #2839, #115892 ) ;
#181519=( GEOMETRIC_REPRESENTATION_CONTEXT ( 3 ) GLOBAL_UNCERTAINTY_ASSIGNED_CONTEXT ( ( #941 ) ) GLOBAL_UNIT_ASSIGNED_CONTEXT ( ( #199056, #80350, #200335 ) ) REPRESENTATION_CONTEXT ( 'NONE', 'WORKASPACE' ) );
#181525=DIRECTION ( 'NONE',  ( -1.000000000000000000, -1.875376730785737719E-16, -0.000000000000000000 ) ) ;
#181634=DIRECTION ( 'NONE',  ( 0.000000000000000000, 0.000000000000000000, 1.000000000000000000 ) ) ;
#181640=VERTEX_POINT ( 'NONE', #143601 ) ;
#181644=AXIS2_PLACEMENT_3D ( 'NONE', #195869, #17229, #163156 ) ;
#181668=ORIENTED_EDGE ( 'NONE', *, *, #180997, .F. ) ;
#181674=EDGE_CURVE ( 'NONE', #146445, #257922, #66965, .T. ) ;
#181711=FACE_OUTER_BOUND ( 'NONE', #19349, .T. ) ;
#181738=DIRECTION ( 'NONE',  ( -0.000000000000000000, -1.000000000000000000, -0.000000000000000000 ) ) ;
#181754=DIRECTION ( 'NONE',  ( 0.000000000000000000, 0.9908441862701596881, 0.1350103645451904977 ) ) ;
#181762=ADVANCED_FACE ( 'NONE', ( #67915 ), #31399, .T. ) ;
#181778=CARTESIAN_POINT ( 'NONE',  ( -20.94999999999999929, 7.021664781911246322, -104.3335654018973315 ) ) ;
#181781=DIRECTION ( 'NONE',  ( 0.000000000000000000, 0.000000000000000000, -1.000000000000000000 ) ) ;
#181790=CARTESIAN_POINT ( 'NONE',  ( 18.59999999999998366, 1.115600667400684642E-11, -100.5000000000000426 ) ) ;
#181797=CARTESIAN_POINT ( 'NONE',  ( 23.25000000000000000, -11.64999999998883595, -55.25000000000004974 ) ) ;
#181801=DIRECTION ( 'NONE',  ( 1.000000000000000000, -0.000000000000000000, -0.000000000000000000 ) ) ;
#181807=CARTESIAN_POINT ( 'NONE',  ( -21.64999999999999858, 7.350000000011155166, -88.15000000000004832 ) ) ;
#181830=ADVANCED_FACE ( 'NONE', ( #159040 ), #233438, .F. ) ;
#181843=VERTEX_POINT ( 'NONE', #54764 ) ;
#181852=DIRECTION ( 'NONE',  ( 0.000000000000000000, 1.000000000000000000, 0.000000000000000000 ) ) ;
#181854=ORIENTED_EDGE ( 'NONE', *, *, #183702, .T. ) ;
#181856=EDGE_CURVE ( 'NONE', #84452, #181843, #96350, .T. ) ;
#181867=CARTESIAN_POINT ( 'NONE',  ( 21.07888907270776002, 10.72506921352637654, -79.22119358683323753 ) ) ;
#181911=ADVANCED_FACE ( 'NONE', ( #196840 ), #138141, .T. ) ;
#181927=AXIS2_PLACEMENT_3D ( 'NONE', #241892, #63250, #125795 ) ;
#181928=DIRECTION ( 'NONE',  ( 1.000000000000000000, 0.000000000000000000, -0.000000000000000000 ) ) ;
#181943=DIRECTION ( 'NONE',  ( -1.000000000000000000, 0.000000000000000000, 0.000000000000000000 ) ) ;
#181963=CARTESIAN_POINT ( 'NONE',  ( -18.50000000000000000, 1.162701749949165642, -75.10000000000003695 ) ) ;
#181964=CIRCLE ( 'NONE', #99114, 0.09999999999999939493 ) ;
#182066=ORIENTED_EDGE ( 'NONE', *, *, #57442, .T. ) ;
#182099=EDGE_CURVE ( 'NONE', #179033, #143962, #192251, .T. ) ;
#182120=AXIS2_PLACEMENT_3D ( 'NONE', #73591, #153140, #35745 ) ;
#182123=FACE_OUTER_BOUND ( 'NONE', #145293, .T. ) ;
#182130=CARTESIAN_POINT ( 'NONE',  ( 20.85000000000000142, 1.115600667400684642E-11, -100.5000000000000426 ) ) ;
#182149=EDGE_CURVE ( 'NONE', #53335, #120408, #100612, .T. ) ;
#182208=DIRECTION ( 'NONE',  ( 1.000000000000000000, 3.265361837132813093E-16, -0.000000000000000000 ) ) ;
#182220=DIRECTION ( 'NONE',  ( 0.000000000000000000, 1.000000000000000000, 0.000000000000000000 ) ) ;
#182222=EDGE_CURVE ( 'NONE', #242995, #248066, #229828, .T. ) ;
#182251=CARTESIAN_POINT ( 'NONE',  ( 18.52351027002947959, -9.642162904684026259, -107.2150469505098300 ) ) ;
#182253=DIRECTION ( 'NONE',  ( -1.000000000000000000, -0.000000000000000000, -0.000000000000000000 ) ) ;
#182254=VECTOR ( 'NONE', #64572, 1000.000000000000000 ) ;
#182255=ORIENTED_EDGE ( 'NONE', *, *, #118951, .F. ) ;
#182290=ORIENTED_EDGE ( 'NONE', *, *, #206634, .T. ) ;
#182344=CARTESIAN_POINT ( 'NONE',  ( 18.59999996954842771, -9.523204137847672612, -107.3830417119164906 ) ) ;
#182372=ADVANCED_FACE ( 'NONE', ( #233141 ), #54463, .T. ) ;
#182380=CARTESIAN_POINT ( 'NONE',  ( -20.94999999999999929, -11.64999999998884483, -69.90000000000004832 ) ) ;
#182422=CARTESIAN_POINT ( 'NONE',  ( 22.47071067811865319, 0.09909245471376171288, -59.27992525550200043 ) ) ;
#182437=DIRECTION ( 'NONE',  ( 0.000000000000000000, 0.000000000000000000, -1.000000000000000000 ) ) ;
#182445=CIRCLE ( 'NONE', #211465, 7.900000000000003908 ) ;
#182467=ADVANCED_FACE ( 'NONE', ( #101241 ), #233927, .T. ) ;
#182472=EDGE_CURVE ( 'NONE', #27072, #134711, #68598, .T. ) ;
#182498=DIRECTION ( 'NONE',  ( 0.000000000000000000, -0.1495327102803586661, -0.9887567792719350601 ) ) ;
#182513=EDGE_CURVE ( 'NONE', #229956, #246051, #205518, .T. ) ;
#182562=ORIENTED_EDGE ( 'NONE', *, *, #201271, .T. ) ;
#182567=FACE_OUTER_BOUND ( 'NONE', #241159, .T. ) ;
#182568=CARTESIAN_POINT ( 'NONE',  ( 20.94999999999999574, 8.926614585098251453, -75.47168301922316402 ) ) ;
#182570=ORIENTED_EDGE ( 'NONE', *, *, #242937, .T. ) ;
#182579=CYLINDRICAL_SURFACE ( 'NONE', #14455, 0.09999999999999939493 ) ;
#182637=CARTESIAN_POINT ( 'NONE',  ( -20.64999999999999858, 2.000000000011154189, -80.22462192276213955 ) ) ;
#182673=DIRECTION ( 'NONE',  ( 0.000000000000000000, 0.000000000000000000, -1.000000000000000000 ) ) ;
#182709=CARTESIAN_POINT ( 'NONE',  ( -20.94788355080264353, 10.30207779525983014, -105.9895520716782897 ) ) ;
#182778=EDGE_CURVE ( 'NONE', #257895, #201510, #220918, .T. ) ;
#182827=CONICAL_SURFACE ( 'NONE', #257749, 4.049999999999998046, 0.7853981633974604915 ) ;
#182854=CARTESIAN_POINT ( 'NONE',  ( -21.05000000000000071, 1.115653327213047955E-11, -62.70000000000008811 ) ) ;
#182934=ADVANCED_FACE ( 'NONE', ( #212620 ), #245644, .F. ) ;
#182941=CARTESIAN_POINT ( 'NONE',  ( -21.14999999999999858, -11.74999999998884448, -67.00000000000004263 ) ) ;
#182998=CARTESIAN_POINT ( 'NONE',  ( 23.15000000000000213, -9.499999999988844479, -90.60603087734760663 ) ) ;
#183005=ADVANCED_FACE ( 'NONE', ( #34012 ), #237313, .F. ) ;
#183017=CARTESIAN_POINT ( 'NONE',  ( 21.05000000000000071, 10.72371710471867701, -79.15000000000004832 ) ) ;
#183031=CARTESIAN_POINT ( 'NONE',  ( 23.14999999999999858, 5.500000000011153745, -79.40526601891313874 ) ) ;
#183032=CARTESIAN_POINT ( 'NONE',  ( 21.05000000000000071, 1.115600667400684642E-11, -100.5000000000000426 ) ) ;
#183048=DIRECTION ( 'NONE',  ( 0.000000000000000000, -0.1350103645451876666, -0.9908441862701600211 ) ) ;
#183072=DIRECTION ( 'NONE',  ( 1.000000000000000000, 0.000000000000000000, 0.000000000000000000 ) ) ;
#183077=EDGE_CURVE ( 'NONE', #4930, #83940, #216448, .T. ) ;
#183097=DIRECTION ( 'NONE',  ( -2.252264143451594314E-15, -0.1298341882520124002, -0.9915357197604841577 ) ) ;
#183134=VERTEX_POINT ( 'NONE', #7697 ) ;
#183171=VECTOR ( 'NONE', #98410, 1000.000000000000000 ) ;
#183183=DIRECTION ( 'NONE',  ( 1.000000000000000000, 0.000000000000000000, 0.000000000000000000 ) ) ;
#183190=DIRECTION ( 'NONE',  ( -1.000000000000000000, -2.952720810173289112E-16, 0.000000000000000000 ) ) ;
#183257=ORIENTED_EDGE ( 'NONE', *, *, #134131, .T. ) ;
#183299=EDGE_CURVE ( 'NONE', #242093, #39515, #246205, .T. ) ;
#183317=EDGE_CURVE ( 'NONE', #94180, #172403, #254703, .T. ) ;
#183326=DIRECTION ( 'NONE',  ( -0.000000000000000000, -0.000000000000000000, 1.000000000000000000 ) ) ;
#183353=VECTOR ( 'NONE', #86436, 1000.000000000000000 ) ;
#183444=CARTESIAN_POINT ( 'NONE',  ( -18.47140463609786920, -9.671474685209730637, -107.1727604582741407 ) ) ;
#183458=CARTESIAN_POINT ( 'NONE',  ( -20.54999999999999716, 1.925233644870972816, -79.73024353312617052 ) ) ;
#183496=AXIS2_PLACEMENT_3D ( 'NONE', #22702, #222126, #86469 ) ;
#183498=CARTESIAN_POINT ( 'NONE',  ( -20.85000000000000142, 11.75000000001115197, -93.71613433702194129 ) ) ;
#183501=ORIENTED_EDGE ( 'NONE', *, *, #243629, .F. ) ;
#183529=CARTESIAN_POINT ( 'NONE',  ( -18.59999999999999787, 11.65000000001115232, -74.01480577065404987 ) ) ;
#183550=CARTESIAN_POINT ( 'NONE',  ( 21.05000000000000071, 5.400000000011154988, -88.09473398108696074 ) ) ;
#183559=ADVANCED_FACE ( 'NONE', ( #70711 ), #31588, .F. ) ;
#183573=ORIENTED_EDGE ( 'NONE', *, *, #195927, .T. ) ;
#183627=ORIENTED_EDGE ( 'NONE', *, *, #17538, .F. ) ;
#183629=EDGE_LOOP ( 'NONE', ( #34235, #21536, #105797, #240163 ) ) ;
#183643=CARTESIAN_POINT ( 'NONE',  ( 18.59999999999999076, 11.75000000001115907, -55.25000000000004974 ) ) ;
#183644=VERTEX_POINT ( 'NONE', #2681 ) ;
#183657=CARTESIAN_POINT ( 'NONE',  ( 22.44352723754029810, 0.009277095054436620969, -55.35027865465133345 ) ) ;
#183672=DIRECTION ( 'NONE',  ( 0.000000000000000000, 0.000000000000000000, 1.000000000000000000 ) ) ;
#183697=LINE ( 'NONE', #67589, #178000 ) ;
#183698=CARTESIAN_POINT ( 'NONE',  ( 21.07928932188134397, 1.115600667400684642E-11, -67.00000000000004263 ) ) ;
#183702=EDGE_CURVE ( 'NONE', #137777, #211036, #82197, .T. ) ;
#183710=DIRECTION ( 'NONE',  ( 0.000000000000000000, 0.000000000000000000, 1.000000000000000000 ) ) ;
#183712=ORIENTED_EDGE ( 'NONE', *, *, #124742, .F. ) ;
#183730=EDGE_LOOP ( 'NONE', ( #28970, #101766, #32948, #10388 ) ) ;
#183733=DIRECTION ( 'NONE',  ( 0.000000000000000000, -0.9999176327611369874, 0.01283462868041987913 ) ) ;
#183743=CARTESIAN_POINT ( 'NONE',  ( 21.05000000000000071, 10.68429367439822997, -74.52667393863758605 ) ) ;
#183767=CARTESIAN_POINT ( 'NONE',  ( -23.15000000000000213, -11.64999999998884483, -97.50000000000004263 ) ) ;
#183820=EDGE_CURVE ( 'NONE', #244409, #115244, #96684, .T. ) ;
#183825=DIRECTION ( 'NONE',  ( 0.000000000000000000, 0.000000000000000000, -1.000000000000000000 ) ) ;
#183830=DIRECTION ( 'NONE',  ( 0.000000000000000000, 1.000000000000000000, 0.000000000000000000 ) ) ;
#183843=FACE_OUTER_BOUND ( 'NONE', #93123, .T. ) ;
#183907=ADVANCED_FACE ( 'NONE', ( #232036 ), #53378, .T. ) ;
#183920=VERTEX_POINT ( 'NONE', #233324 ) ;
#183986=FACE_OUTER_BOUND ( 'NONE', #6506, .T. ) ;
#183991=CARTESIAN_POINT ( 'NONE',  ( -21.05000000000000071, 1.115526128501326264E-11, -60.45934304829882677 ) ) ;
#183993=AXIS2_PLACEMENT_3D ( 'NONE', #48458, #5459, #246655 ) ;
#184034=CIRCLE ( 'NONE', #34230, 0.5000000000000004441 ) ;
#184050=CARTESIAN_POINT ( 'NONE',  ( -18.59999999999999787, 1.162701749949165642, -75.10000000000003695 ) ) ;
#184081=AXIS2_PLACEMENT_3D ( 'NONE', #106683, #224071, #107993 ) ;
#184100=CYLINDRICAL_SURFACE ( 'NONE', #169905, 0.09999999999999939493 ) ;
#184114=DIRECTION ( 'NONE',  ( 4.408576920032447355E-17, -0.1350103645451876666, 0.9908441862701600211 ) ) ;
#184154=ADVANCED_FACE ( 'NONE', ( #106270 ), #30636, .F. ) ;
#184163=EDGE_LOOP ( 'NONE', ( #46628, #204763, #122728, #131874 ) ) ;
#184176=CARTESIAN_POINT ( 'NONE',  ( -21.03922262424656253, 11.62390063401577933, -73.85920804289372654 ) ) ;
#184182=ADVANCED_FACE ( 'NONE', ( #5891 ), #46812, .T. ) ;
#184247=DIRECTION ( 'NONE',  ( -1.000000000000000000, 0.000000000000000000, 0.000000000000000000 ) ) ;
#184251=EDGE_CURVE ( 'NONE', #151819, #159539, #59291, .T. ) ;
#184310=CARTESIAN_POINT ( 'NONE',  ( -18.50000000000000000, -1.866714910046153308, -78.75267524628205251 ) ) ;
#184313=DIRECTION ( 'NONE',  ( -0.000000000000000000, -0.8700118002898321601, 0.4930308989875230030 ) ) ;
#184316=ORIENTED_EDGE ( 'NONE', *, *, #19670, .F. ) ;
#184322=DIRECTION ( 'NONE',  ( -0.000000000000000000, 0.000000000000000000, 1.000000000000000000 ) ) ;
#184330=CARTESIAN_POINT ( 'NONE',  ( 21.05000000000000071, 6.540656951712400691, -67.00000000000004263 ) ) ;
#184348=ORIENTED_EDGE ( 'NONE', *, *, #54643, .T. ) ;
#184385=AXIS2_PLACEMENT_3D ( 'NONE', #192362, #52834, #151979 ) ;
#184391=FACE_BOUND ( 'NONE', #14276, .T. ) ;
#184416=VECTOR ( 'NONE', #149576, 1000.000000000000000 ) ;
#184442=EDGE_CURVE ( 'NONE', #201917, #374, #255049, .T. ) ;
#184449=CARTESIAN_POINT ( 'NONE',  ( -23.15000000000000213, 1.115600667400684642E-11, -71.05000000000003979 ) ) ;
#184459=ADVANCED_FACE ( 'NONE', ( #42180 ), #119146, .T. ) ;
#184493=CARTESIAN_POINT ( 'NONE',  ( 23.14999999999998437, 1.115600667400684642E-11, -67.00000000000004263 ) ) ;
#184517=CARTESIAN_POINT ( 'NONE',  ( -18.59999999999999787, -1.835341550213255957, -78.65515129256301918 ) ) ;
#184532=CARTESIAN_POINT ( 'NONE',  ( 18.49999999999999289, 6.450000000011156587, -88.15000000000004832 ) ) ;
#184535=CARTESIAN_POINT ( 'NONE',  ( -23.25000000000000000, -11.48912529306489994, -97.40000000000004832 ) ) ;
#184537=CYLINDRICAL_SURFACE ( 'NONE', #253799, 0.1000000000000028644 ) ;
#184539=CARTESIAN_POINT ( 'NONE',  ( -20.15000000000000568, 9.291421356248463326, -79.35000000000005116 ) ) ;
#184545=AXIS2_PLACEMENT_3D ( 'NONE', #96855, #21379, #160885 ) ;
#184554=CIRCLE ( 'NONE', #67863, 0.1000000000000028644 ) ;
#184594=CARTESIAN_POINT ( 'NONE',  ( 18.49999999999999289, 10.23906162413259402, -91.75439743459725150 ) ) ;
#184615=TOROIDAL_SURFACE ( 'NONE', #80536, 11.89999999999999858, 0.1000000000000000056 ) ;
#184627=DIRECTION ( 'NONE',  ( 0.000000000000000000, 0.000000000000000000, -1.000000000000000000 ) ) ;
#184637=CARTESIAN_POINT ( 'NONE',  ( 20.95520789717937404, 10.57693059939611224, -74.58023297387489947 ) ) ;
#184640=DIRECTION ( 'NONE',  ( 0.000000000000000000, 0.000000000000000000, -1.000000000000000000 ) ) ;
#184710=EDGE_CURVE ( 'NONE', #50987, #76744, #184554, .T. ) ;
#184713=DIRECTION ( 'NONE',  ( 1.000000000000000000, -0.000000000000000000, -0.000000000000000000 ) ) ;
#184731=AXIS2_PLACEMENT_3D ( 'NONE', #249255, #94007, #173617 ) ;
#184752=VERTEX_POINT ( 'NONE', #111131 ) ;
#184754=CARTESIAN_POINT ( 'NONE',  ( 20.94999999999999574, -1.835341550213255957, -78.55515129256302487 ) ) ;
#184762=EDGE_CURVE ( 'NONE', #178346, #214744, #232386, .T. ) ;
#184885=CARTESIAN_POINT ( 'NONE',  ( -22.39999999999999858, 7.790779598384560245, -66.90000000000004832 ) ) ;
#184947=AXIS2_PLACEMENT_3D ( 'NONE', #234083, #189838, #114137 ) ;
#184961=ORIENTED_EDGE ( 'NONE', *, *, #132700, .T. ) ;
#184964=ORIENTED_EDGE ( 'NONE', *, *, #156955, .F. ) ;
#184967=DIRECTION ( 'NONE',  ( 0.000000000000000000, 0.000000000000000000, -1.000000000000000000 ) ) ;
#184974=CARTESIAN_POINT ( 'NONE',  ( 21.05000000000000071, -1.736257131586239844, -78.56865232901753870 ) ) ;
#185003=ORIENTED_EDGE ( 'NONE', *, *, #139679, .T. ) ;
#185018=ADVANCED_FACE ( 'NONE', ( #69157 ), #187818, .T. ) ;
#185029=CARTESIAN_POINT ( 'NONE',  ( -18.39999999999999858, -9.499999999988849808, -74.03206939669971121 ) ) ;
#185062=CIRCLE ( 'NONE', #218361, 0.2000000000000005107 ) ;
#185068=ADVANCED_FACE ( 'NONE', ( #127834 ), #1389, .T. ) ;
#185092=FACE_OUTER_BOUND ( 'NONE', #73661, .T. ) ;
#185120=DIRECTION ( 'NONE',  ( 1.000000000000000000, -0.000000000000000000, -0.000000000000000000 ) ) ;
#185135=CARTESIAN_POINT ( 'NONE',  ( 20.96077737575326694, 11.62390063401587348, -93.64079195710665715 ) ) ;
#185159=AXIS2_PLACEMENT_3D ( 'NONE', #97285, #56883, #174352 ) ;
#185164=EDGE_CURVE ( 'NONE', #185550, #6865, #76398, .T. ) ;
#185179=ADVANCED_FACE ( 'NONE', ( #194247 ), #174707, .T. ) ;
#185199=ORIENTED_EDGE ( 'NONE', *, *, #250888, .F. ) ;
#185209=DIRECTION ( 'NONE',  ( -1.000000000000000000, -0.000000000000000000, -0.000000000000000000 ) ) ;
#185255=DIRECTION ( 'NONE',  ( 0.000000000000000000, -0.000000000000000000, 1.000000000000000000 ) ) ;
#185259=CARTESIAN_POINT ( 'NONE',  ( -18.50000000000000000, 11.65000000001115232, -55.25000000000004974 ) ) ;
#185284=FACE_OUTER_BOUND ( 'NONE', #107331, .T. ) ;
#185324=CARTESIAN_POINT ( 'NONE',  ( 18.59999999999999787, -1.249999999988843369, -108.3004807544151191 ) ) ;
#185331=VECTOR ( 'NONE', #96492, 1000.000000000000000 ) ;
#185358=ORIENTED_EDGE ( 'NONE', *, *, #182472, .F. ) ;
#185381=ORIENTED_EDGE ( 'NONE', *, *, #227096, .T. ) ;
#185472=CARTESIAN_POINT ( 'NONE',  ( -21.45000000000000284, 7.708578643773852157, -88.25000000000005684 ) ) ;
#185486=FACE_OUTER_BOUND ( 'NONE', #211963, .T. ) ;
#185515=AXIS2_PLACEMENT_3D ( 'NONE', #74248, #192883, #175905 ) ;
#185544=DIRECTION ( 'NONE',  ( 1.000000000000000000, 0.000000000000000000, 0.000000000000000000 ) ) ;
#185550=VERTEX_POINT ( 'NONE', #128812 ) ;
#185552=EDGE_CURVE ( 'NONE', #61933, #230047, #68844, .T. ) ;
#185558=CARTESIAN_POINT ( 'NONE',  ( -23.25000000000000000, -11.74999999998884448, -55.25000000000004974 ) ) ;
#185579=AXIS2_PLACEMENT_3D ( 'NONE', #103059, #144753, #245167 ) ;
#185597=EDGE_LOOP ( 'NONE', ( #179732, #197949, #141287, #201181 ) ) ;
#185607=DIRECTION ( 'NONE',  ( 0.000000000000000000, -0.9999631594459056361, -0.008583690987124413183 ) ) ;
#185615=ORIENTED_EDGE ( 'NONE', *, *, #55122, .T. ) ;
#185616=CARTESIAN_POINT ( 'NONE',  ( 21.05000000000000071, 6.350000000011161383, -76.84382208968317229 ) ) ;
#185617=CARTESIAN_POINT ( 'NONE',  ( 20.95512828230152280, 8.876151312336450161, -79.20243026550316756 ) ) ;
#185622=AXIS2_PLACEMENT_3D ( 'NONE', #242485, #80832, #160424 ) ;
#185638=EDGE_CURVE ( 'NONE', #83997, #72480, #59494, .T. ) ;
#185646=DIRECTION ( 'NONE',  ( 1.000000000000000000, 0.000000000000000000, 0.000000000000000000 ) ) ;
#185683=CARTESIAN_POINT ( 'NONE',  ( -23.15000000000000213, 4.350000000011156054, -88.15000000000004832 ) ) ;
#185692=DIRECTION ( 'NONE',  ( 0.000000000000000000, 0.000000000000000000, -1.000000000000000000 ) ) ;
#185694=CARTESIAN_POINT ( 'NONE',  ( 20.89192007715127986, 10.32898536001801304, -106.0826683222764899 ) ) ;
#185700=EDGE_LOOP ( 'NONE', ( #61211, #225240, #39570, #141810 ) ) ;
#185702=DIRECTION ( 'NONE',  ( 1.000000000000000000, 0.000000000000000000, 0.000000000000000000 ) ) ;
#185715=CIRCLE ( 'NONE', #39993, 7.791421356237310469 ) ;
#185728=DIRECTION ( 'NONE',  ( 1.000000000000000000, 0.000000000000000000, 0.000000000000000000 ) ) ;
#185741=DIRECTION ( 'NONE',  ( -0.000000000000000000, 0.000000000000000000, 1.000000000000000000 ) ) ;
#185747=DIRECTION ( 'NONE',  ( 3.616040088954497272E-32, -1.224646799147352961E-16, 1.000000000000000000 ) ) ;
#185748=DIRECTION ( 'NONE',  ( 2.694716079187272946E-16, -1.000000000000000000, 0.000000000000000000 ) ) ;
#185771=CARTESIAN_POINT ( 'NONE',  ( -21.07954640115336176, 6.329287696035376776, -66.93399229286031016 ) ) ;
#185823=ORIENTED_EDGE ( 'NONE', *, *, #107424, .F. ) ;
#185830=CIRCLE ( 'NONE', #227351, 12.87499999999999822 ) ;
#185839=CIRCLE ( 'NONE', #139857, 11.89999999999999325 ) ;
#185845=ORIENTED_EDGE ( 'NONE', *, *, #135082, .T. ) ;
#185879=VECTOR ( 'NONE', #78779, 1000.000000000000000 ) ;
#185886=ORIENTED_EDGE ( 'NONE', *, *, #4562, .T. ) ;
#185887=ORIENTED_EDGE ( 'NONE', *, *, #86162, .T. ) ;
#185927=EDGE_LOOP ( 'NONE', ( #28487, #56861, #55109, #104163 ) ) ;
#185928=EDGE_CURVE ( 'NONE', #161687, #43295, #43823, .T. ) ;
#185929=DIRECTION ( 'NONE',  ( 0.7071067811865388020, -0.7071067811865561215, 0.000000000000000000 ) ) ;
#185938=CARTESIAN_POINT ( 'NONE',  ( 20.94999999999997442, -1.263275465206102233, -108.4018646667464481 ) ) ;
#185944=AXIS2_PLACEMENT_3D ( 'NONE', #111524, #191084, #214457 ) ;
#185945=B_SPLINE_CURVE_WITH_KNOTS ( 'NONE', 3,
 ( #203080, #179689, #122273, #243491, #182251, #61002, #83097, #102675 ),
 .UNSPECIFIED., .F., .F.,
 ( 4, 2, 2, 4 ),
 ( 0.000000000000000000, 0.0002181133598169135998, 0.0003271700397253561425, 0.0004362267196337987936 ),
 .UNSPECIFIED. ) ;
#185973=AXIS2_PLACEMENT_3D ( 'NONE', #230030, #9692, #89226 ) ;
#185979=CARTESIAN_POINT ( 'NONE',  ( 23.14999999999999858, 5.950000000011160139, -90.19429769496522908 ) ) ;
#185981=AXIS2_PLACEMENT_3D ( 'NONE', #231619, #235437, #52955 ) ;
#185992=CIRCLE ( 'NONE', #102760, 0.09999999999999939493 ) ;
#186005=DIRECTION ( 'NONE',  ( 0.000000000000000000, -1.000000000000000000, 0.000000000000000000 ) ) ;
#186030=EDGE_CURVE ( 'NONE', #179663, #140297, #251942, .T. ) ;
#186098=ORIENTED_EDGE ( 'NONE', *, *, #219772, .T. ) ;
#186113=ORIENTED_EDGE ( 'NONE', *, *, #30699, .F. ) ;
#186152=AXIS2_PLACEMENT_3D ( 'NONE', #174808, #39121, #75674 ) ;
#186167=ORIENTED_EDGE ( 'NONE', *, *, #481, .F. ) ;
#186181=CARTESIAN_POINT ( 'NONE',  ( -23.15000000000000213, 11.75000000001116263, -79.15000000000004832 ) ) ;
#186205=LINE ( 'NONE', #183643, #234932 ) ;
#186214=ORIENTED_EDGE ( 'NONE', *, *, #177181, .T. ) ;
#186237=CARTESIAN_POINT ( 'NONE',  ( 21.05000000000000071, 10.72371710471867701, -74.66491356908764487 ) ) ;
#186258=ADVANCED_FACE ( 'NONE', ( #48325 ), #9199, .T. ) ;
#186267=ORIENTED_EDGE ( 'NONE', *, *, #240118, .T. ) ;
#186271=DIRECTION ( 'NONE',  ( 1.000000000000000000, -0.000000000000000000, -0.000000000000000000 ) ) ;
#186281=EDGE_LOOP ( 'NONE', ( #203499, #44811, #45439, #136541 ) ) ;
#186288=ORIENTED_EDGE ( 'NONE', *, *, #209262, .F. ) ;
#186291=AXIS2_PLACEMENT_3D ( 'NONE', #160446, #20934, #236096 ) ;
#186357=VECTOR ( 'NONE', #75173, 1000.000000000000000 ) ;
#186400=EDGE_LOOP ( 'NONE', ( #237109, #226473, #90976, #5723 ) ) ;
#186434=CARTESIAN_POINT ( 'NONE',  ( 20.99551997958378635, 11.75000000001123901, -93.65165913769003225 ) ) ;
#186461=ORIENTED_EDGE ( 'NONE', *, *, #204459, .F. ) ;
#186462=ORIENTED_EDGE ( 'NONE', *, *, #182472, .T. ) ;
#186464=CARTESIAN_POINT ( 'NONE',  ( -18.31572283045302285, -9.548437830874318522, -107.3506256510583086 ) ) ;
#186493=EDGE_LOOP ( 'NONE', ( #134036, #97622, #145896, #225391 ) ) ;
#186518=ORIENTED_EDGE ( 'NONE', *, *, #54710, .F. ) ;
#186521=CIRCLE ( 'NONE', #231746, 0.1000000000000028644 ) ;
#186531=CARTESIAN_POINT ( 'NONE',  ( -21.05000000000000071, 1.162701749949165642, -75.10000000000003695 ) ) ;
#186541=ORIENTED_EDGE ( 'NONE', *, *, #135206, .F. ) ;
#186543=ADVANCED_FACE ( 'NONE', ( #101540 ), #160298, .T. ) ;
#186561=CIRCLE ( 'NONE', #128292, 2.100000000000002309 ) ;
#186576=CARTESIAN_POINT ( 'NONE',  ( 20.94999999999999929, 1.115600667400684642E-11, -100.5000000000000426 ) ) ;
#186583=DIRECTION ( 'NONE',  ( 0.000000000000000000, 0.000000000000000000, -1.000000000000000000 ) ) ;
#186623=DIRECTION ( 'NONE',  ( 1.000000000000000000, -0.000000000000000000, -0.000000000000000000 ) ) ;
#186629=CARTESIAN_POINT ( 'NONE',  ( -21.65000000000000213, 7.708578643773852157, -79.25000000000004263 ) ) ;
#186651=EDGE_CURVE ( 'NONE', #60888, #188088, #222789, .T. ) ;
#186670=DIRECTION ( 'NONE',  ( 0.000000000000000000, 0.000000000000000000, -1.000000000000000000 ) ) ;
#186672=ORIENTED_EDGE ( 'NONE', *, *, #215716, .F. ) ;
#186722=CARTESIAN_POINT ( 'NONE',  ( 18.49999999999999289, 10.25000000001115552, -88.35000000000003695 ) ) ;
#186760=AXIS2_PLACEMENT_3D ( 'NONE', #118671, #95231, #233485 ) ;
#186770=DIRECTION ( 'NONE',  ( 0.000000000000000000, 0.000000000000000000, -1.000000000000000000 ) ) ;
#186773=CARTESIAN_POINT ( 'NONE',  ( -20.94999999999999574, 11.75000000001115552, -73.84160068989719150 ) ) ;
#186791=FACE_OUTER_BOUND ( 'NONE', #125193, .T. ) ;
#186814=ORIENTED_EDGE ( 'NONE', *, *, #239861, .T. ) ;
#186843=CARTESIAN_POINT ( 'NONE',  ( 20.85000000000000142, 11.65000000001115943, -93.71613433702195550 ) ) ;
#186851=ORIENTED_EDGE ( 'NONE', *, *, #188421, .T. ) ;
#186867=DIRECTION ( 'NONE',  ( 1.000000000000000000, 0.000000000000000000, -0.000000000000000000 ) ) ;
#186914=ORIENTED_EDGE ( 'NONE', *, *, #213966, .F. ) ;
#186921=CARTESIAN_POINT ( 'NONE',  ( -21.05000000000000071, 1.115600667400684642E-11, -88.80000000000003979 ) ) ;
#186951=CARTESIAN_POINT ( 'NONE',  ( 22.39999999999999503, 11.75000000001116263, -67.10000000000005116 ) ) ;
#186974=DIRECTION ( 'NONE',  ( 1.000000000000000000, 0.000000000000000000, 0.000000000000000000 ) ) ;
#186988=CARTESIAN_POINT ( 'NONE',  ( -20.54999999999999716, 1.115600667400684642E-11, -67.00000000000004263 ) ) ;
#186990=DIRECTION ( 'NONE',  ( 0.000000000000000000, -1.000000000000000000, 0.000000000000000000 ) ) ;
#186997=CARTESIAN_POINT ( 'NONE',  ( -21.14999999999999858, 1.115600667400684642E-11, -60.74142135623734617 ) ) ;
#186999=CARTESIAN_POINT ( 'NONE',  ( 20.94999027547553894, 10.29326151435327219, -105.9592822510415431 ) ) ;
#187031=ADVANCED_FACE ( 'NONE', ( #3435 ), #172028, .F. ) ;
#187093=CIRCLE ( 'NONE', #3725, 2.100000000000004530 ) ;
#187113=CARTESIAN_POINT ( 'NONE',  ( 18.52643265882457868, 10.31973158071402885, -106.0505334713354983 ) ) ;
#187117=ORIENTED_EDGE ( 'NONE', *, *, #171061, .F. ) ;
#187119=CARTESIAN_POINT ( 'NONE',  ( -20.54999999999999716, 4.350000000011156054, -88.15000000000004832 ) ) ;
#187241=ORIENTED_EDGE ( 'NONE', *, *, #4499, .T. ) ;
#187249=CARTESIAN_POINT ( 'NONE',  ( -23.15000000000000213, -8.663551401858004652, -76.52410111806734960 ) ) ;
#187250=DIRECTION ( 'NONE',  ( 0.000000000000000000, 0.000000000000000000, -1.000000000000000000 ) ) ;
#187290=CARTESIAN_POINT ( 'NONE',  ( 22.39999999999999503, 1.115600667400684642E-11, -59.20922040162666633 ) ) ;
#187296=CARTESIAN_POINT ( 'NONE',  ( -23.15000000000000213, 1.115600667400684642E-11, -100.5000000000000426 ) ) ;
#187297=FACE_OUTER_BOUND ( 'NONE', #97979, .T. ) ;
#187316=CARTESIAN_POINT ( 'NONE',  ( -23.15000000000000213, 1.115600667400684642E-11, -67.00000000000004263 ) ) ;
#187354=VERTEX_POINT ( 'NONE', #242894 ) ;
#187363=ORIENTED_EDGE ( 'NONE', *, *, #121550, .F. ) ;
#187394=VERTEX_POINT ( 'NONE', #148952 ) ;
#187409=VERTEX_POINT ( 'NONE', #254578 ) ;
#187441=VERTEX_POINT ( 'NONE', #154277 ) ;
#187477=EDGE_LOOP ( 'NONE', ( #247732, #107328, #249992, #57110 ) ) ;
#187519=DIRECTION ( 'NONE',  ( 0.000000000000000000, 0.000000000000000000, 1.000000000000000000 ) ) ;
#187545=ORIENTED_EDGE ( 'NONE', *, *, #122426, .F. ) ;
#187610=CARTESIAN_POINT ( 'NONE',  ( 20.95512820512820085, 10.62384868372303615, -74.66491356908764487 ) ) ;
#187619=DIRECTION ( 'NONE',  ( 0.000000000000000000, 0.000000000000000000, -1.000000000000000000 ) ) ;
#187656=DIRECTION ( 'NONE',  ( 1.000000000000000000, 7.304098846218134667E-16, -4.607487905232622991E-31 ) ) ;
#187659=CARTESIAN_POINT ( 'NONE',  ( 23.15000000000000213, -9.599999999988842347, -90.60603087734760663 ) ) ;
#187677=CARTESIAN_POINT ( 'NONE',  ( -20.93284271247462058, 11.75000000001115019, -93.48519422934609224 ) ) ;
#187688=CIRCLE ( 'NONE', #12908, 0.1000000000000028644 ) ;
#187758=CARTESIAN_POINT ( 'NONE',  ( -18.58744394320964233, -9.566385154537629276, -107.3228480538757310 ) ) ;
#187772=VERTEX_POINT ( 'NONE', #251408 ) ;
#187777=VERTEX_POINT ( 'NONE', #206190 ) ;
#187788=CARTESIAN_POINT ( 'NONE',  ( -20.07928932188135107, 9.220710678129810489, -79.35000000000005116 ) ) ;
#187809=DIRECTION ( 'NONE',  ( 1.000000000000000000, 0.000000000000000000, -0.000000000000000000 ) ) ;
#187818=SPHERICAL_SURFACE ( 'NONE', #209708, 0.1000000000000000056 ) ;
#187820=VERTEX_POINT ( 'NONE', #196563 ) ;
#187821=AXIS2_PLACEMENT_3D ( 'NONE', #89599, #90893, #149615 ) ;
#187825=CARTESIAN_POINT ( 'NONE',  ( -21.05000000000000426, 6.332272273946816910, -67.03753606328571379 ) ) ;
#187833=CIRCLE ( 'NONE', #75410, 0.1000000000000028644 ) ;
#187856=FACE_OUTER_BOUND ( 'NONE', #118514, .T. ) ;
#187886=DIRECTION ( 'NONE',  ( 0.000000000000000000, 0.000000000000000000, 1.000000000000000000 ) ) ;
#187932=CARTESIAN_POINT ( 'NONE',  ( 20.94999999999999929, 6.650000000011155876, -88.25000000000005684 ) ) ;
#187980=LINE ( 'NONE', #112298, #9930 ) ;
#188040=CIRCLE ( 'NONE', #129765, 0.1000000000000028644 ) ;
#188044=ORIENTED_EDGE ( 'NONE', *, *, #173862, .F. ) ;
#188050=CARTESIAN_POINT ( 'NONE',  ( -20.97625342178416474, 11.60000000083146077, -73.92820322980200842 ) ) ;
#188072=LINE ( 'NONE', #68123, #65725 ) ;
#188087=CYLINDRICAL_SURFACE ( 'NONE', #85745, 0.1000000000000028644 ) ;
#188088=VERTEX_POINT ( 'NONE', #223816 ) ;
#188095=EDGE_LOOP ( 'NONE', ( #78398, #242537, #59281, #216911, #227505, #249529, #202083, #27101, #169113, #175254, #21847, #18473, #140491, #198795, #154059, #63723, #237644, #256538, #51124, #186914, #132515, #112402, #159503 ) ) ;
#188126=VERTEX_POINT ( 'NONE', #107733 ) ;
#188135=FACE_OUTER_BOUND ( 'NONE', #186400, .T. ) ;
#188161=PLANE ( 'NONE',  #221375 ) ;
#188191=CARTESIAN_POINT ( 'NONE',  ( 21.13461538461538325, 8.885417037985614996, -79.25000000000004263 ) ) ;
#188276=ORIENTED_EDGE ( 'NONE', *, *, #174249, .F. ) ;
#188290=ORIENTED_EDGE ( 'NONE', *, *, #35833, .F. ) ;
#188298=FACE_OUTER_BOUND ( 'NONE', #220601, .T. ) ;
#188334=VECTOR ( 'NONE', #188527, 1000.000000000000000 ) ;
#188344=FACE_OUTER_BOUND ( 'NONE', #70723, .T. ) ;
#188347=EDGE_LOOP ( 'NONE', ( #2851, #169262, #85028, #23093 ) ) ;
#188364=CARTESIAN_POINT ( 'NONE',  ( -18.40000000000000568, -9.499999999988851584, -73.99936209718016755 ) ) ;
#188370=DIRECTION ( 'NONE',  ( 0.9880948137434723000, 0.1538461538461484146, -0.000000000000000000 ) ) ;
#188376=DIRECTION ( 'NONE',  ( -0.000000000000000000, 1.000000000000000000, -1.224646799147352961E-16 ) ) ;
#188395=ADVANCED_FACE ( 'NONE', ( #202676 ), #40286, .F. ) ;
#188413=EDGE_LOOP ( 'NONE', ( #11695, #146288, #212868, #37569 ) ) ;
#188421=EDGE_CURVE ( 'NONE', #143795, #188088, #185992, .T. ) ;
#188435=DIRECTION ( 'NONE',  ( 1.000000000000000000, -0.000000000000000000, -0.000000000000000000 ) ) ;
#188475=DIRECTION ( 'NONE',  ( 1.000000000000000000, 0.000000000000000000, 0.000000000000000000 ) ) ;
#188483=CARTESIAN_POINT ( 'NONE',  ( 20.72390388899108515, 10.58996311843486993, -74.51134829574417040 ) ) ;
#188488=CIRCLE ( 'NONE', #113477, 0.3999999999999975797 ) ;
#188527=DIRECTION ( 'NONE',  ( -1.000000000000000000, 0.000000000000000000, 0.000000000000000000 ) ) ;
#188559=EDGE_CURVE ( 'NONE', #12719, #63408, #200365, .T. ) ;
#188622=AXIS2_PLACEMENT_3D ( 'NONE', #47398, #245623, #27893 ) ;
#188631=ORIENTED_EDGE ( 'NONE', *, *, #199968, .T. ) ;
#188644=CARTESIAN_POINT ( 'NONE',  ( 20.85000000000000142, 7.021664781911246322, -104.3335654018973315 ) ) ;
#188672=CIRCLE ( 'NONE', #47010, 0.09999999999999761857 ) ;
#188711=EDGE_CURVE ( 'NONE', #214700, #130026, #52322, .T. ) ;
#188742=CYLINDRICAL_SURFACE ( 'NONE', #228234, 4.000000000000003553 ) ;
#188757=AXIS2_PLACEMENT_3D ( 'NONE', #235773, #16753, #233244 ) ;
#188758=CARTESIAN_POINT ( 'NONE',  ( -21.05000000000000071, -1.851028230129704522, -78.65391326942254580 ) ) ;
#188787=CARTESIAN_POINT ( 'NONE',  ( -18.50000000000000000, 5.341242990002803559, -57.19334979351202719 ) ) ;
#188792=ORIENTED_EDGE ( 'NONE', *, *, #38822, .F. ) ;
#188803=CARTESIAN_POINT ( 'NONE',  ( 21.05000000000000071, 5.850000000011105428, -77.13249722427801203 ) ) ;
#188804=AXIS2_PLACEMENT_3D ( 'NONE', #5440, #100683, #81139 ) ;
#188816=DIRECTION ( 'NONE',  ( 1.000000000000000000, 0.000000000000000000, -0.000000000000000000 ) ) ;
#188822=CARTESIAN_POINT ( 'NONE',  ( 18.59999999999999076, 10.20857864377385127, -88.35000000000003695 ) ) ;
#188836=DIRECTION ( 'NONE',  ( 1.000000000000000000, 0.000000000000000000, 0.000000000000000000 ) ) ;
#188839=DIRECTION ( 'NONE',  ( 0.000000000000000000, 0.000000000000000000, -1.000000000000000000 ) ) ;
#188852=CIRCLE ( 'NONE', #180480, 0.1000000000000002554 ) ;
#188874=EDGE_CURVE ( 'NONE', #87673, #27504, #139809, .T. ) ;
#188904=ORIENTED_EDGE ( 'NONE', *, *, #256246, .T. ) ;
#188920=DIRECTION ( 'NONE',  ( -1.000000000000000000, -0.000000000000000000, 0.000000000000000000 ) ) ;
#188924=CARTESIAN_POINT ( 'NONE',  ( -22.47007471830799474, 1.115297090792388701E-11, -59.27928934807356143 ) ) ;
#188934=ORIENTED_EDGE ( 'NONE', *, *, #251052, .F. ) ;
#188948=DIRECTION ( 'NONE',  ( 2.557131231893037478E-16, -0.8660254037844385966, 0.5000000000000003331 ) ) ;
#188971=VERTEX_POINT ( 'NONE', #116133 ) ;
#188992=ORIENTED_EDGE ( 'NONE', *, *, #231751, .T. ) ;
#189013=ORIENTED_EDGE ( 'NONE', *, *, #55160, .F. ) ;
#189024=AXIS2_PLACEMENT_3D ( 'NONE', #195027, #16388, #76320 ) ;
#189026=CARTESIAN_POINT ( 'NONE',  ( -18.40000000000000213, -9.499999999988849808, -107.4221498493304949 ) ) ;
#189032=DIRECTION ( 'NONE',  ( 1.000000000000000000, 0.000000000000000000, 0.000000000000000000 ) ) ;
#189036=ORIENTED_EDGE ( 'NONE', *, *, #244800, .T. ) ;
#189037=DIRECTION ( 'NONE',  ( 0.000000000000000000, 0.9998779222360096863, -0.01562500000001061998 ) ) ;
#189061=VERTEX_POINT ( 'NONE', #54842 ) ;
#189069=ADVANCED_FACE ( 'NONE', ( #194398 ), #31481, .F. ) ;
#189084=ORIENTED_EDGE ( 'NONE', *, *, #103227, .F. ) ;
#189095=DIRECTION ( 'NONE',  ( 0.000000000000000000, 2.891205793294679805E-16, -1.000000000000000000 ) ) ;
#189112=DIRECTION ( 'NONE',  ( -0.000000000000000000, -0.000000000000000000, 1.000000000000000000 ) ) ;
#189183=LINE ( 'NONE', #185324, #209065 ) ;
#189184=VECTOR ( 'NONE', #237719, 1000.000000000000000 ) ;
#189194=CIRCLE ( 'NONE', #89399, 0.1000000000000028644 ) ;
#189196=CARTESIAN_POINT ( 'NONE',  ( 21.05000000000000071, 1.115600667400684642E-11, -100.5000000000000426 ) ) ;
#189321=CIRCLE ( 'NONE', #39516, 11.65000000000000746 ) ;
#189334=ORIENTED_EDGE ( 'NONE', *, *, #189465, .T. ) ;
#189349=CARTESIAN_POINT ( 'NONE',  ( -21.05000000000000071, -11.41227409413852989, -70.00000000000004263 ) ) ;
#189387=ORIENTED_EDGE ( 'NONE', *, *, #45499, .F. ) ;
#189461=VERTEX_POINT ( 'NONE', #152401 ) ;
#189463=CIRCLE ( 'NONE', #135272, 0.1000000000000028644 ) ;
#189465=EDGE_CURVE ( 'NONE', #66864, #57960, #174559, .T. ) ;
#189466=DIRECTION ( 'NONE',  ( 0.000000000000000000, 0.000000000000000000, -1.000000000000000000 ) ) ;
#189474=VERTEX_POINT ( 'NONE', #192790 ) ;
#189484=FACE_OUTER_BOUND ( 'NONE', #103001, .T. ) ;
#189527=CARTESIAN_POINT ( 'NONE',  ( 22.49999999999999645, 11.64957080755595520, -66.90000000000004832 ) ) ;
#189542=FACE_OUTER_BOUND ( 'NONE', #133468, .T. ) ;
#189558=AXIS2_PLACEMENT_3D ( 'NONE', #43419, #60399, #122967 ) ;
#189573=ORIENTED_EDGE ( 'NONE', *, *, #255068, .T. ) ;
#189602=ORIENTED_EDGE ( 'NONE', *, *, #123062, .T. ) ;
#189611=DIRECTION ( 'NONE',  ( 0.000000000000000000, -0.000000000000000000, 1.000000000000000000 ) ) ;
#189644=ORIENTED_EDGE ( 'NONE', *, *, #195768, .T. ) ;
#189649=DIRECTION ( 'NONE',  ( 1.000000000000000000, 2.952720810173289112E-16, -0.000000000000000000 ) ) ;
#189671=DIRECTION ( 'NONE',  ( 0.000000000000000000, 1.000000000000000000, -6.308085367188393199E-16 ) ) ;
#189674=DIRECTION ( 'NONE',  ( 1.000000000000000000, 7.304098846218134667E-16, 0.000000000000000000 ) ) ;
#189675=CARTESIAN_POINT ( 'NONE',  ( 18.59999999999999432, -1.162701749926853712, -75.10000000000003695 ) ) ;
#189688=CARTESIAN_POINT ( 'NONE',  ( -21.08479644141223019, 6.345038657743046429, -66.94144555743589819 ) ) ;
#189711=AXIS2_PLACEMENT_3D ( 'NONE', #56152, #95297, #11934 ) ;
#189761=DIRECTION ( 'NONE',  ( -1.000000000000000000, 0.000000000000000000, 0.000000000000000000 ) ) ;
#189772=CARTESIAN_POINT ( 'NONE',  ( 20.77766267348356166, 10.44904239063021123, -74.59270891587755159 ) ) ;
#189783=ORIENTED_EDGE ( 'NONE', *, *, #42243, .F. ) ;
#189792=ORIENTED_EDGE ( 'NONE', *, *, #255243, .F. ) ;
#189810=AXIS2_PLACEMENT_3D ( 'NONE', #72756, #55680, #115702 ) ;
#189821=DIRECTION ( 'NONE',  ( 0.000000000000000000, 1.000000000000000000, 0.000000000000000000 ) ) ;
#189827=DIRECTION ( 'NONE',  ( 1.000000000000000000, 0.000000000000000000, 0.000000000000000000 ) ) ;
#189831=VERTEX_POINT ( 'NONE', #212993 ) ;
#189838=DIRECTION ( 'NONE',  ( -1.000000000000000000, 0.000000000000000000, 0.000000000000000000 ) ) ;
#189849=CARTESIAN_POINT ( 'NONE',  ( 21.06600267594171783, 8.775166069211060460, -79.20426278237478357 ) ) ;
#189896=CARTESIAN_POINT ( 'NONE',  ( 18.49999999999999289, 11.65000000001115943, -55.25000000000004974 ) ) ;
#189905=ORIENTED_EDGE ( 'NONE', *, *, #57199, .F. ) ;
#189941=EDGE_CURVE ( 'NONE', #87571, #59101, #144436, .T. ) ;
#189983=CARTESIAN_POINT ( 'NONE',  ( -20.64999999999999858, 7.150000000011155876, -79.25000000000004263 ) ) ;
#190003=CYLINDRICAL_SURFACE ( 'NONE', #202338, 0.8750000000000007772 ) ;
#190014=DIRECTION ( 'NONE',  ( 0.000000000000000000, 0.000000000000000000, -1.000000000000000000 ) ) ;
#190057=VERTEX_POINT ( 'NONE', #208843 ) ;
#190069=CARTESIAN_POINT ( 'NONE',  ( 18.59999999999999076, 11.65000000001115943, -91.85000000000003695 ) ) ;
#190103=AXIS2_PLACEMENT_3D ( 'NONE', #243290, #107639, #4672 ) ;
#190107=ORIENTED_EDGE ( 'NONE', *, *, #180063, .T. ) ;
#190124=VECTOR ( 'NONE', #60741, 1000.000000000000000 ) ;
#190141=DIRECTION ( 'NONE',  ( 1.000000000000000000, -0.000000000000000000, -0.000000000000000000 ) ) ;
#190152=DIRECTION ( 'NONE',  ( -1.000000000000000000, 0.000000000000000000, 0.000000000000000000 ) ) ;
#190153=DIRECTION ( 'NONE',  ( -1.000000000000000000, 0.000000000000000000, 0.000000000000000000 ) ) ;
#190158=EDGE_LOOP ( 'NONE', ( #75235, #236570, #155079, #138842 ) ) ;
#190161=TOROIDAL_SURFACE ( 'NONE', #223447, 0.2000000000000000111, 0.1000000000000000056 ) ;
#190189=CIRCLE ( 'NONE', #86085, 12.87500000000000000 ) ;
#190190=CARTESIAN_POINT ( 'NONE',  ( -20.94999999999999929, 11.63687328911526109, -93.67824078667543120 ) ) ;
#190222=VERTEX_POINT ( 'NONE', #134412 ) ;
#190224=AXIS2_PLACEMENT_3D ( 'NONE', #58510, #216313, #155104 ) ;
#190237=CARTESIAN_POINT ( 'NONE',  ( 23.14999999999999503, 14.10000000001115694, -94.89970238886068898 ) ) ;
#190264=CARTESIAN_POINT ( 'NONE',  ( 20.85000000000000142, -1.736705739456431807, -112.0174225876237699 ) ) ;
#190270=DIRECTION ( 'NONE',  ( 1.000000000000000000, -0.000000000000000000, -0.000000000000000000 ) ) ;
#190275=CARTESIAN_POINT ( 'NONE',  ( 21.05000000000000071, -8.730841121484171907, -76.59807471898437825 ) ) ;
#190286=DIRECTION ( 'NONE',  ( 0.000000000000000000, -0.4791956752371546169, -0.8777080977375152360 ) ) ;
#190288=CARTESIAN_POINT ( 'NONE',  ( -23.15000000000000213, 2.500000000011156409, -80.22462192276213955 ) ) ;
#190325=CARTESIAN_POINT ( 'NONE',  ( -18.40000000000000213, -9.682403433465244902, -107.1568433774128266 ) ) ;
#190328=DIRECTION ( 'NONE',  ( -1.000000000000000000, -0.000000000000000000, 0.000000000000000000 ) ) ;
#190334=ORIENTED_EDGE ( 'NONE', *, *, #51650, .T. ) ;
#190354=ORIENTED_EDGE ( 'NONE', *, *, #180665, .T. ) ;
#190394=CARTESIAN_POINT ( 'NONE',  ( 19.83283456528359423, 11.75000000001116263, -91.84999999941936721 ) ) ;
#190406=EDGE_LOOP ( 'NONE', ( #25895, #8741, #255550, #250295 ) ) ;
#190409=DIRECTION ( 'NONE',  ( 0.000000000000000000, -0.1350103645451904977, 0.9908441862701596881 ) ) ;
#190429=VERTEX_POINT ( 'NONE', #46874 ) ;
#190440=DIRECTION ( 'NONE',  ( 0.000000000000000000, 0.1298341882520022972, 0.9915357197604853789 ) ) ;
#190466=DIRECTION ( 'NONE',  ( 1.000000000000000000, 0.000000000000000000, 0.000000000000000000 ) ) ;
#190481=ADVANCED_FACE ( 'NONE', ( #36337 ), #52008, .F. ) ;
#190544=FACE_OUTER_BOUND ( 'NONE', #227069, .T. ) ;
#190576=TOROIDAL_SURFACE ( 'NONE', #15624, 12.77499999999999858, 0.1000000000000000056 ) ;
#190593=ORIENTED_EDGE ( 'NONE', *, *, #11489, .F. ) ;
#190632=EDGE_CURVE ( 'NONE', #55890, #194521, #76710, .T. ) ;
#190637=ORIENTED_EDGE ( 'NONE', *, *, #51339, .F. ) ;
#190651=CARTESIAN_POINT ( 'NONE',  ( -20.94999999999999929, -11.64999999998884483, -69.90000000000004832 ) ) ;
#190665=ORIENTED_EDGE ( 'NONE', *, *, #91497, .T. ) ;
#190780=EDGE_CURVE ( 'NONE', #114130, #197089, #174287, .T. ) ;
#190785=CARTESIAN_POINT ( 'NONE',  ( 18.49999999999999645, 5.950000000011100632, -77.30570230503489881 ) ) ;
#190786=CARTESIAN_POINT ( 'NONE',  ( 21.04999999999999716, 8.871279686006799281, -79.15000000000004832 ) ) ;
#190818=CARTESIAN_POINT ( 'NONE',  ( 21.05000000000000071, -11.64999999998883595, -97.50000000000004263 ) ) ;
#190820=CIRCLE ( 'NONE', #170163, 0.3999999999999975797 ) ;
#190835=CARTESIAN_POINT ( 'NONE',  ( 22.49999999999999645, 11.74956712350054744, -66.89914163090132604 ) ) ;
#190849=STYLED_ITEM ( 'NONE', ( #78376 ), #21812 ) ;
#190864=CARTESIAN_POINT ( 'NONE',  ( 20.94999999999999929, 10.29288807859936838, -105.9580020160122160 ) ) ;
#190898=ORIENTED_EDGE ( 'NONE', *, *, #220846, .F. ) ;
#190902=EDGE_CURVE ( 'NONE', #3373, #86852, #140930, .T. ) ;
#190937=ORIENTED_EDGE ( 'NONE', *, *, #41430, .T. ) ;
#190950=ORIENTED_EDGE ( 'NONE', *, *, #120878, .T. ) ;
#190958=ORIENTED_EDGE ( 'NONE', *, *, #11387, .T. ) ;
#190967=DIRECTION ( 'NONE',  ( -1.000000000000000000, -7.304098846218134667E-16, 0.000000000000000000 ) ) ;
#191009=ORIENTED_EDGE ( 'NONE', *, *, #98244, .F. ) ;
#191034=FACE_OUTER_BOUND ( 'NONE', #15894, .T. ) ;
#191073=DIRECTION ( 'NONE',  ( 1.000000000000000000, -7.304098846218134667E-16, -0.000000000000000000 ) ) ;
#191084=DIRECTION ( 'NONE',  ( 0.000000000000000000, 0.000000000000000000, -1.000000000000000000 ) ) ;
#191094=EDGE_CURVE ( 'NONE', #111692, #150875, #111903, .T. ) ;
#191111=CIRCLE ( 'NONE', #132839, 11.75000000000000000 ) ;
#191164=CARTESIAN_POINT ( 'NONE',  ( -21.05000000000000071, 5.850000000011108092, -77.13249722427801203 ) ) ;
#191181=TOROIDAL_SURFACE ( 'NONE', #249438, 11.65000000000000036, 0.1000000000000000056 ) ;
#191192=CIRCLE ( 'NONE', #78721, 4.100000000000006750 ) ;
#191195=ORIENTED_EDGE ( 'NONE', *, *, #76956, .T. ) ;
#191240=CIRCLE ( 'NONE', #141156, 0.09999999999999939493 ) ;
#191252=DIRECTION ( 'NONE',  ( 1.000000000000000000, -0.000000000000000000, -0.000000000000000000 ) ) ;
#191261=DIRECTION ( 'NONE',  ( 0.000000000000000000, 0.000000000000000000, -1.000000000000000000 ) ) ;
#191286=LINE ( 'NONE', #152157, #173742 ) ;
#191372=ADVANCED_FACE ( 'NONE', ( #93809 ), #170847, .T. ) ;
#191374=CARTESIAN_POINT ( 'NONE',  ( -23.25000000000000000, 1.115600667400684642E-11, -71.05000000000003979 ) ) ;
#191385=ORIENTED_EDGE ( 'NONE', *, *, #224877, .F. ) ;
#191394=CYLINDRICAL_SURFACE ( 'NONE', #171897, 0.1000000000000028644 ) ;
#191410=EDGE_CURVE ( 'NONE', #33467, #34181, #191192, .T. ) ;
#191454=DIRECTION ( 'NONE',  ( 0.000000000000000000, 0.01562500000001045344, 0.9998779222360096863 ) ) ;
#191466=DIRECTION ( 'NONE',  ( 0.000000000000000000, 1.000000000000000000, 0.000000000000000000 ) ) ;
#191524=EDGE_LOOP ( 'NONE', ( #220752, #155983, #149769, #107488 ) ) ;
#191533=CYLINDRICAL_SURFACE ( 'NONE', #9523, 11.80000000000000426 ) ;
#191552=DIRECTION ( 'NONE',  ( 0.000000000000000000, -1.000000000000000000, 0.000000000000000000 ) ) ;
#191560=CARTESIAN_POINT ( 'NONE',  ( 23.14999999999998437, 1.115600667400684642E-11, -67.00000000000004263 ) ) ;
#191571=AXIS2_PLACEMENT_3D ( 'NONE', #140722, #113768, #79449 ) ;
#191583=CARTESIAN_POINT ( 'NONE',  ( 20.94999999999999574, 1.250000000011155299, -75.00000000000004263 ) ) ;
#191595=DIRECTION ( 'NONE',  ( -1.000000000000000000, 0.000000000000000000, 0.000000000000000000 ) ) ;
#191604=LINE ( 'NONE', #74228, #118044 ) ;
#191611=ADVANCED_FACE ( 'NONE', ( #106626 ), #205745, .T. ) ;
#191666=DIRECTION ( 'NONE',  ( 1.000000000000000000, 0.000000000000000000, 0.000000000000000000 ) ) ;
#191668=VERTEX_POINT ( 'NONE', #21999 ) ;
#191703=ORIENTED_EDGE ( 'NONE', *, *, #4499, .F. ) ;
#191709=DIRECTION ( 'NONE',  ( 0.000000000000000000, 0.000000000000000000, -1.000000000000000000 ) ) ;
#191742=ORIENTED_EDGE ( 'NONE', *, *, #82853, .F. ) ;
#191783=VECTOR ( 'NONE', #118773, 1000.000000000000000 ) ;
#191792=DIRECTION ( 'NONE',  ( -0.000000000000000000, 0.8660254037844411501, 0.4999999999999956701 ) ) ;
#191817=VECTOR ( 'NONE', #225310, 1000.000000000000000 ) ;
#191853=SPHERICAL_SURFACE ( 'NONE', #202461, 0.1000000000000000056 ) ;
#191856=ADVANCED_FACE ( 'NONE', ( #55624 ), #174379, .F. ) ;
#191866=DIRECTION ( 'NONE',  ( -0.000000000000000000, -0.7397360091702755991, -0.6728971962616832059 ) ) ;
#191884=EDGE_CURVE ( 'NONE', #9696, #229956, #257645, .T. ) ;
#191911=AXIS2_PLACEMENT_3D ( 'NONE', #120940, #126027, #161337 ) ;
#191925=AXIS2_PLACEMENT_3D ( 'NONE', #122327, #201859, #45353 ) ;
#191940=AXIS2_PLACEMENT_3D ( 'NONE', #106699, #62466, #7622 ) ;
#191946=CARTESIAN_POINT ( 'NONE',  ( 20.94999999999999929, -8.999999999988844479, -76.89396912265249284 ) ) ;
#191965=DIRECTION ( 'NONE',  ( 0.000000000000000000, 0.000000000000000000, 1.000000000000000000 ) ) ;
#191971=TOROIDAL_SURFACE ( 'NONE', #25376, 0.2000000000000000111, 0.1000000000000000056 ) ;
#191995=ORIENTED_EDGE ( 'NONE', *, *, #219423, .T. ) ;
#192037=ORIENTED_EDGE ( 'NONE', *, *, #76956, .F. ) ;
#192057=LINE ( 'NONE', #73405, #233715 ) ;
#192064=VERTEX_POINT ( 'NONE', #148041 ) ;
#192065=TOROIDAL_SURFACE ( 'NONE', #475, 0.2000000000000000111, 0.1000000000000000056 ) ;
#192066=DIRECTION ( 'NONE',  ( 0.000000000000000000, -1.000000000000000000, 0.000000000000000000 ) ) ;
#192087=VERTEX_POINT ( 'NONE', #129753 ) ;
#192102=CARTESIAN_POINT ( 'NONE',  ( 20.94999999999999574, -11.48912529306490349, -69.90000000000004832 ) ) ;
#192127=CARTESIAN_POINT ( 'NONE',  ( 21.05000000000000071, 5.000000000011153745, -88.09473398108696074 ) ) ;
#192158=AXIS2_PLACEMENT_3D ( 'NONE', #116641, #155799, #235295 ) ;
#192184=CARTESIAN_POINT ( 'NONE',  ( 21.10320863425824811, 6.400277386470322405, -66.97497774877291477 ) ) ;
#192197=AXIS2_PLACEMENT_3D ( 'NONE', #184493, #227474, #247034 ) ;
#192208=CARTESIAN_POINT ( 'NONE',  ( 21.05000000000000071, -8.999999999988844479, -76.89396912265249284 ) ) ;
#192231=ADVANCED_FACE ( 'NONE', ( #141309 ), #202568, .F. ) ;
#192251=CIRCLE ( 'NONE', #208813, 0.09999999999999949207 ) ;
#192261=ORIENTED_EDGE ( 'NONE', *, *, #27564, .T. ) ;
#192264=ORIENTED_EDGE ( 'NONE', *, *, #114067, .T. ) ;
#192285=EDGE_LOOP ( 'NONE', ( #154117, #96371, #105824, #230214 ) ) ;
#192297=DIRECTION ( 'NONE',  ( 0.000000000000000000, 0.1575844902526835067, 0.9875055080513738259 ) ) ;
#192352=EDGE_CURVE ( 'NONE', #81417, #113044, #9495, .T. ) ;
#192358=ORIENTED_EDGE ( 'NONE', *, *, #152519, .T. ) ;
#192362=CARTESIAN_POINT ( 'NONE',  ( -20.00857864376270001, 9.150000000011157653, -88.15000000000004832 ) ) ;
#192365=DIRECTION ( 'NONE',  ( 1.000000000000000000, 0.000000000000000000, 0.000000000000000000 ) ) ;
#192374=DIRECTION ( 'NONE',  ( 1.000000000000000000, 0.000000000000000000, 0.000000000000000000 ) ) ;
#192398=VERTEX_POINT ( 'NONE', #109872 ) ;
#192413=CIRCLE ( 'NONE', #234091, 0.1000000000000028644 ) ;
#192431=DIRECTION ( 'NONE',  ( -1.000000000000000000, 0.000000000000000000, 0.000000000000000000 ) ) ;
#192435=DIRECTION ( 'NONE',  ( 1.000000000000000000, 2.952720810173289112E-16, -0.000000000000000000 ) ) ;
#192456=CARTESIAN_POINT ( 'NONE',  ( -20.54999999999999716, 1.115600667400684642E-11, -100.5000000000000426 ) ) ;
#192485=DIRECTION ( 'NONE',  ( 1.000000000000000000, -0.000000000000000000, -0.000000000000000000 ) ) ;
#192487=ORIENTED_EDGE ( 'NONE', *, *, #190780, .T. ) ;
#192489=CARTESIAN_POINT ( 'NONE',  ( -20.54999999999999716, 1.115625160336667635E-11, -102.5000000000000426 ) ) ;
#192502=CARTESIAN_POINT ( 'NONE',  ( -21.05000000000000071, -1.162701749926853712, -75.10000000000003695 ) ) ;
#192541=ORIENTED_EDGE ( 'NONE', *, *, #102265, .T. ) ;
#192600=CARTESIAN_POINT ( 'NONE',  ( 21.05000000000000071, 8.776282895303632259, -75.55862899514100661 ) ) ;
#192617=ORIENTED_EDGE ( 'NONE', *, *, #217735, .F. ) ;
#192624=CARTESIAN_POINT ( 'NONE',  ( -18.59999999999999787, 11.65000000001115232, -88.35000000000003695 ) ) ;
#192640=FACE_OUTER_BOUND ( 'NONE', #210345, .T. ) ;
#192669=DIRECTION ( 'NONE',  ( -0.000000000000000000, 0.000000000000000000, -1.000000000000000000 ) ) ;
#192682=CARTESIAN_POINT ( 'NONE',  ( 20.94999999999999929, 11.65000000001115943, -93.65839931010299324 ) ) ;
#192731=ORIENTED_EDGE ( 'NONE', *, *, #39592, .T. ) ;
#192749=DIRECTION ( 'NONE',  ( 0.000000000000000000, 0.000000000000000000, -1.000000000000000000 ) ) ;
#192751=DIRECTION ( 'NONE',  ( 0.000000000000000000, 1.000000000000000000, 0.000000000000000000 ) ) ;
#192787=DIRECTION ( 'NONE',  ( 1.000000000000000000, 0.000000000000000000, 0.000000000000000000 ) ) ;
#192788=DIRECTION ( 'NONE',  ( 0.000000000000000000, -1.000000000000000000, 0.000000000000000000 ) ) ;
#192790=CARTESIAN_POINT ( 'NONE',  ( -22.39999999999999858, 1.115600667400684642E-11, -59.20922040162664501 ) ) ;
#192803=EDGE_CURVE ( 'NONE', #181065, #101672, #158608, .T. ) ;
#192809=LINE ( 'NONE', #14188, #139770 ) ;
#192813=CARTESIAN_POINT ( 'NONE',  ( 23.14999999999999858, 1.115600667400684642E-11, -100.5000000000000426 ) ) ;
#192832=AXIS2_PLACEMENT_3D ( 'NONE', #10362, #148578, #24808 ) ;
#192848=CARTESIAN_POINT ( 'NONE',  ( -20.94999999999999929, -1.162701749926853712, -75.00000000000004263 ) ) ;
#192881=ORIENTED_EDGE ( 'NONE', *, *, #255791, .F. ) ;
#192883=DIRECTION ( 'NONE',  ( 1.000000000000000000, 0.000000000000000000, -0.000000000000000000 ) ) ;
#192916=CARTESIAN_POINT ( 'NONE',  ( 18.39999999999999858, -9.682403433465237796, -107.1568433774128408 ) ) ;
#192930=FACE_OUTER_BOUND ( 'NONE', #179831, .T. ) ;
#192954=DIRECTION ( 'NONE',  ( 1.000000000000000000, 0.000000000000000000, 0.000000000000000000 ) ) ;
#192957=ORIENTED_EDGE ( 'NONE', *, *, #149911, .T. ) ;
#192965=DIRECTION ( 'NONE',  ( 0.000000000000000000, 0.000000000000000000, -1.000000000000000000 ) ) ;
#192967=DIRECTION ( 'NONE',  ( 1.000000000000000000, 0.000000000000000000, 0.000000000000000000 ) ) ;
#192973=FACE_OUTER_BOUND ( 'NONE', #233321, .T. ) ;
#192977=VECTOR ( 'NONE', #36401, 1000.000000000000000 ) ;
#192984=ADVANCED_FACE ( 'NONE', ( #202921 ), #21730, .T. ) ;
#192990=CIRCLE ( 'NONE', #34784, 0.09999999999999761857 ) ;
#193044=CARTESIAN_POINT ( 'NONE',  ( 18.59999999999999787, 1.115600667400684642E-11, -67.00000000000004263 ) ) ;
#193074=ORIENTED_EDGE ( 'NONE', *, *, #177860, .F. ) ;
#193078=AXIS2_PLACEMENT_3D ( 'NONE', #9651, #246968, #150465 ) ;
#193080=DIRECTION ( 'NONE',  ( 1.000000000000000000, 0.000000000000000000, 0.000000000000000000 ) ) ;
#193087=DIRECTION ( 'NONE',  ( 0.000000000000000000, -0.1455152366551522025, -0.9893560106964505163 ) ) ;
#193115=VECTOR ( 'NONE', #167772, 1000.000000000000000 ) ;
#193140=VERTEX_POINT ( 'NONE', #249755 ) ;
#193160=ORIENTED_EDGE ( 'NONE', *, *, #41414, .T. ) ;
#193182=EDGE_CURVE ( 'NONE', #97606, #137421, #158391, .T. ) ;
#193192=EDGE_LOOP ( 'NONE', ( #187241, #162946, #213732, #58141 ) ) ;
#193199=CARTESIAN_POINT ( 'NONE',  ( -23.25000000000000000, 1.115600667400684642E-11, -100.5000000000000426 ) ) ;
#193200=EDGE_LOOP ( 'NONE', ( #64169, #110841, #236187, #220487 ) ) ;
#193207=ORIENTED_EDGE ( 'NONE', *, *, #188711, .T. ) ;
#193220=DIRECTION ( 'NONE',  ( 1.000000000000000000, 0.000000000000000000, 0.000000000000000000 ) ) ;
#193223=AXIS2_PLACEMENT_3D ( 'NONE', #27341, #130232, #67705 ) ;
#193257=CARTESIAN_POINT ( 'NONE',  ( 18.54116936837188589, -9.463564198361288149, -74.04854249088833740 ) ) ;
#193259=ORIENTED_EDGE ( 'NONE', *, *, #68420, .T. ) ;
#193263=ORIENTED_EDGE ( 'NONE', *, *, #146256, .F. ) ;
#193284=EDGE_CURVE ( 'NONE', #67110, #247198, #174826, .T. ) ;
#193288=EDGE_CURVE ( 'NONE', #60368, #143581, #116656, .T. ) ;
#193336=DIRECTION ( 'NONE',  ( 1.000000000000000000, 3.469446951953704435E-14, -2.003086131649669752E-14 ) ) ;
#193337=EDGE_CURVE ( 'NONE', #118383, #66864, #70941, .T. ) ;
#193392=EDGE_CURVE ( 'NONE', #6741, #254308, #8375, .T. ) ;
#193399=CARTESIAN_POINT ( 'NONE',  ( -23.25000000000000000, 4.350000000011156054, -79.35000000000005116 ) ) ;
#193419=CARTESIAN_POINT ( 'NONE',  ( 21.53699400385583118, 6.353297217273429908E-12, -60.21228820676886784 ) ) ;
#193421=DIRECTION ( 'NONE',  ( -1.000000000000000000, 0.000000000000000000, 0.000000000000000000 ) ) ;
#193455=DIRECTION ( 'NONE',  ( -3.265361837132813093E-16, 1.000000000000000000, 0.000000000000000000 ) ) ;
#193466=CIRCLE ( 'NONE', #31172, 4.049999999999998046 ) ;
#193486=EDGE_CURVE ( 'NONE', #221706, #53335, #148514, .T. ) ;
#193517=CARTESIAN_POINT ( 'NONE',  ( -18.50000000000001066, -9.421308209727946803, -74.24236321405062711 ) ) ;
#193559=DIRECTION ( 'NONE',  ( -1.000000000000000000, 0.000000000000000000, 0.000000000000000000 ) ) ;
#193575=CARTESIAN_POINT ( 'NONE',  ( 18.59999999999999076, 6.550000000011156231, -88.25000000000005684 ) ) ;
#193616=SPHERICAL_SURFACE ( 'NONE', #163111, 0.1000000000000000056 ) ;
#193620=CARTESIAN_POINT ( 'NONE',  ( -20.94999999999999929, 5.850000000011160495, -90.36750277572211587 ) ) ;
#193659=DIRECTION ( 'NONE',  ( -1.000000000000000000, 0.000000000000000000, 0.000000000000000000 ) ) ;
#193660=EDGE_CURVE ( 'NONE', #224594, #61798, #129339, .T. ) ;
#193695=EDGE_CURVE ( 'NONE', #201851, #95314, #208482, .T. ) ;
#193709=CARTESIAN_POINT ( 'NONE',  ( -20.94999999999999929, -11.48912529306489994, -97.40000000000004832 ) ) ;
#193710=AXIS2_PLACEMENT_3D ( 'NONE', #194364, #177375, #256814 ) ;
#193718=CARTESIAN_POINT ( 'NONE',  ( 20.04142135623730070, 11.65000000001115943, -88.35000000000003695 ) ) ;
#193758=DIRECTION ( 'NONE',  ( 0.000000000000000000, -1.000000000000000000, -0.000000000000000000 ) ) ;
#193778=DIRECTION ( 'NONE',  ( 1.000000000000000000, -0.000000000000000000, 0.000000000000000000 ) ) ;
#193816=CARTESIAN_POINT ( 'NONE',  ( -21.07928932188134041, 0.09889514566555068775, -60.67148334360675221 ) ) ;
#193820=LINE ( 'NONE', #218481, #13728 ) ;
#193871=CARTESIAN_POINT ( 'NONE',  ( -18.59999999999999787, 14.05000000001115623, -72.51369507076104526 ) ) ;
#193875=CIRCLE ( 'NONE', #35687, 0.1000000000000028644 ) ;
#193904=LINE ( 'NONE', #94781, #147770 ) ;
#193955=DIRECTION ( 'NONE',  ( -1.000000000000000000, 0.000000000000000000, 0.000000000000000000 ) ) ;
#193962=DIRECTION ( 'NONE',  ( 0.000000000000000000, -1.000000000000000000, 0.000000000000000000 ) ) ;
#193985=ADVANCED_FACE ( 'NONE', ( #92613 ), #96195, .F. ) ;
#193995=EDGE_LOOP ( 'NONE', ( #219836, #245480, #30187, #44695 ) ) ;
#194003=DIRECTION ( 'NONE',  ( 1.000000000000000000, -0.000000000000000000, -0.000000000000000000 ) ) ;
#194015=CARTESIAN_POINT ( 'NONE',  ( -20.64999999999999858, -9.399999999988846611, -90.60603087734760663 ) ) ;
#194038=DIRECTION ( 'NONE',  ( 0.000000000000000000, -1.000000000000000000, 0.000000000000000000 ) ) ;
#194052=DIRECTION ( 'NONE',  ( -3.265361837132813093E-16, 1.000000000000000000, -0.000000000000000000 ) ) ;
#194062=LINE ( 'NONE', #97472, #14386 ) ;
#194092=DIRECTION ( 'NONE',  ( -0.000000000000000000, 0.1350103645451876666, -0.9908441862701600211 ) ) ;
#194100=ORIENTED_EDGE ( 'NONE', *, *, #150705, .F. ) ;
#194115=ORIENTED_EDGE ( 'NONE', *, *, #134402, .T. ) ;
#194116=DIRECTION ( 'NONE',  ( 1.000000000000000000, 0.000000000000000000, 0.000000000000000000 ) ) ;
#194135=EDGE_CURVE ( 'NONE', #102833, #225971, #83698, .T. ) ;
#194152=VERTEX_POINT ( 'NONE', #256783 ) ;
#194155=DIRECTION ( 'NONE',  ( -1.000000000000000000, -2.952720810173289112E-16, 0.000000000000000000 ) ) ;
#194179=CARTESIAN_POINT ( 'NONE',  ( -21.05000000000000071, -11.74999999998884448, -97.40000000000004832 ) ) ;
#194188=ORIENTED_EDGE ( 'NONE', *, *, #51339, .T. ) ;
#194204=ADVANCED_FACE ( 'NONE', ( #157793 ), #99021, .T. ) ;
#194211=ORIENTED_EDGE ( 'NONE', *, *, #225634, .F. ) ;
#194220=CARTESIAN_POINT ( 'NONE',  ( 18.43466021071411731, -9.494190690445389436, -107.1170615601277802 ) ) ;
#194222=CARTESIAN_POINT ( 'NONE',  ( -20.54999999999999716, -8.999999999988844479, -90.60603087734760663 ) ) ;
#194227=CARTESIAN_POINT ( 'NONE',  ( 18.42555734704284376, -9.497158361925558623, -74.03983049773501079 ) ) ;
#194246=EDGE_CURVE ( 'NONE', #214743, #142573, #133796, .T. ) ;
#194247=FACE_OUTER_BOUND ( 'NONE', #170577, .T. ) ;
#194259=VECTOR ( 'NONE', #23332, 1000.000000000000000 ) ;
#194316=CARTESIAN_POINT ( 'NONE',  ( -23.25000000000000000, 6.982009704867601307, -104.1961521182563359 ) ) ;
#194318=VECTOR ( 'NONE', #126738, 1000.000000000000000 ) ;
#194331=DIRECTION ( 'NONE',  ( 1.000000000000000000, 0.000000000000000000, 0.000000000000000000 ) ) ;
#194340=DIRECTION ( 'NONE',  ( 0.000000000000000000, -1.000000000000000000, 0.000000000000000000 ) ) ;
#194343=DIRECTION ( 'NONE',  ( 1.000000000000000000, -0.000000000000000000, -0.000000000000000000 ) ) ;
#194347=AXIS2_PLACEMENT_3D ( 'NONE', #42263, #100894, #37141 ) ;
#194364=CARTESIAN_POINT ( 'NONE',  ( 20.94999999999999929, -1.835341550213257733, -78.55515129256302487 ) ) ;
#194395=FACE_OUTER_BOUND ( 'NONE', #113881, .T. ) ;
#194398=FACE_OUTER_BOUND ( 'NONE', #153578, .T. ) ;
#194490=ORIENTED_EDGE ( 'NONE', *, *, #200338, .T. ) ;
#194502=VERTEX_POINT ( 'NONE', #171142 ) ;
#194521=VERTEX_POINT ( 'NONE', #151560 ) ;
#194542=TOROIDAL_SURFACE ( 'NONE', #82057, 0.6000000000000004219, 0.1000000000000000056 ) ;
#194585=AXIS2_PLACEMENT_3D ( 'NONE', #65284, #220519, #101810 ) ;
#194596=DIRECTION ( 'NONE',  ( 1.000000000000000000, -0.000000000000000000, -0.000000000000000000 ) ) ;
#194597=DIRECTION ( 'NONE',  ( 1.000000000000000000, 0.000000000000000000, 0.000000000000000000 ) ) ;
#194614=ADVANCED_FACE ( 'NONE', ( #252646 ), #38324, .F. ) ;
#194624=AXIS2_PLACEMENT_3D ( 'NONE', #227859, #113052, #71379 ) ;
#194630=DIRECTION ( 'NONE',  ( 0.000000000000000000, 0.000000000000000000, 1.000000000000000000 ) ) ;
#194703=CARTESIAN_POINT ( 'NONE',  ( -23.15000000000000213, 1.115600667400684642E-11, -100.5000000000000426 ) ) ;
#194714=DIRECTION ( 'NONE',  ( 0.000000000000000000, -0.6728971962616792091, 0.7397360091702790408 ) ) ;
#194737=LINE ( 'NONE', #10951, #84360 ) ;
#194753=DIRECTION ( 'NONE',  ( 0.000000000000000000, 0.000000000000000000, -1.000000000000000000 ) ) ;
#194760=CARTESIAN_POINT ( 'NONE',  ( 21.14250536705908345, 6.518172176891879666, -67.00000000000004263 ) ) ;
#194774=AXIS2_PLACEMENT_3D ( 'NONE', #130389, #189095, #110829 ) ;
#194808=CYLINDRICAL_SURFACE ( 'NONE', #155584, 0.09999999999999939493 ) ;
#194814=CARTESIAN_POINT ( 'NONE',  ( -18.51555513499570083, -9.352657054493093369, -74.19516989569670784 ) ) ;
#194821=ORIENTED_EDGE ( 'NONE', *, *, #87285, .T. ) ;
#194830=ORIENTED_EDGE ( 'NONE', *, *, #148267, .T. ) ;
#194850=EDGE_CURVE ( 'NONE', #225971, #81417, #204896, .T. ) ;
#194852=CARTESIAN_POINT ( 'NONE',  ( -22.48970261584618058, 11.65000000001115588, -66.94463051178263413 ) ) ;
#194878=DIRECTION ( 'NONE',  ( -1.000000000000000000, 0.000000000000000000, 0.000000000000000000 ) ) ;
#194910=ORIENTED_EDGE ( 'NONE', *, *, #41752, .F. ) ;
#194913=AXIS2_PLACEMENT_3D ( 'NONE', #24380, #239560, #59599 ) ;
#194917=AXIS2_PLACEMENT_3D ( 'NONE', #2387, #25833, #81906 ) ;
#194918=CARTESIAN_POINT ( 'NONE',  ( -23.15000000000000213, -11.64999999998884483, -97.40000000000004832 ) ) ;
#194953=AXIS2_PLACEMENT_3D ( 'NONE', #76837, #73034, #16889 ) ;
#194974=CYLINDRICAL_SURFACE ( 'NONE', #211261, 0.09999999999999939493 ) ;
#194979=AXIS2_PLACEMENT_3D ( 'NONE', #77837, #235629, #193962 ) ;
#194984=CIRCLE ( 'NONE', #220091, 0.5000000000000004441 ) ;
#195005=FACE_OUTER_BOUND ( 'NONE', #11314, .T. ) ;
#195011=CARTESIAN_POINT ( 'NONE',  ( 20.94999999999999574, 1.835341550235567887, -78.55515129256303908 ) ) ;
#195020=EDGE_CURVE ( 'NONE', #95981, #168864, #84234, .T. ) ;
#195027=CARTESIAN_POINT ( 'NONE',  ( -18.50000000000000000, 1.115600667400684642E-11, -100.5000000000000426 ) ) ;
#195041=DIRECTION ( 'NONE',  ( -1.000000000000000000, -0.000000000000000000, -0.000000000000000000 ) ) ;
#195042=DIRECTION ( 'NONE',  ( 1.000000000000000000, 0.000000000000000000, 0.000000000000000000 ) ) ;
#195057=DIRECTION ( 'NONE',  ( 0.000000000000000000, 0.5000000000000144329, 0.8660254037844302699 ) ) ;
#195068=EDGE_CURVE ( 'NONE', #74473, #202477, #34431, .T. ) ;
#195075=CARTESIAN_POINT ( 'NONE',  ( -18.50000000000000000, -1.835341550213255957, -78.55515129256302487 ) ) ;
#195076=VERTEX_POINT ( 'NONE', #153295 ) ;
#195112=ORIENTED_EDGE ( 'NONE', *, *, #217535, .F. ) ;
#195118=CARTESIAN_POINT ( 'NONE',  ( -21.08621493067320429, 0.05619483948720407906, -60.65070570882810586 ) ) ;
#195126=ORIENTED_EDGE ( 'NONE', *, *, #99018, .T. ) ;
#195152=EDGE_CURVE ( 'NONE', #126808, #78012, #111566, .T. ) ;
#195187=ORIENTED_EDGE ( 'NONE', *, *, #92454, .F. ) ;
#195188=VERTEX_POINT ( 'NONE', #232816 ) ;
#195189=ORIENTED_EDGE ( 'NONE', *, *, #32502, .T. ) ;
#195279=ORIENTED_EDGE ( 'NONE', *, *, #74557, .T. ) ;
#195329=CIRCLE ( 'NONE', #82827, 12.77500000000000036 ) ;
#195337=CYLINDRICAL_SURFACE ( 'NONE', #116267, 12.87499999999999822 ) ;
#195352=LINE ( 'NONE', #233197, #105719 ) ;
#195367=DIRECTION ( 'NONE',  ( 1.000000000000000000, 0.000000000000000000, 0.000000000000000000 ) ) ;
#195377=EDGE_CURVE ( 'NONE', #167725, #125649, #72010, .T. ) ;
#195379=DIRECTION ( 'NONE',  ( 0.000000000000000000, 0.9274965247785529332, -0.3738317757009255171 ) ) ;
#195397=CIRCLE ( 'NONE', #112199, 0.09999999999999939493 ) ;
#195409=EDGE_CURVE ( 'NONE', #223804, #236296, #51119, .T. ) ;
#195425=DIRECTION ( 'NONE',  ( -0.000000000000000000, -0.000000000000000000, 1.000000000000000000 ) ) ;
#195460=DIRECTION ( 'NONE',  ( 0.000000000000000000, 0.000000000000000000, -1.000000000000000000 ) ) ;
#195478=ORIENTED_EDGE ( 'NONE', *, *, #70103, .T. ) ;
#195492=ADVANCED_FACE ( 'NONE', ( #248208 ), #33060, .T. ) ;
#195495=CARTESIAN_POINT ( 'NONE',  ( -23.15000000000000213, -8.999999999988844479, -90.60603087734760663 ) ) ;
#195503=ORIENTED_EDGE ( 'NONE', *, *, #193288, .T. ) ;
#195504=ADVANCED_FACE ( 'NONE', ( #172575 ), #167703, .F. ) ;
#195505=DIRECTION ( 'NONE',  ( -1.000000000000000000, 0.000000000000000000, 0.000000000000000000 ) ) ;
#195510=CARTESIAN_POINT ( 'NONE',  ( -20.54999999999999716, -8.999999999988844479, -90.60603087734760663 ) ) ;
#195516=CARTESIAN_POINT ( 'NONE',  ( -21.05000000000000071, -11.64999999998884483, -69.90000000000004832 ) ) ;
#195518=CIRCLE ( 'NONE', #199788, 4.049999999999998934 ) ;
#195553=DIRECTION ( 'NONE',  ( 1.000000000000000000, -0.000000000000000000, -0.000000000000000000 ) ) ;
#195562=VERTEX_POINT ( 'NONE', #9582 ) ;
#195582=DIRECTION ( 'NONE',  ( 0.000000000000000000, 0.000000000000000000, -1.000000000000000000 ) ) ;
#195584=AXIS2_PLACEMENT_3D ( 'NONE', #135586, #198141, #155203 ) ;
#195585=EDGE_CURVE ( 'NONE', #75869, #101410, #59487, .T. ) ;
#195602=ADVANCED_FACE ( 'NONE', ( #30458 ), #80548, .T. ) ;
#195653=CIRCLE ( 'NONE', #174833, 1.899999999999999023 ) ;
#195660=AXIS2_PLACEMENT_3D ( 'NONE', #32001, #151951, #112803 ) ;
#195671=DIRECTION ( 'NONE',  ( 0.000000000000000000, 0.000000000000000000, -1.000000000000000000 ) ) ;
#195696=FACE_OUTER_BOUND ( 'NONE', #141428, .T. ) ;
#195722=CIRCLE ( 'NONE', #120895, 0.1000000000000001860 ) ;
#195768=EDGE_CURVE ( 'NONE', #13313, #75395, #204901, .T. ) ;
#195769=ORIENTED_EDGE ( 'NONE', *, *, #172412, .F. ) ;
#195869=CARTESIAN_POINT ( 'NONE',  ( 21.14999999999999858, -11.64999999998883595, -67.00000000000004263 ) ) ;
#195873=CARTESIAN_POINT ( 'NONE',  ( 20.04142135623730070, 11.65000000001115943, -88.35000000000003695 ) ) ;
#195877=CYLINDRICAL_SURFACE ( 'NONE', #91207, 0.1000000000000001443 ) ;
#195880=TOROIDAL_SURFACE ( 'NONE', #83391, 11.65000000000000036, 0.1000000000000000056 ) ;
#195895=EDGE_LOOP ( 'NONE', ( #192358, #178515, #72081, #23003 ) ) ;
#195910=ADVANCED_FACE ( 'NONE', ( #245336 ), #6713, .F. ) ;
#195912=ORIENTED_EDGE ( 'NONE', *, *, #201402, .F. ) ;
#195927=EDGE_CURVE ( 'NONE', #251583, #80091, #55385, .T. ) ;
#195935=CIRCLE ( 'NONE', #25244, 0.1000000000000028644 ) ;
#195958=TOROIDAL_SURFACE ( 'NONE', #54459, 0.6000000000000013101, 0.1000000000000000056 ) ;
#195963=ORIENTED_EDGE ( 'NONE', *, *, #100465, .T. ) ;
#195986=ORIENTED_EDGE ( 'NONE', *, *, #238557, .F. ) ;
#195989=LINE ( 'NONE', #218078, #122173 ) ;
#195993=CYLINDRICAL_SURFACE ( 'NONE', #18833, 0.1000000000000028644 ) ;
#196042=EDGE_CURVE ( 'NONE', #97847, #241878, #160046, .T. ) ;
#196044=AXIS2_PLACEMENT_3D ( 'NONE', #199946, #236478, #78674 ) ;
#196062=VERTEX_POINT ( 'NONE', #77902 ) ;
#196090=DIRECTION ( 'NONE',  ( 0.000000000000000000, -1.000000000000000000, 0.000000000000000000 ) ) ;
#196109=AXIS2_PLACEMENT_3D ( 'NONE', #243050, #181801, #164811 ) ;
#196110=LINE ( 'NONE', #44425, #155781 ) ;
#196117=DIRECTION ( 'NONE',  ( 0.000000000000000000, -0.000000000000000000, 1.000000000000000000 ) ) ;
#196122=DIRECTION ( 'NONE',  ( 1.000000000000000000, 0.000000000000000000, 0.000000000000000000 ) ) ;
#196123=DIRECTION ( 'NONE',  ( -1.000000000000000000, -2.952720810173289112E-16, 0.000000000000000000 ) ) ;
#196132=EDGE_LOOP ( 'NONE', ( #244229, #24995, #25174, #66935, #55618 ) ) ;
#196163=VERTEX_POINT ( 'NONE', #162598 ) ;
#196195=CARTESIAN_POINT ( 'NONE',  ( -20.54999999999999716, 1.925233644870967487, -87.76975646687391475 ) ) ;
#196213=CIRCLE ( 'NONE', #158661, 0.1000000000000028644 ) ;
#196278=ADVANCED_FACE ( 'NONE', ( #29526 ), #133721, .T. ) ;
#196359=ORIENTED_EDGE ( 'NONE', *, *, #166566, .F. ) ;
#196364=CARTESIAN_POINT ( 'NONE',  ( -23.15000000000000213, 2.500000000011154633, -87.27537807723794572 ) ) ;
#196374=LINE ( 'NONE', #58127, #102355 ) ;
#196395=AXIS2_PLACEMENT_3D ( 'NONE', #132349, #112798, #210607 ) ;
#196415=EDGE_LOOP ( 'NONE', ( #170124, #145444, #94876 ) ) ;
#196426=AXIS2_PLACEMENT_3D ( 'NONE', #148472, #46776, #228003 ) ;
#196470=EDGE_CURVE ( 'NONE', #223804, #101672, #20217, .T. ) ;
#196509=ADVANCED_FACE ( 'NONE', ( #103567 ), #142703, .F. ) ;
#196533=CARTESIAN_POINT ( 'NONE',  ( -18.59999999999999787, -1.164121893230052995, -108.2148480855716457 ) ) ;
#196552=CARTESIAN_POINT ( 'NONE',  ( -20.94999999999999929, -1.835859311432479268, -112.0044391687985694 ) ) ;
#196563=CARTESIAN_POINT ( 'NONE',  ( 21.14999999999999858, 1.115600667400684642E-11, -60.45934304829879835 ) ) ;
#196573=CARTESIAN_POINT ( 'NONE',  ( 23.14999999999999858, 1.115625160336667635E-11, -98.50000000000004263 ) ) ;
#196574=EDGE_CURVE ( 'NONE', #76744, #257895, #217768, .T. ) ;
#196586=EDGE_CURVE ( 'NONE', #211036, #146445, #92008, .T. ) ;
#196610=DIRECTION ( 'NONE',  ( -1.000000000000000000, 0.000000000000000000, 0.000000000000000000 ) ) ;
#196635=ORIENTED_EDGE ( 'NONE', *, *, #2504, .F. ) ;
#196660=DIRECTION ( 'NONE',  ( -2.602085213965226419E-14, -0.000000000000000000, 1.000000000000000000 ) ) ;
#196674=ORIENTED_EDGE ( 'NONE', *, *, #36266, .F. ) ;
#196679=DIRECTION ( 'NONE',  ( 0.000000000000000000, 0.008583690987128059571, -0.9999631594459056361 ) ) ;
#196695=CIRCLE ( 'NONE', #5138, 0.1000000000000028644 ) ;
#196709=EDGE_CURVE ( 'NONE', #214744, #100973, #9676, .T. ) ;
#196744=CARTESIAN_POINT ( 'NONE',  ( -21.64999999999999858, 7.350000000011155166, -79.25000000000004263 ) ) ;
#196761=EDGE_CURVE ( 'NONE', #127382, #188971, #176302, .T. ) ;
#196781=VECTOR ( 'NONE', #190141, 1000.000000000000000 ) ;
#196840=FACE_OUTER_BOUND ( 'NONE', #74893, .T. ) ;
#196882=DIRECTION ( 'NONE',  ( 0.000000000000000000, 8.673617379884087537E-15, -1.000000000000000000 ) ) ;
#196884=AXIS2_PLACEMENT_3D ( 'NONE', #145381, #82808, #42434 ) ;
#196892=CARTESIAN_POINT ( 'NONE',  ( 18.59999999999998366, 1.115600667400684642E-11, -100.5000000000000426 ) ) ;
#196908=CARTESIAN_POINT ( 'NONE',  ( 20.94999999999999929, 5.000000000011153745, -88.09473398108696074 ) ) ;
#196915=VERTEX_POINT ( 'NONE', #2889 ) ;
#196960=ADVANCED_FACE ( 'NONE', ( #221924 ), #241519, .F. ) ;
#196982=CIRCLE ( 'NONE', #251127, 0.1000000000000028644 ) ;
#196983=AXIS2_PLACEMENT_3D ( 'NONE', #76420, #16482, #78966 ) ;
#196995=VECTOR ( 'NONE', #44851, 1000.000000000000000 ) ;
#197001=CYLINDRICAL_SURFACE ( 'NONE', #2303, 0.09999999999999781286 ) ;
#197032=LINE ( 'NONE', #73288, #32301 ) ;
#197049=EDGE_LOOP ( 'NONE', ( #224006, #110071, #194211, #175072 ) ) ;
#197066=AXIS2_PLACEMENT_3D ( 'NONE', #226000, #147798, #30422 ) ;
#197071=ORIENTED_EDGE ( 'NONE', *, *, #126242, .F. ) ;
#197089=VERTEX_POINT ( 'NONE', #47141 ) ;
#197102=ORIENTED_EDGE ( 'NONE', *, *, #24050, .F. ) ;
#197123=DIRECTION ( 'NONE',  ( -0.000000000000000000, 1.000000000000000000, -0.000000000000000000 ) ) ;
#197125=B_SPLINE_CURVE_WITH_KNOTS ( 'NONE', 3,
 ( #201974, #62464, #139402, #221507, #119889, #199420, #100271, #122438, #160302, #182422 ),
 .UNSPECIFIED., .F., .F.,
 ( 4, 3, 3, 4 ),
 ( 0.000000000000000000, 0.0002000000000008536833, 0.001000000000082972495, 0.001967863649483314603 ),
 .UNSPECIFIED. ) ;
#197143=CIRCLE ( 'NONE', #172065, 0.2000000000000057288 ) ;
#197167=AXIS2_PLACEMENT_3D ( 'NONE', #94290, #99416, #193421 ) ;
#197196=EDGE_CURVE ( 'NONE', #56225, #82405, #173594, .T. ) ;
#197209=CARTESIAN_POINT ( 'NONE',  ( -21.05000000000000071, -0.09999999998884338825, -55.35042919245524473 ) ) ;
#197227=EDGE_CURVE ( 'NONE', #83940, #237434, #126578, .T. ) ;
#197259=LINE ( 'NONE', #126379, #100997 ) ;
#197262=EDGE_CURVE ( 'NONE', #39695, #144636, #222387, .T. ) ;
#197270=ORIENTED_EDGE ( 'NONE', *, *, #76177, .F. ) ;
#197283=EDGE_LOOP ( 'NONE', ( #91627, #198227, #219498, #223683 ) ) ;
#197304=ORIENTED_EDGE ( 'NONE', *, *, #99752, .T. ) ;
#197351=EDGE_CURVE ( 'NONE', #127795, #198825, #211071, .T. ) ;
#197379=DIRECTION ( 'NONE',  ( 1.000000000000000000, 0.000000000000000000, 0.000000000000000000 ) ) ;
#197394=AXIS2_PLACEMENT_3D ( 'NONE', #40512, #236097, #178734 ) ;
#197396=FACE_OUTER_BOUND ( 'NONE', #175921, .T. ) ;
#197409=EDGE_CURVE ( 'NONE', #205612, #3192, #114089, .T. ) ;
#197421=VERTEX_POINT ( 'NONE', #209791 ) ;
#197513=TOROIDAL_SURFACE ( 'NONE', #51748, 7.791421356237335338, 0.1000000000000000056 ) ;
#197527=VECTOR ( 'NONE', #181738, 1000.000000000000000 ) ;
#197530=EDGE_CURVE ( 'NONE', #231071, #85621, #72609, .T. ) ;
#197560=DIRECTION ( 'NONE',  ( -0.000000000000000000, 0.01283462868039629209, -0.9999176327611372095 ) ) ;
#197563=DIRECTION ( 'NONE',  ( -1.000000000000000000, 0.000000000000000000, 0.000000000000000000 ) ) ;
#197566=DIRECTION ( 'NONE',  ( -4.391705002472929091E-16, 1.000000000000000000, 0.000000000000000000 ) ) ;
#197572=AXIS2_PLACEMENT_3D ( 'NONE', #3255, #118089, #142762 ) ;
#197597=CARTESIAN_POINT ( 'NONE',  ( -18.50016250449483479, 10.29766095125287073, -105.9743663933276139 ) ) ;
#197621=ORIENTED_EDGE ( 'NONE', *, *, #80902, .T. ) ;
#197630=DIRECTION ( 'NONE',  ( 0.000000000000000000, 0.000000000000000000, -1.000000000000000000 ) ) ;
#197640=CARTESIAN_POINT ( 'NONE',  ( -18.59999999999999787, 7.021664781911246322, -104.3335654018973315 ) ) ;
#197668=ORIENTED_EDGE ( 'NONE', *, *, #39855, .T. ) ;
#197693=VERTEX_POINT ( 'NONE', #68366 ) ;
#197717=ADVANCED_FACE ( 'NONE', ( #132188 ), #222587, .T. ) ;
#197718=ADVANCED_FACE ( 'NONE', ( #188298 ), #176843, .F. ) ;
#197748=ORIENTED_EDGE ( 'NONE', *, *, #118285, .F. ) ;
#197791=DIRECTION ( 'NONE',  ( 1.000000000000000000, 0.000000000000000000, 0.000000000000000000 ) ) ;
#197935=AXIS2_PLACEMENT_3D ( 'NONE', #4854, #182253, #27053 ) ;
#197949=ORIENTED_EDGE ( 'NONE', *, *, #139361, .T. ) ;
#197955=UNCERTAINTY_MEASURE_WITH_UNIT (LENGTH_MEASURE( 1.000000000000000082E-05 ), #1399, 'distance_accuracy_value', 'NONE');
#197970=CYLINDRICAL_SURFACE ( 'NONE', #68254, 0.09999999999999939493 ) ;
#197984=ORIENTED_EDGE ( 'NONE', *, *, #152519, .F. ) ;
#197986=VERTEX_POINT ( 'NONE', #201142 ) ;
#197997=CARTESIAN_POINT ( 'NONE',  ( 23.14999999999999503, 11.65000000001116298, -93.48519422934610645 ) ) ;
#198002=DIRECTION ( 'NONE',  ( 0.000000000000000000, 0.000000000000000000, -1.000000000000000000 ) ) ;
#198012=DIRECTION ( 'NONE',  ( 0.000000000000000000, 0.000000000000000000, 1.000000000000000000 ) ) ;
#198035=DIRECTION ( 'NONE',  ( 1.000000000000000000, -0.000000000000000000, -0.000000000000000000 ) ) ;
#198068=CARTESIAN_POINT ( 'NONE',  ( 22.49066049874202022, 0.05634325154338429287, -55.34998776248293950 ) ) ;
#198075=VERTEX_POINT ( 'NONE', #199439 ) ;
#198097=DIRECTION ( 'NONE',  ( 0.000000000000000000, 1.000000000000000000, 0.000000000000000000 ) ) ;
#198120=CARTESIAN_POINT ( 'NONE',  ( 18.59999999999999432, 1.736257131608553550, -78.56865232901755292 ) ) ;
#198127=ORIENTED_EDGE ( 'NONE', *, *, #77126, .F. ) ;
#198141=DIRECTION ( 'NONE',  ( 1.000000000000000000, 0.000000000000000000, 0.000000000000000000 ) ) ;
#198146=DIRECTION ( 'NONE',  ( 0.000000000000000000, 0.000000000000000000, -1.000000000000000000 ) ) ;
#198161=ORIENTED_EDGE ( 'NONE', *, *, #78120, .T. ) ;
#198174=CARTESIAN_POINT ( 'NONE',  ( 18.50000000000000000, -9.499999999988842703, -74.03206939669971121 ) ) ;
#198207=FACE_OUTER_BOUND ( 'NONE', #14745, .T. ) ;
#198225=CARTESIAN_POINT ( 'NONE',  ( -23.25000000000000000, -0.1008583690875562017, -55.25043287651065782 ) ) ;
#198227=ORIENTED_EDGE ( 'NONE', *, *, #174921, .F. ) ;
#198262=CARTESIAN_POINT ( 'NONE',  ( 21.05000000000000071, -0.09999993529482767429, -60.52192177890540847 ) ) ;
#198276=ORIENTED_EDGE ( 'NONE', *, *, #167983, .F. ) ;
#198304=ORIENTED_EDGE ( 'NONE', *, *, #39440, .F. ) ;
#198313=ORIENTED_EDGE ( 'NONE', *, *, #29908, .T. ) ;
#198324=ORIENTED_EDGE ( 'NONE', *, *, #72837, .F. ) ;
#198357=VECTOR ( 'NONE', #11118, 1000.000000000000000 ) ;
#198361=EDGE_CURVE ( 'NONE', #219131, #55413, #119919, .T. ) ;
#198396=DIRECTION ( 'NONE',  ( 0.000000000000000000, 0.000000000000000000, -1.000000000000000000 ) ) ;
#198400=CARTESIAN_POINT ( 'NONE',  ( -20.93975676684922504, 10.31104185824063180, -106.0204516983106231 ) ) ;
#198403=DIRECTION ( 'NONE',  ( 0.000000000000000000, 8.881784197000696176E-16, -1.000000000000000000 ) ) ;
#198421=DIRECTION ( 'NONE',  ( 0.000000000000000000, 1.224646799142015331E-16, 1.000000000000000000 ) ) ;
#198461=ORIENTED_EDGE ( 'NONE', *, *, #115475, .T. ) ;
#198466=LINE ( 'NONE', #104473, #161706 ) ;
#198510=AXIS2_PLACEMENT_3D ( 'NONE', #95390, #13293, #169838 ) ;
#198536=DIRECTION ( 'NONE',  ( 0.000000000000000000, -0.8777080977375132376, 0.4791956752371582251 ) ) ;
#198546=AXIS2_PLACEMENT_3D ( 'NONE', #73384, #53783, #176328 ) ;
#198581=ORIENTED_EDGE ( 'NONE', *, *, #94732, .F. ) ;
#198598=AXIS2_PLACEMENT_3D ( 'NONE', #217883, #241338, #80945 ) ;
#198610=VERTEX_POINT ( 'NONE', #75350 ) ;
#198632=AXIS2_PLACEMENT_3D ( 'NONE', #156735, #199706, #234961 ) ;
#198645=VECTOR ( 'NONE', #112140, 1000.000000000000000 ) ;
#198678=TOROIDAL_SURFACE ( 'NONE', #7124, 0.2000000000000000111, 0.1000000000000000056 ) ;
#198710=ORIENTED_EDGE ( 'NONE', *, *, #245256, .F. ) ;
#198726=DIRECTION ( 'NONE',  ( 0.000000000000000000, 0.000000000000000000, -1.000000000000000000 ) ) ;
#198731=CARTESIAN_POINT ( 'NONE',  ( 20.94999999999999929, 1.835341550235569663, -78.55515129256303908 ) ) ;
#198743=DIRECTION ( 'NONE',  ( 0.000000000000000000, 0.000000000000000000, -1.000000000000000000 ) ) ;
#198765=DIRECTION ( 'NONE',  ( 1.000000000000000000, -0.000000000000000000, -0.000000000000000000 ) ) ;
#198776=CARTESIAN_POINT ( 'NONE',  ( 22.57320508075688537, 11.65000000001115588, -67.00000000000004263 ) ) ;
#198795=ORIENTED_EDGE ( 'NONE', *, *, #89592, .T. ) ;
#198818=ADVANCED_FACE ( 'NONE', ( #48688 ), #130800, .T. ) ;
#198825=VERTEX_POINT ( 'NONE', #190818 ) ;
#198836=ORIENTED_EDGE ( 'NONE', *, *, #241478, .F. ) ;
#198848=CARTESIAN_POINT ( 'NONE',  ( 21.14999999999999858, 10.71339244341104013, -79.25000000000004263 ) ) ;
#198890=CARTESIAN_POINT ( 'NONE',  ( -20.64999999999999858, 2.000000000011154189, -79.72462192276213955 ) ) ;
#198892=CARTESIAN_POINT ( 'NONE',  ( 23.25000000000000000, -11.74999999998883560, -97.40000000000004832 ) ) ;
#198934=CYLINDRICAL_SURFACE ( 'NONE', #196884, 0.5000000000000004441 ) ;
#198936=AXIS2_PLACEMENT_3D ( 'NONE', #65302, #185255, #2747 ) ;
#198948=LINE ( 'NONE', #179413, #100502 ) ;
#199004=EDGE_CURVE ( 'NONE', #237745, #6498, #106043, .T. ) ;
#199024=CARTESIAN_POINT ( 'NONE',  ( 22.39999999999999503, 1.115600667400684642E-11, -59.20922040162666633 ) ) ;
#199027=CARTESIAN_POINT ( 'NONE',  ( -23.25000000000000000, 11.75000000001115552, -67.00000000000004263 ) ) ;
#199029=CIRCLE ( 'NONE', #257234, 0.1000000000000028644 ) ;
#199041=ORIENTED_EDGE ( 'NONE', *, *, #189941, .T. ) ;
#199043=ORIENTED_EDGE ( 'NONE', *, *, #107963, .T. ) ;
#199044=DIRECTION ( 'NONE',  ( 0.000000000000000000, 0.000000000000000000, -1.000000000000000000 ) ) ;
#199056=( LENGTH_UNIT ( ) NAMED_UNIT ( * ) SI_UNIT ( .MILLI., .METRE. ) );
#199093=CARTESIAN_POINT ( 'NONE',  ( -23.15000000000000213, -8.999999999988846255, -76.39396912265249284 ) ) ;
#199101=DIRECTION ( 'NONE',  ( -0.000000000000000000, 0.9876197685951276783, 0.1568667991644721316 ) ) ;
#199133=CARTESIAN_POINT ( 'NONE',  ( -23.15000000000000213, 2.000000000011154189, -79.72462192276213955 ) ) ;
#199204=ORIENTED_EDGE ( 'NONE', *, *, #183299, .T. ) ;
#199229=CARTESIAN_POINT ( 'NONE',  ( -20.54999999999999716, 7.150000000011155876, -79.35000000000005116 ) ) ;
#199232=DIRECTION ( 'NONE',  ( 0.000000000000000000, -0.000000000000000000, -1.000000000000000000 ) ) ;
#199236=CARTESIAN_POINT ( 'NONE',  ( 22.39999999999999503, 11.65000000001116298, -66.90000000000004832 ) ) ;
#199243=AXIS2_PLACEMENT_3D ( 'NONE', #17256, #57634, #95487 ) ;
#199245=CARTESIAN_POINT ( 'NONE',  ( -21.14999999999999858, -0.1008583690875562017, -55.25043287651065782 ) ) ;
#199271=CARTESIAN_POINT ( 'NONE',  ( -20.94999999999999929, 1.115600667400684642E-11, -100.5000000000000426 ) ) ;
#199282=CIRCLE ( 'NONE', #95223, 0.09999999999999749367 ) ;
#199283=DIRECTION ( 'NONE',  ( -0.000000000000000000, -1.897661533703519897E-16, 1.000000000000000000 ) ) ;
#199286=AXIS2_PLACEMENT_3D ( 'NONE', #48380, #154905, #246582 ) ;
#199298=ORIENTED_EDGE ( 'NONE', *, *, #82853, .T. ) ;
#199336=EDGE_LOOP ( 'NONE', ( #221993, #225200, #122261, #173905 ) ) ;
#199338=CARTESIAN_POINT ( 'NONE',  ( 18.60000000000000142, -9.480686695267818820, -107.4411151687579036 ) ) ;
#199364=CARTESIAN_POINT ( 'NONE',  ( -20.94999999999999929, -11.74999999998884448, -70.10000000000005116 ) ) ;
#199365=DIRECTION ( 'NONE',  ( 0.000000000000000000, 0.000000000000000000, -1.000000000000000000 ) ) ;
#199412=ORIENTED_EDGE ( 'NONE', *, *, #256145, .F. ) ;
#199416=CARTESIAN_POINT ( 'NONE',  ( -23.15000000000000213, 11.65000000001115588, -55.25000000000004974 ) ) ;
#199420=CARTESIAN_POINT ( 'NONE',  ( 21.59780538579342135, 0.09897866960914131207, -60.15290947005679101 ) ) ;
#199439=CARTESIAN_POINT ( 'NONE',  ( 23.14999999999999858, 1.115649653272650466E-11, -96.50000000000004263 ) ) ;
#199500=DIRECTION ( 'NONE',  ( 0.000000000000000000, 0.000000000000000000, -1.000000000000000000 ) ) ;
#199509=EDGE_CURVE ( 'NONE', #21996, #36999, #93774, .T. ) ;
#199532=AXIS2_PLACEMENT_3D ( 'NONE', #210088, #56106, #193087 ) ;
#199541=DIRECTION ( 'NONE',  ( -1.000000000000000000, 0.000000000000000000, 0.000000000000000000 ) ) ;
#199584=CARTESIAN_POINT ( 'NONE',  ( 18.59999999999999076, 6.400000000011158541, -76.93042463006162279 ) ) ;
#199671=AXIS2_PLACEMENT_3D ( 'NONE', #110849, #192967, #191709 ) ;
#199673=EDGE_CURVE ( 'NONE', #187409, #219130, #156361, .T. ) ;
#199698=VERTEX_POINT ( 'NONE', #54501 ) ;
#199706=DIRECTION ( 'NONE',  ( -1.000000000000000000, -0.000000000000000000, 0.000000000000000000 ) ) ;
#199717=DIRECTION ( 'NONE',  ( -0.000000000000000000, -0.1350103645451876666, -0.9908441862701600211 ) ) ;
#199788=AXIS2_PLACEMENT_3D ( 'NONE', #179013, #192435, #114171 ) ;
#199796=CIRCLE ( 'NONE', #145588, 0.1000000000000028644 ) ;
#199817=DIRECTION ( 'NONE',  ( 1.000000000000000000, 0.000000000000000000, 0.000000000000000000 ) ) ;
#199822=ADVANCED_FACE ( 'NONE', ( #100018 ), #60622, .T. ) ;
#199827=CARTESIAN_POINT ( 'NONE',  ( -21.05000000000000071, 1.162701749949165642, -75.10000000000003695 ) ) ;
#199840=ORIENTED_EDGE ( 'NONE', *, *, #92120, .F. ) ;
#199846=DIRECTION ( 'NONE',  ( -0.000000000000000000, -0.1350103645451904977, 0.9908441862701596881 ) ) ;
#199859=EDGE_CURVE ( 'NONE', #178238, #56894, #177391, .T. ) ;
#199871=VECTOR ( 'NONE', #28666, 1000.000000000000000 ) ;
#199900=CYLINDRICAL_SURFACE ( 'NONE', #104246, 0.1000000000000000472 ) ;
#199914=CARTESIAN_POINT ( 'NONE',  ( -20.54999999999999716, -8.663551401858001100, -90.97589888193274987 ) ) ;
#199927=ADVANCED_FACE ( 'NONE', ( #67342 ), #56520, .F. ) ;
#199946=CARTESIAN_POINT ( 'NONE',  ( -23.15000000000000213, 4.350000000011156054, -88.15000000000004832 ) ) ;
#199949=ORIENTED_EDGE ( 'NONE', *, *, #223539, .F. ) ;
#199954=ORIENTED_EDGE ( 'NONE', *, *, #32682, .F. ) ;
#199955=ORIENTED_EDGE ( 'NONE', *, *, #218446, .T. ) ;
#199968=EDGE_CURVE ( 'NONE', #4930, #173330, #85550, .T. ) ;
#200001=DIRECTION ( 'NONE',  ( -1.000000000000000000, -1.836970198721029934E-16, 0.000000000000000000 ) ) ;
#200008=DIRECTION ( 'NONE',  ( -1.000000000000000000, -2.952720810173289112E-16, 0.000000000000000000 ) ) ;
#200039=CARTESIAN_POINT ( 'NONE',  ( 20.85000000000000142, -1.835859311432481045, -112.0044391687985694 ) ) ;
#200051=DIRECTION ( 'NONE',  ( 0.000000000000000000, 0.000000000000000000, -1.000000000000000000 ) ) ;
#200105=CARTESIAN_POINT ( 'NONE',  ( -23.25000000000000000, -1.835859311432481045, -112.0044391687985694 ) ) ;
#200112=CARTESIAN_POINT ( 'NONE',  ( 20.94999999999999929, -9.399999999988844834, -90.60603087734760663 ) ) ;
#200113=AXIS2_PLACEMENT_3D ( 'NONE', #144756, #87353, #65236 ) ;
#200115=EDGE_CURVE ( 'NONE', #178346, #252694, #173320, .T. ) ;
#200118=EDGE_LOOP ( 'NONE', ( #47834, #239995, #45699 ) ) ;
#200155=EDGE_CURVE ( 'NONE', #49762, #208340, #155899, .T. ) ;
#200177=DIRECTION ( 'NONE',  ( -1.000000000000000000, 0.000000000000000000, 0.000000000000000000 ) ) ;
#200183=CARTESIAN_POINT ( 'NONE',  ( -18.50211644919735576, 10.30207779525982836, -105.9895520716782897 ) ) ;
#200187=ADVANCED_FACE ( 'NONE', ( #161015 ), #202485, .F. ) ;
#200210=DIRECTION ( 'NONE',  ( 1.000000000000000000, 0.000000000000000000, 0.000000000000000000 ) ) ;
#200233=B_SPLINE_CURVE_WITH_KNOTS ( 'NONE', 3,
 ( #42247, #212241, #56967, #33636, #135234, #34904, #115693, #121792, #93553, #214782 ),
 .UNSPECIFIED., .F., .F.,
 ( 4, 3, 3, 4 ),
 ( 0.000000000000000000, 3.394313611811197040E-05, 6.779740500700327799E-05, 0.0001049857339142765996 ),
 .UNSPECIFIED. ) ;
#200234=CARTESIAN_POINT ( 'NONE',  ( 18.50000972452444969, 10.29326151435342851, -105.9592822510414862 ) ) ;
#200288=AXIS2_PLACEMENT_3D ( 'NONE', #121093, #158926, #80619 ) ;
#200335=( NAMED_UNIT ( * ) SI_UNIT ( $, .STERADIAN. ) SOLID_ANGLE_UNIT ( ) );
#200338=EDGE_CURVE ( 'NONE', #39555, #149634, #8366, .T. ) ;
#200365=B_SPLINE_CURVE_WITH_KNOTS ( 'NONE', 3,
 ( #31790, #249530, #244365, #111298, #67029, #185694, #128296, #164851, #146537, #226066, #30488, #47440, #207853, #107434, #9614, #186999, #149153, #190864, #167439 ),
 .UNSPECIFIED., .F., .F.,
 ( 4, 3, 3, 3, 3, 3, 4 ),
 ( 1.387778780781445676E-17, 2.646747978908994698E-05, 5.271166642128863382E-05, 9.008788829885137981E-05, 0.0001426648776561022008, 0.0001897378458659801945, 0.0001917382627806380965 ),
 .UNSPECIFIED. ) ;
#200374=DIRECTION ( 'NONE',  ( 0.000000000000000000, -0.000000000000000000, 1.000000000000000000 ) ) ;
#200392=EDGE_CURVE ( 'NONE', #108958, #101410, #166180, .T. ) ;
#200417=DIRECTION ( 'NONE',  ( 1.000000000000000000, -0.000000000000000000, -0.000000000000000000 ) ) ;
#200436=DIRECTION ( 'NONE',  ( -0.000000000000000000, -1.000000000000000000, 0.000000000000000000 ) ) ;
#200453=CARTESIAN_POINT ( 'NONE',  ( -22.47886152344871036, 0.03750093887284931121, -55.35001135695211616 ) ) ;
#200465=ORIENTED_EDGE ( 'NONE', *, *, #80725, .T. ) ;
#200488=LINE ( 'NONE', #21854, #63692 ) ;
#200508=DIRECTION ( 'NONE',  ( 1.000000000000000000, 0.000000000000000000, 0.000000000000000000 ) ) ;
#200516=AXIS2_PLACEMENT_3D ( 'NONE', #54107, #210622, #230 ) ;
#200524=AXIS2_PLACEMENT_3D ( 'NONE', #241181, #160374, #61244 ) ;
#200540=DIRECTION ( 'NONE',  ( 0.000000000000000000, 0.000000000000000000, 1.000000000000000000 ) ) ;
#200577=DIRECTION ( 'NONE',  ( 1.000000000000000000, 0.000000000000000000, 0.000000000000000000 ) ) ;
#200588=ORIENTED_EDGE ( 'NONE', *, *, #181284, .F. ) ;
#200601=VERTEX_POINT ( 'NONE', #24749 ) ;
#200631=CIRCLE ( 'NONE', #38321, 0.09999999999999939493 ) ;
#200659=DIRECTION ( 'NONE',  ( 0.000000000000000000, 0.9887567792719341719, -0.1495327102803664099 ) ) ;
#200668=ORIENTED_EDGE ( 'NONE', *, *, #138885, .T. ) ;
#200671=ORIENTED_EDGE ( 'NONE', *, *, #77415, .F. ) ;
#200672=DIRECTION ( 'NONE',  ( 0.000000000000000000, 0.000000000000000000, -1.000000000000000000 ) ) ;
#200688=CARTESIAN_POINT ( 'NONE',  ( 21.14999999999999858, 6.650000000011155876, -79.25000000000004263 ) ) ;
#200703=ADVANCED_FACE ( 'NONE', ( #231922 ), #254017, .T. ) ;
#200738=DIRECTION ( 'NONE',  ( 1.000000000000000000, -0.000000000000000000, -0.000000000000000000 ) ) ;
#200780=DIRECTION ( 'NONE',  ( 0.000000000000000000, 0.5000000000000078826, -0.8660254037844340447 ) ) ;
#200805=PLANE ( 'NONE',  #185622 ) ;
#200854=AXIS2_PLACEMENT_3D ( 'NONE', #203226, #122417, #79409 ) ;
#200886=DIRECTION ( 'NONE',  ( -1.000000000000000000, -0.000000000000000000, 0.000000000000000000 ) ) ;
#200917=DIRECTION ( 'NONE',  ( -4.448008912761043807E-16, 1.000000000000000000, 0.000000000000000000 ) ) ;
#200954=ORIENTED_EDGE ( 'NONE', *, *, #45292, .F. ) ;
#200967=CARTESIAN_POINT ( 'NONE',  ( -20.90851465518106167, 10.32532329027886320, -106.0699343018359997 ) ) ;
#200973=AXIS2_PLACEMENT_3D ( 'NONE', #91249, #229475, #166964 ) ;
#200982=CARTESIAN_POINT ( 'NONE',  ( -21.05000000000000071, -0.09999999998884338825, -60.45934304829880546 ) ) ;
#200987=CARTESIAN_POINT ( 'NONE',  ( 20.94999999999999574, 1.849084418638171856, -78.65601052144717187 ) ) ;
#201012=AXIS2_PLACEMENT_3D ( 'NONE', #84137, #120784, #123332 ) ;
#201030=CARTESIAN_POINT ( 'NONE',  ( -23.25000000000000000, 4.350000000011156054, -88.35000000000003695 ) ) ;
#201048=DIRECTION ( 'NONE',  ( 1.000000000000000000, 0.000000000000000000, 0.000000000000000000 ) ) ;
#201054=CIRCLE ( 'NONE', #5389, 0.1000000000000028644 ) ;
#201071=LINE ( 'NONE', #86233, #38609 ) ;
#201106=CARTESIAN_POINT ( 'NONE',  ( 21.14999999999999858, 6.540656951712400691, -67.10000000000005116 ) ) ;
#201138=VECTOR ( 'NONE', #70750, 1000.000000000000114 ) ;
#201142=CARTESIAN_POINT ( 'NONE',  ( -18.59999999999999787, 6.933893972137497030, -104.2856458343736250 ) ) ;
#201153=CARTESIAN_POINT ( 'NONE',  ( 21.14999999999999503, 11.75000000001115552, -67.00000000000004263 ) ) ;
#201159=ORIENTED_EDGE ( 'NONE', *, *, #167462, .T. ) ;
#201167=AXIS2_PLACEMENT_3D ( 'NONE', #213566, #146216, #127954 ) ;
#201181=ORIENTED_EDGE ( 'NONE', *, *, #43194, .F. ) ;
#201185=VERTEX_POINT ( 'NONE', #161051 ) ;
#201197=LINE ( 'NONE', #139920, #82844 ) ;
#201238=CARTESIAN_POINT ( 'NONE',  ( 18.59999999999999076, 6.450000000011156587, -88.25000000000005684 ) ) ;
#201256=CIRCLE ( 'NONE', #234582, 0.09999999999999939493 ) ;
#201260=DIRECTION ( 'NONE',  ( -1.836970198721029934E-16, 1.000000000000000000, 0.000000000000000000 ) ) ;
#201271=EDGE_CURVE ( 'NONE', #95067, #77584, #57262, .T. ) ;
#201290=LINE ( 'NONE', #137453, #197527 ) ;
#201300=EDGE_CURVE ( 'NONE', #111810, #13016, #12268, .T. ) ;
#201325=ORIENTED_EDGE ( 'NONE', *, *, #71221, .F. ) ;
#201338=VERTEX_POINT ( 'NONE', #133477 ) ;
#201373=AXIS2_PLACEMENT_3D ( 'NONE', #204367, #13568, #222635 ) ;
#201399=ORIENTED_EDGE ( 'NONE', *, *, #136712, .F. ) ;
#201402=EDGE_CURVE ( 'NONE', #48905, #156376, #155645, .T. ) ;
#201425=VECTOR ( 'NONE', #185728, 1000.000000000000000 ) ;
#201426=EDGE_CURVE ( 'NONE', #118177, #31646, #8513, .T. ) ;
#201428=CIRCLE ( 'NONE', #147641, 0.1000000000000028644 ) ;
#201453=CARTESIAN_POINT ( 'NONE',  ( -20.64999999999999858, 7.150000000011155876, -79.35000000000005116 ) ) ;
#201510=VERTEX_POINT ( 'NONE', #98161 ) ;
#201521=CIRCLE ( 'NONE', #172363, 0.2000000000000057288 ) ;
#201535=CARTESIAN_POINT ( 'NONE',  ( 18.49999999999999645, 1.115600667400684642E-11, -100.5000000000000426 ) ) ;
#201575=ORIENTED_EDGE ( 'NONE', *, *, #167268, .F. ) ;
#201636=DIRECTION ( 'NONE',  ( 0.000000000000000000, 0.000000000000000000, -1.000000000000000000 ) ) ;
#201678=CIRCLE ( 'NONE', #51815, 0.1000000000000028644 ) ;
#201679=DIRECTION ( 'NONE',  ( 0.000000000000000000, 0.000000000000000000, -1.000000000000000000 ) ) ;
#201696=AXIS2_PLACEMENT_3D ( 'NONE', #7230, #183326, #4659 ) ;
#201706=AXIS2_PLACEMENT_3D ( 'NONE', #215768, #78819, #239202 ) ;
#201712=CARTESIAN_POINT ( 'NONE',  ( -21.93340585971692391, 7.324147022868191748, -67.00000000000004263 ) ) ;
#201725=DIRECTION ( 'NONE',  ( -1.000000000000000000, 0.000000000000000000, 0.000000000000000000 ) ) ;
#201728=CARTESIAN_POINT ( 'NONE',  ( -22.50000000000000000, 0.09263750062063526303, -55.35030279295929745 ) ) ;
#201729=ADVANCED_FACE ( 'NONE', ( #33889 ), #249056, .T. ) ;
#201738=DIRECTION ( 'NONE',  ( -1.000000000000000000, -0.000000000000000000, -0.000000000000000000 ) ) ;
#201745=DIRECTION ( 'NONE',  ( -0.000000000000000000, -0.9875055080513799322, 0.1575844902526464253 ) ) ;
#201758=DIRECTION ( 'NONE',  ( -1.000000000000000000, -2.952720810173289112E-16, 0.000000000000000000 ) ) ;
#201803=VECTOR ( 'NONE', #232205, 1000.000000000000000 ) ;
#201815=AXIS2_PLACEMENT_3D ( 'NONE', #123191, #223550, #51323 ) ;
#201834=VECTOR ( 'NONE', #116836, 1000.000000000000000 ) ;
#201851=VERTEX_POINT ( 'NONE', #70439 ) ;
#201859=DIRECTION ( 'NONE',  ( 1.000000000000000000, 0.000000000000000000, 0.000000000000000000 ) ) ;
#201869=CARTESIAN_POINT ( 'NONE',  ( 20.94999999999999929, 11.65000000001115943, -100.5000000000000426 ) ) ;
#201878=EDGE_CURVE ( 'NONE', #189061, #4212, #55942, .T. ) ;
#201911=ADVANCED_FACE ( 'NONE', ( #255395 ), #76808, .F. ) ;
#201917=VERTEX_POINT ( 'NONE', #2389 ) ;
#201924=EDGE_CURVE ( 'NONE', #114500, #97606, #98910, .T. ) ;
#201936=ORIENTED_EDGE ( 'NONE', *, *, #50008, .T. ) ;
#201938=ORIENTED_EDGE ( 'NONE', *, *, #78014, .T. ) ;
#201965=EDGE_LOOP ( 'NONE', ( #42464, #148906, #39590, #87793 ) ) ;
#201973=FACE_OUTER_BOUND ( 'NONE', #61708, .T. ) ;
#201974=CARTESIAN_POINT ( 'NONE',  ( 21.07928932188134397, 0.09889514566555242248, -60.67148334360673800 ) ) ;
#202005=CARTESIAN_POINT ( 'NONE',  ( -20.64999999999999858, -8.999999999988846255, -76.89396912265249284 ) ) ;
#202006=DIRECTION ( 'NONE',  ( 0.000000000000000000, 0.000000000000000000, -1.000000000000000000 ) ) ;
#202007=DIRECTION ( 'NONE',  ( 0.000000000000000000, -1.000000000000000000, 0.000000000000000000 ) ) ;
#202034=FACE_OUTER_BOUND ( 'NONE', #48525, .T. ) ;
#202037=DIRECTION ( 'NONE',  ( 0.000000000000000000, 1.000000000000000000, 0.000000000000000000 ) ) ;
#202055=ORIENTED_EDGE ( 'NONE', *, *, #216471, .T. ) ;
#202075=AXIS2_PLACEMENT_3D ( 'NONE', #151005, #92297, #231833 ) ;
#202083=ORIENTED_EDGE ( 'NONE', *, *, #120878, .F. ) ;
#202102=AXIS2_PLACEMENT_3D ( 'NONE', #41085, #65759, #26657 ) ;
#202135=ORIENTED_EDGE ( 'NONE', *, *, #24050, .T. ) ;
#202136=EDGE_CURVE ( 'NONE', #187820, #120408, #79599, .T. ) ;
#202172=ORIENTED_EDGE ( 'NONE', *, *, #227821, .F. ) ;
#202179=DIRECTION ( 'NONE',  ( 1.000000000000000000, -0.000000000000000000, -0.000000000000000000 ) ) ;
#202181=ORIENTED_EDGE ( 'NONE', *, *, #78112, .T. ) ;
#202201=DIRECTION ( 'NONE',  ( -1.000000000000000000, 0.000000000000000000, 0.000000000000000000 ) ) ;
#202209=CYLINDRICAL_SURFACE ( 'NONE', #139979, 4.000000000000003553 ) ;
#202223=EDGE_CURVE ( 'NONE', #237745, #105777, #109195, .T. ) ;
#202279=B_SPLINE_CURVE_WITH_KNOTS ( 'NONE', 3,
 ( #67539, #87084, #66266, #62417 ),
 .UNSPECIFIED., .F., .F.,
 ( 4, 4 ),
 ( 0.000000000000000000, 0.0001048066582182451801 ),
 .UNSPECIFIED. ) ;
#202292=AXIS2_PLACEMENT_3D ( 'NONE', #77840, #213505, #235632 ) ;
#202330=CARTESIAN_POINT ( 'NONE',  ( -23.15000000000000213, 4.350000000011156054, -88.35000000000003695 ) ) ;
#202334=CARTESIAN_POINT ( 'NONE',  ( 18.50000000000000000, -9.399999999988843058, -107.3820418481727188 ) ) ;
#202338=AXIS2_PLACEMENT_3D ( 'NONE', #152185, #50456, #171751 ) ;
#202347=CARTESIAN_POINT ( 'NONE',  ( -20.64999999999999858, 4.350000000011156054, -79.25000000000004263 ) ) ;
#202353=ORIENTED_EDGE ( 'NONE', *, *, #219772, .F. ) ;
#202377=CARTESIAN_POINT ( 'NONE',  ( -21.05000000000000071, 1.250000000011155299, -75.00000000000004263 ) ) ;
#202380=ORIENTED_EDGE ( 'NONE', *, *, #39991, .T. ) ;
#202384=DIRECTION ( 'NONE',  ( 0.000000000000000000, 0.000000000000000000, 1.000000000000000000 ) ) ;
#202399=DIRECTION ( 'NONE',  ( 0.000000000000000000, 1.000000000000000000, 1.224646799147353207E-16 ) ) ;
#202405=VERTEX_POINT ( 'NONE', #24250 ) ;
#202459=AXIS2_PLACEMENT_3D ( 'NONE', #243611, #64968, #144489 ) ;
#202460=CYLINDRICAL_SURFACE ( 'NONE', #52012, 0.09999999999999939493 ) ;
#202461=AXIS2_PLACEMENT_3D ( 'NONE', #32784, #113565, #74479 ) ;
#202477=VERTEX_POINT ( 'NONE', #127186 ) ;
#202485=TOROIDAL_SURFACE ( 'NONE', #252353, 0.2000000000000000111, 0.1000000000000000056 ) ;
#202508=ORIENTED_EDGE ( 'NONE', *, *, #217535, .T. ) ;
#202517=AXIS2_PLACEMENT_3D ( 'NONE', #54148, #152008, #13751 ) ;
#202545=VECTOR ( 'NONE', #102323, 1000.000000000000000 ) ;
#202548=ORIENTED_EDGE ( 'NONE', *, *, #251012, .F. ) ;
#202551=EDGE_CURVE ( 'NONE', #56225, #178238, #207694, .T. ) ;
#202568=CYLINDRICAL_SURFACE ( 'NONE', #116707, 0.5000000000000004441 ) ;
#202604=CARTESIAN_POINT ( 'NONE',  ( -21.05000000000000071, 11.75000000001115552, -93.48519422934610645 ) ) ;
#202605=DIRECTION ( 'NONE',  ( 0.000000000000000000, -1.000000000000000000, 0.000000000000000000 ) ) ;
#202608=DIRECTION ( 'NONE',  ( 0.000000000000000000, 1.224646799142015331E-16, 1.000000000000000000 ) ) ;
#202644=VERTEX_POINT ( 'NONE', #232718 ) ;
#202676=FACE_OUTER_BOUND ( 'NONE', #20278, .T. ) ;
#202700=ORIENTED_EDGE ( 'NONE', *, *, #230352, .T. ) ;
#202703=CARTESIAN_POINT ( 'NONE',  ( 21.13507111622890022, 10.71768338700954537, -79.24916858636082395 ) ) ;
#202725=CARTESIAN_POINT ( 'NONE',  ( -20.85000000000000142, 11.65000000001115232, -100.5000000000000426 ) ) ;
#202727=CIRCLE ( 'NONE', #65361, 0.1000000000000017958 ) ;
#202733=EDGE_LOOP ( 'NONE', ( #110498, #50496, #61191 ) ) ;
#202744=CARTESIAN_POINT ( 'NONE',  ( 22.49231231312462853, 11.64998490368843953, -66.93894711239866524 ) ) ;
#202756=ADVANCED_FACE ( 'NONE', ( #22666 ), #7960, .T. ) ;
#202762=VERTEX_POINT ( 'NONE', #111174 ) ;
#202827=LINE ( 'NONE', #7179, #160881 ) ;
#202840=FACE_OUTER_BOUND ( 'NONE', #927, .T. ) ;
#202843=B_SPLINE_CURVE_WITH_KNOTS ( 'NONE', 3,
 ( #69958, #209438, #169077, #30837, #110339, #11252 ),
 .UNSPECIFIED., .F., .F.,
 ( 4, 2, 4 ),
 ( 0.000000000000000000, 0.0001497467027049187481, 0.0002994934054098374963 ),
 .UNSPECIFIED. ) ;
#202865=DIRECTION ( 'NONE',  ( 0.000000000000000000, -1.000000000000000000, 0.000000000000000000 ) ) ;
#202882=PRODUCT_DEFINITION_FORMATION_WITH_SPECIFIED_SOURCE ( 'ANY', '', #126320, .NOT_KNOWN. ) ;
#202886=ORIENTED_EDGE ( 'NONE', *, *, #93778, .T. ) ;
#202894=VERTEX_POINT ( 'NONE', #68192 ) ;
#202895=ADVANCED_FACE ( 'NONE', ( #29109 ), #208980, .T. ) ;
#202904=LINE ( 'NONE', #227599, #178038 ) ;
#202907=DIRECTION ( 'NONE',  ( -1.000000000000000000, -2.952720810173289112E-16, 0.000000000000000000 ) ) ;
#202915=DIRECTION ( 'NONE',  ( 1.000000000000000000, -0.000000000000000000, -0.000000000000000000 ) ) ;
#202921=FACE_OUTER_BOUND ( 'NONE', #205617, .T. ) ;
#202950=DIRECTION ( 'NONE',  ( 2.840903330521631775E-16, -0.8700118002898321601, 0.4930308989875230585 ) ) ;
#202977=DIRECTION ( 'NONE',  ( -1.000000000000000000, -7.304098846218134667E-16, 4.217023435051678980E-16 ) ) ;
#202998=AXIS2_PLACEMENT_3D ( 'NONE', #205809, #105390, #184967 ) ;
#202999=AXIS2_PLACEMENT_3D ( 'NONE', #53483, #251677, #73085 ) ;
#203004=SPHERICAL_SURFACE ( 'NONE', #79437, 0.1000000000000000056 ) ;
#203017=DIRECTION ( 'NONE',  ( -3.265361837132813093E-16, 1.000000000000000000, 0.000000000000000000 ) ) ;
#203025=DIRECTION ( 'NONE',  ( 0.000000000000000000, -0.9887567792719341719, -0.1495327102803664099 ) ) ;
#203080=CARTESIAN_POINT ( 'NONE',  ( 18.59999999999999432, -9.480686695267811714, -107.4411151687579036 ) ) ;
#203097=CARTESIAN_POINT ( 'NONE',  ( -18.60000000000000853, -9.364240527579749340, -74.18024858184081438 ) ) ;
#203104=VERTEX_POINT ( 'NONE', #2760 ) ;
#203145=CIRCLE ( 'NONE', #173983, 0.3999999999999975797 ) ;
#203147=CARTESIAN_POINT ( 'NONE',  ( -22.50000000000000000, 7.790779598384560245, -66.90000000000004832 ) ) ;
#203160=VECTOR ( 'NONE', #148531, 1000.000000000000114 ) ;
#203169=CARTESIAN_POINT ( 'NONE',  ( 18.37172112093850274, -9.570961652232023553, -107.3167344534833916 ) ) ;
#203183=ORIENTED_EDGE ( 'NONE', *, *, #190902, .F. ) ;
#203190=VERTEX_POINT ( 'NONE', #61474 ) ;
#203194=CARTESIAN_POINT ( 'NONE',  ( -23.25000000000000000, 1.115600667400684642E-11, -100.5000000000000426 ) ) ;
#203203=CARTESIAN_POINT ( 'NONE',  ( 22.47809213839789066, 0.03753706763967752658, -55.35002666521224057 ) ) ;
#203205=ORIENTED_EDGE ( 'NONE', *, *, #65877, .T. ) ;
#203221=CARTESIAN_POINT ( 'NONE',  ( -18.59999999999999787, -1.164121893230052995, -108.4148480855716485 ) ) ;
#203226=CARTESIAN_POINT ( 'NONE',  ( 20.94999999999999574, 1.162701749949165642, -74.90000000000004832 ) ) ;
#203273=AXIS2_PLACEMENT_3D ( 'NONE', #192127, #150431, #250785 ) ;
#203278=CIRCLE ( 'NONE', #90832, 7.720710678118663850 ) ;
#203283=CARTESIAN_POINT ( 'NONE',  ( -22.39999999999999858, 0.1000000000111554016, -59.20922040162664501 ) ) ;
#203374=CARTESIAN_POINT ( 'NONE',  ( 18.39999999999999858, -9.599999999988842347, -74.03206939669971121 ) ) ;
#203399=VECTOR ( 'NONE', #94239, 1000.000000000000000 ) ;
#203413=PLANE ( 'NONE',  #118490 ) ;
#203425=EDGE_LOOP ( 'NONE', ( #230679, #244904, #42482 ) ) ;
#203426=CIRCLE ( 'NONE', #115937, 0.09999999999999939493 ) ;
#203459=DIRECTION ( 'NONE',  ( -3.787827842127535236E-15, 0.7397360091702777085, 0.6728971962616808744 ) ) ;
#203478=ORIENTED_EDGE ( 'NONE', *, *, #46310, .T. ) ;
#203487=VERTEX_POINT ( 'NONE', #8571 ) ;
#203488=ORIENTED_EDGE ( 'NONE', *, *, #205657, .T. ) ;
#203499=ORIENTED_EDGE ( 'NONE', *, *, #47471, .T. ) ;
#203511=ORIENTED_EDGE ( 'NONE', *, *, #51425, .T. ) ;
#203520=DIRECTION ( 'NONE',  ( -4.408576920032448588E-17, 0.1350103645451876944, -0.9908441862701601321 ) ) ;
#203533=DIRECTION ( 'NONE',  ( -1.000000000000000000, -2.952720810173289112E-16, 0.000000000000000000 ) ) ;
#203536=LINE ( 'NONE', #143552, #136366 ) ;
#203558=CARTESIAN_POINT ( 'NONE',  ( -21.04999999999999716, 0.01485563490477569658, -60.65564095795671307 ) ) ;
#203587=DIRECTION ( 'NONE',  ( 1.000000000000000000, -0.000000000000000000, -0.000000000000000000 ) ) ;
#203616=CIRCLE ( 'NONE', #91193, 0.09999999999999892308 ) ;
#203631=DIRECTION ( 'NONE',  ( 1.000000000000000000, -0.000000000000000000, -0.000000000000000000 ) ) ;
#203658=DIRECTION ( 'NONE',  ( 0.000000000000000000, 0.000000000000000000, -1.000000000000000000 ) ) ;
#203681=ADVANCED_FACE ( 'NONE', ( #17531 ), #115359, .F. ) ;
#203717=CYLINDRICAL_SURFACE ( 'NONE', #45487, 0.1000000000000028644 ) ;
#203816=ORIENTED_EDGE ( 'NONE', *, *, #94732, .T. ) ;
#203878=LINE ( 'NONE', #244282, #107468 ) ;
#203885=DIRECTION ( 'NONE',  ( 0.000000000000000000, 0.000000000000000000, -1.000000000000000000 ) ) ;
#203901=VERTEX_POINT ( 'NONE', #129495 ) ;
#203928=CARTESIAN_POINT ( 'NONE',  ( -20.85000000000000142, 7.021664781911246322, -104.3335654018973315 ) ) ;
#203990=FACE_OUTER_BOUND ( 'NONE', #146366, .T. ) ;
#204020=EDGE_CURVE ( 'NONE', #32089, #66589, #45534, .T. ) ;
#204053=VERTEX_POINT ( 'NONE', #34276 ) ;
#204070=AXIS2_PLACEMENT_3D ( 'NONE', #132182, #193455, #34391 ) ;
#204071=ORIENTED_EDGE ( 'NONE', *, *, #174155, .F. ) ;
#204121=DIRECTION ( 'NONE',  ( 1.000000000000000000, 0.000000000000000000, 0.000000000000000000 ) ) ;
#204126=ORIENTED_EDGE ( 'NONE', *, *, #214597, .F. ) ;
#204159=CARTESIAN_POINT ( 'NONE',  ( 18.55857864376267941, 10.36715728753653565, -91.75000000000005684 ) ) ;
#204163=EDGE_CURVE ( 'NONE', #123901, #197693, #253275, .T. ) ;
#204175=CARTESIAN_POINT ( 'NONE',  ( -20.85000000000000142, -1.164121893230052995, -108.4148480855716485 ) ) ;
#204193=CARTESIAN_POINT ( 'NONE',  ( 20.95325940946048249, 10.52339007070744437, -74.56446212924012684 ) ) ;
#204206=ORIENTED_EDGE ( 'NONE', *, *, #113583, .F. ) ;
#204225=EDGE_CURVE ( 'NONE', #181843, #87673, #2797, .T. ) ;
#204265=CARTESIAN_POINT ( 'NONE',  ( -21.46681500593267700, 6.857511159395791367, -67.00000000000004263 ) ) ;
#204272=AXIS2_PLACEMENT_3D ( 'NONE', #44822, #124369, #203885 ) ;
#204273=EDGE_CURVE ( 'NONE', #242599, #33168, #195397, .T. ) ;
#204357=CARTESIAN_POINT ( 'NONE',  ( 21.05000000000000426, 6.413826288824128419, -67.08574093703344943 ) ) ;
#204367=CARTESIAN_POINT ( 'NONE',  ( -23.15000000000000213, -11.48912529306489816, -97.40000000000004832 ) ) ;
#204402=CARTESIAN_POINT ( 'NONE',  ( -23.15000000000000213, -11.48912529306489994, -97.40000000000004832 ) ) ;
#204413=CARTESIAN_POINT ( 'NONE',  ( 21.14999999999999858, 10.71339244341104013, -79.25000000000004263 ) ) ;
#204428=ORIENTED_EDGE ( 'NONE', *, *, #162483, .T. ) ;
#204458=AXIS2_PLACEMENT_3D ( 'NONE', #199827, #177707, #255874 ) ;
#204459=EDGE_CURVE ( 'NONE', #91651, #13016, #16505, .T. ) ;
#204477=EDGE_CURVE ( 'NONE', #237011, #130783, #166368, .T. ) ;
#204498=CARTESIAN_POINT ( 'NONE',  ( 20.95512820512820440, 8.876151316299273120, -79.20017285912881277 ) ) ;
#204518=FACE_OUTER_BOUND ( 'NONE', #167139, .T. ) ;
#204525=LINE ( 'NONE', #184974, #237328 ) ;
#204558=ORIENTED_EDGE ( 'NONE', *, *, #93626, .F. ) ;
#204587=CARTESIAN_POINT ( 'NONE',  ( -20.94999999999999929, -1.162701749926853712, -74.90000000000004832 ) ) ;
#204591=CARTESIAN_POINT ( 'NONE',  ( -20.94999999999999929, 1.835341550235567887, -78.65515129256301918 ) ) ;
#204664=CYLINDRICAL_SURFACE ( 'NONE', #48292, 11.74999999999999645 ) ;
#204687=AXIS2_PLACEMENT_3D ( 'NONE', #43237, #78487, #98032 ) ;
#204717=EDGE_CURVE ( 'NONE', #58672, #83997, #159049, .T. ) ;
#204720=DIRECTION ( 'NONE',  ( 0.000000000000000000, -1.000000000000000000, 0.000000000000000000 ) ) ;
#204737=FACE_OUTER_BOUND ( 'NONE', #46234, .T. ) ;
#204763=ORIENTED_EDGE ( 'NONE', *, *, #104411, .T. ) ;
#204768=AXIS2_PLACEMENT_3D ( 'NONE', #216432, #112226, #194340 ) ;
#204805=EDGE_CURVE ( 'NONE', #256646, #212939, #108041, .T. ) ;
#204818=DIRECTION ( 'NONE',  ( 0.000000000000000000, 0.000000000000000000, -1.000000000000000000 ) ) ;
#204832=LINE ( 'NONE', #103161, #27550 ) ;
#204860=CIRCLE ( 'NONE', #125754, 6.329289321881370611 ) ;
#204868=DIRECTION ( 'NONE',  ( -1.000000000000000000, -2.952720810173289112E-16, 0.000000000000000000 ) ) ;
#204896=CIRCLE ( 'NONE', #92468, 12.87499999999999822 ) ;
#204901=LINE ( 'NONE', #143654, #147198 ) ;
#204908=ORIENTED_EDGE ( 'NONE', *, *, #93257, .T. ) ;
#204933=ORIENTED_EDGE ( 'NONE', *, *, #227671, .F. ) ;
#204935=DIRECTION ( 'NONE',  ( -1.000000000000000000, 0.000000000000000000, 0.000000000000000000 ) ) ;
#204942=ORIENTED_EDGE ( 'NONE', *, *, #32682, .T. ) ;
#204947=ORIENTED_EDGE ( 'NONE', *, *, #169866, .T. ) ;
#204967=DIRECTION ( 'NONE',  ( 0.000000000000000000, 0.000000000000000000, -1.000000000000000000 ) ) ;
#205005=CARTESIAN_POINT ( 'NONE',  ( 18.59999999999999787, -9.399999999988843058, -107.3820418481727188 ) ) ;
#205019=AXIS2_PLACEMENT_3D ( 'NONE', #245207, #187809, #49565 ) ;
#205031=AXIS2_PLACEMENT_3D ( 'NONE', #111540, #35874, #168989 ) ;
#205048=VERTEX_POINT ( 'NONE', #2183 ) ;
#205115=CARTESIAN_POINT ( 'NONE',  ( 23.14999999999999503, 11.65000000001116298, -88.35000000000003695 ) ) ;
#205138=EDGE_LOOP ( 'NONE', ( #119333, #238180, #188044 ) ) ;
#205146=DIRECTION ( 'NONE',  ( 0.000000000000000000, 0.000000000000000000, -1.000000000000000000 ) ) ;
#205162=CARTESIAN_POINT ( 'NONE',  ( 21.05000000000000071, -0.01681986837452062455, -60.69257478043463294 ) ) ;
#205166=AXIS2_PLACEMENT_3D ( 'NONE', #242223, #220111, #200540 ) ;
#205170=CARTESIAN_POINT ( 'NONE',  ( 21.14999999999999858, 6.540656951712401579, -67.00000000000004263 ) ) ;
#205206=VERTEX_POINT ( 'NONE', #45178 ) ;
#205249=CARTESIAN_POINT ( 'NONE',  ( -20.94999999999999929, -11.64999999998884483, -100.5000000000000426 ) ) ;
#205251=ADVANCED_FACE ( 'NONE', ( #34608 ), #114110, .F. ) ;
#205310=CARTESIAN_POINT ( 'NONE',  ( -21.05000000000000071, 6.258842723548713849, -66.96798630681233533 ) ) ;
#205326=EDGE_CURVE ( 'NONE', #255102, #95156, #95942, .T. ) ;
#205338=ORIENTED_EDGE ( 'NONE', *, *, #50060, .F. ) ;
#205346=EDGE_LOOP ( 'NONE', ( #49543, #70777, #252880, #121811 ) ) ;
#205393=ORIENTED_EDGE ( 'NONE', *, *, #145340, .T. ) ;
#205397=EDGE_CURVE ( 'NONE', #21107, #245368, #18864, .T. ) ;
#205409=VERTEX_POINT ( 'NONE', #218331 ) ;
#205458=ADVANCED_FACE ( 'NONE', ( #25317 ), #8320, .F. ) ;
#205480=ADVANCED_FACE ( 'NONE', ( #22751 ), #87809, .F. ) ;
#205501=AXIS2_PLACEMENT_3D ( 'NONE', #51342, #171375, #30556 ) ;
#205507=ORIENTED_EDGE ( 'NONE', *, *, #234558, .T. ) ;
#205513=DIRECTION ( 'NONE',  ( 0.000000000000000000, 0.000000000000000000, -1.000000000000000000 ) ) ;
#205518=LINE ( 'NONE', #209380, #175688 ) ;
#205523=ORIENTED_EDGE ( 'NONE', *, *, #40974, .T. ) ;
#205573=CARTESIAN_POINT ( 'NONE',  ( -22.39999999999999858, 11.75000000001115552, -67.00000000000004263 ) ) ;
#205600=VERTEX_POINT ( 'NONE', #91690 ) ;
#205612=VERTEX_POINT ( 'NONE', #111260 ) ;
#205617=EDGE_LOOP ( 'NONE', ( #186851, #4032, #152531, #118138 ) ) ;
#205624=DIRECTION ( 'NONE',  ( -0.000000000000000000, -0.000000000000000000, -1.000000000000000000 ) ) ;
#205638=CIRCLE ( 'NONE', #168297, 11.74999999999999645 ) ;
#205657=EDGE_CURVE ( 'NONE', #201917, #243244, #33052, .T. ) ;
#205682=ORIENTED_EDGE ( 'NONE', *, *, #167061, .T. ) ;
#205683=AXIS2_PLACEMENT_3D ( 'NONE', #92564, #174738, #33944 ) ;
#205685=DIRECTION ( 'NONE',  ( 0.000000000000000000, 0.000000000000000000, -1.000000000000000000 ) ) ;
#205716=VECTOR ( 'NONE', #166362, 1000.000000000000000 ) ;
#205745=CYLINDRICAL_SURFACE ( 'NONE', #257936, 0.1000000000000028644 ) ;
#205764=CARTESIAN_POINT ( 'NONE',  ( 23.24999999999999289, 11.65000000001116298, -55.25000000000004974 ) ) ;
#205809=CARTESIAN_POINT ( 'NONE',  ( -18.50000000000000000, 9.350000000011156942, -79.35000000000005116 ) ) ;
#205817=DIRECTION ( 'NONE',  ( 1.000000000000000000, 0.000000000000000000, 0.000000000000000000 ) ) ;
#205851=LINE ( 'NONE', #243694, #142510 ) ;
#205859=AXIS2_PLACEMENT_3D ( 'NONE', #252744, #195379, #96239 ) ;
#205874=CARTESIAN_POINT ( 'NONE',  ( -21.14999999999999858, 1.115600667400684642E-11, -55.35042919245524473 ) ) ;
#205889=ORIENTED_EDGE ( 'NONE', *, *, #174921, .T. ) ;
#205894=CARTESIAN_POINT ( 'NONE',  ( -20.94999999999999929, 1.360870587203197646, -75.07299792709100927 ) ) ;
#205899=ORIENTED_EDGE ( 'NONE', *, *, #220573, .T. ) ;
#205917=CARTESIAN_POINT ( 'NONE',  ( -21.44999999999999929, 7.150000000011155876, -88.25000000000005684 ) ) ;
#205938=DIRECTION ( 'NONE',  ( 0.000000000000000000, 0.000000000000000000, -1.000000000000000000 ) ) ;
#205962=DIRECTION ( 'NONE',  ( 0.000000000000000000, 0.000000000000000000, -1.000000000000000000 ) ) ;
#205970=DIRECTION ( 'NONE',  ( 0.000000000000000000, 0.6728971962616697722, 0.7397360091702875895 ) ) ;
#205982=CARTESIAN_POINT ( 'NONE',  ( 21.02374657821571446, 11.60000000083146787, -93.57179677019814790 ) ) ;
#206020=EDGE_CURVE ( 'NONE', #66775, #38016, #38543, .T. ) ;
#206024=CARTESIAN_POINT ( 'NONE',  ( -18.37151313414686982, -9.571014125767112191, -107.3166629092389854 ) ) ;
#206026=CARTESIAN_POINT ( 'NONE',  ( -23.15000000000000213, 1.115600667400684642E-11, -67.00000000000004263 ) ) ;
#206034=DIRECTION ( 'NONE',  ( 1.000000000000000000, 0.000000000000000000, 0.000000000000000000 ) ) ;
#206036=DIRECTION ( 'NONE',  ( 0.000000000000000000, 0.000000000000000000, -1.000000000000000000 ) ) ;
#206040=ORIENTED_EDGE ( 'NONE', *, *, #170687, .T. ) ;
#206053=DIRECTION ( 'NONE',  ( -0.000000000000000000, -0.1298341882520022694, -0.9915357197604853789 ) ) ;
#206058=SPHERICAL_SURFACE ( 'NONE', #98394, 0.1000000000000000056 ) ;
#206073=ORIENTED_EDGE ( 'NONE', *, *, #150293, .F. ) ;
#206074=EDGE_LOOP ( 'NONE', ( #67258, #182562, #2544, #223234, #196674 ) ) ;
#206087=CARTESIAN_POINT ( 'NONE',  ( -21.05000000000000426, 6.477046381801003783, -67.10000000000006537 ) ) ;
#206105=LINE ( 'NONE', #185259, #109073 ) ;
#206109=FACE_OUTER_BOUND ( 'NONE', #14001, .T. ) ;
#206130=CARTESIAN_POINT ( 'NONE',  ( -21.05000000000000071, 0.09779029131994597390, -60.74218538952392521 ) ) ;
#206145=AXIS2_PLACEMENT_3D ( 'NONE', #999, #160140, #180968 ) ;
#206190=CARTESIAN_POINT ( 'NONE',  ( -18.59999999999999787, 1.736257131608553550, -78.56865232901755292 ) ) ;
#206279=DIRECTION ( 'NONE',  ( 1.000000000000000000, 0.000000000000000000, 0.000000000000000000 ) ) ;
#206281=ADVANCED_FACE ( 'NONE', ( #221573 ), #63138, .T. ) ;
#206312=EDGE_LOOP ( 'NONE', ( #128811, #139937, #113274, #116273 ) ) ;
#206321=ADVANCED_FACE ( 'NONE', ( #5084 ), #146342, .F. ) ;
#206326=CARTESIAN_POINT ( 'NONE',  ( -21.00219873199074883, 11.60538868788787070, -73.91264742829459067 ) ) ;
#206335=ORIENTED_EDGE ( 'NONE', *, *, #227671, .T. ) ;
#206351=FACE_OUTER_BOUND ( 'NONE', #243605, .T. ) ;
#206382=FACE_OUTER_BOUND ( 'NONE', #31574, .T. ) ;
#206407=ORIENTED_EDGE ( 'NONE', *, *, #142246, .T. ) ;
#206412=DIRECTION ( 'NONE',  ( 0.000000000000000000, -1.000000000000000000, 0.000000000000000000 ) ) ;
#206418=CARTESIAN_POINT ( 'NONE',  ( -21.05000000000000071, -11.64999999998884483, -70.00000000000004263 ) ) ;
#206425=DIRECTION ( 'NONE',  ( -0.000000000000000000, -0.000000000000000000, 1.000000000000000000 ) ) ;
#206446=ORIENTED_EDGE ( 'NONE', *, *, #216856, .T. ) ;
#206491=DIRECTION ( 'NONE',  ( 0.7071067811865475727, 0.7071067811865475727, 2.044391222244500083E-16 ) ) ;
#206499=DIRECTION ( 'NONE',  ( -1.000000000000000000, -8.673617379884087537E-15, 0.000000000000000000 ) ) ;
#206500=CARTESIAN_POINT ( 'NONE',  ( -23.25000000000000000, 1.115600667400684642E-11, -71.15000000000004832 ) ) ;
#206515=EDGE_CURVE ( 'NONE', #195188, #74473, #167240, .T. ) ;
#206532=CARTESIAN_POINT ( 'NONE',  ( -20.54999999999999716, 2.000000000011154189, -87.67537807723795140 ) ) ;
#206555=DIRECTION ( 'NONE',  ( -0.000000000000000000, 1.000000000000000000, 1.734723475976807292E-15 ) ) ;
#206557=CIRCLE ( 'NONE', #94116, 0.09999999999999939493 ) ;
#206559=CIRCLE ( 'NONE', #27713, 0.1000000000000028644 ) ;
#206598=CARTESIAN_POINT ( 'NONE',  ( 22.48970261584622321, 11.65000000001115588, -66.94463051178263413 ) ) ;
#206615=EDGE_LOOP ( 'NONE', ( #257390, #119604, #73298 ) ) ;
#206634=EDGE_CURVE ( 'NONE', #95314, #104861, #64471, .T. ) ;
#206652=ORIENTED_EDGE ( 'NONE', *, *, #11210, .T. ) ;
#206653=CARTESIAN_POINT ( 'NONE',  ( 18.54148534481893762, 10.32532329027886853, -106.0699343018359997 ) ) ;
#206684=AXIS2_PLACEMENT_3D ( 'NONE', #135075, #155974, #214622 ) ;
#206710=ORIENTED_EDGE ( 'NONE', *, *, #92352, .F. ) ;
#206733=LINE ( 'NONE', #127202, #205716 ) ;
#206771=CARTESIAN_POINT ( 'NONE',  ( 20.84451136049631259, 10.62014191481791059, -74.49392455952968817 ) ) ;
#206846=CARTESIAN_POINT ( 'NONE',  ( 21.07199075132371746, 8.774944999127242795, -79.21353216161290334 ) ) ;
#206867=FACE_OUTER_BOUND ( 'NONE', #142420, .T. ) ;
#206870=CARTESIAN_POINT ( 'NONE',  ( -20.94999999999999929, -11.64999999998884306, -70.10000000000005116 ) ) ;
#206873=TOROIDAL_SURFACE ( 'NONE', #227704, 12.77500000000000036, 0.1000000000000000056 ) ;
#206879=DIRECTION ( 'NONE',  ( 0.000000000000000000, 0.000000000000000000, 1.000000000000000000 ) ) ;
#206906=DIRECTION ( 'NONE',  ( 0.000000000000000000, -1.000000000000000000, 0.000000000000000000 ) ) ;
#206928=DIRECTION ( 'NONE',  ( -1.000000000000000000, 0.000000000000000000, 0.000000000000000000 ) ) ;
#206931=ORIENTED_EDGE ( 'NONE', *, *, #237462, .T. ) ;
#206950=VERTEX_POINT ( 'NONE', #26328 ) ;
#206958=EDGE_CURVE ( 'NONE', #137562, #187441, #134238, .T. ) ;
#206968=ORIENTED_EDGE ( 'NONE', *, *, #228149, .T. ) ;
#206970=CARTESIAN_POINT ( 'NONE',  ( -18.50000000000000000, 11.65000000001115232, -88.35000000000003695 ) ) ;
#206992=VERTEX_POINT ( 'NONE', #4176 ) ;
#207005=ORIENTED_EDGE ( 'NONE', *, *, #222088, .T. ) ;
#207009=ORIENTED_EDGE ( 'NONE', *, *, #251336, .F. ) ;
#207129=DIRECTION ( 'NONE',  ( 1.000000000000000000, 2.952720810173289112E-16, -0.000000000000000000 ) ) ;
#207130=CARTESIAN_POINT ( 'NONE',  ( -23.25000000000000000, -8.999999999988844479, -90.60603087734760663 ) ) ;
#207143=ORIENTED_EDGE ( 'NONE', *, *, #47232, .T. ) ;
#207161=EDGE_LOOP ( 'NONE', ( #156635, #17780, #43130, #257595 ) ) ;
#207164=VERTEX_POINT ( 'NONE', #57414 ) ;
#207165=CARTESIAN_POINT ( 'NONE',  ( 21.04999999999999716, 10.54375127550682301, -74.55638780866505044 ) ) ;
#207176=CARTESIAN_POINT ( 'NONE',  ( -22.47071067811865319, 1.115600667400684642E-11, -67.00000000000004263 ) ) ;
#207187=CARTESIAN_POINT ( 'NONE',  ( -18.59999999999999787, -1.851617760457748618, -112.1031897196037050 ) ) ;
#207221=ORIENTED_EDGE ( 'NONE', *, *, #88720, .T. ) ;
#207228=ORIENTED_EDGE ( 'NONE', *, *, #39947, .F. ) ;
#207265=VECTOR ( 'NONE', #232895, 1000.000000000000000 ) ;
#207270=DIRECTION ( 'NONE',  ( 0.000000000000000000, 1.776356839400254803E-15, -1.000000000000000000 ) ) ;
#207318=EDGE_LOOP ( 'NONE', ( #143211, #166939, #254052, #162826 ) ) ;
#207322=DIRECTION ( 'NONE',  ( 1.000000000000000000, 0.000000000000000000, 0.000000000000000000 ) ) ;
#207361=EDGE_LOOP ( 'NONE', ( #16811, #10654, #69820 ) ) ;
#207384=CARTESIAN_POINT ( 'NONE',  ( 19.97071067811865674, 11.72071067812981937, -91.65000000000004832 ) ) ;
#207398=VECTOR ( 'NONE', #156298, 1000.000000000000000 ) ;
#207402=CIRCLE ( 'NONE', #53259, 0.1000000000000028644 ) ;
#207471=DIRECTION ( 'NONE',  ( 0.000000000000000000, -5.204170427930272346E-14, 1.000000000000000000 ) ) ;
#207482=ADVANCED_FACE ( 'NONE', ( #111981 ), #191533, .F. ) ;
#207529=AXIS2_PLACEMENT_3D ( 'NONE', #235609, #256399, #153572 ) ;
#207545=EDGE_LOOP ( 'NONE', ( #179373, #80028, #211454, #165533 ) ) ;
#207592=ORIENTED_EDGE ( 'NONE', *, *, #87285, .F. ) ;
#207595=CARTESIAN_POINT ( 'NONE',  ( 21.05000000000000071, 1.115600667400684642E-11, -67.00000000000004263 ) ) ;
#207635=FACE_OUTER_BOUND ( 'NONE', #205138, .T. ) ;
#207650=DIRECTION ( 'NONE',  ( -1.000000000000000000, -2.952720810173289112E-16, 0.000000000000000000 ) ) ;
#207676=DIRECTION ( 'NONE',  ( -1.000000000000000000, -3.265361837132813093E-16, 0.000000000000000000 ) ) ;
#207694=CIRCLE ( 'NONE', #257679, 0.09999999999999939493 ) ;
#207716=EDGE_CURVE ( 'NONE', #246680, #242521, #200488, .T. ) ;
#207726=EDGE_LOOP ( 'NONE', ( #31877, #188904, #36605, #145391 ) ) ;
#207739=CARTESIAN_POINT ( 'NONE',  ( 20.04142135623730070, 11.65000000001115943, -88.35000000000003695 ) ) ;
#207770=CARTESIAN_POINT ( 'NONE',  ( 21.14999999999999858, 8.786607556611267356, -79.25000000000004263 ) ) ;
#207772=DIRECTION ( 'NONE',  ( 0.000000000000000000, 0.000000000000000000, -1.000000000000000000 ) ) ;
#207780=CARTESIAN_POINT ( 'NONE',  ( -18.59999999999999787, 7.250000000011155521, -88.35000000000003695 ) ) ;
#207786=CARTESIAN_POINT ( 'NONE',  ( -21.05000000000000071, -0.2561057920810652089, -66.96510355832775474 ) ) ;
#207796=CIRCLE ( 'NONE', #78588, 0.1000000000000000472 ) ;
#207807=DIRECTION ( 'NONE',  ( 1.000000000000000000, 0.000000000000000000, 0.000000000000000000 ) ) ;
#207825=CARTESIAN_POINT ( 'NONE',  ( 23.14999999999998437, 1.115600667400684642E-11, -71.05000000000003979 ) ) ;
#207830=CIRCLE ( 'NONE', #116231, 0.1000000000000028644 ) ;
#207835=TOROIDAL_SURFACE ( 'NONE', #116235, 0.2000000000000000111, 0.1000000000000000056 ) ;
#207851=FACE_OUTER_BOUND ( 'NONE', #2371, .T. ) ;
#207853=CARTESIAN_POINT ( 'NONE',  ( 20.94403535211772294, 10.30632246271647467, -106.0041836778896283 ) ) ;
#207873=CIRCLE ( 'NONE', #78811, 0.09999999999999939493 ) ;
#207898=DIRECTION ( 'NONE',  ( 0.000000000000000000, 0.000000000000000000, -1.000000000000000000 ) ) ;
#207920=CIRCLE ( 'NONE', #124518, 0.1000000000000000472 ) ;
#207959=CARTESIAN_POINT ( 'NONE',  ( 22.40000000000010516, 1.020945751984553285E-11, -55.35042919245493209 ) ) ;
#207971=ORIENTED_EDGE ( 'NONE', *, *, #102652, .F. ) ;
#207984=CARTESIAN_POINT ( 'NONE',  ( -21.07946286933444568, 6.329037319018858021, -66.92331615674363832 ) ) ;
#207998=DIRECTION ( 'NONE',  ( -7.304098846218134667E-16, 1.000000000000000000, -0.000000000000000000 ) ) ;
#208024=EDGE_CURVE ( 'NONE', #225548, #236288, #87590, .T. ) ;
#208077=CARTESIAN_POINT ( 'NONE',  ( 20.95545211741311320, 10.58641331155510379, -74.58614685958833945 ) ) ;
#208111=CARTESIAN_POINT ( 'NONE',  ( 20.04142135623730070, 11.65000000001115943, -55.25000000000004974 ) ) ;
#208122=CARTESIAN_POINT ( 'NONE',  ( 22.39999999999999858, 0.1000000000111554016, -59.20922040162665922 ) ) ;
#208124=EDGE_CURVE ( 'NONE', #152543, #229766, #255552, .T. ) ;
#208150=DIRECTION ( 'NONE',  ( 1.000000000000000000, -7.304098846218135653E-16, 0.000000000000000000 ) ) ;
#208156=LINE ( 'NONE', #109018, #158085 ) ;
#208157=CARTESIAN_POINT ( 'NONE',  ( 23.24999999999999645, 5.000000000011153745, -79.40526601891313874 ) ) ;
#208214=CARTESIAN_POINT ( 'NONE',  ( -18.59999999999999787, 1.250000000011155299, -75.00000000000004263 ) ) ;
#208219=ORIENTED_EDGE ( 'NONE', *, *, #45419, .T. ) ;
#208231=FACE_OUTER_BOUND ( 'NONE', #257488, .T. ) ;
#208258=ORIENTED_EDGE ( 'NONE', *, *, #39592, .F. ) ;
#208298=CARTESIAN_POINT ( 'NONE',  ( -23.25000000000000000, -11.74999999998884448, -97.40000000000004832 ) ) ;
#208299=ADVANCED_FACE ( 'NONE', ( #94019 ), #104165, .T. ) ;
#208300=CIRCLE ( 'NONE', #79268, 12.77499999999999503 ) ;
#208316=ADVANCED_FACE ( 'NONE', ( #174914 ), #239038, .F. ) ;
#208320=CARTESIAN_POINT ( 'NONE',  ( 20.94999999999999929, 5.400000000011154988, -88.09473398108696074 ) ) ;
#208325=DIRECTION ( 'NONE',  ( 0.000000000000000000, 0.000000000000000000, 1.000000000000000000 ) ) ;
#208328=ADVANCED_FACE ( 'NONE', ( #39223 ), #76525, .T. ) ;
#208340=VERTEX_POINT ( 'NONE', #199584 ) ;
#208353=DIRECTION ( 'NONE',  ( -0.000000000000000000, -0.000000000000000000, 1.000000000000000000 ) ) ;
#208354=VERTEX_POINT ( 'NONE', #212268 ) ;
#208366=CARTESIAN_POINT ( 'NONE',  ( -18.50000000000000000, -1.637172712959223952, -78.58215336547205254 ) ) ;
#208379=DIRECTION ( 'NONE',  ( 0.000000000000000000, 0.000000000000000000, -1.000000000000000000 ) ) ;
#208445=EDGE_CURVE ( 'NONE', #134186, #66864, #240804, .T. ) ;
#208459=AXIS2_PLACEMENT_3D ( 'NONE', #253901, #55671, #36170 ) ;
#208467=CARTESIAN_POINT ( 'NONE',  ( -20.85000000000000142, 1.115600667400684642E-11, -100.5000000000000426 ) ) ;
#208478=CARTESIAN_POINT ( 'NONE',  ( -20.94560253601877164, 11.75000000001115197, -93.51008351251550721 ) ) ;
#208482=CIRCLE ( 'NONE', #71102, 0.1000000000000028644 ) ;
#208511=ORIENTED_EDGE ( 'NONE', *, *, #232990, .F. ) ;
#208513=CARTESIAN_POINT ( 'NONE',  ( 18.59999999999999432, -1.162701749926853712, -75.10000000000003695 ) ) ;
#208514=VERTEX_POINT ( 'NONE', #122140 ) ;
#208523=DIRECTION ( 'NONE',  ( -0.000000000000000000, -0.000000000000000000, 1.000000000000000000 ) ) ;
#208527=ADVANCED_FACE ( 'NONE', ( #20486 ), #197513, .F. ) ;
#208542=EDGE_LOOP ( 'NONE', ( #151905, #124673, #9230, #200465 ) ) ;
#208606=CARTESIAN_POINT ( 'NONE',  ( -18.43634282235122868, -9.679787199916756180, -107.1606518854540440 ) ) ;
#208624=CARTESIAN_POINT ( 'NONE',  ( -18.50000000000000000, 7.021664781911246322, -104.3335654018973315 ) ) ;
#208636=ORIENTED_EDGE ( 'NONE', *, *, #251052, .T. ) ;
#208644=DIRECTION ( 'NONE',  ( 0.000000000000000000, -1.000000000000000000, 6.308085367188393199E-16 ) ) ;
#208665=CARTESIAN_POINT ( 'NONE',  ( 20.94999999999999929, -11.29603075032412995, -70.04789915966391334 ) ) ;
#208718=CARTESIAN_POINT ( 'NONE',  ( 19.75857864376268935, 11.65000000001115943, -91.75000000000005684 ) ) ;
#208721=EDGE_CURVE ( 'NONE', #119770, #201185, #97532, .T. ) ;
#208732=VERTEX_POINT ( 'NONE', #16864 ) ;
#208736=ADVANCED_FACE ( 'NONE', ( #192930 ), #180780, .T. ) ;
#208759=EDGE_LOOP ( 'NONE', ( #2276, #190354, #80761, #135913 ) ) ;
#208768=EDGE_CURVE ( 'NONE', #39159, #121769, #33896, .T. ) ;
#208797=LINE ( 'NONE', #8037, #249253 ) ;
#208801=CYLINDRICAL_SURFACE ( 'NONE', #170546, 0.1000000000000028644 ) ;
#208803=DIRECTION ( 'NONE',  ( 0.000000000000000000, 0.4999999999999956701, -0.8660254037844411501 ) ) ;
#208813=AXIS2_PLACEMENT_3D ( 'NONE', #72786, #92304, #53185 ) ;
#208818=TOROIDAL_SURFACE ( 'NONE', #79783, 3.899999999999999467, 0.1000000000000000056 ) ;
#208826=VERTEX_POINT ( 'NONE', #195516 ) ;
#208843=CARTESIAN_POINT ( 'NONE',  ( 20.94999999999999929, 1.115624548013267999E-11, -98.60000000000005116 ) ) ;
#208847=CARTESIAN_POINT ( 'NONE',  ( 21.05000000000000071, -0.01454569055837845459, -60.50298221356805328 ) ) ;
#208853=VERTEX_POINT ( 'NONE', #41574 ) ;
#208872=AXIS2_PLACEMENT_3D ( 'NONE', #102387, #45021, #121992 ) ;
#208886=ORIENTED_EDGE ( 'NONE', *, *, #51045, .F. ) ;
#208900=DIRECTION ( 'NONE',  ( 0.000000000000000000, 1.000000000000000000, 1.734723475976807292E-15 ) ) ;
#208908=DIRECTION ( 'NONE',  ( 0.000000000000000000, 0.1568667991644863147, 0.9876197685951252359 ) ) ;
#208924=EDGE_LOOP ( 'NONE', ( #171129, #70365, #254330, #178285 ) ) ;
#208943=CARTESIAN_POINT ( 'NONE',  ( 18.60000000000000497, 1.115600667400684642E-11, -67.00000000000004263 ) ) ;
#208977=CARTESIAN_POINT ( 'NONE',  ( -23.15000000000000213, -9.599999999988844124, -55.25000000000004974 ) ) ;
#208978=DIRECTION ( 'NONE',  ( -1.000000000000000000, -0.000000000000000000, -0.000000000000000000 ) ) ;
#208980=CYLINDRICAL_SURFACE ( 'NONE', #78842, 0.1000000000000028644 ) ;
#208991=CIRCLE ( 'NONE', #179789, 0.1000000000000000472 ) ;
#209029=DIRECTION ( 'NONE',  ( 1.000000000000000000, 0.000000000000000000, 0.000000000000000000 ) ) ;
#209049=ORIENTED_EDGE ( 'NONE', *, *, #243211, .F. ) ;
#209065=VECTOR ( 'NONE', #109627, 999.9999999999998863 ) ;
#209097=CARTESIAN_POINT ( 'NONE',  ( -23.15000000000000213, 2.000000000011154189, -80.22462192276213955 ) ) ;
#209099=SPHERICAL_SURFACE ( 'NONE', #82376, 0.1000000000000000056 ) ;
#209144=CARTESIAN_POINT ( 'NONE',  ( -21.14999999999999858, 1.115600667400684642E-11, -67.00000000000004263 ) ) ;
#209148=DIRECTION ( 'NONE',  ( -1.000000000000000000, 0.000000000000000000, 0.000000000000000000 ) ) ;
#209178=CARTESIAN_POINT ( 'NONE',  ( -21.05000000000000071, 6.299230910103438497, -66.90156249999972715 ) ) ;
#209194=ORIENTED_EDGE ( 'NONE', *, *, #108665, .T. ) ;
#209226=ORIENTED_EDGE ( 'NONE', *, *, #207716, .T. ) ;
#209259=ORIENTED_EDGE ( 'NONE', *, *, #50934, .F. ) ;
#209262=EDGE_CURVE ( 'NONE', #68386, #55997, #157367, .T. ) ;
#209274=FACE_OUTER_BOUND ( 'NONE', #170356, .T. ) ;
#209305=ORIENTED_EDGE ( 'NONE', *, *, #27877, .F. ) ;
#209319=DIRECTION ( 'NONE',  ( -1.000000000000000000, -0.000000000000000000, -0.000000000000000000 ) ) ;
#209329=CARTESIAN_POINT ( 'NONE',  ( 20.95203847575071521, 10.50106053928516303, -74.56707134862361386 ) ) ;
#209344=CARTESIAN_POINT ( 'NONE',  ( -21.05000000000000071, -1.360870587180885716, -75.07299792709100927 ) ) ;
#209354=EDGE_CURVE ( 'NONE', #3192, #95067, #238845, .T. ) ;
#209368=DIRECTION ( 'NONE',  ( 0.000000000000000000, 0.000000000000000000, 1.000000000000000000 ) ) ;
#209369=DIRECTION ( 'NONE',  ( 0.000000000000000000, 0.000000000000000000, 1.000000000000000000 ) ) ;
#209380=CARTESIAN_POINT ( 'NONE',  ( 18.49999999999999645, 1.736257131608553550, -78.56865232901755292 ) ) ;
#209423=ORIENTED_EDGE ( 'NONE', *, *, #231666, .F. ) ;
#209426=B_SPLINE_CURVE_WITH_KNOTS ( 'NONE', 3,
 ( #202334, #81084, #120271, #23734, #181508, #39445, #2831, #142354, #100631, #160674 ),
 .UNSPECIFIED., .F., .F.,
 ( 4, 2, 2, 2, 4 ),
 ( 0.000000000000000000, 0.0001660831991682438027, 0.0002491247987523657176, 0.0002906455985444088264, 0.0003321663983364519894 ),
 .UNSPECIFIED. ) ;
#209438=CARTESIAN_POINT ( 'NONE',  ( 21.08489834409762764, 10.62232389474667293, -79.35000000000005116 ) ) ;
#209443=CARTESIAN_POINT ( 'NONE',  ( 21.87500000000000355, 9.750000000011153745, -79.35000000000005116 ) ) ;
#209550=ORIENTED_EDGE ( 'NONE', *, *, #208024, .T. ) ;
#209554=AXIS2_PLACEMENT_3D ( 'NONE', #236305, #34293, #155525 ) ;
#209597=DIRECTION ( 'NONE',  ( -1.000000000000000000, 0.000000000000000000, 0.000000000000000000 ) ) ;
#209675=DIRECTION ( 'NONE',  ( 0.000000000000000000, 1.000000000000000000, 0.000000000000000000 ) ) ;
#209698=EDGE_CURVE ( 'NONE', #77369, #19542, #30947, .T. ) ;
#209708=AXIS2_PLACEMENT_3D ( 'NONE', #66575, #5274, #125260 ) ;
#209724=ORIENTED_EDGE ( 'NONE', *, *, #16576, .T. ) ;
#209759=CIRCLE ( 'NONE', #146806, 0.1000000000000016431 ) ;
#209768=DIRECTION ( 'NONE',  ( 0.000000000000000000, 1.000000000000000000, 0.000000000000000000 ) ) ;
#209791=CARTESIAN_POINT ( 'NONE',  ( -18.59999999999999787, -9.480686695267820596, -107.4411151687578894 ) ) ;
#209792=DIRECTION ( 'NONE',  ( 1.000000000000000000, 3.265361837132813093E-16, -0.000000000000000000 ) ) ;
#209847=ORIENTED_EDGE ( 'NONE', *, *, #458, .F. ) ;
#209859=ORIENTED_EDGE ( 'NONE', *, *, #9887, .F. ) ;
#209871=EDGE_CURVE ( 'NONE', #157348, #133253, #14195, .T. ) ;
#209886=DIRECTION ( 'NONE',  ( 0.000000000000000000, 0.000000000000000000, -1.000000000000000000 ) ) ;
#209892=ORIENTED_EDGE ( 'NONE', *, *, #27039, .T. ) ;
#209904=EDGE_CURVE ( 'NONE', #105777, #138550, #39137, .T. ) ;
#209916=CARTESIAN_POINT ( 'NONE',  ( 20.85000000000000142, 1.115600667400684642E-11, -108.3000000000000540 ) ) ;
#209921=ORIENTED_EDGE ( 'NONE', *, *, #47205, .F. ) ;
#209953=CARTESIAN_POINT ( 'NONE',  ( 19.97071067695831559, 11.72071067696947644, -91.67625343280374750 ) ) ;
#209960=ADVANCED_FACE ( 'NONE', ( #35214 ), #95148, .T. ) ;
#209971=VERTEX_POINT ( 'NONE', #18178 ) ;
#210015=CARTESIAN_POINT ( 'NONE',  ( -20.94999999999999929, 5.900000000011102586, -77.21909976465646253 ) ) ;
#210023=CARTESIAN_POINT ( 'NONE',  ( -18.39999999999999858, -9.499999999988849808, -74.03206939669971121 ) ) ;
#210049=ADVANCED_FACE ( 'NONE', ( #39046 ), #100251, .T. ) ;
#210086=EDGE_CURVE ( 'NONE', #83940, #13313, #19472, .T. ) ;
#210088=CARTESIAN_POINT ( 'NONE',  ( -20.85000000000000142, -1.135018845899022466, -108.2169768834323662 ) ) ;
#210090=AXIS2_PLACEMENT_3D ( 'NONE', #11092, #71079, #115312 ) ;
#210094=CARTESIAN_POINT ( 'NONE',  ( -23.15000000000000213, 11.75000000001115552, -79.25000000000004263 ) ) ;
#210123=EDGE_LOOP ( 'NONE', ( #12928, #161832, #128840, #91437 ) ) ;
#210156=DIRECTION ( 'NONE',  ( 1.000000000000000000, 0.000000000000000000, 0.000000000000000000 ) ) ;
#210158=AXIS2_PLACEMENT_3D ( 'NONE', #90480, #30539, #228738 ) ;
#210162=EDGE_LOOP ( 'NONE', ( #254533, #189084, #26041, #50136 ) ) ;
#210165=DIRECTION ( 'NONE',  ( 0.000000000000000000, 0.000000000000000000, -1.000000000000000000 ) ) ;
#210167=FACE_OUTER_BOUND ( 'NONE', #232303, .T. ) ;
#210178=VERTEX_POINT ( 'NONE', #6302 ) ;
#210182=ORIENTED_EDGE ( 'NONE', *, *, #197262, .T. ) ;
#210201=CIRCLE ( 'NONE', #214287, 0.1000000000000053069 ) ;
#210206=ORIENTED_EDGE ( 'NONE', *, *, #1964, .F. ) ;
#210207=DIRECTION ( 'NONE',  ( 0.000000000000000000, 0.000000000000000000, -1.000000000000000000 ) ) ;
#210222=CARTESIAN_POINT ( 'NONE',  ( -23.15000000000000213, 11.65000000001115588, -93.48519422934610645 ) ) ;
#210283=EDGE_LOOP ( 'NONE', ( #376, #124999, #51193, #180869 ) ) ;
#210284=CIRCLE ( 'NONE', #247868, 11.75000000000000000 ) ;
#210308=VERTEX_POINT ( 'NONE', #70170 ) ;
#210322=CARTESIAN_POINT ( 'NONE',  ( -21.14999999999999858, 6.540656951712397138, -67.00000000000004263 ) ) ;
#210340=DIRECTION ( 'NONE',  ( -0.000000000000000000, 0.1350103645451876666, 0.9908441862701600211 ) ) ;
#210342=CARTESIAN_POINT ( 'NONE',  ( 21.05000000000000071, -11.64999999998883595, -67.00000000000004263 ) ) ;
#210345=EDGE_LOOP ( 'NONE', ( #153697, #202886, #151451, #238704 ) ) ;
#210355=VECTOR ( 'NONE', #179978, 999.9999999999998863 ) ;
#210356=CARTESIAN_POINT ( 'NONE',  ( 20.94999999999999929, -11.48912529306489994, -97.40000000000004832 ) ) ;
#210373=DIRECTION ( 'NONE',  ( 0.000000000000000000, 0.000000000000000000, -1.000000000000000000 ) ) ;
#210393=AXIS2_PLACEMENT_3D ( 'NONE', #70925, #112595, #150449 ) ;
#210404=LINE ( 'NONE', #186997, #7579 ) ;
#210431=CARTESIAN_POINT ( 'NONE',  ( 20.85000000000000142, -1.362429037182151470, -108.3888812479212476 ) ) ;
#210437=ADVANCED_FACE ( 'NONE', ( #139058 ), #242042, .F. ) ;
#210482=DIRECTION ( 'NONE',  ( 1.000000000000000000, 0.000000000000000000, -0.000000000000000000 ) ) ;
#210492=EDGE_LOOP ( 'NONE', ( #123949, #70487, #45981, #10568 ) ) ;
#210507=CYLINDRICAL_SURFACE ( 'NONE', #142875, 0.09999999999999804878 ) ;
#210553=ORIENTED_EDGE ( 'NONE', *, *, #56336, .F. ) ;
#210556=DIRECTION ( 'NONE',  ( 1.000000000000000000, 0.000000000000000000, 0.000000000000000000 ) ) ;
#210593=ORIENTED_EDGE ( 'NONE', *, *, #158782, .T. ) ;
#210607=DIRECTION ( 'NONE',  ( 0.000000000000000000, 0.000000000000000000, -1.000000000000000000 ) ) ;
#210617=FACE_OUTER_BOUND ( 'NONE', #21266, .T. ) ;
#210622=DIRECTION ( 'NONE',  ( 1.000000000000000000, -0.000000000000000000, 0.000000000000000000 ) ) ;
#210644=DIRECTION ( 'NONE',  ( -1.000000000000000000, 0.000000000000000000, 0.000000000000000000 ) ) ;
#210649=CIRCLE ( 'NONE', #131542, 11.80000000000000426 ) ;
#210703=DIRECTION ( 'NONE',  ( -1.000000000000000000, -0.000000000000000000, -0.000000000000000000 ) ) ;
#210727=CIRCLE ( 'NONE', #44153, 4.000000000000003553 ) ;
#210788=CARTESIAN_POINT ( 'NONE',  ( 23.25000000000000000, -8.596261682231828516, -91.04987248284976431 ) ) ;
#210807=CARTESIAN_POINT ( 'NONE',  ( -21.29999999999995808, 1.115600667400684642E-11, -67.00000000000004263 ) ) ;
#210821=VERTEX_POINT ( 'NONE', #143914 ) ;
#210822=EDGE_CURVE ( 'NONE', #142573, #140921, #163490, .T. ) ;
#210828=CARTESIAN_POINT ( 'NONE',  ( -20.00857864376270001, 9.250000000011157297, -79.35000000000005116 ) ) ;
#210836=EDGE_CURVE ( 'NONE', #237818, #113968, #64772, .T. ) ;
#210857=DIRECTION ( 'NONE',  ( 0.000000000000000000, 0.000000000000000000, 1.000000000000000000 ) ) ;
#210882=CARTESIAN_POINT ( 'NONE',  ( 19.99999999999998934, 11.75000000001115552, -88.35000000000003695 ) ) ;
#210932=AXIS2_PLACEMENT_3D ( 'NONE', #178069, #97176, #138877 ) ;
#210934=DIRECTION ( 'NONE',  ( 1.000000000000000000, 0.000000000000000000, 0.000000000000000000 ) ) ;
#210992=CARTESIAN_POINT ( 'NONE',  ( 18.49999999999999289, 10.32573593129922607, -91.85000000000003695 ) ) ;
#211002=AXIS2_PLACEMENT_3D ( 'NONE', #221555, #105451, #147179 ) ;
#211011=DIRECTION ( 'NONE',  ( -1.000000000000000000, -2.952720810173289112E-16, 0.000000000000000000 ) ) ;
#211031=DIRECTION ( 'NONE',  ( 0.000000000000000000, 0.000000000000000000, 1.000000000000000000 ) ) ;
#211036=VERTEX_POINT ( 'NONE', #116368 ) ;
#211071=LINE ( 'NONE', #225471, #214057 ) ;
#211105=CARTESIAN_POINT ( 'NONE',  ( 20.94999999999999929, 5.000000000011153745, -88.09473398108696074 ) ) ;
#211108=DIRECTION ( 'NONE',  ( 1.000000000000000000, 0.000000000000000000, -0.000000000000000000 ) ) ;
#211124=CARTESIAN_POINT ( 'NONE',  ( 18.43579564894474387, -9.519327535281719932, -73.97297664385990856 ) ) ;
#211133=CARTESIAN_POINT ( 'NONE',  ( 21.05000000000000071, 1.115600667400684642E-11, -67.00000000000004263 ) ) ;
#211155=ORIENTED_EDGE ( 'NONE', *, *, #104544, .T. ) ;
#211192=DIRECTION ( 'NONE',  ( 1.000000000000000000, 0.000000000000000000, 0.000000000000000000 ) ) ;
#211193=CARTESIAN_POINT ( 'NONE',  ( 20.94999999999999929, 5.000000000011153745, -88.09473398108696074 ) ) ;
#211208=ORIENTED_EDGE ( 'NONE', *, *, #94182, .T. ) ;
#211259=DIRECTION ( 'NONE',  ( -1.000000000000000000, -0.000000000000000000, -0.000000000000000000 ) ) ;
#211261=AXIS2_PLACEMENT_3D ( 'NONE', #133690, #72454, #249791 ) ;
#211280=FACE_OUTER_BOUND ( 'NONE', #32399, .T. ) ;
#211288=DIRECTION ( 'NONE',  ( 0.000000000000000000, 0.000000000000000000, -1.000000000000000000 ) ) ;
#211307=CARTESIAN_POINT ( 'NONE',  ( 21.05000000000000071, -0.09999999998884338825, -55.35042919245524473 ) ) ;
#211311=CONICAL_SURFACE ( 'NONE', #19788, 6.250000000000005329, 0.7853981633974431720 ) ;
#211353=EDGE_LOOP ( 'NONE', ( #21975, #4670, #150261, #63965, #37739 ) ) ;
#211371=DIRECTION ( 'NONE',  ( 0.000000000000000000, 0.8660254037844383745, -0.5000000000000003331 ) ) ;
#211387=DIRECTION ( 'NONE',  ( 0.000000000000000000, 0.000000000000000000, 1.000000000000000000 ) ) ;
#211388=ORIENTED_EDGE ( 'NONE', *, *, #112335, .F. ) ;
#211396=ORIENTED_EDGE ( 'NONE', *, *, #151209, .T. ) ;
#211418=LINE ( 'NONE', #47176, #194318 ) ;
#211423=DIRECTION ( 'NONE',  ( 1.000000000000000000, -0.000000000000000000, 0.000000000000000000 ) ) ;
#211426=VERTEX_POINT ( 'NONE', #62178 ) ;
#211428=AXIS2_PLACEMENT_3D ( 'NONE', #168306, #247790, #69186 ) ;
#211435=CARTESIAN_POINT ( 'NONE',  ( -18.50000000000000000, -9.399999999988850163, -107.3820418481727046 ) ) ;
#211437=VECTOR ( 'NONE', #243058, 1000.000000000000000 ) ;
#211445=AXIS2_PLACEMENT_3D ( 'NONE', #148189, #150764, #51624 ) ;
#211454=ORIENTED_EDGE ( 'NONE', *, *, #117572, .F. ) ;
#211465=AXIS2_PLACEMENT_3D ( 'NONE', #132132, #219358, #115137 ) ;
#211486=ADVANCED_FACE ( 'NONE', ( #257743 ), #137836, .T. ) ;
#211515=ORIENTED_EDGE ( 'NONE', *, *, #73638, .F. ) ;
#211526=DIRECTION ( 'NONE',  ( 0.000000000000000000, 0.000000000000000000, -1.000000000000000000 ) ) ;
#211645=VERTEX_POINT ( 'NONE', #247214 ) ;
#211687=EDGE_CURVE ( 'NONE', #187394, #110538, #160846, .T. ) ;
#211689=FACE_OUTER_BOUND ( 'NONE', #78161, .T. ) ;
#211741=CARTESIAN_POINT ( 'NONE',  ( 18.50000000000000000, -9.399999999988843058, -74.29725975966333351 ) ) ;
#211745=DIRECTION ( 'NONE',  ( 0.000000000000000000, -1.000000000000000000, -2.891205793294679805E-16 ) ) ;
#211798=ADVANCED_FACE ( 'NONE', ( #56687 ), #215779, .F. ) ;
#211800=CARTESIAN_POINT ( 'NONE',  ( 18.50211644919734866, 10.30207779525984613, -105.9895520716782897 ) ) ;
#211811=DIRECTION ( 'NONE',  ( 2.952720810173289112E-16, -1.000000000000000000, 0.000000000000000000 ) ) ;
#211819=ORIENTED_EDGE ( 'NONE', *, *, #251487, .F. ) ;
#211854=ORIENTED_EDGE ( 'NONE', *, *, #140449, .T. ) ;
#211866=VERTEX_POINT ( 'NONE', #59244 ) ;
#211963=EDGE_LOOP ( 'NONE', ( #83310, #238810, #37977, #159252 ) ) ;
#211995=AXIS2_PLACEMENT_3D ( 'NONE', #111793, #73975, #51788 ) ;
#212046=ORIENTED_EDGE ( 'NONE', *, *, #139948, .T. ) ;
#212050=CARTESIAN_POINT ( 'NONE',  ( 20.95263205890712399, 8.895740107905197647, -75.48950840694165265 ) ) ;
#212061=AXIS2_PLACEMENT_3D ( 'NONE', #128996, #170735, #252768 ) ;
#212077=DIRECTION ( 'NONE',  ( 1.000000000000000000, 0.000000000000000000, 0.000000000000000000 ) ) ;
#212089=DIRECTION ( 'NONE',  ( 2.915501640297155269E-16, -1.000000000000000000, 0.000000000000000000 ) ) ;
#212107=ORIENTED_EDGE ( 'NONE', *, *, #38810, .T. ) ;
#212119=FACE_OUTER_BOUND ( 'NONE', #67240, .T. ) ;
#212126=ORIENTED_EDGE ( 'NONE', *, *, #19230, .T. ) ;
#212131=CARTESIAN_POINT ( 'NONE',  ( -21.14999999999999858, 11.65000000001115588, -67.10000000000005116 ) ) ;
#212186=EDGE_LOOP ( 'NONE', ( #217804, #145762, #208886, #198276 ) ) ;
#212198=FACE_OUTER_BOUND ( 'NONE', #36385, .T. ) ;
#212219=AXIS2_PLACEMENT_3D ( 'NONE', #60909, #84275, #161323 ) ;
#212227=LINE ( 'NONE', #188787, #213345 ) ;
#212238=CARTESIAN_POINT ( 'NONE',  ( -20.54999999999999716, 2.000000000011154189, -87.27537807723794572 ) ) ;
#212241=CARTESIAN_POINT ( 'NONE',  ( 20.95083306685154056, 8.916842641901356004, -75.47732485325839491 ) ) ;
#212268=CARTESIAN_POINT ( 'NONE',  ( -22.39999999999999858, 7.790779598384560245, -67.00000000000004263 ) ) ;
#212270=DIRECTION ( 'NONE',  ( 0.000000000000000000, 0.9908441862701596881, -0.1350103645451904977 ) ) ;
#212312=FACE_OUTER_BOUND ( 'NONE', #11066, .T. ) ;
#212328=CARTESIAN_POINT ( 'NONE',  ( 21.04999999999999716, 10.62872031401550466, -79.15000000000004832 ) ) ;
#212359=ORIENTED_EDGE ( 'NONE', *, *, #137671, .T. ) ;
#212371=VECTOR ( 'NONE', #108300, 1000.000000000000000 ) ;
#212377=ORIENTED_EDGE ( 'NONE', *, *, #60726, .F. ) ;
#212387=EDGE_CURVE ( 'NONE', #156376, #256436, #86322, .T. ) ;
#212404=CARTESIAN_POINT ( 'NONE',  ( 23.24999999999999289, 11.65000000001116298, -79.15000000000004832 ) ) ;
#212447=CIRCLE ( 'NONE', #29309, 12.97499999999999964 ) ;
#212478=ADVANCED_FACE ( 'NONE', ( #42697 ), #40165, .F. ) ;
#212484=ORIENTED_EDGE ( 'NONE', *, *, #171350, .F. ) ;
#212496=ORIENTED_EDGE ( 'NONE', *, *, #217389, .T. ) ;
#212587=DIRECTION ( 'NONE',  ( -0.000000000000000000, -0.000000000000000000, -1.000000000000000000 ) ) ;
#212596=ORIENTED_EDGE ( 'NONE', *, *, #162483, .F. ) ;
#212597=CARTESIAN_POINT ( 'NONE',  ( 20.94999999999999929, -8.663551401857999323, -90.97589888193273566 ) ) ;
#212620=FACE_OUTER_BOUND ( 'NONE', #195895, .T. ) ;
#212631=CIRCLE ( 'NONE', #125145, 0.2000000000000057288 ) ;
#212632=ORIENTED_EDGE ( 'NONE', *, *, #116633, .F. ) ;
#212654=CARTESIAN_POINT ( 'NONE',  ( -22.48660254037843487, 11.65000000001115588, -66.95000000000005969 ) ) ;
#212666=EDGE_LOOP ( 'NONE', ( #41826, #24289, #180616, #215301 ) ) ;
#212679=VECTOR ( 'NONE', #2463, 1000.000000000000000 ) ;
#212683=CARTESIAN_POINT ( 'NONE',  ( 22.50000000000000000, 1.115600667400684642E-11, -67.00000000000004263 ) ) ;
#212685=ORIENTED_EDGE ( 'NONE', *, *, #162636, .T. ) ;
#212699=CYLINDRICAL_SURFACE ( 'NONE', #184731, 0.09999999999999781286 ) ;
#212730=ORIENTED_EDGE ( 'NONE', *, *, #137902, .F. ) ;
#212757=ORIENTED_EDGE ( 'NONE', *, *, #49151, .T. ) ;
#212793=CARTESIAN_POINT ( 'NONE',  ( 18.59999999999999076, 10.20857864377385127, -91.75000000000005684 ) ) ;
#212794=B_SPLINE_CURVE_WITH_KNOTS ( 'NONE', 3,
 ( #16425, #157227, #236716, #174237, #41128, #135041, #115494, #38539, #154661, #118067, #238005, #214591, #75124, #200183, #197597, #235433, #138873, #253714, #35982 ),
 .UNSPECIFIED., .F., .F.,
 ( 4, 3, 3, 3, 3, 3, 4 ),
 ( 0.000000000000000000, 2.646747978908405840E-05, 5.271166642128090210E-05, 9.008788829884082239E-05, 0.0001426648776560918196, 0.0001897378458659811703, 0.0001917382627806267395 ),
 .UNSPECIFIED. ) ;
#212803=TOROIDAL_SURFACE ( 'NONE', #100343, 0.4000000000000005773, 0.1000000000000000056 ) ;
#212810=ORIENTED_EDGE ( 'NONE', *, *, #210822, .T. ) ;
#212811=DIRECTION ( 'NONE',  ( 1.000000000000000000, -0.000000000000000000, -0.000000000000000000 ) ) ;
#212821=CARTESIAN_POINT ( 'NONE',  ( 18.52130828395272033, -9.481395502614633486, -74.02450672388368957 ) ) ;
#212868=ORIENTED_EDGE ( 'NONE', *, *, #22766, .F. ) ;
#212901=FACE_OUTER_BOUND ( 'NONE', #170813, .T. ) ;
#212925=DIRECTION ( 'NONE',  ( 0.000000000000000000, 0.000000000000000000, -1.000000000000000000 ) ) ;
#212929=ORIENTED_EDGE ( 'NONE', *, *, #118732, .F. ) ;
#212939=VERTEX_POINT ( 'NONE', #70975 ) ;
#212957=CARTESIAN_POINT ( 'NONE',  ( -21.14999999999999858, 11.75000000001115552, -67.00000000000004263 ) ) ;
#212958=ORIENTED_EDGE ( 'NONE', *, *, #216856, .F. ) ;
#212993=CARTESIAN_POINT ( 'NONE',  ( 21.05000000000000071, 8.876614585098254295, -75.38508047884472774 ) ) ;
#213010=ORIENTED_EDGE ( 'NONE', *, *, #204717, .T. ) ;
#213023=CARTESIAN_POINT ( 'NONE',  ( 22.47071067811865319, 1.115600667400684642E-11, -67.00000000000004263 ) ) ;
#213038=FACE_OUTER_BOUND ( 'NONE', #70477, .T. ) ;
#213055=CARTESIAN_POINT ( 'NONE',  ( -18.48550754432021748, -9.463399778548760466, -74.04878975241544481 ) ) ;
#213067=DIRECTION ( 'NONE',  ( 1.000000000000000000, 0.000000000000000000, 0.000000000000000000 ) ) ;
#213118=ADVANCED_FACE ( 'NONE', ( #219418 ), #78627, .F. ) ;
#213122=ORIENTED_EDGE ( 'NONE', *, *, #20603, .T. ) ;
#213141=DIRECTION ( 'NONE',  ( 0.000000000000000000, 0.4930308989875324399, 0.8700118002898268310 ) ) ;
#213160=EDGE_LOOP ( 'NONE', ( #38196, #247203, #61049, #207228 ) ) ;
#213164=VECTOR ( 'NONE', #63699, 1000.000000000000000 ) ;
#213165=ORIENTED_EDGE ( 'NONE', *, *, #168203, .T. ) ;
#213190=CYLINDRICAL_SURFACE ( 'NONE', #144838, 0.09999999999999939493 ) ;
#213191=ORIENTED_EDGE ( 'NONE', *, *, #47205, .T. ) ;
#213306=AXIS2_PLACEMENT_3D ( 'NONE', #28488, #145809, #89682 ) ;
#213345=VECTOR ( 'NONE', #92246, 1000.000000000000114 ) ;
#213357=DIRECTION ( 'NONE',  ( 0.000000000000000000, 0.000000000000000000, 1.000000000000000000 ) ) ;
#213360=EDGE_CURVE ( 'NONE', #75395, #8169, #113017, .T. ) ;
#213379=EDGE_LOOP ( 'NONE', ( #94638, #110773, #56712, #115814 ) ) ;
#213409=DIRECTION ( 'NONE',  ( 0.000000000000000000, 0.000000000000000000, -1.000000000000000000 ) ) ;
#213417=ORIENTED_EDGE ( 'NONE', *, *, #135082, .F. ) ;
#213446=AXIS2_PLACEMENT_3D ( 'NONE', #41663, #218984, #76906 ) ;
#213454=FACE_OUTER_BOUND ( 'NONE', #168549, .T. ) ;
#213461=AXIS2_PLACEMENT_3D ( 'NONE', #181807, #100929, #121845 ) ;
#213466=ORIENTED_EDGE ( 'NONE', *, *, #222787, .T. ) ;
#213494=CARTESIAN_POINT ( 'NONE',  ( -21.45000000000000284, 7.708578643773852157, -88.25000000000005684 ) ) ;
#213505=DIRECTION ( 'NONE',  ( -1.000000000000000000, 0.000000000000000000, 0.000000000000000000 ) ) ;
#213531=CARTESIAN_POINT ( 'NONE',  ( 20.85000000000000142, -0.3238857010591806307, -100.4575895893140256 ) ) ;
#213549=AXIS2_PLACEMENT_3D ( 'NONE', #28088, #29383, #24224 ) ;
#213556=ORIENTED_EDGE ( 'NONE', *, *, #99441, .F. ) ;
#213566=CARTESIAN_POINT ( 'NONE',  ( -18.59999999999999787, 9.350000000011156942, -79.35000000000005116 ) ) ;
#213624=EDGE_CURVE ( 'NONE', #77390, #239872, #243830, .T. ) ;
#213628=CARTESIAN_POINT ( 'NONE',  ( -18.59999999999999787, 1.750000000011155743, -78.66951155790169992 ) ) ;
#213637=DIRECTION ( 'NONE',  ( 0.000000000000000000, 0.000000000000000000, -1.000000000000000000 ) ) ;
#213655=DIRECTION ( 'NONE',  ( -0.7070776581709311559, 0.000000000000000000, 0.7071359030027479786 ) ) ;
#213684=CARTESIAN_POINT ( 'NONE',  ( 18.58703555225022797, -9.406336740777600625, -74.12494464124685578 ) ) ;
#213695=EDGE_CURVE ( 'NONE', #153546, #112516, #228393, .T. ) ;
#213703=ORIENTED_EDGE ( 'NONE', *, *, #242992, .F. ) ;
#213732=ORIENTED_EDGE ( 'NONE', *, *, #148267, .F. ) ;
#213740=CARTESIAN_POINT ( 'NONE',  ( -18.59999999999999787, -1.736257131586239844, -78.56865232901753870 ) ) ;
#213751=CARTESIAN_POINT ( 'NONE',  ( 18.41815437325349691, -9.498709853130263170, -107.1039458388021615 ) ) ;
#213758=CARTESIAN_POINT ( 'NONE',  ( 18.46858270002952906, -9.474202674699409243, -74.10202193470389886 ) ) ;
#213804=ORIENTED_EDGE ( 'NONE', *, *, #46310, .F. ) ;
#213874=LINE ( 'NONE', #19540, #7678 ) ;
#213881=CYLINDRICAL_SURFACE ( 'NONE', #227725, 0.09999999999999939493 ) ;
#213890=LINE ( 'NONE', #92652, #80644 ) ;
#213894=SPHERICAL_SURFACE ( 'NONE', #193710, 0.1000000000000000056 ) ;
#213931=EDGE_LOOP ( 'NONE', ( #256721, #52844, #48941, #112645 ) ) ;
#213946=DIRECTION ( 'NONE',  ( -0.000000000000000000, -0.000000000000000000, 1.000000000000000000 ) ) ;
#213947=DIRECTION ( 'NONE',  ( 1.000000000000000000, 0.000000000000000000, 0.000000000000000000 ) ) ;
#213963=ORIENTED_EDGE ( 'NONE', *, *, #91497, .F. ) ;
#213966=EDGE_CURVE ( 'NONE', #156656, #116760, #86492, .T. ) ;
#213972=AXIS2_PLACEMENT_3D ( 'NONE', #71228, #154629, #152052 ) ;
#213984=EDGE_LOOP ( 'NONE', ( #106498, #229162, #68148, #75957 ) ) ;
#214046=EDGE_LOOP ( 'NONE', ( #67806, #227899, #62068, #15478 ) ) ;
#214056=VERTEX_POINT ( 'NONE', #87946 ) ;
#214057=VECTOR ( 'NONE', #29892, 1000.000000000000000 ) ;
#214092=CARTESIAN_POINT ( 'NONE',  ( -21.05000000000000071, 14.05000000001115623, -72.51369507076104526 ) ) ;
#214104=AXIS2_PLACEMENT_3D ( 'NONE', #126661, #164521, #107090 ) ;
#214162=LINE ( 'NONE', #135881, #173658 ) ;
#214198=CARTESIAN_POINT ( 'NONE',  ( -20.94999999999999929, 1.162701749949165642, -75.10000000000003695 ) ) ;
#214205=AXIS2_PLACEMENT_3D ( 'NONE', #117838, #5252, #200917 ) ;
#214238=ORIENTED_EDGE ( 'NONE', *, *, #169537, .F. ) ;
#214244=DIRECTION ( 'NONE',  ( -1.000000000000000000, -2.952720810173289112E-16, 0.000000000000000000 ) ) ;
#214256=DIRECTION ( 'NONE',  ( -1.000000000000000000, 0.000000000000000000, 0.000000000000000000 ) ) ;
#214287=AXIS2_PLACEMENT_3D ( 'NONE', #161657, #102916, #182498 ) ;
#214298=EDGE_CURVE ( 'NONE', #229766, #116664, #239046, .T. ) ;
#214306=CIRCLE ( 'NONE', #201815, 0.1000000000000002692 ) ;
#214333=VECTOR ( 'NONE', #107838, 1000.000000000000000 ) ;
#214342=AXIS2_PLACEMENT_3D ( 'NONE', #166874, #215879, #7773 ) ;
#214384=CARTESIAN_POINT ( 'NONE',  ( -20.64999999999999858, 1.115625160336667635E-11, -102.5000000000000426 ) ) ;
#214392=CARTESIAN_POINT ( 'NONE',  ( -20.94999999999999929, 1.162701749949165642, -75.10000000000003695 ) ) ;
#214396=DIRECTION ( 'NONE',  ( 0.000000000000000000, -1.000000000000000000, 0.000000000000000000 ) ) ;
#214401=VERTEX_POINT ( 'NONE', #182941 ) ;
#214457=DIRECTION ( 'NONE',  ( -1.000000000000000000, 0.000000000000000000, 0.000000000000000000 ) ) ;
#214466=EDGE_CURVE ( 'NONE', #81812, #241878, #107364, .T. ) ;
#214501=LINE ( 'NONE', #176689, #238140 ) ;
#214559=DIRECTION ( 'NONE',  ( 1.000000000000000000, 0.000000000000000000, 0.000000000000000000 ) ) ;
#214583=ORIENTED_EDGE ( 'NONE', *, *, #239759, .T. ) ;
#214591=CARTESIAN_POINT ( 'NONE',  ( -18.51024323315077424, 10.31104185824062647, -106.0204516983106373 ) ) ;
#214597=EDGE_CURVE ( 'NONE', #139104, #208826, #107543, .T. ) ;
#214611=AXIS2_PLACEMENT_3D ( 'NONE', #60079, #155378, #177514 ) ;
#214622=DIRECTION ( 'NONE',  ( 1.000000000000000000, 0.000000000000000000, 0.000000000000000000 ) ) ;
#214646=CARTESIAN_POINT ( 'NONE',  ( -23.15000000000000213, 11.60000000001115517, -93.57179676972454274 ) ) ;
#214695=ORIENTED_EDGE ( 'NONE', *, *, #197351, .T. ) ;
#214700=VERTEX_POINT ( 'NONE', #221714 ) ;
#214707=EDGE_LOOP ( 'NONE', ( #245142, #248666, #65184, #142658 ) ) ;
#214743=VERTEX_POINT ( 'NONE', #219158 ) ;
#214744=VERTEX_POINT ( 'NONE', #140933 ) ;
#214765=DIRECTION ( 'NONE',  ( -2.827886303505248766E-16, 0.8660254037844411501, 0.4999999999999956146 ) ) ;
#214782=CARTESIAN_POINT ( 'NONE',  ( 20.95512820512820440, 8.876151316299271343, -75.55862899514100661 ) ) ;
#214830=AXIS2_PLACEMENT_3D ( 'NONE', #101964, #220668, #202384 ) ;
#214832=CARTESIAN_POINT ( 'NONE',  ( 20.94999999999999574, 10.42338541492406279, -74.49205192387015018 ) ) ;
#214833=TOROIDAL_SURFACE ( 'NONE', #69113, 0.2000000000000000111, 0.1000000000000000056 ) ;
#214865=CARTESIAN_POINT ( 'NONE',  ( 21.12400247839502754, 10.72148804404156586, -79.25000000000005684 ) ) ;
#214867=EDGE_CURVE ( 'NONE', #124485, #145626, #249219, .T. ) ;
#214870=ORIENTED_EDGE ( 'NONE', *, *, #51727, .T. ) ;
#214889=ORIENTED_EDGE ( 'NONE', *, *, #115989, .T. ) ;
#214941=CARTESIAN_POINT ( 'NONE',  ( -18.59999999999999787, 1.162701749949165642, -75.10000000000003695 ) ) ;
#214946=AXIS2_PLACEMENT_3D ( 'NONE', #21093, #1487, #45758 ) ;
#214951=CARTESIAN_POINT ( 'NONE',  ( -18.50000000000000000, -1.835859311432484375, -112.0044391687985694 ) ) ;
#214955=VECTOR ( 'NONE', #210703, 1000.000000000000000 ) ;
#214970=EDGE_LOOP ( 'NONE', ( #237671, #167637, #159406, #257146 ) ) ;
#215001=CARTESIAN_POINT ( 'NONE',  ( -20.54999999999999716, -8.999999999988846255, -76.39396912265249284 ) ) ;
#215063=SHAPE_REPRESENTATION ( 'Injection Molded Chain Links 3', ( #2425 ), #94000 ) ;
#215104=EDGE_CURVE ( 'NONE', #56430, #68386, #98884, .T. ) ;
#215119=CARTESIAN_POINT ( 'NONE',  ( 21.05000000000000071, 1.115600667400684642E-11, -67.00000000000004263 ) ) ;
#215204=ORIENTED_EDGE ( 'NONE', *, *, #91905, .F. ) ;
#215291=CARTESIAN_POINT ( 'NONE',  ( -23.15000000000000213, -4.831324760611774849, -83.96969694219879443 ) ) ;
#215301=ORIENTED_EDGE ( 'NONE', *, *, #35354, .F. ) ;
#215311=AXIS2_PLACEMENT_3D ( 'NONE', #214198, #74724, #52535 ) ;
#215382=ADVANCED_FACE ( 'NONE', ( #135149 ), #75287, .F. ) ;
#215423=EDGE_LOOP ( 'NONE', ( #166692, #157423, #99600, #128330 ) ) ;
#215448=DIRECTION ( 'NONE',  ( -3.469446951953635015E-14, 1.000000000000000000, 0.000000000000000000 ) ) ;
#215464=EDGE_CURVE ( 'NONE', #183644, #102952, #29509, .T. ) ;
#215467=DIRECTION ( 'NONE',  ( -1.000000000000000000, -0.000000000000000000, -0.000000000000000000 ) ) ;
#215476=ORIENTED_EDGE ( 'NONE', *, *, #222787, .F. ) ;
#215522=VERTEX_POINT ( 'NONE', #136419 ) ;
#215525=DIRECTION ( 'NONE',  ( 0.000000000000000000, 0.000000000000000000, -1.000000000000000000 ) ) ;
#215583=AXIS2_PLACEMENT_3D ( 'NONE', #222178, #183097, #8319 ) ;
#215586=AXIS2_PLACEMENT_3D ( 'NONE', #201238, #180408, #196122 ) ;
#215615=CARTESIAN_POINT ( 'NONE',  ( -23.25000000000000000, -11.74999999998884448, -70.10000000000005116 ) ) ;
#215635=ADVANCED_FACE ( 'NONE', ( #206382 ), #148992, .F. ) ;
#215646=AXIS2_PLACEMENT_3D ( 'NONE', #180827, #2158, #161269 ) ;
#215663=AXIS2_PLACEMENT_3D ( 'NONE', #151234, #211192, #153840 ) ;
#215671=ORIENTED_EDGE ( 'NONE', *, *, #97986, .T. ) ;
#215675=ORIENTED_EDGE ( 'NONE', *, *, #157343, .T. ) ;
#215683=LINE ( 'NONE', #39668, #93734 ) ;
#215702=EDGE_CURVE ( 'NONE', #204053, #241599, #117145, .T. ) ;
#215711=LINE ( 'NONE', #236562, #40376 ) ;
#215716=EDGE_CURVE ( 'NONE', #38637, #70992, #25389, .T. ) ;
#215726=TOROIDAL_SURFACE ( 'NONE', #78364, 4.099999999999999645, 0.1000000000000000056 ) ;
#215755=CARTESIAN_POINT ( 'NONE',  ( 23.14999999999999503, 11.65000000001116298, -79.25000000000004263 ) ) ;
#215763=AXIS2_PLACEMENT_3D ( 'NONE', #118969, #156831, #177679 ) ;
#215768=CARTESIAN_POINT ( 'NONE',  ( 20.94999999999999574, -11.74999999998883560, -69.90000000000004832 ) ) ;
#215777=ORIENTED_EDGE ( 'NONE', *, *, #22766, .T. ) ;
#215779=CYLINDRICAL_SURFACE ( 'NONE', #156764, 0.5000000000000004441 ) ;
#215857=CARTESIAN_POINT ( 'NONE',  ( 21.05000000000000071, 5.850000000011156942, -90.36750277572213008 ) ) ;
#215861=EDGE_LOOP ( 'NONE', ( #38270, #249914, #119916, #93468 ) ) ;
#215879=DIRECTION ( 'NONE',  ( -0.000000000000000000, -0.9887567792719339499, -0.1495327102803676589 ) ) ;
#215912=LINE ( 'NONE', #196364, #201834 ) ;
#215914=CARTESIAN_POINT ( 'NONE',  ( -21.08198257630413508, 0.07264332379574613141, -60.66340326598497512 ) ) ;
#215947=ORIENTED_EDGE ( 'NONE', *, *, #73638, .T. ) ;
#215950=DIRECTION ( 'NONE',  ( -1.000000000000000000, 0.000000000000000000, 0.000000000000000000 ) ) ;
#215991=EDGE_CURVE ( 'NONE', #19542, #158987, #21307, .T. ) ;
#216003=CARTESIAN_POINT ( 'NONE',  ( 19.94784844284971115, 11.71308993304012525, -91.70219871729848649 ) ) ;
#216030=VECTOR ( 'NONE', #101320, 1000.000000000000000 ) ;
#216061=FACE_OUTER_BOUND ( 'NONE', #127956, .T. ) ;
#216086=DIRECTION ( 'NONE',  ( 2.952720810173289112E-16, -1.000000000000000000, -0.000000000000000000 ) ) ;
#216097=DIRECTION ( 'NONE',  ( 1.000000000000000000, -0.000000000000000000, -0.000000000000000000 ) ) ;
#216117=CARTESIAN_POINT ( 'NONE',  ( -23.15000000000000213, -9.599999999988847676, -76.89396912265249284 ) ) ;
#216138=DIRECTION ( 'NONE',  ( -0.000000000000000000, -2.891205793294679805E-16, 1.000000000000000000 ) ) ;
#216145=LINE ( 'NONE', #179616, #81332 ) ;
#216147=EDGE_CURVE ( 'NONE', #116664, #29779, #89562, .T. ) ;
#216193=AXIS2_PLACEMENT_3D ( 'NONE', #249701, #224973, #71081 ) ;
#216214=AXIS2_PLACEMENT_3D ( 'NONE', #12571, #152082, #133769 ) ;
#216232=EDGE_CURVE ( 'NONE', #68295, #3192, #193820, .T. ) ;
#216253=ORIENTED_EDGE ( 'NONE', *, *, #24055, .T. ) ;
#216256=CARTESIAN_POINT ( 'NONE',  ( 21.05000000000000071, -9.499999999988844479, -90.60603087734760663 ) ) ;
#216261=DIRECTION ( 'NONE',  ( 1.000000000000000000, 0.000000000000000000, 0.000000000000000000 ) ) ;
#216263=CARTESIAN_POINT ( 'NONE',  ( 20.94999999999999929, -11.39257802169451317, -97.42605042016811012 ) ) ;
#216264=EDGE_LOOP ( 'NONE', ( #50013, #226748, #161340, #193259, #79342, #185887, #66278, #256454, #21884, #146372, #228688, #19694 ) ) ;
#216266=EDGE_CURVE ( 'NONE', #196163, #219149, #63608, .T. ) ;
#216279=LINE ( 'NONE', #215001, #192977 ) ;
#216281=DIRECTION ( 'NONE',  ( 0.000000000000000000, 0.9908441862701596881, -0.1350103645451904977 ) ) ;
#216284=ORIENTED_EDGE ( 'NONE', *, *, #196761, .F. ) ;
#216296=ADVANCED_FACE ( 'NONE', ( #140231 ), #198934, .F. ) ;
#216299=DIRECTION ( 'NONE',  ( 0.000000000000000000, 1.144917494144691673E-13, -1.000000000000000000 ) ) ;
#216311=ADVANCED_FACE ( 'NONE', ( #239358 ), #20327, .T. ) ;
#216313=DIRECTION ( 'NONE',  ( 1.000000000000000000, 0.000000000000000000, 0.000000000000000000 ) ) ;
#216314=DIRECTION ( 'NONE',  ( 0.000000000000000000, 0.000000000000000000, -1.000000000000000000 ) ) ;
#216315=CARTESIAN_POINT ( 'NONE',  ( -18.59999999999999787, -1.164121893230052995, -108.4148480855716485 ) ) ;
#216346=FACE_OUTER_BOUND ( 'NONE', #100067, .T. ) ;
#216363=EDGE_CURVE ( 'NONE', #61134, #231898, #126136, .T. ) ;
#216413=EDGE_CURVE ( 'NONE', #231071, #73311, #180327, .T. ) ;
#216432=CARTESIAN_POINT ( 'NONE',  ( 23.14999999999998437, 1.115600667400684642E-11, -67.00000000000004263 ) ) ;
#216440=CARTESIAN_POINT ( 'NONE',  ( -23.25000000000000000, 4.250000000011156409, -79.15000000000004832 ) ) ;
#216448=LINE ( 'NONE', #198174, #154640 ) ;
#216471=EDGE_CURVE ( 'NONE', #190222, #242599, #111408, .T. ) ;
#216513=ADVANCED_FACE ( 'NONE', ( #249643 ), #210507, .T. ) ;
#216534=VECTOR ( 'NONE', #241678, 1000.000000000000000 ) ;
#216572=DIRECTION ( 'NONE',  ( 0.000000000000000000, 0.000000000000000000, -1.000000000000000000 ) ) ;
#216615=VECTOR ( 'NONE', #247277, 1000.000000000000000 ) ;
#216723=CARTESIAN_POINT ( 'NONE',  ( -21.14999999999999858, 6.257814610487270279, -66.90220970869124528 ) ) ;
#216780=ORIENTED_EDGE ( 'NONE', *, *, #216266, .T. ) ;
#216808=TOROIDAL_SURFACE ( 'NONE', #208459, 0.9750000000000019762, 0.1000000000000000056 ) ;
#216814=ORIENTED_EDGE ( 'NONE', *, *, #78524, .F. ) ;
#216823=ORIENTED_EDGE ( 'NONE', *, *, #39771, .T. ) ;
#216829=CIRCLE ( 'NONE', #254233, 0.09999999999999439892 ) ;
#216840=CARTESIAN_POINT ( 'NONE',  ( -20.64999999999999858, 7.150000000011155876, -88.15000000000004832 ) ) ;
#216843=EDGE_LOOP ( 'NONE', ( #62376, #160663, #111364, #222968 ) ) ;
#216855=ORIENTED_EDGE ( 'NONE', *, *, #60325, .F. ) ;
#216856=EDGE_CURVE ( 'NONE', #200601, #229766, #55562, .T. ) ;
#216875=ORIENTED_EDGE ( 'NONE', *, *, #154561, .F. ) ;
#216911=ORIENTED_EDGE ( 'NONE', *, *, #195020, .T. ) ;
#217021=FACE_OUTER_BOUND ( 'NONE', #190158, .T. ) ;
#217024=DIRECTION ( 'NONE',  ( -1.000000000000000000, 0.000000000000000000, 0.000000000000000000 ) ) ;
#217032=CARTESIAN_POINT ( 'NONE',  ( 21.14999999999999858, 6.550000000011156231, -79.15000000000004832 ) ) ;
#217048=DIRECTION ( 'NONE',  ( 1.000000000000000000, -7.304098846218133681E-16, 4.217023435051677994E-16 ) ) ;
#217054=CARTESIAN_POINT ( 'NONE',  ( 18.59999999999999432, -1.736257131586239844, -78.56865232901753870 ) ) ;
#217075=CARTESIAN_POINT ( 'NONE',  ( -23.15000000000000213, 1.115600667400684642E-11, -67.00000000000004263 ) ) ;
#217093=DIRECTION ( 'NONE',  ( -6.938893903907224433E-15, 1.000000000000000000, 0.000000000000000000 ) ) ;
#217095=ORIENTED_EDGE ( 'NONE', *, *, #39111, .F. ) ;
#217097=CARTESIAN_POINT ( 'NONE',  ( -20.85000000000000142, -1.835859311432481045, -112.0044391687985694 ) ) ;
#217113=CIRCLE ( 'NONE', #158901, 0.09999999999999939493 ) ;
#217117=EDGE_CURVE ( 'NONE', #127795, #6867, #222346, .T. ) ;
#217119=CARTESIAN_POINT ( 'NONE',  ( -1.820710678118657944, -9.929289321870186313, -91.75000000000005684 ) ) ;
#217121=VECTOR ( 'NONE', #220475, 1000.000000000000000 ) ;
#217125=LINE ( 'NONE', #5786, #65591 ) ;
#217127=DIRECTION ( 'NONE',  ( 1.000000000000000000, 0.000000000000000000, -0.000000000000000000 ) ) ;
#217159=DIRECTION ( 'NONE',  ( -1.000000000000000000, 0.000000000000000000, 0.000000000000000000 ) ) ;
#217161=VERTEX_POINT ( 'NONE', #50462 ) ;
#217191=VECTOR ( 'NONE', #174741, 1000.000000000000000 ) ;
#217226=ADVANCED_FACE ( 'NONE', ( #132605 ), #168464, .F. ) ;
#217229=AXIS2_PLACEMENT_3D ( 'NONE', #194918, #33296, #254812 ) ;
#217277=ORIENTED_EDGE ( 'NONE', *, *, #61753, .F. ) ;
#217282=EDGE_CURVE ( 'NONE', #63545, #106375, #170495, .T. ) ;
#217293=EDGE_LOOP ( 'NONE', ( #187363, #42941, #240545, #149154 ) ) ;
#217336=ORIENTED_EDGE ( 'NONE', *, *, #244932, .F. ) ;
#217389=EDGE_CURVE ( 'NONE', #144504, #211036, #251608, .T. ) ;
#217416=AXIS2_PLACEMENT_3D ( 'NONE', #49661, #186623, #207471 ) ;
#217460=FACE_OUTER_BOUND ( 'NONE', #141825, .T. ) ;
#217478=DIRECTION ( 'NONE',  ( 0.000000000000000000, 0.9915357197604792727, -0.1298341882520475943 ) ) ;
#217505=ADVANCED_FACE ( 'NONE', ( #64601 ), #126712, .F. ) ;
#217530=VERTEX_POINT ( 'NONE', #26799 ) ;
#217535=EDGE_CURVE ( 'NONE', #138090, #5531, #143275, .T. ) ;
#217566=CARTESIAN_POINT ( 'NONE',  ( -22.59999999999999787, 0.1008583691098682150, -55.25043287651065782 ) ) ;
#217587=VERTEX_POINT ( 'NONE', #248390 ) ;
#217597=EDGE_LOOP ( 'NONE', ( #65911, #61079, #91785, #73416 ) ) ;
#217648=DIRECTION ( 'NONE',  ( 1.000000000000000000, -0.000000000000000000, -0.000000000000000000 ) ) ;
#217663=CARTESIAN_POINT ( 'NONE',  ( -23.15000000000000213, 11.65000000001115588, -88.35000000000003695 ) ) ;
#217664=ORIENTED_EDGE ( 'NONE', *, *, #88853, .T. ) ;
#217677=ORIENTED_EDGE ( 'NONE', *, *, #155352, .T. ) ;
#217735=EDGE_CURVE ( 'NONE', #78259, #4064, #31077, .T. ) ;
#217741=DIRECTION ( 'NONE',  ( 0.000000000000000000, 0.000000000000000000, -1.000000000000000000 ) ) ;
#217756=ORIENTED_EDGE ( 'NONE', *, *, #209354, .T. ) ;
#217768=CIRCLE ( 'NONE', #22181, 0.1000000000000028644 ) ;
#217781=ADVANCED_FACE ( 'NONE', ( #16222 ), #73633, .T. ) ;
#217789=DIRECTION ( 'NONE',  ( 1.000000000000000000, 2.952720810173289112E-16, -0.000000000000000000 ) ) ;
#217803=CARTESIAN_POINT ( 'NONE',  ( 18.59999999999999076, 10.20857864377385127, -88.35000000000003695 ) ) ;
#217804=ORIENTED_EDGE ( 'NONE', *, *, #188874, .T. ) ;
#217807=CARTESIAN_POINT ( 'NONE',  ( 21.05000000000000071, 0.09843750001147391626, -60.70076908990778009 ) ) ;
#217824=LINE ( 'NONE', #36681, #238891 ) ;
#217826=CARTESIAN_POINT ( 'NONE',  ( -22.50000000000000000, 11.65000000001113278, -67.00000000000004263 ) ) ;
#217849=DIRECTION ( 'NONE',  ( 0.000000000000000000, -1.000000000000000000, -0.000000000000000000 ) ) ;
#217868=EDGE_LOOP ( 'NONE', ( #91805, #218472, #127502, #217095, #198461 ) ) ;
#217883=CARTESIAN_POINT ( 'NONE',  ( -23.15000000000000213, -11.64999999998884483, -97.40000000000004832 ) ) ;
#217885=ORIENTED_EDGE ( 'NONE', *, *, #58020, .F. ) ;
#217919=CARTESIAN_POINT ( 'NONE',  ( 18.46921299892753865, -9.509378177812608968, -73.98657870937046255 ) ) ;
#217932=EDGE_CURVE ( 'NONE', #208514, #32089, #42191, .T. ) ;
#217974=CIRCLE ( 'NONE', #147069, 11.65000000000000746 ) ;
#217993=ORIENTED_EDGE ( 'NONE', *, *, #193288, .F. ) ;
#217999=EDGE_CURVE ( 'NONE', #240985, #179279, #105628, .T. ) ;
#218026=EDGE_LOOP ( 'NONE', ( #42803, #36471, #39201, #195912 ) ) ;
#218048=DIRECTION ( 'NONE',  ( 0.000000000000000000, 0.000000000000000000, -1.000000000000000000 ) ) ;
#218054=AXIS2_PLACEMENT_3D ( 'NONE', #254172, #79384, #157706 ) ;
#218057=AXIS2_PLACEMENT_3D ( 'NONE', #214832, #151027, #134012 ) ;
#218078=CARTESIAN_POINT ( 'NONE',  ( 18.59999999999999076, 6.982009704867611077, -104.1961521182563359 ) ) ;
#218083=DIRECTION ( 'NONE',  ( 0.000000000000000000, 6.308085367182471812E-16, 1.000000000000000000 ) ) ;
#218115=CARTESIAN_POINT ( 'NONE',  ( -21.98333005346336932, 1.115600667400684642E-11, -59.62592467094336968 ) ) ;
#218145=VERTEX_POINT ( 'NONE', #173738 ) ;
#218236=DIRECTION ( 'NONE',  ( 0.000000000000000000, 1.000000000000000000, 0.000000000000000000 ) ) ;
#218255=DIRECTION ( 'NONE',  ( -6.938893903907222856E-15, 1.000000000000000000, 2.891205793294679805E-16 ) ) ;
#218268=AXIS2_PLACEMENT_3D ( 'NONE', #255371, #37694, #198012 ) ;
#218323=CYLINDRICAL_SURFACE ( 'NONE', #59601, 12.87499999999999822 ) ;
#218331=CARTESIAN_POINT ( 'NONE',  ( -18.50000000000000000, -9.399999999988850163, -74.29725975966333351 ) ) ;
#218361=AXIS2_PLACEMENT_3D ( 'NONE', #236268, #19812, #141035 ) ;
#218370=DIRECTION ( 'NONE',  ( -0.000000000000000000, -0.000000000000000000, -1.000000000000000000 ) ) ;
#218371=AXIS2_PLACEMENT_3D ( 'NONE', #41484, #156313, #38911 ) ;
#218387=DIRECTION ( 'NONE',  ( 3.265361837132813093E-16, -1.000000000000000000, -0.000000000000000000 ) ) ;
#218416=DIRECTION ( 'NONE',  ( 0.000000000000000000, 0.000000000000000000, -1.000000000000000000 ) ) ;
#218428=ORIENTED_EDGE ( 'NONE', *, *, #15350, .T. ) ;
#218446=EDGE_CURVE ( 'NONE', #51379, #204053, #109213, .T. ) ;
#218465=FACE_OUTER_BOUND ( 'NONE', #85436, .T. ) ;
#218472=ORIENTED_EDGE ( 'NONE', *, *, #62645, .T. ) ;
#218481=CARTESIAN_POINT ( 'NONE',  ( 20.94999999999999929, 1.115600667400684642E-11, -102.5000000000000426 ) ) ;
#218492=DIRECTION ( 'NONE',  ( 1.000000000000000000, -0.000000000000000000, -0.000000000000000000 ) ) ;
#218513=DIRECTION ( 'NONE',  ( 0.000000000000000000, 0.000000000000000000, -1.000000000000000000 ) ) ;
#218525=ORIENTED_EDGE ( 'NONE', *, *, #213624, .T. ) ;
#218536=AXIS2_PLACEMENT_3D ( 'NONE', #252704, #35003, #234427 ) ;
#218548=DIRECTION ( 'NONE',  ( 1.000000000000000000, 0.000000000000000000, 0.000000000000000000 ) ) ;
#218554=EDGE_CURVE ( 'NONE', #142448, #64371, #72541, .T. ) ;
#218555=DIRECTION ( 'NONE',  ( -0.000000000000000000, 0.000000000000000000, -1.000000000000000000 ) ) ;
#218561=CIRCLE ( 'NONE', #255948, 2.100000000000002309 ) ;
#218564=CARTESIAN_POINT ( 'NONE',  ( 21.14999999999999858, 1.115600667400684642E-11, -60.45934304829879835 ) ) ;
#218568=CARTESIAN_POINT ( 'NONE',  ( 21.05000000000000071, 10.48443348965288635, -74.45680580149196715 ) ) ;
#218597=DIRECTION ( 'NONE',  ( 1.000000000000000000, 0.000000000000000000, 0.000000000000000000 ) ) ;
#218641=EDGE_CURVE ( 'NONE', #166675, #57960, #181054, .T. ) ;
#218682=ORIENTED_EDGE ( 'NONE', *, *, #199673, .T. ) ;
#218687=CARTESIAN_POINT ( 'NONE',  ( -20.07928932188135107, 9.220710678129810489, -88.25000000000005684 ) ) ;
#218738=ORIENTED_EDGE ( 'NONE', *, *, #2504, .T. ) ;
#218801=CIRCLE ( 'NONE', #106370, 0.09999999999999939493 ) ;
#218802=EDGE_LOOP ( 'NONE', ( #34897, #102090, #51182, #136336 ) ) ;
#218831=ORIENTED_EDGE ( 'NONE', *, *, #228149, .F. ) ;
#218869=CARTESIAN_POINT ( 'NONE',  ( 23.14999999999998437, 4.050000000011155343, -67.00000000000004263 ) ) ;
#218876=CARTESIAN_POINT ( 'NONE',  ( -21.78635804494510708, 7.035661485164336426, -66.90099493449235979 ) ) ;
#218888=VECTOR ( 'NONE', #246432, 1000.000000000000000 ) ;
#218933=DIRECTION ( 'NONE',  ( 1.000000000000000000, 0.000000000000000000, 0.000000000000000000 ) ) ;
#218966=CARTESIAN_POINT ( 'NONE',  ( 20.99142135623731065, 11.60000000001116049, -93.57179676972454274 ) ) ;
#218984=DIRECTION ( 'NONE',  ( 0.000000000000000000, -0.9893560106964500722, 0.1455152366551550613 ) ) ;
#219001=EDGE_LOOP ( 'NONE', ( #67456, #256991, #32882, #115531, #202135, #215947, #56312, #40884, #235096, #77104, #141964, #222071, #203488, #152015, #98014, #104252 ) ) ;
#219025=PLANE ( 'NONE',  #172815 ) ;
#219027=ORIENTED_EDGE ( 'NONE', *, *, #254563, .T. ) ;
#219039=CARTESIAN_POINT ( 'NONE',  ( -18.59999999999999787, -1.835341550213255957, -78.55515129256302487 ) ) ;
#219071=VERTEX_POINT ( 'NONE', #183031 ) ;
#219075=AXIS2_PLACEMENT_3D ( 'NONE', #42787, #124899, #84426 ) ;
#219099=CARTESIAN_POINT ( 'NONE',  ( 21.04999999999999716, -0.01759718699747322632, -60.55922910633812251 ) ) ;
#219106=DIRECTION ( 'NONE',  ( 0.000000000000000000, -0.4930308989875248349, -0.8700118002898312719 ) ) ;
#219130=VERTEX_POINT ( 'NONE', #145154 ) ;
#219131=VERTEX_POINT ( 'NONE', #224695 ) ;
#219149=VERTEX_POINT ( 'NONE', #111189 ) ;
#219158=CARTESIAN_POINT ( 'NONE',  ( 22.47071067811865319, 0.09909245471376171288, -59.27992525550200043 ) ) ;
#219199=AXIS2_PLACEMENT_3D ( 'NONE', #190069, #130078, #253874 ) ;
#219211=DIRECTION ( 'NONE',  ( 1.000000000000000000, 0.000000000000000000, 0.000000000000000000 ) ) ;
#219214=CARTESIAN_POINT ( 'NONE',  ( 21.05000000000000071, -1.249999999988843369, -74.90000000000004832 ) ) ;
#219231=DIRECTION ( 'NONE',  ( 0.000000000000000000, 0.9999631594459053030, 0.008583690987162899758 ) ) ;
#219279=DIRECTION ( 'NONE',  ( 1.000000000000000000, 0.000000000000000000, 0.000000000000000000 ) ) ;
#219291=LINE ( 'NONE', #4102, #92265 ) ;
#219319=DIRECTION ( 'NONE',  ( 0.000000000000000000, 0.000000000000000000, -1.000000000000000000 ) ) ;
#219358=DIRECTION ( 'NONE',  ( -1.000000000000000000, 0.000000000000000000, 0.000000000000000000 ) ) ;
#219383=AXIS2_PLACEMENT_3D ( 'NONE', #86615, #200177, #4523 ) ;
#219403=ORIENTED_EDGE ( 'NONE', *, *, #77126, .T. ) ;
#219418=FACE_OUTER_BOUND ( 'NONE', #163388, .T. ) ;
#219423=EDGE_CURVE ( 'NONE', #250224, #192087, #143617, .T. ) ;
#219441=ORIENTED_EDGE ( 'NONE', *, *, #150171, .F. ) ;
#219476=B_SPLINE_CURVE_WITH_KNOTS ( 'NONE', 3,
 ( #199024, #159917, #36116, #218564 ),
 .UNSPECIFIED., .F., .F.,
 ( 4, 4 ),
 ( 0.000000000000000000, 0.001767853679387103869 ),
 .UNSPECIFIED. ) ;
#219496=AXIS2_PLACEMENT_3D ( 'NONE', #37071, #196123, #117850 ) ;
#219498=ORIENTED_EDGE ( 'NONE', *, *, #115475, .F. ) ;
#219535=AXIS2_PLACEMENT_3D ( 'NONE', #151737, #232555, #72187 ) ;
#219541=DIRECTION ( 'NONE',  ( -0.000000000000000000, -0.000000000000000000, -1.000000000000000000 ) ) ;
#219545=DIRECTION ( 'NONE',  ( -1.000000000000000000, 0.000000000000000000, 0.000000000000000000 ) ) ;
#219552=CARTESIAN_POINT ( 'NONE',  ( 18.49999999999996803, 7.070967871809997973, -104.2465642218683541 ) ) ;
#219565=EDGE_CURVE ( 'NONE', #134711, #102952, #135601, .T. ) ;
#219603=EDGE_LOOP ( 'NONE', ( #101372, #84723, #30194, #152306, #199840 ) ) ;
#219604=CARTESIAN_POINT ( 'NONE',  ( 21.13422380239055087, 6.493326514816704531, -67.00000000000004263 ) ) ;
#219608=DIRECTION ( 'NONE',  ( 0.000000000000000000, 0.000000000000000000, 1.000000000000000000 ) ) ;
#219616=LINE ( 'NONE', #41018, #165804 ) ;
#219621=CARTESIAN_POINT ( 'NONE',  ( -21.05000000000000071, -11.64999999998884483, -67.00000000000004263 ) ) ;
#219667=ORIENTED_EDGE ( 'NONE', *, *, #184442, .F. ) ;
#219672=DIRECTION ( 'NONE',  ( 0.000000000000000000, 0.000000000000000000, -1.000000000000000000 ) ) ;
#219695=DIRECTION ( 'NONE',  ( -1.000000000000000000, 0.000000000000000000, 0.000000000000000000 ) ) ;
#219706=DIRECTION ( 'NONE',  ( 0.7071067811865474617, 0.7071067811865474617, 0.000000000000000000 ) ) ;
#219729=EDGE_CURVE ( 'NONE', #242995, #60888, #218801, .T. ) ;
#219771=CARTESIAN_POINT ( 'NONE',  ( -21.07971444708686093, 0.08782343632898161057, -60.67020791837349236 ) ) ;
#219772=EDGE_CURVE ( 'NONE', #102720, #214056, #56305, .T. ) ;
#219816=CARTESIAN_POINT ( 'NONE',  ( -20.94999999999999929, 0.2561057921033771945, -66.96510355832775474 ) ) ;
#219821=CARTESIAN_POINT ( 'NONE',  ( -20.00857864376270001, 9.150000000011157653, -88.25000000000005684 ) ) ;
#219833=AXIS2_PLACEMENT_3D ( 'NONE', #211105, #190270, #113285 ) ;
#219836=ORIENTED_EDGE ( 'NONE', *, *, #159032, .T. ) ;
#219859=DIRECTION ( 'NONE',  ( 1.000000000000000000, -0.000000000000000000, -0.000000000000000000 ) ) ;
#219866=CARTESIAN_POINT ( 'NONE',  ( 21.05000000000000426, 10.56275983746217406, -74.45681395791866919 ) ) ;
#219881=CARTESIAN_POINT ( 'NONE',  ( -21.05000000000000071, 1.115600667400684642E-11, -96.40000000000003411 ) ) ;
#219884=CARTESIAN_POINT ( 'NONE',  ( 21.05000000000000071, 1.115600667400684642E-11, -79.15000000000004832 ) ) ;
#219894=SURFACE_STYLE_FILL_AREA ( #3397 ) ;
#219916=CARTESIAN_POINT ( 'NONE',  ( 23.24999999999999645, 4.775700934590584090, -78.84876810404601599 ) ) ;
#219924=DIRECTION ( 'NONE',  ( 1.000000000000000000, 0.000000000000000000, 0.000000000000000000 ) ) ;
#219933=DIRECTION ( 'NONE',  ( 1.000000000000000000, 0.000000000000000000, 0.000000000000000000 ) ) ;
#219974=LINE ( 'NONE', #238251, #124635 ) ;
#219985=CYLINDRICAL_SURFACE ( 'NONE', #78357, 0.1000000000000028644 ) ;
#220016=VECTOR ( 'NONE', #101638, 1000.000000000000000 ) ;
#220030=PLANE ( 'NONE',  #236959 ) ;
#220040=VERTEX_POINT ( 'NONE', #44845 ) ;
#220045=VERTEX_POINT ( 'NONE', #186951 ) ;
#220055=DIRECTION ( 'NONE',  ( 0.000000000000000000, -0.8700118002898321601, 0.4930308989875230030 ) ) ;
#220056=AXIS2_PLACEMENT_3D ( 'NONE', #113453, #256762, #16938 ) ;
#220075=FACE_OUTER_BOUND ( 'NONE', #144920, .T. ) ;
#220091=AXIS2_PLACEMENT_3D ( 'NONE', #110766, #190328, #102081 ) ;
#220111=DIRECTION ( 'NONE',  ( -1.000000000000000000, 0.000000000000000000, 0.000000000000000000 ) ) ;
#220185=CARTESIAN_POINT ( 'NONE',  ( -22.01447462590972748, 7.263800201241075172, -66.90096299994051776 ) ) ;
#220205=CARTESIAN_POINT ( 'NONE',  ( -18.59999999999999787, 1.162701749949165642, -75.00000000000004263 ) ) ;
#220236=CARTESIAN_POINT ( 'NONE',  ( 21.05000000000000071, 5.500000000011153745, -88.09473398108696074 ) ) ;
#220275=VECTOR ( 'NONE', #227266, 1000.000000000000000 ) ;
#220288=CIRCLE ( 'NONE', #107830, 11.65000000000000746 ) ;
#220304=CARTESIAN_POINT ( 'NONE',  ( 23.14999999999999858, 1.115600667400684642E-11, -67.00000000000004263 ) ) ;
#220370=ORIENTED_EDGE ( 'NONE', *, *, #92120, .T. ) ;
#220410=EDGE_LOOP ( 'NONE', ( #8229, #34722, #211854, #198710 ) ) ;
#220447=AXIS2_PLACEMENT_3D ( 'NONE', #253247, #74668, #30378 ) ;
#220450=ORIENTED_EDGE ( 'NONE', *, *, #237408, .T. ) ;
#220475=DIRECTION ( 'NONE',  ( -0.000000000000000000, -0.000000000000000000, -1.000000000000000000 ) ) ;
#220487=ORIENTED_EDGE ( 'NONE', *, *, #84640, .F. ) ;
#220506=CIRCLE ( 'NONE', #199671, 0.1000000000000028644 ) ;
#220519=DIRECTION ( 'NONE',  ( 0.000000000000000000, 1.000000000000000000, -6.308085367188393199E-16 ) ) ;
#220526=CIRCLE ( 'NONE', #216214, 11.79999999999999893 ) ;
#220555=ADVANCED_FACE ( 'NONE', ( #56068 ), #213881, .F. ) ;
#220573=EDGE_CURVE ( 'NONE', #177869, #169137, #173642, .T. ) ;
#220593=VECTOR ( 'NONE', #144166, 1000.000000000000000 ) ;
#220601=EDGE_LOOP ( 'NONE', ( #192731, #167843, #110180, #248289 ) ) ;
#220605=EDGE_LOOP ( 'NONE', ( #230273, #186461, #89145, #189792 ) ) ;
#220607=CARTESIAN_POINT ( 'NONE',  ( 21.14999999999999858, 11.65000000001115943, -67.10000000000005116 ) ) ;
#220622=ORIENTED_EDGE ( 'NONE', *, *, #24830, .T. ) ;
#220668=DIRECTION ( 'NONE',  ( -1.000000000000000000, 0.000000000000000000, 0.000000000000000000 ) ) ;
#220685=AXIS2_PLACEMENT_3D ( 'NONE', #194703, #138516, #155585 ) ;
#220699=AXIS2_PLACEMENT_3D ( 'NONE', #122595, #97842, #100417 ) ;
#220742=LINE ( 'NONE', #199914, #233689 ) ;
#220744=FACE_OUTER_BOUND ( 'NONE', #23517, .T. ) ;
#220747=CIRCLE ( 'NONE', #224999, 0.09999999999999939493 ) ;
#220752=ORIENTED_EDGE ( 'NONE', *, *, #53447, .F. ) ;
#220762=VECTOR ( 'NONE', #44498, 1000.000000000000000 ) ;
#220765=DIRECTION ( 'NONE',  ( 0.000000000000000000, -0.8660254037844411501, -0.4999999999999956701 ) ) ;
#220766=AXIS2_PLACEMENT_3D ( 'NONE', #1787, #23959, #63049 ) ;
#220829=CARTESIAN_POINT ( 'NONE',  ( 21.05000000000000071, 0.09779029131994770863, -60.74218538952391810 ) ) ;
#220846=EDGE_CURVE ( 'NONE', #104861, #189061, #140226, .T. ) ;
#220888=CARTESIAN_POINT ( 'NONE',  ( 21.05000000000000071, 6.304516329275136499, -67.02110330805874128 ) ) ;
#220889=AXIS2_PLACEMENT_3D ( 'NONE', #87765, #47353, #64375 ) ;
#220914=CIRCLE ( 'NONE', #158593, 0.1000000000000053069 ) ;
#220918=LINE ( 'NONE', #1864, #46093 ) ;
#220923=AXIS2_PLACEMENT_3D ( 'NONE', #79529, #20894, #57402 ) ;
#220935=CARTESIAN_POINT ( 'NONE',  ( -23.25000000000000000, 11.65000000001115588, -88.35000000000003695 ) ) ;
#220987=ORIENTED_EDGE ( 'NONE', *, *, #196574, .F. ) ;
#221003=LINE ( 'NONE', #106186, #137131 ) ;
#221062=DIRECTION ( 'NONE',  ( 0.000000000000000000, -0.9915357197604792727, 0.1298341882520475943 ) ) ;
#221072=LINE ( 'NONE', #141540, #182254 ) ;
#221078=DIRECTION ( 'NONE',  ( -1.000000000000000000, -0.000000000000000000, -0.000000000000000000 ) ) ;
#221107=CARTESIAN_POINT ( 'NONE',  ( 20.94999999999999929, 4.850467289730776344, -88.46573259099837117 ) ) ;
#221108=VECTOR ( 'NONE', #92730, 1000.000000000000000 ) ;
#221118=ORIENTED_EDGE ( 'NONE', *, *, #117028, .F. ) ;
#221121=VERTEX_POINT ( 'NONE', #905 ) ;
#221131=CARTESIAN_POINT ( 'NONE',  ( -21.95218792049438861, 0.09902843981107177507, -59.79849243875336384 ) ) ;
#221155=DIRECTION ( 'NONE',  ( -0.000000000000000000, -0.000000000000000000, -1.000000000000000000 ) ) ;
#221178=DIRECTION ( 'NONE',  ( 1.000000000000000000, 0.000000000000000000, 0.000000000000000000 ) ) ;
#221192=DIRECTION ( 'NONE',  ( -0.000000000000000000, 1.000000000000000000, 0.000000000000000000 ) ) ;
#221193=DIRECTION ( 'NONE',  ( 0.000000000000000000, 0.000000000000000000, -1.000000000000000000 ) ) ;
#221225=DIRECTION ( 'NONE',  ( 0.000000000000000000, 0.9915357197604792727, -0.1298341882520473722 ) ) ;
#221238=FACE_OUTER_BOUND ( 'NONE', #202733, .T. ) ;
#221242=DIRECTION ( 'NONE',  ( 0.000000000000000000, 0.000000000000000000, -1.000000000000000000 ) ) ;
#221271=LINE ( 'NONE', #183458, #8535 ) ;
#221310=ADVANCED_FACE ( 'NONE', ( #110309 ), #103188, .T. ) ;
#221375=AXIS2_PLACEMENT_3D ( 'NONE', #10806, #89041, #30383 ) ;
#221412=CARTESIAN_POINT ( 'NONE',  ( -18.59999999999999787, 10.33248238083634440, -106.0948465439131922 ) ) ;
#221421=AXIS2_PLACEMENT_3D ( 'NONE', #125342, #67928, #44526 ) ;
#221431=CARTESIAN_POINT ( 'NONE',  ( 21.12230431290520372, 0.005209851700162637655, -60.54243334670702836 ) ) ;
#221453=ORIENTED_EDGE ( 'NONE', *, *, #166573, .T. ) ;
#221475=DIRECTION ( 'NONE',  ( 0.000000000000000000, 0.1575844902526876978, 0.9875055080513731598 ) ) ;
#221507=CARTESIAN_POINT ( 'NONE',  ( 21.22070241538126467, 0.09891903054618129965, -60.53005372713042220 ) ) ;
#221515=( BOUNDED_SURFACE ( )  B_SPLINE_SURFACE ( 3, 2, ( 
 ( #79190, #212328, #175766 ),
 ( #115771, #154929, #156210 ),
 ( #114487, #235705, #137876 ),
 ( #57048, #158776, #117059 ),
 ( #118350, #98731, #214865 ),
 ( #256497, #33717, #252699 ) ),
 .UNSPECIFIED., .F., .F., .F. ) 
 B_SPLINE_SURFACE_WITH_KNOTS ( ( 4, 2, 4 ),
 ( 3, 3 ),
 ( 0.0001342700090130156216, 0.0002909192928057487745, 0.0004475685765984819273 ),
 ( 0.000000000000000000, 1.000000000000000000 ),
 .UNSPECIFIED. ) 
 GEOMETRIC_REPRESENTATION_ITEM ( )  RATIONAL_B_SPLINE_SURFACE ( (
 ( 1.000000000000000000, 0.7250110520819876836, 1.000000000000000000),
 ( 1.000000000000000000, 0.7257599279134827608, 1.000000000000000000),
 ( 1.000000000000000000, 0.7137594617283012921, 1.000000000000000000),
 ( 1.000000000000000000, 0.6959270178810966767, 1.000000000000000000),
 ( 1.000000000000000000, 0.6919879549338106006, 1.000000000000000000),
 ( 1.000000000000000000, 0.7071067811865475727, 1.000000000000000000) ) ) 
 REPRESENTATION_ITEM ( '' )  SURFACE ( )  );
#221535=CARTESIAN_POINT ( 'NONE',  ( 21.14999999999999858, 11.65000000001115943, -67.10000000000005116 ) ) ;
#221544=ORIENTED_EDGE ( 'NONE', *, *, #28260, .T. ) ;
#221552=CARTESIAN_POINT ( 'NONE',  ( 21.05000000000000071, 10.42338541492405390, -74.49205192387015018 ) ) ;
#221554=DIRECTION ( 'NONE',  ( 0.000000000000000000, 0.000000000000000000, -1.000000000000000000 ) ) ;
#221555=CARTESIAN_POINT ( 'NONE',  ( 21.14999999999999503, 1.115600667400684642E-11, -67.00000000000004263 ) ) ;
#221573=FACE_OUTER_BOUND ( 'NONE', #238192, .T. ) ;
#221582=CARTESIAN_POINT ( 'NONE',  ( 22.59999999999999076, 11.74987124438766273, -66.93457040898637445 ) ) ;
#221597=CIRCLE ( 'NONE', #38465, 0.09999999999999939493 ) ;
#221620=DIRECTION ( 'NONE',  ( -1.000000000000000000, 0.000000000000000000, 0.000000000000000000 ) ) ;
#221625=CIRCLE ( 'NONE', #55033, 0.1000000000000028644 ) ;
#221631=ORIENTED_EDGE ( 'NONE', *, *, #188874, .F. ) ;
#221706=VERTEX_POINT ( 'NONE', #246944 ) ;
#221714=CARTESIAN_POINT ( 'NONE',  ( -20.85000000000000142, -1.164121893230052995, -108.3148480855716542 ) ) ;
#221715=ORIENTED_EDGE ( 'NONE', *, *, #164468, .T. ) ;
#221775=LINE ( 'NONE', #223082, #116044 ) ;
#221793=AXIS2_PLACEMENT_3D ( 'NONE', #35058, #191552, #33779 ) ;
#221799=DIRECTION ( 'NONE',  ( -1.000000000000000000, -0.000000000000000000, -0.000000000000000000 ) ) ;
#221801=DIRECTION ( 'NONE',  ( 1.000000000000000000, 0.000000000000000000, 0.000000000000000000 ) ) ;
#221882=CYLINDRICAL_SURFACE ( 'NONE', #226744, 0.1000000000000028644 ) ;
#221912=VERTEX_POINT ( 'NONE', #83367 ) ;
#221920=DIRECTION ( 'NONE',  ( -1.000000000000000000, -2.952720810173289112E-16, 0.000000000000000000 ) ) ;
#221924=FACE_OUTER_BOUND ( 'NONE', #140577, .T. ) ;
#221931=VECTOR ( 'NONE', #40296, 1000.000000000000000 ) ;
#221935=EDGE_CURVE ( 'NONE', #80211, #113007, #11843, .T. ) ;
#221985=DIRECTION ( 'NONE',  ( -5.603264701231743991E-32, 1.897661533703520143E-16, -1.000000000000000000 ) ) ;
#221993=ORIENTED_EDGE ( 'NONE', *, *, #126909, .F. ) ;
#222008=DIRECTION ( 'NONE',  ( 1.000000000000000000, -0.000000000000000000, -0.000000000000000000 ) ) ;
#222043=ORIENTED_EDGE ( 'NONE', *, *, #113330, .T. ) ;
#222057=EDGE_CURVE ( 'NONE', #142448, #13227, #135340, .T. ) ;
#222071=ORIENTED_EDGE ( 'NONE', *, *, #174488, .T. ) ;
#222088=EDGE_CURVE ( 'NONE', #212939, #111810, #253413, .T. ) ;
#222125=VECTOR ( 'NONE', #108414, 1000.000000000000000 ) ;
#222126=DIRECTION ( 'NONE',  ( 0.000000000000000000, -0.8700118002898359348, 0.4930308989875165082 ) ) ;
#222144=AXIS2_PLACEMENT_3D ( 'NONE', #194015, #113174, #191466 ) ;
#222178=CARTESIAN_POINT ( 'NONE',  ( -20.85000000000000142, -1.362429037182151470, -108.3888812479212476 ) ) ;
#222190=DIRECTION ( 'NONE',  ( -1.000000000000000000, 0.000000000000000000, 0.000000000000000000 ) ) ;
#222201=ORIENTED_EDGE ( 'NONE', *, *, #89513, .T. ) ;
#222202=CYLINDRICAL_SURFACE ( 'NONE', #68279, 0.1000000000000028644 ) ;
#222206=CARTESIAN_POINT ( 'NONE',  ( -23.15000000000000213, 1.115600667400684642E-11, -71.15000000000004832 ) ) ;
#222218=VERTEX_POINT ( 'NONE', #57077 ) ;
#222233=ORIENTED_EDGE ( 'NONE', *, *, #7311, .F. ) ;
#222242=CARTESIAN_POINT ( 'NONE',  ( 21.10642757222115051, 10.72315628916975250, -79.24069752378524356 ) ) ;
#222297=DIRECTION ( 'NONE',  ( 2.952720810173289112E-16, -1.000000000000000000, 0.000000000000000000 ) ) ;
#222301=CIRCLE ( 'NONE', #97409, 0.1000000000000028644 ) ;
#222321=ORIENTED_EDGE ( 'NONE', *, *, #79344, .F. ) ;
#222326=VECTOR ( 'NONE', #31011, 1000.000000000000000 ) ;
#222332=CIRCLE ( 'NONE', #118330, 0.09999999999999824307 ) ;
#222346=CIRCLE ( 'NONE', #72373, 0.09999999999999939493 ) ;
#222387=CIRCLE ( 'NONE', #55802, 0.2000000000000057288 ) ;
#222390=ORIENTED_EDGE ( 'NONE', *, *, #85818, .T. ) ;
#222394=ORIENTED_EDGE ( 'NONE', *, *, #222088, .F. ) ;
#222395=CARTESIAN_POINT ( 'NONE',  ( -21.30740335185486245, 0.09893452578700702438, -60.44334207797204073 ) ) ;
#222399=CARTESIAN_POINT ( 'NONE',  ( 18.49999999999999645, 1.162701749949165642, -75.10000000000003695 ) ) ;
#222479=CARTESIAN_POINT ( 'NONE',  ( 21.05000000000000071, 5.400000000011154988, -79.40526601891313874 ) ) ;
#222539=CARTESIAN_POINT ( 'NONE',  ( -18.39999999999999858, -9.682403433465239573, -107.1568433774128408 ) ) ;
#222542=VECTOR ( 'NONE', #29677, 1000.000000000000000 ) ;
#222561=EDGE_CURVE ( 'NONE', #219130, #236185, #252408, .T. ) ;
#222568=CARTESIAN_POINT ( 'NONE',  ( -23.25000000000000000, 1.115600667400684642E-11, -100.5000000000000426 ) ) ;
#222581=CARTESIAN_POINT ( 'NONE',  ( -20.64999999999999858, 7.150000000011155876, -88.15000000000004832 ) ) ;
#222587=TOROIDAL_SURFACE ( 'NONE', #110171, 11.65000000000000036, 0.1000000000000000056 ) ;
#222609=DIRECTION ( 'NONE',  ( 1.000000000000000000, 7.304098846218135653E-16, 0.000000000000000000 ) ) ;
#222635=DIRECTION ( 'NONE',  ( 0.000000000000000000, 0.000000000000000000, 1.000000000000000000 ) ) ;
#222639=CARTESIAN_POINT ( 'NONE',  ( -18.54118089899632693, -9.463537631836942410, -74.04857759786816018 ) ) ;
#222647=CARTESIAN_POINT ( 'NONE',  ( 18.49999999999999645, -1.835341550213255957, -78.55515129256302487 ) ) ;
#222676=DIRECTION ( 'NONE',  ( 0.000000000000000000, 0.9654727137038726648, -0.2605042016806632943 ) ) ;
#222679=AXIS2_PLACEMENT_3D ( 'NONE', #53273, #113237, #192788 ) ;
#222685=CARTESIAN_POINT ( 'NONE',  ( -20.85000000000000142, 7.021664781911246322, -104.2335654018973372 ) ) ;
#222713=ORIENTED_EDGE ( 'NONE', *, *, #244313, .F. ) ;
#222721=CARTESIAN_POINT ( 'NONE',  ( 18.50000000000000355, -9.421074344975995274, -107.3244720594301356 ) ) ;
#222740=DIRECTION ( 'NONE',  ( 0.000000000000000000, 0.5000000000000209832, 0.8660254037844264952 ) ) ;
#222750=CARTESIAN_POINT ( 'NONE',  ( -22.40000000000000213, 1.115486826172573664E-11, -55.24956710754144495 ) ) ;
#222752=CARTESIAN_POINT ( 'NONE',  ( -21.29999999999995808, 1.115600667400684642E-11, -71.05000000000003979 ) ) ;
#222755=CARTESIAN_POINT ( 'NONE',  ( 18.59999999999999787, -1.362429037182151470, -108.3888812479212476 ) ) ;
#222756=ORIENTED_EDGE ( 'NONE', *, *, #17544, .T. ) ;
#222787=EDGE_CURVE ( 'NONE', #58814, #185550, #217125, .T. ) ;
#222789=LINE ( 'NONE', #27210, #177143 ) ;
#222810=ADVANCED_FACE ( 'NONE', ( #142737 ), #102303, .T. ) ;
#222824=EDGE_CURVE ( 'NONE', #141973, #97847, #7331, .T. ) ;
#222862=CARTESIAN_POINT ( 'NONE',  ( -23.15000000000000213, -8.663551401858001100, -90.97589888193274987 ) ) ;
#222866=DIRECTION ( 'NONE',  ( 0.000000000000000000, 0.000000000000000000, 1.000000000000000000 ) ) ;
#222881=ORIENTED_EDGE ( 'NONE', *, *, #8996, .T. ) ;
#222883=VECTOR ( 'NONE', #59376, 1000.000000000000000 ) ;
#222897=DIRECTION ( 'NONE',  ( 0.000000000000000000, 0.000000000000000000, -1.000000000000000000 ) ) ;
#222940=DIRECTION ( 'NONE',  ( 1.000000000000000000, 0.000000000000000000, -0.000000000000000000 ) ) ;
#222961=CYLINDRICAL_SURFACE ( 'NONE', #177817, 0.5000000000000004441 ) ;
#222968=ORIENTED_EDGE ( 'NONE', *, *, #181241, .F. ) ;
#223002=CARTESIAN_POINT ( 'NONE',  ( -18.59999999999999787, 9.350000000011156942, -88.35000000000003695 ) ) ;
#223019=B_SPLINE_CURVE_WITH_KNOTS ( 'NONE', 3,
 ( #253406, #38230, #218115, #119047 ),
 .UNSPECIFIED., .F., .F.,
 ( 4, 4 ),
 ( 0.000000000000000000, 0.001767853679387133359 ),
 .UNSPECIFIED. ) ;
#223021=AXIS2_PLACEMENT_3D ( 'NONE', #179985, #238661, #241242 ) ;
#223025=ORIENTED_EDGE ( 'NONE', *, *, #45499, .T. ) ;
#223028=CARTESIAN_POINT ( 'NONE',  ( -21.14999999999999858, 11.75000000001115552, -67.10000000000005116 ) ) ;
#223033=EDGE_LOOP ( 'NONE', ( #79798, #188290, #63886 ) ) ;
#223041=LINE ( 'NONE', #84783, #47579 ) ;
#223052=ORIENTED_EDGE ( 'NONE', *, *, #195068, .F. ) ;
#223063=VERTEX_POINT ( 'NONE', #158213 ) ;
#223082=CARTESIAN_POINT ( 'NONE',  ( -18.50000000000000000, 9.250000000011157297, -88.15000000000004832 ) ) ;
#223086=DIRECTION ( 'NONE',  ( 1.000000000000000000, 7.304098846218133681E-16, -4.217023435051677501E-16 ) ) ;
#223102=DIRECTION ( 'NONE',  ( 0.000000000000000000, 1.192622389734062135E-14, -1.000000000000000000 ) ) ;
#223104=CARTESIAN_POINT ( 'NONE',  ( 22.39999999999999503, 11.65000000001116298, -67.10000000000005116 ) ) ;
#223109=FACE_OUTER_BOUND ( 'NONE', #197049, .T. ) ;
#223126=LINE ( 'NONE', #83129, #154233 ) ;
#223130=VERTEX_POINT ( 'NONE', #155638 ) ;
#223152=DIRECTION ( 'NONE',  ( 0.000000000000000000, 1.897661533703519897E-16, -1.000000000000000000 ) ) ;
#223163=CYLINDRICAL_SURFACE ( 'NONE', #111670, 0.09999999999999939493 ) ;
#223197=DIRECTION ( 'NONE',  ( 4.408576920032447355E-17, -0.1350103645451876666, -0.9908441862701600211 ) ) ;
#223208=DIRECTION ( 'NONE',  ( -1.000000000000000000, 0.000000000000000000, 0.000000000000000000 ) ) ;
#223227=ORIENTED_EDGE ( 'NONE', *, *, #25309, .T. ) ;
#223234=ORIENTED_EDGE ( 'NONE', *, *, #137639, .F. ) ;
#223237=FACE_OUTER_BOUND ( 'NONE', #105200, .T. ) ;
#223239=CARTESIAN_POINT ( 'NONE',  ( 18.50000000000000000, -9.399999999988843058, -107.3820418481727188 ) ) ;
#223322=VERTEX_POINT ( 'NONE', #179870 ) ;
#223331=EDGE_CURVE ( 'NONE', #223130, #177869, #103541, .T. ) ;
#223368=FACE_OUTER_BOUND ( 'NONE', #26848, .T. ) ;
#223397=CARTESIAN_POINT ( 'NONE',  ( 18.59999999999999432, -1.135018845899022466, -108.2169768834323662 ) ) ;
#223436=CARTESIAN_POINT ( 'NONE',  ( 20.85000000000000142, 6.982009704867603972, -104.1961521182563359 ) ) ;
#223447=AXIS2_PLACEMENT_3D ( 'NONE', #216315, #37717, #14305 ) ;
#223503=DIRECTION ( 'NONE',  ( 1.000000000000000000, 0.000000000000000000, -0.000000000000000000 ) ) ;
#223539=EDGE_CURVE ( 'NONE', #95156, #130026, #180660, .T. ) ;
#223550=DIRECTION ( 'NONE',  ( -0.000000000000000000, 0.1350103645451649625, -0.9908441862701631297 ) ) ;
#223563=DIRECTION ( 'NONE',  ( 0.000000000000000000, -1.000000000000000000, 0.000000000000000000 ) ) ;
#223571=AXIS2_PLACEMENT_3D ( 'NONE', #59271, #82697, #159712 ) ;
#223646=CIRCLE ( 'NONE', #198546, 0.1000000000000002831 ) ;
#223681=CARTESIAN_POINT ( 'NONE',  ( 20.94999999999999929, -1.835859311432481045, -112.0044391687985694 ) ) ;
#223683=ORIENTED_EDGE ( 'NONE', *, *, #116504, .F. ) ;
#223688=FACE_OUTER_BOUND ( 'NONE', #151794, .T. ) ;
#223708=CARTESIAN_POINT ( 'NONE',  ( 18.52928932304149967, 10.27928932305266407, -91.67625343280367645 ) ) ;
#223715=ORIENTED_EDGE ( 'NONE', *, *, #174407, .F. ) ;
#223735=DIRECTION ( 'NONE',  ( 0.000000000000000000, 0.000000000000000000, 1.000000000000000000 ) ) ;
#223774=ADVANCED_FACE ( 'NONE', ( #55233 ), #137355, .T. ) ;
#223788=CIRCLE ( 'NONE', #136286, 0.1000000000000028644 ) ;
#223795=AXIS2_PLACEMENT_3D ( 'NONE', #239816, #61164, #143263 ) ;
#223804=VERTEX_POINT ( 'NONE', #237756 ) ;
#223816=CARTESIAN_POINT ( 'NONE',  ( -20.94999999999999929, -11.64999999998884483, -97.60000000000005116 ) ) ;
#223844=EDGE_CURVE ( 'NONE', #39976, #143381, #220288, .T. ) ;
#223856=DIRECTION ( 'NONE',  ( 0.000000000000000000, 0.000000000000000000, -1.000000000000000000 ) ) ;
#223930=ORIENTED_EDGE ( 'NONE', *, *, #174241, .F. ) ;
#223931=EDGE_CURVE ( 'NONE', #154967, #181023, #201197, .T. ) ;
#223950=DIRECTION ( 'NONE',  ( -3.265361837132813093E-16, 1.000000000000000000, 0.000000000000000000 ) ) ;
#223952=CIRCLE ( 'NONE', #124038, 11.65000000000000746 ) ;
#223958=ADVANCED_FACE ( 'NONE', ( #186791 ), #228483, .F. ) ;
#223959=ADVANCED_FACE ( 'NONE', ( #10709 ), #207835, .T. ) ;
#224006=ORIENTED_EDGE ( 'NONE', *, *, #230723, .T. ) ;
#224031=EDGE_CURVE ( 'NONE', #38016, #66775, #66138, .T. ) ;
#224047=EDGE_LOOP ( 'NONE', ( #150077, #236227, #12826 ) ) ;
#224055=LINE ( 'NONE', #246206, #170562 ) ;
#224071=DIRECTION ( 'NONE',  ( 1.000000000000000000, 2.952720810173289112E-16, -0.000000000000000000 ) ) ;
#224105=ORIENTED_EDGE ( 'NONE', *, *, #48174, .T. ) ;
#224115=AXIS2_PLACEMENT_3D ( 'NONE', #34838, #156071, #118196 ) ;
#224137=CARTESIAN_POINT ( 'NONE',  ( 21.05000000000000071, 10.62872031401550288, -74.66491356908764487 ) ) ;
#224146=CARTESIAN_POINT ( 'NONE',  ( -18.50000000000000355, -9.419203418015493767, -74.24778581042869519 ) ) ;
#224180=CARTESIAN_POINT ( 'NONE',  ( 21.05000000000000071, -11.74999999998883560, -97.60000000000005116 ) ) ;
#224195=VERTEX_POINT ( 'NONE', #94078 ) ;
#224205=CARTESIAN_POINT ( 'NONE',  ( 18.49999999999999645, 1.728086936805617757, -53.88443500516780915 ) ) ;
#224212=LINE ( 'NONE', #20919, #210355 ) ;
#224216=ORIENTED_EDGE ( 'NONE', *, *, #216413, .T. ) ;
#224227=EDGE_CURVE ( 'NONE', #83831, #196062, #117508, .T. ) ;
#224232=ORIENTED_EDGE ( 'NONE', *, *, #54167, .T. ) ;
#224291=CARTESIAN_POINT ( 'NONE',  ( -18.41809261886924176, -9.682403314745313239, -107.1568435500914092 ) ) ;
#224372=DIRECTION ( 'NONE',  ( 0.000000000000000000, 0.000000000000000000, -1.000000000000000000 ) ) ;
#224385=CARTESIAN_POINT ( 'NONE',  ( -20.54999999999999716, 2.000000000011154189, -80.22462192276213955 ) ) ;
#224391=CARTESIAN_POINT ( 'NONE',  ( -21.14999999999999858, 1.115526128501326264E-11, -60.45934304829881256 ) ) ;
#224395=EDGE_CURVE ( 'NONE', #248044, #191668, #108032, .T. ) ;
#224426=CARTESIAN_POINT ( 'NONE',  ( -20.85000000000000142, 1.115600667400684642E-11, -100.5000000000000426 ) ) ;
#224438=CARTESIAN_POINT ( 'NONE',  ( 23.14999999999999858, 5.000000000011153745, -88.09473398108696074 ) ) ;
#224444=AXIS2_PLACEMENT_3D ( 'NONE', #185558, #201260, #4337 ) ;
#224452=CARTESIAN_POINT ( 'NONE',  ( -20.94999999999999929, 5.850000000011105428, -77.13249722427802624 ) ) ;
#224461=ORIENTED_EDGE ( 'NONE', *, *, #105016, .F. ) ;
#224474=AXIS2_PLACEMENT_3D ( 'NONE', #255213, #110624, #12833 ) ;
#224518=CARTESIAN_POINT ( 'NONE',  ( 22.50000000000000000, 7.790779598384538929, -66.90000000000004832 ) ) ;
#224522=FACE_OUTER_BOUND ( 'NONE', #19123, .T. ) ;
#224573=VECTOR ( 'NONE', #202977, 1000.000000000000000 ) ;
#224594=VERTEX_POINT ( 'NONE', #139304 ) ;
#224604=DIRECTION ( 'NONE',  ( 0.000000000000000000, 0.000000000000000000, 1.000000000000000000 ) ) ;
#224607=VERTEX_POINT ( 'NONE', #201869 ) ;
#224624=CARTESIAN_POINT ( 'NONE',  ( -18.39999999999999858, -9.599999999988845900, -107.2001893912220964 ) ) ;
#224642=CARTESIAN_POINT ( 'NONE',  ( -18.50000000000000000, 9.250000000011157297, -88.25000000000005684 ) ) ;
#224643=VERTEX_POINT ( 'NONE', #235850 ) ;
#224658=CIRCLE ( 'NONE', #195660, 0.1000000000000008937 ) ;
#224664=VERTEX_POINT ( 'NONE', #121086 ) ;
#224670=DIRECTION ( 'NONE',  ( 0.000000000000000000, 0.000000000000000000, -1.000000000000000000 ) ) ;
#224684=ORIENTED_EDGE ( 'NONE', *, *, #73807, .F. ) ;
#224686=CIRCLE ( 'NONE', #45649, 0.09999999999999939493 ) ;
#224695=CARTESIAN_POINT ( 'NONE',  ( -20.85000000000000142, -1.736705739456431807, -112.0174225876237699 ) ) ;
#224702=ORIENTED_EDGE ( 'NONE', *, *, #41362, .T. ) ;
#224755=VERTEX_POINT ( 'NONE', #42800 ) ;
#224777=ORIENTED_EDGE ( 'NONE', *, *, #120984, .F. ) ;
#224802=ORIENTED_EDGE ( 'NONE', *, *, #144665, .T. ) ;
#224825=ORIENTED_EDGE ( 'NONE', *, *, #106163, .F. ) ;
#224826=CARTESIAN_POINT ( 'NONE',  ( 21.08750232978087524, 10.72486338602132250, -79.22885817299962241 ) ) ;
#224843=AXIS2_PLACEMENT_3D ( 'NONE', #7403, #201758, #126061 ) ;
#224859=EDGE_LOOP ( 'NONE', ( #67937, #179696, #32629, #129368 ) ) ;
#224867=ADVANCED_FACE ( 'NONE', ( #149623 ), #15238, .F. ) ;
#224877=EDGE_CURVE ( 'NONE', #149698, #75395, #224883, .T. ) ;
#224883=CIRCLE ( 'NONE', #150109, 0.1000000000000028644 ) ;
#224909=CARTESIAN_POINT ( 'NONE',  ( 21.14999999999999858, 8.786607556611267356, -79.35000000000005116 ) ) ;
#224937=DIRECTION ( 'NONE',  ( -1.000000000000000000, -0.000000000000000000, -0.000000000000000000 ) ) ;
#224973=DIRECTION ( 'NONE',  ( 4.377807931758638789E-15, 0.2605042016806672911, 0.9654727137038716656 ) ) ;
#224988=ORIENTED_EDGE ( 'NONE', *, *, #68420, .F. ) ;
#224989=ORIENTED_EDGE ( 'NONE', *, *, #102886, .F. ) ;
#224999=AXIS2_PLACEMENT_3D ( 'NONE', #94938, #174547, #113226 ) ;
#225004=SHAPE_REPRESENTATION_RELATIONSHIP ( 'NONE' , 'NONE' ,  #215063, #42038 ) ;
#225022=ORIENTED_EDGE ( 'NONE', *, *, #250068, .F. ) ;
#225023=CARTESIAN_POINT ( 'NONE',  ( 20.11144452914042091, 9.933610851134151432, -74.89029345395306336 ) ) ;
#225027=CARTESIAN_POINT ( 'NONE',  ( 20.95539060131842746, 10.62386215766680131, -74.65373381365624539 ) ) ;
#225046=AXIS2_PLACEMENT_3D ( 'NONE', #44375, #225530, #143452 ) ;
#225078=CARTESIAN_POINT ( 'NONE',  ( -20.54999999999999716, -8.999999999988844479, -91.00603087734759811 ) ) ;
#225079=DIRECTION ( 'NONE',  ( 0.000000000000000000, -0.5000000000000144329, -0.8660254037844302699 ) ) ;
#225106=AXIS2_PLACEMENT_3D ( 'NONE', #186576, #65320, #109574 ) ;
#225165=LINE ( 'NONE', #244737, #77236 ) ;
#225200=ORIENTED_EDGE ( 'NONE', *, *, #5967, .F. ) ;
#225223=DIRECTION ( 'NONE',  ( 0.000000000000000000, 0.000000000000000000, -1.000000000000000000 ) ) ;
#225240=ORIENTED_EDGE ( 'NONE', *, *, #102032, .T. ) ;
#225265=CARTESIAN_POINT ( 'NONE',  ( 23.24999999999999645, 2.100000000011158274, -100.5000000000000426 ) ) ;
#225289=DIRECTION ( 'NONE',  ( 0.000000000000000000, 0.000000000000000000, -1.000000000000000000 ) ) ;
#225310=DIRECTION ( 'NONE',  ( -0.000000000000000000, -0.000000000000000000, 1.000000000000000000 ) ) ;
#225351=AXIS2_PLACEMENT_3D ( 'NONE', #30101, #112208, #108335 ) ;
#225378=DIRECTION ( 'NONE',  ( 1.000000000000000000, 0.000000000000000000, -0.000000000000000000 ) ) ;
#225391=ORIENTED_EDGE ( 'NONE', *, *, #239344, .T. ) ;
#225398=CARTESIAN_POINT ( 'NONE',  ( 20.94999999999999929, 1.115600667400684642E-11, -104.5000000000000568 ) ) ;
#225436=ORIENTED_EDGE ( 'NONE', *, *, #227096, .F. ) ;
#225441=DIRECTION ( 'NONE',  ( 0.000000000000000000, 0.000000000000000000, -1.000000000000000000 ) ) ;
#225471=CARTESIAN_POINT ( 'NONE',  ( 20.94999999999999929, -11.64999999998883595, -97.50000000000004263 ) ) ;
#225498=CARTESIAN_POINT ( 'NONE',  ( 20.95512820512820440, 8.876151316299271343, -88.25000000000005684 ) ) ;
#225503=EDGE_LOOP ( 'NONE', ( #10396, #99871, #108001, #230421 ) ) ;
#225530=DIRECTION ( 'NONE',  ( 1.000000000000000000, -7.304098846218133681E-16, 0.000000000000000000 ) ) ;
#225531=CIRCLE ( 'NONE', #133974, 0.09999999999999484301 ) ;
#225534=AXIS2_PLACEMENT_3D ( 'NONE', #159134, #199541, #20907 ) ;
#225535=DIRECTION ( 'NONE',  ( -0.000000000000000000, -0.000000000000000000, 1.000000000000000000 ) ) ;
#225548=VERTEX_POINT ( 'NONE', #105662 ) ;
#225627=FACE_OUTER_BOUND ( 'NONE', #190406, .T. ) ;
#225634=EDGE_CURVE ( 'NONE', #195188, #68571, #86089, .T. ) ;
#225695=ORIENTED_EDGE ( 'NONE', *, *, #158026, .T. ) ;
#225718=FACE_OUTER_BOUND ( 'NONE', #65296, .T. ) ;
#225773=CARTESIAN_POINT ( 'NONE',  ( 23.15000000000000213, -9.599999999988845900, -76.89396912265249284 ) ) ;
#225780=ORIENTED_EDGE ( 'NONE', *, *, #61619, .T. ) ;
#225844=ORIENTED_EDGE ( 'NONE', *, *, #156421, .F. ) ;
#225847=EDGE_LOOP ( 'NONE', ( #45978, #198836, #113001, #72672, #117616 ) ) ;
#225864=DIRECTION ( 'NONE',  ( 0.000000000000000000, 0.000000000000000000, 1.000000000000000000 ) ) ;
#225886=ORIENTED_EDGE ( 'NONE', *, *, #238838, .T. ) ;
#225893=VERTEX_POINT ( 'NONE', #199364 ) ;
#225901=EDGE_LOOP ( 'NONE', ( #104380, #106341, #227450, #136048 ) ) ;
#225931=EDGE_CURVE ( 'NONE', #39964, #205600, #6263, .T. ) ;
#225937=LINE ( 'NONE', #228557, #46470 ) ;
#225944=DIRECTION ( 'NONE',  ( 2.952720810173289112E-16, -1.000000000000000000, 0.000000000000000000 ) ) ;
#225966=ORIENTED_EDGE ( 'NONE', *, *, #134222, .F. ) ;
#225971=VERTEX_POINT ( 'NONE', #10137 ) ;
#225992=CARTESIAN_POINT ( 'NONE',  ( 21.04999999999999716, 0.06570161033324389832, -60.74168394266798998 ) ) ;
#226000=CARTESIAN_POINT ( 'NONE',  ( 20.94999999999999574, 1.115600667400684642E-11, -67.00000000000004263 ) ) ;
#226023=DIRECTION ( 'NONE',  ( -1.000000000000000000, 0.000000000000000000, -0.000000000000000000 ) ) ;
#226030=ORIENTED_EDGE ( 'NONE', *, *, #110953, .F. ) ;
#226041=ORIENTED_EDGE ( 'NONE', *, *, #50554, .F. ) ;
#226055=AXIS2_PLACEMENT_3D ( 'NONE', #20153, #44532, #219608 ) ;
#226066=CARTESIAN_POINT ( 'NONE',  ( 20.92356734117541706, 10.31973158071402175, -106.0505334713354841 ) ) ;
#226070=LINE ( 'NONE', #245667, #40539 ) ;
#226086=CARTESIAN_POINT ( 'NONE',  ( -20.94999999999999929, -11.48912529306489994, -97.50000000000004263 ) ) ;
#226087=FACE_OUTER_BOUND ( 'NONE', #217293, .T. ) ;
#226112=DIRECTION ( 'NONE',  ( 0.000000000000000000, 0.000000000000000000, 1.000000000000000000 ) ) ;
#226127=AXIS2_PLACEMENT_3D ( 'NONE', #73491, #34363, #8360 ) ;
#226139=CARTESIAN_POINT ( 'NONE',  ( -21.05000000000000071, 6.300179817925684489, -66.94851711811826078 ) ) ;
#226174=CARTESIAN_POINT ( 'NONE',  ( 18.57399277249656322, 10.33112638556969820, -106.0901228926975080 ) ) ;
#226192=CARTESIAN_POINT ( 'NONE',  ( 18.49999999999999645, 1.115600667400684642E-11, -100.5000000000000426 ) ) ;
#226207=CIRCLE ( 'NONE', #109714, 0.1000000000000028644 ) ;
#226212=CIRCLE ( 'NONE', #30465, 0.09999999999999939493 ) ;
#226224=EDGE_CURVE ( 'NONE', #187394, #87663, #105385, .T. ) ;
#226234=CARTESIAN_POINT ( 'NONE',  ( 23.24999999999999289, 6.450000000011156587, -79.35000000000005116 ) ) ;
#226254=AXIS2_PLACEMENT_3D ( 'NONE', #150344, #69531, #189466 ) ;
#226264=CARTESIAN_POINT ( 'NONE',  ( 18.49999999999999289, 10.34378108836433263, -91.82844527787746358 ) ) ;
#226298=DIRECTION ( 'NONE',  ( 0.000000000000000000, 0.000000000000000000, -1.000000000000000000 ) ) ;
#226305=CARTESIAN_POINT ( 'NONE',  ( 20.97565083910961548, 10.47461740128996510, -74.57794317658860450 ) ) ;
#226309=CARTESIAN_POINT ( 'NONE',  ( 20.95265033839679347, 10.51225083247831371, -74.56576375603000884 ) ) ;
#226343=FACE_OUTER_BOUND ( 'NONE', #86922, .T. ) ;
#226351=CARTESIAN_POINT ( 'NONE',  ( -23.25000000000000000, -9.599999999988838795, -90.60603087734760663 ) ) ;
#226391=DIRECTION ( 'NONE',  ( 1.000000000000000000, -0.000000000000000000, -0.000000000000000000 ) ) ;
#226395=CARTESIAN_POINT ( 'NONE',  ( 21.05000000000000071, 1.115600667400684642E-11, -79.97500000000005116 ) ) ;
#226439=DIRECTION ( 'NONE',  ( -0.000000000000000000, -0.000000000000000000, 1.000000000000000000 ) ) ;
#226446=ORIENTED_EDGE ( 'NONE', *, *, #3250, .T. ) ;
#226460=CARTESIAN_POINT ( 'NONE',  ( 23.14999999999999503, 11.65000000001116298, -55.25000000000004974 ) ) ;
#226473=ORIENTED_EDGE ( 'NONE', *, *, #249459, .F. ) ;
#226513=DIRECTION ( 'NONE',  ( 0.000000000000000000, 2.664535259100315349E-15, 1.000000000000000000 ) ) ;
#226522=EDGE_LOOP ( 'NONE', ( #27764, #224777, #24097, #254359 ) ) ;
#226523=CARTESIAN_POINT ( 'NONE',  ( 21.05000000000000071, 1.115600667400684642E-11, -67.00000000000004263 ) ) ;
#226531=DIRECTION ( 'NONE',  ( 2.710505431213777355E-16, -1.000000000000000000, 0.000000000000000000 ) ) ;
#226548=VECTOR ( 'NONE', #243277, 1000.000000000000114 ) ;
#226561=ADVANCED_FACE ( 'NONE', ( #16271 ), #18801, .F. ) ;
#226589=FACE_OUTER_BOUND ( 'NONE', #218802, .T. ) ;
#226598=ORIENTED_EDGE ( 'NONE', *, *, #51259, .F. ) ;
#226643=ORIENTED_EDGE ( 'NONE', *, *, #125498, .T. ) ;
#226654=CARTESIAN_POINT ( 'NONE',  ( -21.44999999999999929, 7.350000000011155166, -88.25000000000005684 ) ) ;
#226722=CYLINDRICAL_SURFACE ( 'NONE', #249481, 0.09999999999999939493 ) ;
#226744=AXIS2_PLACEMENT_3D ( 'NONE', #23745, #203631, #118974 ) ;
#226748=ORIENTED_EDGE ( 'NONE', *, *, #196470, .T. ) ;
#226749=LINE ( 'NONE', #68992, #12271 ) ;
#226757=DIRECTION ( 'NONE',  ( 1.000000000000000000, -0.000000000000000000, -0.000000000000000000 ) ) ;
#226824=CARTESIAN_POINT ( 'NONE',  ( 20.99780126800942526, 11.60538868788779610, -93.58735257170532407 ) ) ;
#226845=CARTESIAN_POINT ( 'NONE',  ( 21.05000000000000071, -11.48912529306489994, -97.40000000000004832 ) ) ;
#226860=CARTESIAN_POINT ( 'NONE',  ( -18.59999999999999787, -9.480686695267820596, -107.4411151687578894 ) ) ;
#226928=CARTESIAN_POINT ( 'NONE',  ( 19.86930884467567182, 11.68691006698220392, -91.73922263893891227 ) ) ;
#226941=CIRCLE ( 'NONE', #131068, 0.1000000000000028644 ) ;
#226946=CARTESIAN_POINT ( 'NONE',  ( 23.15000000000000213, -11.74999999998883560, -97.40000000000004832 ) ) ;
#226956=CARTESIAN_POINT ( 'NONE',  ( 22.39999999999999858, 0.1000000000111554016, -59.20922040162665922 ) ) ;
#226966=FACE_OUTER_BOUND ( 'NONE', #4417, .T. ) ;
#226985=AXIS2_PLACEMENT_3D ( 'NONE', #28296, #110356, #107791 ) ;
#227010=PLANE ( 'NONE',  #150797 ) ;
#227034=FACE_OUTER_BOUND ( 'NONE', #215423, .T. ) ;
#227061=LINE ( 'NONE', #210094, #222125 ) ;
#227063=PLANE ( 'NONE',  #123971 ) ;
#227069=EDGE_LOOP ( 'NONE', ( #227963, #175289, #49492, #240321 ) ) ;
#227075=DIRECTION ( 'NONE',  ( -0.000000000000000000, -1.000000000000000000, -0.000000000000000000 ) ) ;
#227086=DIRECTION ( 'NONE',  ( 0.7071359030027680737, 0.7070776581709111719, 0.000000000000000000 ) ) ;
#227088=AXIS2_PLACEMENT_3D ( 'NONE', #33951, #170899, #74349 ) ;
#227089=EDGE_CURVE ( 'NONE', #177719, #64371, #13886, .T. ) ;
#227096=EDGE_CURVE ( 'NONE', #131327, #239872, #35284, .T. ) ;
#227128=CIRCLE ( 'NONE', #189558, 0.1000000000000028644 ) ;
#227136=EDGE_CURVE ( 'NONE', #72480, #96293, #143386, .T. ) ;
#227149=ORIENTED_EDGE ( 'NONE', *, *, #206958, .F. ) ;
#227158=CARTESIAN_POINT ( 'NONE',  ( -21.04999999999999361, 11.75000000001115374, -73.78386566297821503 ) ) ;
#227229=EDGE_CURVE ( 'NONE', #247770, #29779, #39367, .T. ) ;
#227247=VECTOR ( 'NONE', #120446, 1000.000000000000000 ) ;
#227266=DIRECTION ( 'NONE',  ( 6.938893903907222067E-15, -1.000000000000000000, -0.000000000000000000 ) ) ;
#227286=EDGE_CURVE ( 'NONE', #60211, #48905, #155022, .T. ) ;
#227351=AXIS2_PLACEMENT_3D ( 'NONE', #247660, #113283, #170747 ) ;
#227355=AXIS2_PLACEMENT_3D ( 'NONE', #68102, #112378, #69405 ) ;
#227358=CARTESIAN_POINT ( 'NONE',  ( 23.25000000000000355, -22.45632476061176774, -73.79389844773164953 ) ) ;
#227365=CARTESIAN_POINT ( 'NONE',  ( -21.44999999999999929, 7.350000000011155166, -79.35000000000005116 ) ) ;
#227414=ORIENTED_EDGE ( 'NONE', *, *, #216363, .T. ) ;
#227450=ORIENTED_EDGE ( 'NONE', *, *, #193392, .F. ) ;
#227451=CARTESIAN_POINT ( 'NONE',  ( -21.14999999999999858, 6.540656951712399803, -67.00000000000004263 ) ) ;
#227454=EDGE_CURVE ( 'NONE', #150237, #211426, #85272, .T. ) ;
#227474=DIRECTION ( 'NONE',  ( -1.000000000000000000, -2.952720810173289112E-16, 0.000000000000000000 ) ) ;
#227483=DIRECTION ( 'NONE',  ( 1.000000000000000000, 0.000000000000000000, 0.000000000000000000 ) ) ;
#227486=CARTESIAN_POINT ( 'NONE',  ( 22.45463910399148233, 1.026727559903907920E-11, -55.35042918981653060 ) ) ;
#227504=DIRECTION ( 'NONE',  ( -2.978066053179067751E-16, 1.000000000000000000, 0.000000000000000000 ) ) ;
#227505=ORIENTED_EDGE ( 'NONE', *, *, #237160, .F. ) ;
#227512=DIRECTION ( 'NONE',  ( -0.000000000000000000, 0.8660254037844502539, 0.4999999999999799050 ) ) ;
#227524=DIRECTION ( 'NONE',  ( 0.000000000000000000, -0.000000000000000000, 1.000000000000000000 ) ) ;
#227540=CIRCLE ( 'NONE', #115134, 0.2000000000000057288 ) ;
#227554=CARTESIAN_POINT ( 'NONE',  ( -21.05000000000000071, 1.750000000011155743, -78.66951155790169992 ) ) ;
#227563=CYLINDRICAL_SURFACE ( 'NONE', #89664, 11.74999999999999645 ) ;
#227599=CARTESIAN_POINT ( 'NONE',  ( 19.99999999999998934, 11.75000000001115907, -91.85000000000003695 ) ) ;
#227606=CARTESIAN_POINT ( 'NONE',  ( 20.41140022480507454, 10.41043084241319683, -74.61500130363459959 ) ) ;
#227610=CARTESIAN_POINT ( 'NONE',  ( 20.95017935633852346, 10.47548927963648246, -74.57743979739053941 ) ) ;
#227613=ORIENTED_EDGE ( 'NONE', *, *, #12921, .T. ) ;
#227618=ORIENTED_EDGE ( 'NONE', *, *, #175401, .F. ) ;
#227620=CARTESIAN_POINT ( 'NONE',  ( 18.59999999999999787, 1.866714910068465239, -78.75267524628205251 ) ) ;
#227627=DIRECTION ( 'NONE',  ( 0.000000000000000000, 0.000000000000000000, 1.000000000000000000 ) ) ;
#227657=ORIENTED_EDGE ( 'NONE', *, *, #10570, .F. ) ;
#227668=CIRCLE ( 'NONE', #127741, 0.1000000000000028644 ) ;
#227671=EDGE_CURVE ( 'NONE', #248044, #125649, #57239, .T. ) ;
#227682=CARTESIAN_POINT ( 'NONE',  ( 23.14999999999999503, 11.65000000001116298, -93.48519422934610645 ) ) ;
#227704=AXIS2_PLACEMENT_3D ( 'NONE', #64345, #86434, #225944 ) ;
#227725=AXIS2_PLACEMENT_3D ( 'NONE', #35291, #172237, #90066 ) ;
#227734=DIRECTION ( 'NONE',  ( 0.000000000000000000, 0.000000000000000000, -1.000000000000000000 ) ) ;
#227772=VECTOR ( 'NONE', #121526, 1000.000000000000000 ) ;
#227811=VECTOR ( 'NONE', #252075, 1000.000000000000000 ) ;
#227821=EDGE_CURVE ( 'NONE', #172403, #196915, #93863, .T. ) ;
#227833=FACE_OUTER_BOUND ( 'NONE', #47612, .T. ) ;
#227841=AXIS2_PLACEMENT_3D ( 'NONE', #36046, #173024, #137675 ) ;
#227859=CARTESIAN_POINT ( 'NONE',  ( 20.94999999999999574, -1.835341550213255957, -78.55515129256303908 ) ) ;
#227860=ADVANCED_FACE ( 'NONE', ( #72283 ), #174288, .T. ) ;
#227865=CYLINDRICAL_SURFACE ( 'NONE', #144616, 0.1000000000000028644 ) ;
#227870=DIRECTION ( 'NONE',  ( 0.000000000000000000, -0.8700118002898359348, 0.4930308989875165082 ) ) ;
#227893=CARTESIAN_POINT ( 'NONE',  ( 23.14999999999999503, 11.65000000001116298, -93.48519422934610645 ) ) ;
#227899=ORIENTED_EDGE ( 'NONE', *, *, #172412, .T. ) ;
#227903=CARTESIAN_POINT ( 'NONE',  ( -22.45437739390952459, 1.115486826172573664E-11, -55.35042918840623116 ) ) ;
#227911=AXIS2_PLACEMENT_3D ( 'NONE', #37439, #60815, #98629 ) ;
#227919=DIRECTION ( 'NONE',  ( 0.000000000000000000, 0.1495327102803586661, 0.9887567792719350601 ) ) ;
#227955=DIRECTION ( 'NONE',  ( 0.000000000000000000, 0.000000000000000000, -1.000000000000000000 ) ) ;
#227962=CIRCLE ( 'NONE', #65632, 6.258578643762710669 ) ;
#227963=ORIENTED_EDGE ( 'NONE', *, *, #87049, .F. ) ;
#227969=DIRECTION ( 'NONE',  ( 0.000000000000000000, 0.000000000000000000, -1.000000000000000000 ) ) ;
#227998=EDGE_CURVE ( 'NONE', #129928, #84058, #227128, .T. ) ;
#228003=DIRECTION ( 'NONE',  ( 0.000000000000000000, 0.000000000000000000, -1.000000000000000000 ) ) ;
#228075=CARTESIAN_POINT ( 'NONE',  ( -20.85000000000000142, 11.75000000001115197, -93.71613433702194129 ) ) ;
#228098=DIRECTION ( 'NONE',  ( 0.000000000000000000, 0.000000000000000000, -1.000000000000000000 ) ) ;
#228146=AXIS2_PLACEMENT_3D ( 'NONE', #75331, #153606, #53167 ) ;
#228149=EDGE_CURVE ( 'NONE', #50987, #54519, #243706, .T. ) ;
#228150=CARTESIAN_POINT ( 'NONE',  ( 21.05000000000000071, 1.115649653272650466E-11, -96.50000000000004263 ) ) ;
#228159=CARTESIAN_POINT ( 'NONE',  ( -18.48408745364664085, -9.664322258651962372, -107.1830785333284126 ) ) ;
#228182=DIRECTION ( 'NONE',  ( 1.000000000000000000, 3.469446951953704435E-14, -2.003086131649669752E-14 ) ) ;
#228183=AXIS2_PLACEMENT_3D ( 'NONE', #137786, #255128, #98633 ) ;
#228234=AXIS2_PLACEMENT_3D ( 'NONE', #171788, #10115, #149645 ) ;
#228274=DIRECTION ( 'NONE',  ( 0.000000000000000000, 0.000000000000000000, -1.000000000000000000 ) ) ;
#228311=DIRECTION ( 'NONE',  ( -0.000000000000000000, 0.1298341882520022694, 0.9915357197604853789 ) ) ;
#228357=CARTESIAN_POINT ( 'NONE',  ( -21.55000000000000426, 7.708578643773852157, -79.35000000000005116 ) ) ;
#228393=CIRCLE ( 'NONE', #66052, 11.65000000000000746 ) ;
#228398=EDGE_CURVE ( 'NONE', #232467, #147343, #77288, .T. ) ;
#228483=PLANE ( 'NONE',  #86954 ) ;
#228501=ORIENTED_EDGE ( 'NONE', *, *, #168203, .F. ) ;
#228523=EDGE_CURVE ( 'NONE', #72835, #3545, #69121, .T. ) ;
#228540=DIRECTION ( 'NONE',  ( -1.000000000000000000, -0.000000000000000000, -0.000000000000000000 ) ) ;
#228553=ORIENTED_EDGE ( 'NONE', *, *, #137639, .T. ) ;
#228557=CARTESIAN_POINT ( 'NONE',  ( -23.25000000000000000, 1.115650265596050101E-11, -62.95000000000004547 ) ) ;
#228558=DIRECTION ( 'NONE',  ( 0.000000000000000000, -1.265107689135680095E-16, 1.000000000000000000 ) ) ;
#228582=AXIS2_PLACEMENT_3D ( 'NONE', #28580, #108067, #130176 ) ;
#228589=VECTOR ( 'NONE', #104187, 1000.000000000000000 ) ;
#228623=AXIS2_PLACEMENT_3D ( 'NONE', #210807, #174300, #175554 ) ;
#228662=DIRECTION ( 'NONE',  ( -0.000000000000000000, 1.000000000000000000, 1.626303258728266709E-15 ) ) ;
#228670=EDGE_LOOP ( 'NONE', ( #143206, #256365, #69349, #238693 ) ) ;
#228688=ORIENTED_EDGE ( 'NONE', *, *, #154561, .T. ) ;
#228719=EDGE_CURVE ( 'NONE', #144504, #252694, #202827, .T. ) ;
#228738=DIRECTION ( 'NONE',  ( 0.000000000000000000, 0.000000000000000000, -1.000000000000000000 ) ) ;
#228743=CARTESIAN_POINT ( 'NONE',  ( 23.14999999999999858, 2.100000000011158274, -100.5000000000000426 ) ) ;
#228757=ORIENTED_EDGE ( 'NONE', *, *, #103227, .T. ) ;
#228798=CARTESIAN_POINT ( 'NONE',  ( 22.59999954896768770, -0.008828232233011105295, -55.24949132593204837 ) ) ;
#228800=CARTESIAN_POINT ( 'NONE',  ( -23.15000000000000213, 2.500000000011154633, -87.27537807723794572 ) ) ;
#228829=PLANE ( 'NONE',  #60895 ) ;
#228858=FACE_OUTER_BOUND ( 'NONE', #119523, .T. ) ;
#228868=CARTESIAN_POINT ( 'NONE',  ( 18.49999999999999289, 10.20857864609425825, -91.70250686562992826 ) ) ;
#228908=CARTESIAN_POINT ( 'NONE',  ( 20.95378194480896639, 10.53491199155394220, -74.56505414814790811 ) ) ;
#228924=FACE_OUTER_BOUND ( 'NONE', #26503, .T. ) ;
#228928=ADVANCED_FACE ( 'NONE', ( #69762, #33227 ), #228829, .F. ) ;
#228957=CIRCLE ( 'NONE', #141453, 0.5000000000000004441 ) ;
#228985=DIRECTION ( 'NONE',  ( 1.000000000000000000, 0.000000000000000000, 0.000000000000000000 ) ) ;
#229014=DIRECTION ( 'NONE',  ( 0.000000000000000000, 0.000000000000000000, 1.000000000000000000 ) ) ;
#229019=EDGE_CURVE ( 'NONE', #6865, #106717, #60434, .T. ) ;
#229028=CARTESIAN_POINT ( 'NONE',  ( -20.64999999999999858, 1.940186915899009490, -79.82911921105336717 ) ) ;
#229030=EDGE_CURVE ( 'NONE', #239916, #158987, #56730, .T. ) ;
#229036=ORIENTED_EDGE ( 'NONE', *, *, #29908, .F. ) ;
#229039=FACE_OUTER_BOUND ( 'NONE', #133620, .T. ) ;
#229049=CARTESIAN_POINT ( 'NONE',  ( -20.94999999999999929, -11.41227409413852989, -70.00000000000004263 ) ) ;
#229075=ORIENTED_EDGE ( 'NONE', *, *, #17504, .F. ) ;
#229082=DIRECTION ( 'NONE',  ( 0.7071067811865475727, 0.7071067811865475727, -0.000000000000000000 ) ) ;
#229094=AXIS2_PLACEMENT_3D ( 'NONE', #54214, #109053, #68663 ) ;
#229101=DIRECTION ( 'NONE',  ( -0.000000000000000000, -0.1350103645451876666, 0.9908441862701600211 ) ) ;
#229154=AXIS2_PLACEMENT_3D ( 'NONE', #208624, #239072, #60416 ) ;
#229162=ORIENTED_EDGE ( 'NONE', *, *, #30312, .F. ) ;
#229166=DIRECTION ( 'NONE',  ( 1.000000000000000000, 0.000000000000000000, -0.000000000000000000 ) ) ;
#229173=LINE ( 'NONE', #210882, #130177 ) ;
#229175=DIRECTION ( 'NONE',  ( 1.000000000000000000, 3.265361837132813093E-16, -0.000000000000000000 ) ) ;
#229201=DIRECTION ( 'NONE',  ( -1.000000000000000000, 0.000000000000000000, 0.000000000000000000 ) ) ;
#229214=LINE ( 'NONE', #10162, #119599 ) ;
#229220=ORIENTED_EDGE ( 'NONE', *, *, #19455, .F. ) ;
#229222=ORIENTED_EDGE ( 'NONE', *, *, #19664, .T. ) ;
#229273=FACE_OUTER_BOUND ( 'NONE', #54468, .T. ) ;
#229280=AXIS2_PLACEMENT_3D ( 'NONE', #142961, #189827, #167719 ) ;
#229282=FACE_OUTER_BOUND ( 'NONE', #205346, .T. ) ;
#229292=AXIS2_PLACEMENT_3D ( 'NONE', #103470, #104739, #181754 ) ;
#229315=DIRECTION ( 'NONE',  ( 0.000000000000000000, 0.000000000000000000, -1.000000000000000000 ) ) ;
#229341=DIRECTION ( 'NONE',  ( -0.000000000000000000, -0.000000000000000000, -1.000000000000000000 ) ) ;
#229352=PLANE ( 'NONE',  #136939 ) ;
#229355=DIRECTION ( 'NONE',  ( -0.000000000000000000, -0.000000000000000000, -1.000000000000000000 ) ) ;
#229367=DIRECTION ( 'NONE',  ( 0.000000000000000000, -1.000000000000000000, 2.775557561562888827E-14 ) ) ;
#229379=CARTESIAN_POINT ( 'NONE',  ( 21.14999999999999503, -0.09999999998884338825, -55.35042919245524473 ) ) ;
#229405=DIRECTION ( 'NONE',  ( 0.000000000000000000, 1.000000000000000000, 0.000000000000000000 ) ) ;
#229438=ORIENTED_EDGE ( 'NONE', *, *, #132732, .T. ) ;
#229471=DIRECTION ( 'NONE',  ( 1.000000000000000000, 0.000000000000000000, 0.000000000000000000 ) ) ;
#229475=DIRECTION ( 'NONE',  ( 1.000000000000000000, -0.000000000000000000, -0.000000000000000000 ) ) ;
#229491=CIRCLE ( 'NONE', #341, 0.1000000000000028644 ) ;
#229493=DIRECTION ( 'NONE',  ( 0.000000000000000000, 0.8700118002898322711, -0.4930308989875231696 ) ) ;
#229497=AXIS2_PLACEMENT_3D ( 'NONE', #44226, #202007, #179891 ) ;
#229538=EDGE_CURVE ( 'NONE', #18191, #39515, #23631, .T. ) ;
#229628=ORIENTED_EDGE ( 'NONE', *, *, #53447, .T. ) ;
#229640=CARTESIAN_POINT ( 'NONE',  ( -18.59999999999999787, 7.070967871809997973, -104.2465642218683541 ) ) ;
#229645=DIRECTION ( 'NONE',  ( 0.000000000000000000, 0.000000000000000000, -1.000000000000000000 ) ) ;
#229648=ADVANCED_FACE ( 'NONE', ( #61436 ), #140987, .F. ) ;
#229663=DIRECTION ( 'NONE',  ( -1.000000000000000000, 0.000000000000000000, 0.000000000000000000 ) ) ;
#229674=DIRECTION ( 'NONE',  ( 0.7070776581709139474, -0.7071359030027652981, -2.453168425935592377E-14 ) ) ;
#229683=EDGE_CURVE ( 'NONE', #6498, #78259, #146099, .T. ) ;
#229692=CIRCLE ( 'NONE', #100656, 12.87500000000000000 ) ;
#229704=DIRECTION ( 'NONE',  ( 1.000000000000000000, 0.000000000000000000, 0.000000000000000000 ) ) ;
#229708=DIRECTION ( 'NONE',  ( -0.000000000000000000, 0.8660254037844411501, 0.4999999999999956146 ) ) ;
#229734=ORIENTED_EDGE ( 'NONE', *, *, #97199, .F. ) ;
#229747=ORIENTED_EDGE ( 'NONE', *, *, #51045, .T. ) ;
#229766=VERTEX_POINT ( 'NONE', #10458 ) ;
#229775=DIRECTION ( 'NONE',  ( 0.000000000000000000, -1.000000000000000000, -0.000000000000000000 ) ) ;
#229788=ORIENTED_EDGE ( 'NONE', *, *, #204805, .T. ) ;
#229823=CIRCLE ( 'NONE', #221421, 0.09999999999999749367 ) ;
#229828=CIRCLE ( 'NONE', #34061, 11.74999999999999645 ) ;
#229871=ORIENTED_EDGE ( 'NONE', *, *, #79931, .T. ) ;
#229874=CYLINDRICAL_SURFACE ( 'NONE', #80505, 0.1000000000000028644 ) ;
#229882=CARTESIAN_POINT ( 'NONE',  ( 21.05000000000000071, 8.776282889879928106, -79.17621514106816960 ) ) ;
#229915=ORIENTED_EDGE ( 'NONE', *, *, #92352, .T. ) ;
#229927=CARTESIAN_POINT ( 'NONE',  ( 22.49533356619860669, 11.65000000631534149, -66.93487741967730642 ) ) ;
#229956=VERTEX_POINT ( 'NONE', #37742 ) ;
#229987=CIRCLE ( 'NONE', #68060, 0.1000000000000028644 ) ;
#230030=CARTESIAN_POINT ( 'NONE',  ( 20.94999999999999929, 1.360870587203197646, -75.07299792709100927 ) ) ;
#230035=DIRECTION ( 'NONE',  ( 0.000000000000000000, 0.000000000000000000, -1.000000000000000000 ) ) ;
#230047=VERTEX_POINT ( 'NONE', #222752 ) ;
#230055=DIRECTION ( 'NONE',  ( 0.000000000000000000, 0.1350103645451876666, -0.9908441862701600211 ) ) ;
#230064=CYLINDRICAL_SURFACE ( 'NONE', #90512, 0.1000000000000028644 ) ;
#230094=ORIENTED_EDGE ( 'NONE', *, *, #25365, .F. ) ;
#230102=VECTOR ( 'NONE', #148128, 1000.000000000000114 ) ;
#230117=CIRCLE ( 'NONE', #242584, 0.09999999999999939493 ) ;
#230130=CARTESIAN_POINT ( 'NONE',  ( 23.15000000000000213, -8.999999999988842703, -90.60603087734760663 ) ) ;
#230133=CARTESIAN_POINT ( 'NONE',  ( -20.94999999999999929, -11.74999999998884448, -69.90000000000004832 ) ) ;
#230143=ADVANCED_FACE ( 'NONE', ( #174063 ), #112765, .T. ) ;
#230149=DIRECTION ( 'NONE',  ( 0.000000000000000000, 0.000000000000000000, -1.000000000000000000 ) ) ;
#230177=CARTESIAN_POINT ( 'NONE',  ( 20.86036036209908318, 10.62104277658211693, -74.66634841850502369 ) ) ;
#230178=CARTESIAN_POINT ( 'NONE',  ( 18.49999999999999289, 10.20857864377385127, -91.65000000000004832 ) ) ;
#230200=ORIENTED_EDGE ( 'NONE', *, *, #50934, .T. ) ;
#230214=ORIENTED_EDGE ( 'NONE', *, *, #63485, .T. ) ;
#230230=CYLINDRICAL_SURFACE ( 'NONE', #13501, 0.1000000000000028644 ) ;
#230248=ORIENTED_EDGE ( 'NONE', *, *, #116767, .F. ) ;
#230249=DIRECTION ( 'NONE',  ( 0.000000000000000000, 0.000000000000000000, -1.000000000000000000 ) ) ;
#230257=DIRECTION ( 'NONE',  ( -1.000000000000000000, -2.952720810173289112E-16, 0.000000000000000000 ) ) ;
#230260=CARTESIAN_POINT ( 'NONE',  ( -20.85000000000000142, -1.835859311432479268, -112.0044391687985694 ) ) ;
#230263=CIRCLE ( 'NONE', #234363, 0.2000000000000057288 ) ;
#230265=CARTESIAN_POINT ( 'NONE',  ( -21.05000000000000071, 1.851028230152016674, -78.65391326942254580 ) ) ;
#230273=ORIENTED_EDGE ( 'NONE', *, *, #150074, .F. ) ;
#230289=FACE_OUTER_BOUND ( 'NONE', #67553, .T. ) ;
#230297=CARTESIAN_POINT ( 'NONE',  ( 20.85000000000000142, -1.164121893230052995, -108.4148480855716485 ) ) ;
#230304=CARTESIAN_POINT ( 'NONE',  ( 20.94999999999999929, 8.926614585098253229, -75.47168301922316402 ) ) ;
#230314=CIRCLE ( 'NONE', #188622, 0.1999999999999987899 ) ;
#230330=DIRECTION ( 'NONE',  ( 0.000000000000000000, 0.000000000000000000, -1.000000000000000000 ) ) ;
#230333=FACE_OUTER_BOUND ( 'NONE', #169197, .T. ) ;
#230349=CIRCLE ( 'NONE', #172149, 0.1000000000000028644 ) ;
#230352=EDGE_CURVE ( 'NONE', #77584, #230995, #186561, .T. ) ;
#230379=ADVANCED_FACE ( 'NONE', ( #59163 ), #95742, .T. ) ;
#230408=DIRECTION ( 'NONE',  ( -1.000000000000000000, -0.000000000000000000, 0.000000000000000000 ) ) ;
#230421=ORIENTED_EDGE ( 'NONE', *, *, #39855, .F. ) ;
#230428=LINE ( 'NONE', #71378, #135333 ) ;
#230434=ORIENTED_EDGE ( 'NONE', *, *, #20863, .F. ) ;
#230441=CYLINDRICAL_SURFACE ( 'NONE', #79166, 0.09999999999999939493 ) ;
#230460=EDGE_CURVE ( 'NONE', #14463, #177157, #140156, .T. ) ;
#230466=VECTOR ( 'NONE', #20404, 1000.000000000000000 ) ;
#230511=CIRCLE ( 'NONE', #138870, 0.09999999999999939493 ) ;
#230536=ORIENTED_EDGE ( 'NONE', *, *, #102886, .T. ) ;
#230542=CARTESIAN_POINT ( 'NONE',  ( 20.94999999999999574, -1.360870587180885716, -75.07299792709100927 ) ) ;
#230555=CARTESIAN_POINT ( 'NONE',  ( -23.25000000000000000, 1.115600667400684642E-11, -100.5000000000000426 ) ) ;
#230565=DIRECTION ( 'NONE',  ( 0.000000000000000000, 0.000000000000000000, -1.000000000000000000 ) ) ;
#230579=DIRECTION ( 'NONE',  ( 0.000000000000000000, -1.000000000000000000, 0.000000000000000000 ) ) ;
#230645=DIRECTION ( 'NONE',  ( 1.000000000000000000, -0.000000000000000000, -0.000000000000000000 ) ) ;
#230654=AXIS2_PLACEMENT_3D ( 'NONE', #80794, #42985, #25992 ) ;
#230661=DIRECTION ( 'NONE',  ( -0.000000000000000000, 0.000000000000000000, -1.000000000000000000 ) ) ;
#230679=ORIENTED_EDGE ( 'NONE', *, *, #200115, .T. ) ;
#230714=CARTESIAN_POINT ( 'NONE',  ( 18.59999999999999076, 10.20857864377385127, -91.65000000000004832 ) ) ;
#230723=EDGE_CURVE ( 'NONE', #74473, #217587, #35531, .T. ) ;
#230751=ORIENTED_EDGE ( 'NONE', *, *, #79950, .T. ) ;
#230764=ORIENTED_EDGE ( 'NONE', *, *, #19513, .T. ) ;
#230766=ORIENTED_EDGE ( 'NONE', *, *, #256666, .F. ) ;
#230774=DIRECTION ( 'NONE',  ( 0.000000000000000000, 0.000000000000000000, -1.000000000000000000 ) ) ;
#230782=AXIS2_PLACEMENT_3D ( 'NONE', #72645, #47910, #173054 ) ;
#230800=ORIENTED_EDGE ( 'NONE', *, *, #104327, .T. ) ;
#230821=DIRECTION ( 'NONE',  ( 1.000000000000000000, 0.000000000000000000, 0.000000000000000000 ) ) ;
#230862=AXIS2_PLACEMENT_3D ( 'NONE', #192624, #153544, #54386 ) ;
#230872=CARTESIAN_POINT ( 'NONE',  ( 20.85000000000000142, -11.64999999998883595, -100.5000000000000426 ) ) ;
#230917=DIRECTION ( 'NONE',  ( 0.000000000000000000, 0.000000000000000000, -1.000000000000000000 ) ) ;
#230932=CARTESIAN_POINT ( 'NONE',  ( 20.94999999999999574, -11.48912529306490349, -70.00000000000004263 ) ) ;
#230941=VERTEX_POINT ( 'NONE', #22310 ) ;
#230946=LINE ( 'NONE', #107116, #149309 ) ;
#230951=CARTESIAN_POINT ( 'NONE',  ( -20.94999999999999929, 14.05000000001115623, -94.98630492923912527 ) ) ;
#230969=FACE_OUTER_BOUND ( 'NONE', #78921, .T. ) ;
#230988=LINE ( 'NONE', #234819, #22643 ) ;
#230995=VERTEX_POINT ( 'NONE', #156694 ) ;
#231071=VERTEX_POINT ( 'NONE', #28756 ) ;
#231072=DIRECTION ( 'NONE',  ( 1.000000000000000000, 0.000000000000000000, 0.000000000000000000 ) ) ;
#231082=VERTEX_POINT ( 'NONE', #45694 ) ;
#231101=EDGE_LOOP ( 'NONE', ( #212107, #100833, #139641, #50729 ) ) ;
#231102=CARTESIAN_POINT ( 'NONE',  ( -18.59999999999999787, -1.835341550213255957, -78.55515129256302487 ) ) ;
#231113=DIRECTION ( 'NONE',  ( -0.000000000000000000, -0.000000000000000000, -1.000000000000000000 ) ) ;
#231117=EDGE_CURVE ( 'NONE', #246766, #100635, #57137, .T. ) ;
#231162=AXIS2_PLACEMENT_3D ( 'NONE', #103715, #4627, #159891 ) ;
#231204=CARTESIAN_POINT ( 'NONE',  ( -22.39999999999999858, 11.65000000001115588, -67.00000000000004263 ) ) ;
#231225=ADVANCED_FACE ( 'NONE', ( #148665 ), #153838, .F. ) ;
#231248=ORIENTED_EDGE ( 'NONE', *, *, #231462, .T. ) ;
#231261=ORIENTED_EDGE ( 'NONE', *, *, #44064, .T. ) ;
#231264=FACE_OUTER_BOUND ( 'NONE', #62342, .T. ) ;
#231297=EDGE_LOOP ( 'NONE', ( #146358, #10383, #73863, #218682 ) ) ;
#231311=CARTESIAN_POINT ( 'NONE',  ( 21.08376601933332495, 6.341947271286813681, -66.93622398907004367 ) ) ;
#231321=CIRCLE ( 'NONE', #168988, 12.97499999999999964 ) ;
#231339=FACE_OUTER_BOUND ( 'NONE', #219603, .T. ) ;
#231361=CARTESIAN_POINT ( 'NONE',  ( -18.40000000000000213, -9.519327731081286714, -73.97297637655937308 ) ) ;
#231380=DIRECTION ( 'NONE',  ( -7.304098846218201720E-16, 1.000000000000000000, 0.000000000000000000 ) ) ;
#231381=DIRECTION ( 'NONE',  ( 1.000000000000000000, 1.734723475976817507E-14, 0.000000000000000000 ) ) ;
#231393=ADVANCED_FACE ( 'NONE', ( #62388 ), #141910, .F. ) ;
#231434=DIRECTION ( 'NONE',  ( 1.000000000000000000, 2.952720810173289112E-16, -0.000000000000000000 ) ) ;
#231462=EDGE_CURVE ( 'NONE', #240894, #205206, #128277, .T. ) ;
#231472=DIRECTION ( 'NONE',  ( 0.000000000000000000, 0.000000000000000000, -1.000000000000000000 ) ) ;
#231544=DIRECTION ( 'NONE',  ( 0.000000000000000000, 1.000000000000000000, 0.000000000000000000 ) ) ;
#231554=CARTESIAN_POINT ( 'NONE',  ( 21.05995757104869526, 8.775389244732430427, -79.19490512299125839 ) ) ;
#231578=ORIENTED_EDGE ( 'NONE', *, *, #208721, .F. ) ;
#231585=ADVANCED_FACE ( 'NONE', ( #152221 ), #188742, .T. ) ;
#231587=AXIS2_PLACEMENT_3D ( 'NONE', #176119, #92694, #14480 ) ;
#231605=ORIENTED_EDGE ( 'NONE', *, *, #208445, .F. ) ;
#231619=CARTESIAN_POINT ( 'NONE',  ( 18.59999999999996945, 7.021664781911246322, -104.3335654018973315 ) ) ;
#231666=EDGE_CURVE ( 'NONE', #19842, #7494, #256352, .T. ) ;
#231673=CARTESIAN_POINT ( 'NONE',  ( 21.14999999999999858, 11.75000000001116263, -55.25000000000004974 ) ) ;
#231678=CARTESIAN_POINT ( 'NONE',  ( -23.15000000000000213, 2.600000000011154278, -87.27537807723794572 ) ) ;
#231686=CYLINDRICAL_SURFACE ( 'NONE', #77640, 2.000000000000001776 ) ;
#231698=ORIENTED_EDGE ( 'NONE', *, *, #233587, .F. ) ;
#231729=EDGE_LOOP ( 'NONE', ( #120000, #12242, #249612, #240019 ) ) ;
#231736=DIRECTION ( 'NONE',  ( -0.000000000000000000, 0.000000000000000000, -1.000000000000000000 ) ) ;
#231746=AXIS2_PLACEMENT_3D ( 'NONE', #142616, #123086, #207772 ) ;
#231747=EDGE_CURVE ( 'NONE', #10263, #111464, #49335, .T. ) ;
#231751=EDGE_CURVE ( 'NONE', #58672, #76466, #11771, .T. ) ;
#231761=EDGE_CURVE ( 'NONE', #179033, #240643, #236571, .T. ) ;
#231767=CARTESIAN_POINT ( 'NONE',  ( -22.50000000000094147, 0.1000000000110504439, -55.35042919245522341 ) ) ;
#231769=CARTESIAN_POINT ( 'NONE',  ( -20.94999999999999929, 1.115600667400684642E-11, -100.5000000000000426 ) ) ;
#231780=DIRECTION ( 'NONE',  ( 0.000000000000000000, 0.000000000000000000, -1.000000000000000000 ) ) ;
#231833=DIRECTION ( 'NONE',  ( 0.000000000000000000, 0.000000000000000000, 1.000000000000000000 ) ) ;
#231835=CARTESIAN_POINT ( 'NONE',  ( -20.64999999999999858, -8.999999999988844479, -90.60603087734760663 ) ) ;
#231884=CARTESIAN_POINT ( 'NONE',  ( -22.39999999999999858, 11.65000000001115588, -67.10000000000005116 ) ) ;
#231898=VERTEX_POINT ( 'NONE', #92863 ) ;
#231918=CARTESIAN_POINT ( 'NONE',  ( -21.46681500597357939, 1.115542391533913547E-11, -60.14248884056706146 ) ) ;
#231922=FACE_OUTER_BOUND ( 'NONE', #89276, .T. ) ;
#231932=EDGE_CURVE ( 'NONE', #76842, #181403, #175035, .T. ) ;
#231940=CARTESIAN_POINT ( 'NONE',  ( -18.59999999999999787, 1.162701749949165642, -75.10000000000003695 ) ) ;
#231954=AXIS2_PLACEMENT_3D ( 'NONE', #143499, #202201, #58805 ) ;
#232031=ORIENTED_EDGE ( 'NONE', *, *, #72837, .T. ) ;
#232036=FACE_OUTER_BOUND ( 'NONE', #252638, .T. ) ;
#232047=ORIENTED_EDGE ( 'NONE', *, *, #156421, .T. ) ;
#232057=CARTESIAN_POINT ( 'NONE',  ( 22.39999999999999503, 11.75000000001115552, -66.90000000000004832 ) ) ;
#232060=CARTESIAN_POINT ( 'NONE',  ( 18.50000000000000000, -9.399999999988843058, -74.29725975966333351 ) ) ;
#232162=DIRECTION ( 'NONE',  ( 0.000000000000000000, 0.000000000000000000, -1.000000000000000000 ) ) ;
#232175=AXIS2_PLACEMENT_3D ( 'NONE', #154550, #153271, #15023 ) ;
#232205=DIRECTION ( 'NONE',  ( 1.000000000000000000, -0.000000000000000000, -0.000000000000000000 ) ) ;
#232214=CIRCLE ( 'NONE', #227911, 0.09999999999999992228 ) ;
#232259=CIRCLE ( 'NONE', #228146, 0.1000000000000008937 ) ;
#232283=ORIENTED_EDGE ( 'NONE', *, *, #147035, .T. ) ;
#232303=EDGE_LOOP ( 'NONE', ( #50359, #115546, #148374, #197102 ) ) ;
#232336=VERTEX_POINT ( 'NONE', #11780 ) ;
#232361=ORIENTED_EDGE ( 'NONE', *, *, #193284, .F. ) ;
#232386=LINE ( 'NONE', #173728, #201138 ) ;
#232398=DIRECTION ( 'NONE',  ( 0.000000000000000000, 0.000000000000000000, -1.000000000000000000 ) ) ;
#232402=ORIENTED_EDGE ( 'NONE', *, *, #67321, .F. ) ;
#232440=AXIS2_PLACEMENT_3D ( 'NONE', #18580, #177680, #113817 ) ;
#232442=AXIS2_PLACEMENT_3D ( 'NONE', #226523, #47902, #247385 ) ;
#232457=CARTESIAN_POINT ( 'NONE',  ( 22.37643362114956247, 7.625789993969535274, -66.90091862631867059 ) ) ;
#232460=AXIS2_PLACEMENT_3D ( 'NONE', #20712, #21992, #216314 ) ;
#232467=VERTEX_POINT ( 'NONE', #220236 ) ;
#232470=ADVANCED_FACE ( 'NONE', ( #243630 ), #237143, .T. ) ;
#232478=VERTEX_POINT ( 'NONE', #85802 ) ;
#232480=EDGE_CURVE ( 'NONE', #196163, #255102, #253688, .T. ) ;
#232508=AXIS2_PLACEMENT_3D ( 'NONE', #152661, #108376, #91379 ) ;
#232514=APPLICATION_CONTEXT ( 'automotive_design' ) ;
#232525=EDGE_CURVE ( 'NONE', #202405, #247484, #224055, .T. ) ;
#232555=DIRECTION ( 'NONE',  ( 0.000000000000000000, -0.000000000000000000, 1.000000000000000000 ) ) ;
#232576=DIRECTION ( 'NONE',  ( 0.000000000000000000, -0.1298341882520124002, -0.9915357197604841577 ) ) ;
#232631=CARTESIAN_POINT ( 'NONE',  ( -22.39999999999999858, 1.115600667400684642E-11, -60.75000000000004974 ) ) ;
#232649=ORIENTED_EDGE ( 'NONE', *, *, #217735, .T. ) ;
#232659=LINE ( 'NONE', #59096, #159579 ) ;
#232677=EDGE_LOOP ( 'NONE', ( #1271, #116189, #199954, #44923, #173379, #224232, #95611 ) ) ;
#232678=CIRCLE ( 'NONE', #111876, 0.09999999999999939493 ) ;
#232718=CARTESIAN_POINT ( 'NONE',  ( 21.05000000000000071, 1.835341550235569663, -78.55515129256303908 ) ) ;
#232723=ORIENTED_EDGE ( 'NONE', *, *, #10570, .T. ) ;
#232734=CIRCLE ( 'NONE', #186760, 6.329289321881356400 ) ;
#232776=EDGE_LOOP ( 'NONE', ( #166250, #63623, #39053, #71047 ) ) ;
#232808=DIRECTION ( 'NONE',  ( -1.000000000000000000, 0.000000000000000000, 0.000000000000000000 ) ) ;
#232816=CARTESIAN_POINT ( 'NONE',  ( 18.59999999999999787, 5.900000000011102586, -77.21909976465646253 ) ) ;
#232855=CARTESIAN_POINT ( 'NONE',  ( -23.15000000000000213, 4.250000000011156409, -88.15000000000004832 ) ) ;
#232886=( BOUNDED_CURVE ( )  B_SPLINE_CURVE ( 3, ( #59668, #160106, #21864, #144335 ),
 .UNSPECIFIED., .F., .F. ) 
 B_SPLINE_CURVE_WITH_KNOTS ( ( 4, 4 ),
 ( 1.570796326794895448, 3.141592653589791784 ),
 .UNSPECIFIED. ) 
 CURVE ( )  GEOMETRIC_REPRESENTATION_ITEM ( )  RATIONAL_B_SPLINE_CURVE ( ( 1.000000000000000000, 0.8047378541243650485, 0.8047378541243650485, 1.000000000000000000 ) ) 
 REPRESENTATION_ITEM ( '' )  );
#232895=DIRECTION ( 'NONE',  ( -0.000000000000000000, -0.000000000000000000, -1.000000000000000000 ) ) ;
#232934=EDGE_CURVE ( 'NONE', #203901, #160493, #228957, .T. ) ;
#232974=DIRECTION ( 'NONE',  ( 0.000000000000000000, -1.000000000000000000, 0.000000000000000000 ) ) ;
#232990=EDGE_CURVE ( 'NONE', #81417, #36999, #224658, .T. ) ;
#233028=CYLINDRICAL_SURFACE ( 'NONE', #53280, 0.09999999999999939493 ) ;
#233042=ORIENTED_EDGE ( 'NONE', *, *, #64343, .F. ) ;
#233073=AXIS2_PLACEMENT_3D ( 'NONE', #77772, #56910, #136458 ) ;
#233075=EDGE_CURVE ( 'NONE', #189061, #95642, #150644, .T. ) ;
#233087=ORIENTED_EDGE ( 'NONE', *, *, #181239, .F. ) ;
#233091=VERTEX_POINT ( 'NONE', #95780 ) ;
#233121=AXIS2_PLACEMENT_3D ( 'NONE', #105711, #124036, #186583 ) ;
#233141=FACE_OUTER_BOUND ( 'NONE', #136723, .T. ) ;
#233153=CARTESIAN_POINT ( 'NONE',  ( -23.15000000000000213, 2.000000000011154189, -87.77537807723795993 ) ) ;
#233161=EDGE_LOOP ( 'NONE', ( #114853, #146018, #215675, #18572 ) ) ;
#233181=CARTESIAN_POINT ( 'NONE',  ( -20.87155475150660777, 11.75000000001115197, -93.59558652915730192 ) ) ;
#233197=CARTESIAN_POINT ( 'NONE',  ( -21.55000000000000071, 7.250000000011155521, -79.35000000000005116 ) ) ;
#233210=DIRECTION ( 'NONE',  ( 0.000000000000000000, 0.000000000000000000, -1.000000000000000000 ) ) ;
#233244=DIRECTION ( 'NONE',  ( 0.000000000000000000, -1.000000000000000000, 0.000000000000000000 ) ) ;
#233274=EDGE_CURVE ( 'NONE', #12719, #174189, #4391, .T. ) ;
#233276=DIRECTION ( 'NONE',  ( 0.000000000000000000, 0.000000000000000000, 1.000000000000000000 ) ) ;
#233280=CARTESIAN_POINT ( 'NONE',  ( 18.59999994388910238, -9.363566187059998214, -74.18111723680094372 ) ) ;
#233308=EDGE_CURVE ( 'NONE', #208354, #159539, #8459, .T. ) ;
#233321=EDGE_LOOP ( 'NONE', ( #181854, #80615, #99858, #223025 ) ) ;
#233324=CARTESIAN_POINT ( 'NONE',  ( 23.14999999999999858, 11.60000000001116227, -93.57179676972454274 ) ) ;
#233340=DIRECTION ( 'NONE',  ( -7.304098846218134667E-16, -1.000000000000000000, 0.000000000000000000 ) ) ;
#233348=CARTESIAN_POINT ( 'NONE',  ( 23.14999999999999858, -3.899999999988843502, -100.5000000000000426 ) ) ;
#233398=DIRECTION ( 'NONE',  ( 0.000000000000000000, 0.000000000000000000, -1.000000000000000000 ) ) ;
#233402=DIRECTION ( 'NONE',  ( 0.000000000000000000, 0.000000000000000000, -1.000000000000000000 ) ) ;
#233403=DIRECTION ( 'NONE',  ( 0.000000000000000000, 0.1575844902526835067, 0.9875055080513738259 ) ) ;
#233410=VERTEX_POINT ( 'NONE', #178598 ) ;
#233429=EDGE_CURVE ( 'NONE', #71547, #24899, #208300, .T. ) ;
#233432=AXIS2_PLACEMENT_3D ( 'NONE', #187659, #166825, #145927 ) ;
#233438=PLANE ( 'NONE',  #154665 ) ;
#233453=EDGE_CURVE ( 'NONE', #8169, #24665, #91764, .T. ) ;
#233454=CARTESIAN_POINT ( 'NONE',  ( -20.94999999999999929, 1.115600667400684642E-11, -67.00000000000004263 ) ) ;
#233468=CARTESIAN_POINT ( 'NONE',  ( 21.00000000000000000, 9.750000000011153745, -79.35000000000005116 ) ) ;
#233470=FACE_OUTER_BOUND ( 'NONE', #70768, .T. ) ;
#233478=DIRECTION ( 'NONE',  ( 0.000000000000000000, 0.1350103645451876666, -0.9908441862701600211 ) ) ;
#233482=EDGE_CURVE ( 'NONE', #179279, #223322, #244284, .T. ) ;
#233485=DIRECTION ( 'NONE',  ( 0.000000000000000000, 0.000000000000000000, 1.000000000000000000 ) ) ;
#233516=DIRECTION ( 'NONE',  ( 1.000000000000000000, 0.000000000000000000, 0.000000000000000000 ) ) ;
#233528=VERTEX_POINT ( 'NONE', #154237 ) ;
#233535=ORIENTED_EDGE ( 'NONE', *, *, #104727, .F. ) ;
#233587=EDGE_CURVE ( 'NONE', #4255, #119770, #50225, .T. ) ;
#233622=ADVANCED_FACE ( 'NONE', ( #3783 ), #102854, .T. ) ;
#233629=FACE_OUTER_BOUND ( 'NONE', #15804, .T. ) ;
#233637=CARTESIAN_POINT ( 'NONE',  ( -23.25000000000000000, 11.65000000001115588, -93.48519422934609224 ) ) ;
#233671=AXIS2_PLACEMENT_3D ( 'NONE', #139385, #218933, #200672 ) ;
#233689=VECTOR ( 'NONE', #139899, 1000.000000000000000 ) ;
#233701=VERTEX_POINT ( 'NONE', #32367 ) ;
#233715=VECTOR ( 'NONE', #117632, 1000.000000000000000 ) ;
#233718=CARTESIAN_POINT ( 'NONE',  ( -20.94999999999999929, 6.846123162363745074, -104.2377262668499043 ) ) ;
#233719=EDGE_LOOP ( 'NONE', ( #185199, #65189, #243703, #40852 ) ) ;
#233731=CARTESIAN_POINT ( 'NONE',  ( 21.07928932188134397, 6.328516656404459262, -66.90110485434564680 ) ) ;
#233790=CARTESIAN_POINT ( 'NONE',  ( -20.54999999999999716, 7.150000000011155876, -88.15000000000004832 ) ) ;
#233791=AXIS2_PLACEMENT_3D ( 'NONE', #202725, #24119, #173933 ) ;
#233812=DIRECTION ( 'NONE',  ( -1.000000000000000000, -3.265361837132813093E-16, 0.000000000000000000 ) ) ;
#233825=CARTESIAN_POINT ( 'NONE',  ( 21.14999999999999858, 1.115600667400684642E-11, -67.10000000000005116 ) ) ;
#233883=DIRECTION ( 'NONE',  ( 0.000000000000000000, 6.938893903907222067E-15, -1.000000000000000000 ) ) ;
#233909=DIRECTION ( 'NONE',  ( 0.000000000000000000, 1.000000000000000000, 0.000000000000000000 ) ) ;
#233910=CARTESIAN_POINT ( 'NONE',  ( -18.49346865148325492, -9.443073798513720973, -74.18519625531534700 ) ) ;
#233913=EDGE_CURVE ( 'NONE', #111692, #127795, #99970, .T. ) ;
#233927=TOROIDAL_SURFACE ( 'NONE', #229280, 11.65000000000000036, 0.1000000000000000056 ) ;
#234012=ORIENTED_EDGE ( 'NONE', *, *, #51746, .T. ) ;
#234048=VECTOR ( 'NONE', #175424, 1000.000000000000227 ) ;
#234083=CARTESIAN_POINT ( 'NONE',  ( -20.85000000000000142, 1.115600667400684642E-11, -100.5000000000000426 ) ) ;
#234091=AXIS2_PLACEMENT_3D ( 'NONE', #212131, #113021, #153480 ) ;
#234106=EDGE_LOOP ( 'NONE', ( #1688, #219027, #147859, #167016 ) ) ;
#234172=DIRECTION ( 'NONE',  ( 1.000000000000000000, 0.000000000000000000, 0.000000000000000000 ) ) ;
#234205=CARTESIAN_POINT ( 'NONE',  ( 21.05000000000000071, -9.499999999988844479, -90.60603087734760663 ) ) ;
#234222=CARTESIAN_POINT ( 'NONE',  ( -21.05000000000000071, -11.74999999998884448, -97.50000000000004263 ) ) ;
#234252=ORIENTED_EDGE ( 'NONE', *, *, #51115, .F. ) ;
#234254=CARTESIAN_POINT ( 'NONE',  ( 20.94999999999999574, -1.349084418615859482, -74.98649896354552880 ) ) ;
#234269=ORIENTED_EDGE ( 'NONE', *, *, #156655, .T. ) ;
#234278=CARTESIAN_POINT ( 'NONE',  ( -23.25000000000000000, 4.150000000011156764, -88.25000000000005684 ) ) ;
#234333=EDGE_LOOP ( 'NONE', ( #205338, #88941, #153390, #70474 ) ) ;
#234363=AXIS2_PLACEMENT_3D ( 'NONE', #193399, #117687, #218048 ) ;
#234394=AXIS2_PLACEMENT_3D ( 'NONE', #64313, #229493, #145114 ) ;
#234417=ADVANCED_FACE ( 'NONE', ( #106088 ), #21416, .T. ) ;
#234418=CARTESIAN_POINT ( 'NONE',  ( -21.44999999999999929, 7.350000000011155166, -79.35000000000005116 ) ) ;
#234427=DIRECTION ( 'NONE',  ( 0.000000000000000000, 0.000000000000000000, 1.000000000000000000 ) ) ;
#234434=DIRECTION ( 'NONE',  ( 0.000000000000000000, 1.000000000000000000, 0.000000000000000000 ) ) ;
#234436=VECTOR ( 'NONE', #137430, 1000.000000000000000 ) ;
#234467=DIRECTION ( 'NONE',  ( 1.000000000000000000, 0.000000000000000000, 0.000000000000000000 ) ) ;
#234471=TOROIDAL_SURFACE ( 'NONE', #159481, 11.65000000000000036, 0.1000000000000000056 ) ;
#234558=EDGE_CURVE ( 'NONE', #23243, #7494, #167179, .T. ) ;
#234577=ORIENTED_EDGE ( 'NONE', *, *, #47159, .F. ) ;
#234582=AXIS2_PLACEMENT_3D ( 'NONE', #235579, #250023, #56919 ) ;
#234585=CIRCLE ( 'NONE', #238877, 7.900000000000003908 ) ;
#234590=ORIENTED_EDGE ( 'NONE', *, *, #137973, .F. ) ;
#234591=DIRECTION ( 'NONE',  ( 0.000000000000000000, 0.000000000000000000, -1.000000000000000000 ) ) ;
#234595=CARTESIAN_POINT ( 'NONE',  ( 21.05000000000000071, 8.826429739528350638, -75.41405471294373797 ) ) ;
#234596=CARTESIAN_POINT ( 'NONE',  ( 18.31572054635740443, -9.548475435767665331, -107.3505701647485324 ) ) ;
#234598=CARTESIAN_POINT ( 'NONE',  ( 18.59999999999999432, 1.261786168576181755, -75.08649896354552311 ) ) ;
#234602=FACE_OUTER_BOUND ( 'NONE', #24014, .T. ) ;
#234605=AXIS2_PLACEMENT_3D ( 'NONE', #250445, #71834, #151372 ) ;
#234653=CARTESIAN_POINT ( 'NONE',  ( 20.94999999999999929, 1.115600667400684642E-11, -100.5000000000000426 ) ) ;
#234654=ORIENTED_EDGE ( 'NONE', *, *, #33845, .T. ) ;
#234688=AXIS2_PLACEMENT_3D ( 'NONE', #29368, #224937, #147991 ) ;
#234701=DIRECTION ( 'NONE',  ( 0.000000000000000000, 0.000000000000000000, 1.000000000000000000 ) ) ;
#234703=VECTOR ( 'NONE', #32131, 1000.000000000000000 ) ;
#234710=CARTESIAN_POINT ( 'NONE',  ( 20.85000000000000142, 1.115600667400684642E-11, -100.5000000000000426 ) ) ;
#234714=EDGE_CURVE ( 'NONE', #133700, #45318, #179628, .T. ) ;
#234722=FACE_OUTER_BOUND ( 'NONE', #65377, .T. ) ;
#234744=DIRECTION ( 'NONE',  ( -2.952720810173288619E-16, 1.000000000000000000, 0.000000000000000000 ) ) ;
#234777=CYLINDRICAL_SURFACE ( 'NONE', #220923, 0.09999999999999811817 ) ;
#234808=DIRECTION ( 'NONE',  ( 0.000000000000000000, 1.000000000000000000, 0.000000000000000000 ) ) ;
#234819=CARTESIAN_POINT ( 'NONE',  ( -18.59999999999999787, -1.249999999988843369, -108.3004807544151191 ) ) ;
#234882=ADVANCED_FACE ( 'NONE', ( #203990 ), #24104, .T. ) ;
#234891=TOROIDAL_SURFACE ( 'NONE', #172389, 0.2000000000000000111, 0.1000000000000000056 ) ;
#234907=DIRECTION ( 'NONE',  ( 1.000000000000000000, 0.000000000000000000, 0.000000000000000000 ) ) ;
#234932=VECTOR ( 'NONE', #208353, 1000.000000000000000 ) ;
#234942=DIRECTION ( 'NONE',  ( -1.836970198721029934E-16, 1.000000000000000000, 0.000000000000000000 ) ) ;
#234961=DIRECTION ( 'NONE',  ( 0.000000000000000000, 0.000000000000000000, -1.000000000000000000 ) ) ;
#234973=ORIENTED_EDGE ( 'NONE', *, *, #195377, .F. ) ;
#234977=VECTOR ( 'NONE', #34757, 1000.000000000000000 ) ;
#235029=CIRCLE ( 'NONE', #247494, 0.5000000000000004441 ) ;
#235051=LINE ( 'NONE', #56383, #203399 ) ;
#235096=ORIENTED_EDGE ( 'NONE', *, *, #197262, .F. ) ;
#235157=AXIS2_PLACEMENT_3D ( 'NONE', #7461, #86974, #166571 ) ;
#235167=CARTESIAN_POINT ( 'NONE',  ( 22.50000000000000000, 0.1000000000111554016, -55.35042919245524473 ) ) ;
#235181=DIRECTION ( 'NONE',  ( 0.000000000000000000, 0.000000000000000000, -1.000000000000000000 ) ) ;
#235191=CIRCLE ( 'NONE', #197572, 0.1000000000000028644 ) ;
#235226=CIRCLE ( 'NONE', #35363, 0.1000000000000008799 ) ;
#235236=CARTESIAN_POINT ( 'NONE',  ( 20.94999999999999929, -8.999999999988842703, -90.60603087734760663 ) ) ;
#235263=EDGE_CURVE ( 'NONE', #244178, #75223, #83697, .T. ) ;
#235270=DIRECTION ( 'NONE',  ( 0.000000000000000000, 1.776356839400310418E-15, -1.000000000000000000 ) ) ;
#235295=DIRECTION ( 'NONE',  ( 0.000000000000000000, 0.000000000000000000, 1.000000000000000000 ) ) ;
#235365=ADVANCED_FACE ( 'NONE', ( #223237 ), #62890, .F. ) ;
#235393=ORIENTED_EDGE ( 'NONE', *, *, #217932, .T. ) ;
#235433=CARTESIAN_POINT ( 'NONE',  ( -18.50000972452446035, 10.29326151435326508, -105.9592822510415431 ) ) ;
#235437=DIRECTION ( 'NONE',  ( 1.000000000000000000, 3.265361837132813093E-16, -0.000000000000000000 ) ) ;
#235450=CARTESIAN_POINT ( 'NONE',  ( 18.59999999999999076, -1.164121893230052995, -108.4148480855716485 ) ) ;
#235488=CARTESIAN_POINT ( 'NONE',  ( -21.08134388332232589, 0.07581891751813461811, -60.66531941948206708 ) ) ;
#235510=LINE ( 'NONE', #121998, #52273 ) ;
#235531=CARTESIAN_POINT ( 'NONE',  ( -18.59999999999999787, -9.399999999988851940, -107.3820418481727046 ) ) ;
#235539=ORIENTED_EDGE ( 'NONE', *, *, #99747, .T. ) ;
#235549=EDGE_LOOP ( 'NONE', ( #58189, #69704, #158024, #4961 ) ) ;
#235561=DIRECTION ( 'NONE',  ( -0.000000000000000000, 0.000000000000000000, -1.000000000000000000 ) ) ;
#235579=CARTESIAN_POINT ( 'NONE',  ( 21.14999999999999503, 11.65000000001116298, -67.10000000000005116 ) ) ;
#235609=CARTESIAN_POINT ( 'NONE',  ( -20.85000000000000142, 11.65000000001115232, -100.5000000000000426 ) ) ;
#235613=VERTEX_POINT ( 'NONE', #179983 ) ;
#235629=DIRECTION ( 'NONE',  ( 1.000000000000000000, 2.952720810173289112E-16, -0.000000000000000000 ) ) ;
#235632=DIRECTION ( 'NONE',  ( 0.000000000000000000, 0.000000000000000000, 1.000000000000000000 ) ) ;
#235644=AXIS2_PLACEMENT_3D ( 'NONE', #60873, #238229, #2173 ) ;
#235675=CARTESIAN_POINT ( 'NONE',  ( -23.15000000000000213, 1.115600667400684642E-11, -67.00000000000004263 ) ) ;
#235705=CARTESIAN_POINT ( 'NONE',  ( 21.06280952165552378, 10.62713230061206460, -79.20405388677831127 ) ) ;
#235723=AXIS2_PLACEMENT_3D ( 'NONE', #150512, #69700, #7121 ) ;
#235739=CARTESIAN_POINT ( 'NONE',  ( 20.94999999999999929, 1.115600667400684642E-11, -100.5000000000000426 ) ) ;
#235754=CARTESIAN_POINT ( 'NONE',  ( 21.05000000000000071, 5.400000000011154988, -90.60603087734760663 ) ) ;
#235773=CARTESIAN_POINT ( 'NONE',  ( -23.25000000000000000, -11.64999999998884483, -70.10000000000005116 ) ) ;
#235780=DIRECTION ( 'NONE',  ( 0.000000000000000000, 1.000000000000000000, 0.000000000000000000 ) ) ;
#235785=AXIS2_PLACEMENT_3D ( 'NONE', #241407, #221801, #204818 ) ;
#235805=CARTESIAN_POINT ( 'NONE',  ( 18.59999999999999787, 1.851028230152016674, -78.65391326942254580 ) ) ;
#235850=CARTESIAN_POINT ( 'NONE',  ( 20.94999999999999929, 7.120270961708750512, -104.1595630418393768 ) ) ;
#235879=DIRECTION ( 'NONE',  ( 0.000000000000000000, 1.084202172485510997E-13, -1.000000000000000000 ) ) ;
#235893=ADVANCED_FACE ( 'NONE', ( #251483 ), #63528, .T. ) ;
#235960=TOROIDAL_SURFACE ( 'NONE', #85906, 0.2000000000000000111, 0.1000000000000000056 ) ;
#235963=DIRECTION ( 'NONE',  ( 0.000000000000000000, -0.9654727137038715545, 0.2605042016806676242 ) ) ;
#235964=ORIENTED_EDGE ( 'NONE', *, *, #1272, .F. ) ;
#235970=DIRECTION ( 'NONE',  ( 0.000000000000000000, 8.881784197000605457E-16, -1.000000000000000000 ) ) ;
#235990=DIRECTION ( 'NONE',  ( -1.000000000000000000, 0.000000000000000000, 0.000000000000000000 ) ) ;
#235999=FACE_OUTER_BOUND ( 'NONE', #117102, .T. ) ;
#236009=CARTESIAN_POINT ( 'NONE',  ( -23.15000000000000213, 11.65000000001115588, -79.15000000000004832 ) ) ;
#236070=VERTEX_POINT ( 'NONE', #199229 ) ;
#236089=CARTESIAN_POINT ( 'NONE',  ( -20.85000000000000142, 11.75000000001115197, -93.65839931010299324 ) ) ;
#236096=DIRECTION ( 'NONE',  ( 0.7071067811865388020, -0.7071067811865561215, 0.000000000000000000 ) ) ;
#236097=DIRECTION ( 'NONE',  ( 0.000000000000000000, 0.000000000000000000, -1.000000000000000000 ) ) ;
#236101=ORIENTED_EDGE ( 'NONE', *, *, #100356, .F. ) ;
#236185=VERTEX_POINT ( 'NONE', #166541 ) ;
#236187=ORIENTED_EDGE ( 'NONE', *, *, #176207, .T. ) ;
#236227=ORIENTED_EDGE ( 'NONE', *, *, #177860, .T. ) ;
#236235=CARTESIAN_POINT ( 'NONE',  ( -23.25000000000000000, 7.021664781911246322, -104.3335654018973315 ) ) ;
#236268=CARTESIAN_POINT ( 'NONE',  ( -20.00857864376270001, 9.150000000011157653, -79.25000000000004263 ) ) ;
#236288=VERTEX_POINT ( 'NONE', #71284 ) ;
#236296=VERTEX_POINT ( 'NONE', #89524 ) ;
#236305=CARTESIAN_POINT ( 'NONE',  ( -18.50000000000000000, -1.164121893230052995, -108.4148480855716485 ) ) ;
#236314=EDGE_CURVE ( 'NONE', #248066, #173700, #201428, .T. ) ;
#236329=CARTESIAN_POINT ( 'NONE',  ( 20.99999999999997868, 1.115600667400684642E-11, -67.00000000000004263 ) ) ;
#236352=ORIENTED_EDGE ( 'NONE', *, *, #254966, .F. ) ;
#236353=CARTESIAN_POINT ( 'NONE',  ( 20.94999999999999929, 1.115600667400684642E-11, -100.5000000000000426 ) ) ;
#236382=ORIENTED_EDGE ( 'NONE', *, *, #256631, .F. ) ;
#236411=DIRECTION ( 'NONE',  ( 0.000000000000000000, 1.000000000000000000, 0.000000000000000000 ) ) ;
#236417=VECTOR ( 'NONE', #130278, 1000.000000000000000 ) ;
#236421=DIRECTION ( 'NONE',  ( 1.000000000000000000, -0.000000000000000000, -0.000000000000000000 ) ) ;
#236457=ORIENTED_EDGE ( 'NONE', *, *, #80902, .F. ) ;
#236463=ORIENTED_EDGE ( 'NONE', *, *, #208721, .T. ) ;
#236468=CARTESIAN_POINT ( 'NONE',  ( 21.14999999999999858, 11.65000000001116298, -55.25000000000004974 ) ) ;
#236478=DIRECTION ( 'NONE',  ( 1.000000000000000000, 0.000000000000000000, -0.000000000000000000 ) ) ;
#236493=DIRECTION ( 'NONE',  ( -1.000000000000000000, 0.000000000000000000, 0.000000000000000000 ) ) ;
#236499=VECTOR ( 'NONE', #107688, 1000.000000000000114 ) ;
#236511=CARTESIAN_POINT ( 'NONE',  ( -20.64999999999999858, -9.499999999988846255, -90.60603087734760663 ) ) ;
#236562=CARTESIAN_POINT ( 'NONE',  ( 21.87500000000000355, 9.750000000011153745, -88.25000000000005684 ) ) ;
#236570=ORIENTED_EDGE ( 'NONE', *, *, #110, .T. ) ;
#236571=CIRCLE ( 'NONE', #61808, 0.8750000000000007772 ) ;
#236579=DIRECTION ( 'NONE',  ( 0.000000000000000000, 0.000000000000000000, -1.000000000000000000 ) ) ;
#236602=EDGE_CURVE ( 'NONE', #155368, #233091, #1868, .T. ) ;
#236607=DIRECTION ( 'NONE',  ( 0.000000000000000000, -2.255140518769784599E-13, 1.000000000000000000 ) ) ;
#236643=AXIS2_PLACEMENT_3D ( 'NONE', #59751, #79323, #143149 ) ;
#236716=CARTESIAN_POINT ( 'NONE',  ( -18.58222699835055280, 10.33200063080771969, -106.0931674956643462 ) ) ;
#236732=ORIENTED_EDGE ( 'NONE', *, *, #188711, .F. ) ;
#236762=DIRECTION ( 'NONE',  ( 0.000000000000000000, -0.000000000000000000, -1.000000000000000000 ) ) ;
#236787=EDGE_CURVE ( 'NONE', #5531, #207164, #40542, .T. ) ;
#236793=ORIENTED_EDGE ( 'NONE', *, *, #42243, .T. ) ;
#236819=DIRECTION ( 'NONE',  ( -0.000000000000000000, -0.000000000000000000, 1.000000000000000000 ) ) ;
#236826=ORIENTED_EDGE ( 'NONE', *, *, #253111, .F. ) ;
#236847=DIRECTION ( 'NONE',  ( -1.000000000000000000, 0.000000000000000000, 0.000000000000000000 ) ) ;
#236934=DIRECTION ( 'NONE',  ( -1.000000000000000000, 7.304098846218133681E-16, -4.217023435051677994E-16 ) ) ;
#236959=AXIS2_PLACEMENT_3D ( 'NONE', #178362, #42671, #59635 ) ;
#236964=CIRCLE ( 'NONE', #33003, 0.1000000000000028644 ) ;
#236991=DIRECTION ( 'NONE',  ( 0.000000000000000000, 0.000000000000000000, -1.000000000000000000 ) ) ;
#237011=VERTEX_POINT ( 'NONE', #251527 ) ;
#237092=VERTEX_POINT ( 'NONE', #15518 ) ;
#237095=DIRECTION ( 'NONE',  ( -1.000000000000000000, 0.000000000000000000, 0.000000000000000000 ) ) ;
#237106=CIRCLE ( 'NONE', #112227, 0.2000000000000057288 ) ;
#237109=ORIENTED_EDGE ( 'NONE', *, *, #86334, .F. ) ;
#237110=DIRECTION ( 'NONE',  ( -1.000000000000000000, -3.265361837132813093E-16, 0.000000000000000000 ) ) ;
#237121=AXIS2_PLACEMENT_3D ( 'NONE', #181778, #143919, #244300 ) ;
#237143=CONICAL_SURFACE ( 'NONE', #28912, 7.750000000000027534, 0.7853981633974531640 ) ;
#237160=EDGE_CURVE ( 'NONE', #127382, #168864, #110399, .T. ) ;
#237175=EDGE_CURVE ( 'NONE', #243244, #230941, #18815, .T. ) ;
#237177=CARTESIAN_POINT ( 'NONE',  ( 18.36493879433202281, -9.500000806177402168, -107.4221486603551909 ) ) ;
#237178=EDGE_LOOP ( 'NONE', ( #48217, #44776 ) ) ;
#237191=ORIENTED_EDGE ( 'NONE', *, *, #124772, .T. ) ;
#237197=ORIENTED_EDGE ( 'NONE', *, *, #87621, .T. ) ;
#237216=EDGE_LOOP ( 'NONE', ( #107878, #100261, #145196, #232649 ) ) ;
#237298=LINE ( 'NONE', #99033, #120321 ) ;
#237313=CYLINDRICAL_SURFACE ( 'NONE', #4746, 0.09999999999999939493 ) ;
#237314=LINE ( 'NONE', #58644, #244699 ) ;
#237325=EDGE_CURVE ( 'NONE', #160493, #219071, #163994, .T. ) ;
#237328=VECTOR ( 'NONE', #67592, 1000.000000000000000 ) ;
#237408=EDGE_CURVE ( 'NONE', #75742, #52970, #114690, .T. ) ;
#237434=VERTEX_POINT ( 'NONE', #36041 ) ;
#237462=EDGE_CURVE ( 'NONE', #237818, #123901, #44149, .T. ) ;
#237519=CARTESIAN_POINT ( 'NONE',  ( 18.60000000000000853, -9.364236010355611484, -74.18025440072464960 ) ) ;
#237525=VECTOR ( 'NONE', #167036, 1000.000000000000000 ) ;
#237530=CARTESIAN_POINT ( 'NONE',  ( -21.05000000000000071, -1.162701749926853712, -75.00000000000004263 ) ) ;
#237584=DIRECTION ( 'NONE',  ( 0.000000000000000000, 0.9998779222360102414, 0.01562499999996356907 ) ) ;
#237644=ORIENTED_EDGE ( 'NONE', *, *, #58973, .T. ) ;
#237657=AXIS2_PLACEMENT_3D ( 'NONE', #18018, #177125, #81804 ) ;
#237671=ORIENTED_EDGE ( 'NONE', *, *, #4107, .T. ) ;
#237680=CIRCLE ( 'NONE', #191911, 0.1000000000000028644 ) ;
#237683=AXIS2_PLACEMENT_3D ( 'NONE', #237686, #59009, #1624 ) ;
#237686=CARTESIAN_POINT ( 'NONE',  ( -20.64999999999999858, 2.000000000011154189, -80.22462192276213955 ) ) ;
#237688=EDGE_CURVE ( 'NONE', #240985, #215522, #196374, .T. ) ;
#237691=CIRCLE ( 'NONE', #187821, 4.299999999999956302 ) ;
#237709=FACE_OUTER_BOUND ( 'NONE', #92562, .T. ) ;
#237719=DIRECTION ( 'NONE',  ( 1.000000000000000000, 7.304098846218134667E-16, -0.000000000000000000 ) ) ;
#237724=ORIENTED_EDGE ( 'NONE', *, *, #171600, .T. ) ;
#237729=ORIENTED_EDGE ( 'NONE', *, *, #174155, .T. ) ;
#237738=CARTESIAN_POINT ( 'NONE',  ( -20.64999999999999858, 1.925233644870972816, -79.73024353312617052 ) ) ;
#237745=VERTEX_POINT ( 'NONE', #181963 ) ;
#237756=CARTESIAN_POINT ( 'NONE',  ( -21.64999999999999858, 7.350000000011155166, -88.25000000000005684 ) ) ;
#237758=DIRECTION ( 'NONE',  ( -0.000000000000000000, 0.000000000000000000, 1.000000000000000000 ) ) ;
#237788=DIRECTION ( 'NONE',  ( 0.000000000000000000, 0.000000000000000000, 1.000000000000000000 ) ) ;
#237797=ADVANCED_FACE ( 'NONE', ( #71023 ), #252398, .T. ) ;
#237803=DIRECTION ( 'NONE',  ( -0.000000000000000000, 0.000000000000000000, -1.000000000000000000 ) ) ;
#237811=CARTESIAN_POINT ( 'NONE',  ( 20.04142135623730070, 11.75000000001115907, -91.65000000000004832 ) ) ;
#237818=VERTEX_POINT ( 'NONE', #228800 ) ;
#237835=AXIS2_PLACEMENT_3D ( 'NONE', #130454, #113460, #52190 ) ;
#237881=ORIENTED_EDGE ( 'NONE', *, *, #65544, .T. ) ;
#237892=EDGE_CURVE ( 'NONE', #233701, #184752, #173365, .T. ) ;
#237917=EDGE_CURVE ( 'NONE', #123588, #44645, #167123, .T. ) ;
#237948=B_SPLINE_CURVE_WITH_KNOTS ( 'NONE', 3,
 ( #102687, #3606, #242215, #63578, #222639, #123566, #203097, #89554 ),
 .UNSPECIFIED., .F., .F.,
 ( 4, 2, 2, 4 ),
 ( 0.000000000000000000, 0.0001049670497869917491, 0.0002099340995739834982, 0.0004198681991479925294 ),
 .UNSPECIFIED. ) ;
#237963=DIRECTION ( 'NONE',  ( 0.000000000000000000, 0.000000000000000000, -1.000000000000000000 ) ) ;
#237980=VERTEX_POINT ( 'NONE', #11893 ) ;
#237987=EDGE_LOOP ( 'NONE', ( #161816, #189644, #178284, #110163 ) ) ;
#238004=EDGE_LOOP ( 'NONE', ( #61039, #113981, #162582, #137138 ) ) ;
#238005=CARTESIAN_POINT ( 'NONE',  ( -18.51697539158857353, 10.31565961587945779, -106.0364194119178762 ) ) ;
#238035=DIRECTION ( 'NONE',  ( -1.000000000000000000, -2.952720810173289112E-16, 0.000000000000000000 ) ) ;
#238109=FACE_OUTER_BOUND ( 'NONE', #161758, .T. ) ;
#238121=ORIENTED_EDGE ( 'NONE', *, *, #163282, .F. ) ;
#238140=VECTOR ( 'NONE', #256133, 1000.000000000000000 ) ;
#238180=ORIENTED_EDGE ( 'NONE', *, *, #51115, .T. ) ;
#238192=EDGE_LOOP ( 'NONE', ( #236463, #187545, #3744, #107717 ) ) ;
#238229=DIRECTION ( 'NONE',  ( 1.000000000000000000, -0.000000000000000000, -0.000000000000000000 ) ) ;
#238251=CARTESIAN_POINT ( 'NONE',  ( -22.50000000000000000, 1.115600667400684642E-11, -66.90000000000004832 ) ) ;
#238271=( BOUNDED_CURVE ( )  B_SPLINE_CURVE ( 3, ( #157620, #119755, #61030, #97571 ),
 .UNSPECIFIED., .F., .F. ) 
 B_SPLINE_CURVE_WITH_KNOTS ( ( 4, 4 ),
 ( 3.141592653589793116, 4.712388980384689674 ),
 .UNSPECIFIED. ) 
 CURVE ( )  GEOMETRIC_REPRESENTATION_ITEM ( )  RATIONAL_B_SPLINE_CURVE ( ( 1.000000000000000000, 0.8047378541243649375, 0.8047378541243649375, 1.000000000000000000 ) ) 
 REPRESENTATION_ITEM ( '' )  );
#238276=CARTESIAN_POINT ( 'NONE',  ( -21.44999999999999929, 7.350000000011155166, -79.25000000000004263 ) ) ;
#238297=FACE_BOUND ( 'NONE', #124265, .T. ) ;
#238326=DIRECTION ( 'NONE',  ( 1.000000000000000000, 0.000000000000000000, 0.000000000000000000 ) ) ;
#238381=VERTEX_POINT ( 'NONE', #231204 ) ;
#238442=VECTOR ( 'NONE', #38682, 1000.000000000000114 ) ;
#238451=CARTESIAN_POINT ( 'NONE',  ( 18.44208962362733573, -9.552340496897292255, -107.3421730554639026 ) ) ;
#238474=ORIENTED_EDGE ( 'NONE', *, *, #116633, .T. ) ;
#238489=VERTEX_POINT ( 'NONE', #34298 ) ;
#238494=LINE ( 'NONE', #258004, #194259 ) ;
#238522=CIRCLE ( 'NONE', #26155, 11.70000000000000284 ) ;
#238537=CARTESIAN_POINT ( 'NONE',  ( -23.25000000000000000, 1.115600667400684642E-11, -67.00000000000004263 ) ) ;
#238545=VECTOR ( 'NONE', #179039, 1000.000000000000000 ) ;
#238557=EDGE_CURVE ( 'NONE', #211426, #45318, #45819, .T. ) ;
#238561=VECTOR ( 'NONE', #18239, 1000.000000000000000 ) ;
#238596=AXIS2_PLACEMENT_3D ( 'NONE', #192102, #228662, #8326 ) ;
#238599=AXIS2_PLACEMENT_3D ( 'NONE', #138464, #253294, #113789 ) ;
#238618=CARTESIAN_POINT ( 'NONE',  ( -18.50000000000000000, 11.75000000001115197, -55.25000000000004974 ) ) ;
#238633=TOROIDAL_SURFACE ( 'NONE', #179822, 11.70000000000000462, 0.1000000000000000056 ) ;
#238661=DIRECTION ( 'NONE',  ( -1.000000000000000000, -0.000000000000000000, -0.000000000000000000 ) ) ;
#238693=ORIENTED_EDGE ( 'NONE', *, *, #216413, .F. ) ;
#238704=ORIENTED_EDGE ( 'NONE', *, *, #155252, .F. ) ;
#238705=FACE_OUTER_BOUND ( 'NONE', #257574, .T. ) ;
#238715=VERTEX_POINT ( 'NONE', #186629 ) ;
#238720=ORIENTED_EDGE ( 'NONE', *, *, #35582, .T. ) ;
#238735=VERTEX_POINT ( 'NONE', #167088 ) ;
#238780=VECTOR ( 'NONE', #98718, 1000.000000000000000 ) ;
#238810=ORIENTED_EDGE ( 'NONE', *, *, #164468, .F. ) ;
#238811=DIRECTION ( 'NONE',  ( -1.000000000000000000, -0.000000000000000000, -0.000000000000000000 ) ) ;
#238817=CARTESIAN_POINT ( 'NONE',  ( -20.94983749550516450, 10.29766095125292402, -105.9743663933276139 ) ) ;
#238831=EDGE_LOOP ( 'NONE', ( #32897, #19051, #109461, #251441, #233087 ) ) ;
#238838=EDGE_CURVE ( 'NONE', #52970, #176730, #138173, .T. ) ;
#238845=CIRCLE ( 'NONE', #172252, 2.000000000000002665 ) ;
#238846=ORIENTED_EDGE ( 'NONE', *, *, #251487, .T. ) ;
#238848=ADVANCED_FACE ( 'NONE', ( #116078 ), #73754, .F. ) ;
#238862=ADVANCED_FACE ( 'NONE', ( #233470 ), #165304, .F. ) ;
#238877=AXIS2_PLACEMENT_3D ( 'NONE', #146543, #129582, #27942 ) ;
#238891=VECTOR ( 'NONE', #180023, 1000.000000000000114 ) ;
#238972=EDGE_LOOP ( 'NONE', ( #62443, #15304, #208258, #154832 ) ) ;
#238973=TOROIDAL_SURFACE ( 'NONE', #105655, 11.70000000000000107, 0.1000000000000000056 ) ;
#238987=AXIS2_PLACEMENT_3D ( 'NONE', #102352, #138907, #197630 ) ;
#239022=CARTESIAN_POINT ( 'NONE',  ( -21.05000000000000071, -1.261786168553869603, -75.08649896354552311 ) ) ;
#239030=DIRECTION ( 'NONE',  ( 0.000000000000000000, 0.000000000000000000, 1.000000000000000000 ) ) ;
#239038=TOROIDAL_SURFACE ( 'NONE', #84872, 12.97499999999999787, 0.1000000000000000056 ) ;
#239040=ADVANCED_FACE ( 'NONE', ( #181197 ), #123776, .F. ) ;
#239046=LINE ( 'NONE', #99502, #115748 ) ;
#239054=ORIENTED_EDGE ( 'NONE', *, *, #99353, .T. ) ;
#239061=ORIENTED_EDGE ( 'NONE', *, *, #171857, .F. ) ;
#239072=DIRECTION ( 'NONE',  ( 1.000000000000000000, -0.000000000000000000, -0.000000000000000000 ) ) ;
#239105=VECTOR ( 'NONE', #20935, 1000.000000000000000 ) ;
#239126=LINE ( 'NONE', #116607, #81276 ) ;
#239141=FACE_OUTER_BOUND ( 'NONE', #76182, .T. ) ;
#239157=ORIENTED_EDGE ( 'NONE', *, *, #254404, .T. ) ;
#239185=CARTESIAN_POINT ( 'NONE',  ( -22.60000000000080433, 0.04781698047652392647, -55.24997756884729938 ) ) ;
#239202=DIRECTION ( 'NONE',  ( -1.000000000000000000, 0.000000000000000000, 0.000000000000000000 ) ) ;
#239211=CARTESIAN_POINT ( 'NONE',  ( 18.49999999999999645, -1.299733671219632791, -57.02812952286944892 ) ) ;
#239250=EDGE_LOOP ( 'NONE', ( #217993, #221715, #122920, #117451, #67422, #83950 ) ) ;
#239344=EDGE_CURVE ( 'NONE', #61020, #135788, #86534, .T. ) ;
#239358=FACE_OUTER_BOUND ( 'NONE', #214970, .T. ) ;
#239360=ADVANCED_FACE ( 'NONE', ( #60905 ), #219985, .F. ) ;
#239394=ADVANCED_FACE ( 'NONE', ( #4762 ), #253145, .F. ) ;
#239408=EDGE_LOOP ( 'NONE', ( #224105, #210206, #100551, #224461 ) ) ;
#239446=DIRECTION ( 'NONE',  ( -1.000000000000000000, -0.000000000000000000, -0.000000000000000000 ) ) ;
#239468=EDGE_LOOP ( 'NONE', ( #41853, #217664, #97211, #77048 ) ) ;
#239487=ORIENTED_EDGE ( 'NONE', *, *, #131760, .T. ) ;
#239559=EDGE_CURVE ( 'NONE', #36418, #95156, #182445, .T. ) ;
#239560=DIRECTION ( 'NONE',  ( -1.000000000000000000, -0.000000000000000000, -0.000000000000000000 ) ) ;
#239568=DIRECTION ( 'NONE',  ( -1.000000000000000000, 0.000000000000000000, 0.000000000000000000 ) ) ;
#239584=CARTESIAN_POINT ( 'NONE',  ( -22.43310005002225438, 0.005636942152031573783, -55.35033787286564433 ) ) ;
#239603=VECTOR ( 'NONE', #124783, 1000.000000000000000 ) ;
#239620=AXIS2_PLACEMENT_3D ( 'NONE', #127102, #90533, #9715 ) ;
#239749=CARTESIAN_POINT ( 'NONE',  ( -21.07928932188134041, 6.328516656404449492, -66.90110485434564680 ) ) ;
#239759=EDGE_CURVE ( 'NONE', #124485, #256436, #4161, .T. ) ;
#239764=STYLED_ITEM ( 'NONE', ( #165058 ), #42038 ) ;
#239769=ORIENTED_EDGE ( 'NONE', *, *, #239903, .F. ) ;
#239799=TOROIDAL_SURFACE ( 'NONE', #14936, 11.65000000000000036, 0.1000000000000000056 ) ;
#239801=CARTESIAN_POINT ( 'NONE',  ( -22.48660254037843487, 11.65000000001115588, -66.95000000000005969 ) ) ;
#239816=CARTESIAN_POINT ( 'NONE',  ( -18.59999999999999787, 9.150000000011157653, -79.35000000000005116 ) ) ;
#239823=DIRECTION ( 'NONE',  ( 0.000000000000000000, 0.000000000000000000, -1.000000000000000000 ) ) ;
#239832=EDGE_LOOP ( 'NONE', ( #127724, #7254, #89314, #141871 ) ) ;
#239842=DIRECTION ( 'NONE',  ( 0.000000000000000000, 0.000000000000000000, -1.000000000000000000 ) ) ;
#239861=EDGE_CURVE ( 'NONE', #20178, #11297, #208797, .T. ) ;
#239872=VERTEX_POINT ( 'NONE', #229640 ) ;
#239886=AXIS2_PLACEMENT_3D ( 'NONE', #90649, #170256, #249742 ) ;
#239903=EDGE_CURVE ( 'NONE', #175744, #142448, #230946, .T. ) ;
#239915=PLANE ( 'NONE',  #85075 ) ;
#239916=VERTEX_POINT ( 'NONE', #212654 ) ;
#239963=CARTESIAN_POINT ( 'NONE',  ( 23.15000000000000213, -11.64999999998883595, -97.50000000000004263 ) ) ;
#239967=FACE_OUTER_BOUND ( 'NONE', #213931, .T. ) ;
#239975=DIRECTION ( 'NONE',  ( 0.000000000000000000, 0.000000000000000000, -1.000000000000000000 ) ) ;
#239982=DIRECTION ( 'NONE',  ( 1.000000000000000000, -0.000000000000000000, -0.000000000000000000 ) ) ;
#239995=ORIENTED_EDGE ( 'NONE', *, *, #118147, .T. ) ;
#240007=EDGE_LOOP ( 'NONE', ( #197621, #244790, #160372, #159435, #8139 ) ) ;
#240019=ORIENTED_EDGE ( 'NONE', *, *, #196470, .F. ) ;
#240027=CARTESIAN_POINT ( 'NONE',  ( -23.15000000000000213, 2.000000000011154189, -80.22462192276213955 ) ) ;
#240032=CARTESIAN_POINT ( 'NONE',  ( 19.97071067811864609, 11.72071067812981404, -91.75000000000005684 ) ) ;
#240104=CARTESIAN_POINT ( 'NONE',  ( -20.91682497891422798, 10.32263460347359363, -106.0605957968672328 ) ) ;
#240107=CARTESIAN_POINT ( 'NONE',  ( -18.59999999999999787, 1.866714910068465239, -78.75267524628205251 ) ) ;
#240110=ORIENTED_EDGE ( 'NONE', *, *, #112399, .T. ) ;
#240111=CIRCLE ( 'NONE', #190224, 0.3999999999999975797 ) ;
#240118=EDGE_CURVE ( 'NONE', #63545, #170195, #111893, .T. ) ;
#240137=VECTOR ( 'NONE', #57862, 1000.000000000000000 ) ;
#240156=ORIENTED_EDGE ( 'NONE', *, *, #58020, .T. ) ;
#240163=ORIENTED_EDGE ( 'NONE', *, *, #56740, .F. ) ;
#240177=DIRECTION ( 'NONE',  ( 0.000000000000000000, 0.000000000000000000, -1.000000000000000000 ) ) ;
#240178=EDGE_CURVE ( 'NONE', #78259, #29887, #162957, .T. ) ;
#240192=DIRECTION ( 'NONE',  ( -0.000000000000000000, -1.000000000000000000, -0.000000000000000000 ) ) ;
#240215=AXIS2_PLACEMENT_3D ( 'NONE', #175553, #254996, #78961 ) ;
#240216=VECTOR ( 'NONE', #244242, 1000.000000000000000 ) ;
#240247=DIRECTION ( 'NONE',  ( -1.000000000000000000, 0.000000000000000000, 0.000000000000000000 ) ) ;
#240273=TOROIDAL_SURFACE ( 'NONE', #215311, 0.2000000000000000111, 0.1000000000000000056 ) ;
#240321=ORIENTED_EDGE ( 'NONE', *, *, #30312, .T. ) ;
#240328=ORIENTED_EDGE ( 'NONE', *, *, #458, .T. ) ;
#240333=ADVANCED_FACE ( 'NONE', ( #48116 ), #50662, .F. ) ;
#240381=CARTESIAN_POINT ( 'NONE',  ( 21.05000000000000071, 1.115600667400684642E-11, -67.00000000000004263 ) ) ;
#240385=AXIS2_PLACEMENT_3D ( 'NONE', #108933, #93221, #89363 ) ;
#240403=CARTESIAN_POINT ( 'NONE',  ( 20.94999999999999929, 1.115600667400684642E-11, -100.5000000000000426 ) ) ;
#240456=ORIENTED_EDGE ( 'NONE', *, *, #155252, .T. ) ;
#240460=ADVANCED_FACE ( 'NONE', ( #238297, #83043 ), #220030, .T. ) ;
#240466=CARTESIAN_POINT ( 'NONE',  ( 21.05000000000000071, 6.258847123090224507, -66.96824164694493220 ) ) ;
#240492=DIRECTION ( 'NONE',  ( -1.000000000000000000, 0.000000000000000000, 0.000000000000000000 ) ) ;
#240545=ORIENTED_EDGE ( 'NONE', *, *, #195768, .F. ) ;
#240564=AXIS2_PLACEMENT_3D ( 'NONE', #64508, #185741, #183183 ) ;
#240582=ORIENTED_EDGE ( 'NONE', *, *, #51425, .F. ) ;
#240609=ORIENTED_EDGE ( 'NONE', *, *, #39372, .T. ) ;
#240624=CYLINDRICAL_SURFACE ( 'NONE', #240690, 12.87499999999999822 ) ;
#240639=CARTESIAN_POINT ( 'NONE',  ( 18.50000324121758055, 10.29307482169091870, -105.9586421466940038 ) ) ;
#240643=VERTEX_POINT ( 'NONE', #209443 ) ;
#240657=ORIENTED_EDGE ( 'NONE', *, *, #14471, .T. ) ;
#240664=ORIENTED_EDGE ( 'NONE', *, *, #131739, .T. ) ;
#240690=AXIS2_PLACEMENT_3D ( 'NONE', #159821, #698, #140215 ) ;
#240693=CYLINDRICAL_SURFACE ( 'NONE', #89930, 0.5000000000000004441 ) ;
#240698=ADVANCED_FACE ( 'NONE', ( #230289 ), #71246, .F. ) ;
#240702=CIRCLE ( 'NONE', #49164, 0.1000000000000028644 ) ;
#240739=AXIS2_PLACEMENT_3D ( 'NONE', #214092, #36779, #178858 ) ;
#240756=( LENGTH_UNIT ( ) NAMED_UNIT ( * ) SI_UNIT ( .MILLI., .METRE. ) );
#240772=DIRECTION ( 'NONE',  ( 0.000000000000000000, -1.000000000000000000, 0.000000000000000000 ) ) ;
#240790=DIRECTION ( 'NONE',  ( 0.000000000000000000, 0.000000000000000000, -1.000000000000000000 ) ) ;
#240804=LINE ( 'NONE', #156156, #180591 ) ;
#240846=DIRECTION ( 'NONE',  ( 1.000000000000000000, 0.000000000000000000, 0.000000000000000000 ) ) ;
#240894=VERTEX_POINT ( 'NONE', #241849 ) ;
#240896=DIRECTION ( 'NONE',  ( 0.000000000000000000, 0.000000000000000000, -1.000000000000000000 ) ) ;
#240898=ORIENTED_EDGE ( 'NONE', *, *, #127030, .F. ) ;
#240911=ORIENTED_EDGE ( 'NONE', *, *, #120704, .F. ) ;
#240985=VERTEX_POINT ( 'NONE', #179336 ) ;
#240990=AXIS2_PLACEMENT_3D ( 'NONE', #250362, #230821, #192965 ) ;
#240992=CARTESIAN_POINT ( 'NONE',  ( 21.97500000000000497, 9.750000000011153745, -88.25000000000005684 ) ) ;
#240998=DIRECTION ( 'NONE',  ( 2.952720810173289112E-16, -1.000000000000000000, 0.000000000000000000 ) ) ;
#241015=ORIENTED_EDGE ( 'NONE', *, *, #22818, .T. ) ;
#241063=CARTESIAN_POINT ( 'NONE',  ( -22.39999999999999858, 1.115486826172573664E-11, -55.35042919245524473 ) ) ;
#241117=AXIS2_PLACEMENT_3D ( 'NONE', #217663, #63748, #183710 ) ;
#241132=DIRECTION ( 'NONE',  ( -1.000000000000000000, -0.000000000000000000, 0.000000000000000000 ) ) ;
#241159=EDGE_LOOP ( 'NONE', ( #98495, #189387, #166407, #247259 ) ) ;
#241176=CARTESIAN_POINT ( 'NONE',  ( -20.94999999999999929, -11.29603075032412995, -70.04789915966391334 ) ) ;
#241181=CARTESIAN_POINT ( 'NONE',  ( -20.64999999999999858, 1.115600667400684642E-11, -100.5000000000000426 ) ) ;
#241203=EDGE_CURVE ( 'NONE', #175862, #253099, #190820, .T. ) ;
#241242=DIRECTION ( 'NONE',  ( 0.000000000000000000, 1.776356839400244943E-15, -1.000000000000000000 ) ) ;
#241250=CARTESIAN_POINT ( 'NONE',  ( -23.15000000000000213, 4.350000000011156054, -79.35000000000005116 ) ) ;
#241291=ADVANCED_FACE ( 'NONE', ( #46864 ), #74487, .T. ) ;
#241302=ORIENTED_EDGE ( 'NONE', *, *, #22695, .F. ) ;
#241338=DIRECTION ( 'NONE',  ( 1.000000000000000000, 0.000000000000000000, 0.000000000000000000 ) ) ;
#241342=SPHERICAL_SURFACE ( 'NONE', #117584, 0.1000000000000000056 ) ;
#241364=EDGE_LOOP ( 'NONE', ( #176118, #173355, #147115, #78655, #71139, #106526 ) ) ;
#241374=CARTESIAN_POINT ( 'NONE',  ( 21.05000000000000071, -8.663551401857999323, -90.97589888193273566 ) ) ;
#241386=CARTESIAN_POINT ( 'NONE',  ( -18.59999999999999787, 1.162701749949165642, -75.10000000000003695 ) ) ;
#241393=CARTESIAN_POINT ( 'NONE',  ( 21.05000000000000071, 6.257814610487280937, -66.90220970869124528 ) ) ;
#241407=CARTESIAN_POINT ( 'NONE',  ( -20.64999999999999858, 1.115600667400684642E-11, -100.5000000000000426 ) ) ;
#241412=CARTESIAN_POINT ( 'NONE',  ( -21.05000000000000071, -0.08579911626297563598, -60.58602111851162419 ) ) ;
#241478=EDGE_CURVE ( 'NONE', #178965, #117385, #124337, .T. ) ;
#241519=CYLINDRICAL_SURFACE ( 'NONE', #84656, 0.09999999999999781286 ) ;
#241573=ORIENTED_EDGE ( 'NONE', *, *, #206634, .F. ) ;
#241575=CARTESIAN_POINT ( 'NONE',  ( -18.59999999999999787, 11.65000000001115232, -74.01480577065404987 ) ) ;
#241581=ORIENTED_EDGE ( 'NONE', *, *, #137171, .T. ) ;
#241599=VERTEX_POINT ( 'NONE', #46425 ) ;
#241640=AXIS2_PLACEMENT_3D ( 'NONE', #156339, #136725, #216261 ) ;
#241658=DIRECTION ( 'NONE',  ( 1.836970198721029934E-16, -1.000000000000000000, -0.000000000000000000 ) ) ;
#241678=DIRECTION ( 'NONE',  ( 0.000000000000000000, 0.000000000000000000, 1.000000000000000000 ) ) ;
#241695=DIRECTION ( 'NONE',  ( 0.000000000000000000, 0.000000000000000000, -1.000000000000000000 ) ) ;
#241715=DIRECTION ( 'NONE',  ( 0.000000000000000000, 1.000000000000000000, 0.000000000000000000 ) ) ;
#241735=DIRECTION ( 'NONE',  ( 0.000000000000000000, 0.000000000000000000, -1.000000000000000000 ) ) ;
#241751=EDGE_CURVE ( 'NONE', #76466, #82405, #154937, .T. ) ;
#241758=DIRECTION ( 'NONE',  ( 0.000000000000000000, 0.000000000000000000, -1.000000000000000000 ) ) ;
#241804=ORIENTED_EDGE ( 'NONE', *, *, #167585, .F. ) ;
#241827=CARTESIAN_POINT ( 'NONE',  ( 21.14261333020286671, 10.71569264926606202, -79.25000000000027001 ) ) ;
#241849=CARTESIAN_POINT ( 'NONE',  ( 21.05000000000000071, -8.663551401858002876, -76.52410111806734960 ) ) ;
#241850=DIRECTION ( 'NONE',  ( 0.000000000000000000, 0.000000000000000000, -1.000000000000000000 ) ) ;
#241878=VERTEX_POINT ( 'NONE', #12186 ) ;
#241892=CARTESIAN_POINT ( 'NONE',  ( -18.59999999999999787, 11.65000000001115232, -55.25000000000004974 ) ) ;
#241898=ORIENTED_EDGE ( 'NONE', *, *, #223931, .T. ) ;
#241943=CARTESIAN_POINT ( 'NONE',  ( -21.05000000000000071, 1.115600667400684642E-11, -100.5000000000000426 ) ) ;
#241988=LINE ( 'NONE', #62077, #93548 ) ;
#242037=EDGE_LOOP ( 'NONE', ( #207005, #68143, #9734, #229788 ) ) ;
#242042=CYLINDRICAL_SURFACE ( 'NONE', #93642, 2.000000000000001776 ) ;
#242045=VECTOR ( 'NONE', #70687, 1000.000000000000000 ) ;
#242053=CARTESIAN_POINT ( 'NONE',  ( 21.53752568617671415, 6.786807874515035977, -66.90102553872934266 ) ) ;
#242093=VERTEX_POINT ( 'NONE', #197209 ) ;
#242094=DIRECTION ( 'NONE',  ( 1.000000000000000000, 0.000000000000000000, 0.000000000000000000 ) ) ;
#242132=CARTESIAN_POINT ( 'NONE',  ( -22.45372860728439690, 0.01492061955964465135, -55.35020286529617550 ) ) ;
#242137=DIRECTION ( 'NONE',  ( -1.000000000000000000, 7.304098846218134667E-16, -4.217023435051678980E-16 ) ) ;
#242195=ORIENTED_EDGE ( 'NONE', *, *, #67340, .F. ) ;
#242215=CARTESIAN_POINT ( 'NONE',  ( -18.46902351632713035, -9.509470118669714367, -73.98645393425734085 ) ) ;
#242223=CARTESIAN_POINT ( 'NONE',  ( -20.94999999999999929, -1.164121893230052995, -108.4148480855716485 ) ) ;
#242226=FACE_OUTER_BOUND ( 'NONE', #212666, .T. ) ;
#242235=CARTESIAN_POINT ( 'NONE',  ( -18.59999999999999787, -1.835859311432481045, -112.0044391687985694 ) ) ;
#242241=ORIENTED_EDGE ( 'NONE', *, *, #238557, .T. ) ;
#242296=CARTESIAN_POINT ( 'NONE',  ( 21.08479644141222309, 0.05855444257529583002, -60.65496134226815172 ) ) ;
#242298=CARTESIAN_POINT ( 'NONE',  ( -21.22070241538126112, 6.469946272880768845, -66.90108096946502769 ) ) ;
#242301=AXIS2_PLACEMENT_3D ( 'NONE', #144510, #67557, #42866 ) ;
#242304=CIRCLE ( 'NONE', #129867, 11.65000000000000746 ) ;
#242335=ORIENTED_EDGE ( 'NONE', *, *, #8448, .T. ) ;
#242403=ORIENTED_EDGE ( 'NONE', *, *, #99950, .T. ) ;
#242409=DIRECTION ( 'NONE',  ( 1.000000000000000000, -0.000000000000000000, -0.000000000000000000 ) ) ;
#242446=AXIS2_PLACEMENT_3D ( 'NONE', #178840, #79680, #159259 ) ;
#242450=ORIENTED_EDGE ( 'NONE', *, *, #154914, .F. ) ;
#242484=CARTESIAN_POINT ( 'NONE',  ( -20.94999999999999929, -11.48912529306489994, -97.40000000000004832 ) ) ;
#242485=CARTESIAN_POINT ( 'NONE',  ( 22.50000000000000000, 1.115600667400684642E-11, -67.00000000000004263 ) ) ;
#242496=FACE_OUTER_BOUND ( 'NONE', #103336, .T. ) ;
#242521=VERTEX_POINT ( 'NONE', #183767 ) ;
#242523=VERTEX_POINT ( 'NONE', #62536 ) ;
#242537=ORIENTED_EDGE ( 'NONE', *, *, #61753, .T. ) ;
#242568=AXIS2_PLACEMENT_3D ( 'NONE', #88426, #109287, #188839 ) ;
#242584=AXIS2_PLACEMENT_3D ( 'NONE', #69067, #88587, #191595 ) ;
#242599=VERTEX_POINT ( 'NONE', #125086 ) ;
#242678=AXIS2_PLACEMENT_3D ( 'NONE', #224909, #188370, #7149 ) ;
#242708=EDGE_LOOP ( 'NONE', ( #52978, #253630, #52961, #29036 ) ) ;
#242754=CARTESIAN_POINT ( 'NONE',  ( 21.00000000000000000, 9.750000000011153745, -88.25000000000005684 ) ) ;
#242759=TOROIDAL_SURFACE ( 'NONE', #46931, 11.70000000000000639, 0.1000000000000000056 ) ;
#242800=EDGE_CURVE ( 'NONE', #100635, #168456, #114496, .T. ) ;
#242825=CIRCLE ( 'NONE', #176214, 0.1000000000000028644 ) ;
#242837=DIRECTION ( 'NONE',  ( -0.000000000000000000, 0.6132151058540549204, -0.7899159663865520375 ) ) ;
#242868=VECTOR ( 'NONE', #210340, 1000.000000000000000 ) ;
#242894=CARTESIAN_POINT ( 'NONE',  ( -23.15000000000000213, 1.115650265596050101E-11, -62.95000000000004547 ) ) ;
#242915=EDGE_CURVE ( 'NONE', #60211, #150205, #162664, .T. ) ;
#242937=EDGE_CURVE ( 'NONE', #13140, #238715, #50207, .T. ) ;
#242943=ORIENTED_EDGE ( 'NONE', *, *, #41362, .F. ) ;
#242972=CARTESIAN_POINT ( 'NONE',  ( 18.49999999999999645, 1.115600667400684642E-11, -67.00000000000004263 ) ) ;
#242992=EDGE_CURVE ( 'NONE', #115244, #221121, #221271, .T. ) ;
#242995=VERTEX_POINT ( 'NONE', #66061 ) ;
#243027=EDGE_CURVE ( 'NONE', #12745, #34181, #237680, .T. ) ;
#243033=AXIS2_PLACEMENT_3D ( 'NONE', #249148, #107028, #69231 ) ;
#243034=ORIENTED_EDGE ( 'NONE', *, *, #45419, .F. ) ;
#243038=DIRECTION ( 'NONE',  ( 1.000000000000000000, -0.000000000000000000, -0.000000000000000000 ) ) ;
#243050=CARTESIAN_POINT ( 'NONE',  ( -23.25000000000000000, 1.115600667400684642E-11, -67.00000000000004263 ) ) ;
#243058=DIRECTION ( 'NONE',  ( 0.000000000000000000, -1.000000000000000000, -1.734723475976807292E-15 ) ) ;
#243063=ADVANCED_FACE ( 'NONE', ( #63484 ), #203004, .T. ) ;
#243067=ORIENTED_EDGE ( 'NONE', *, *, #51746, .F. ) ;
#243106=CIRCLE ( 'NONE', #205501, 12.97499999999999964 ) ;
#243162=EDGE_LOOP ( 'NONE', ( #193263, #88826, #206931, #60774 ) ) ;
#243209=CIRCLE ( 'NONE', #89273, 0.1999999999999996503 ) ;
#243211=EDGE_CURVE ( 'NONE', #187354, #61933, #54503, .T. ) ;
#243220=TOROIDAL_SURFACE ( 'NONE', #218268, 0.2000000000000000111, 0.1000000000000000056 ) ;
#243240=CIRCLE ( 'NONE', #130832, 0.09999999999999939493 ) ;
#243244=VERTEX_POINT ( 'NONE', #175463 ) ;
#243245=EDGE_CURVE ( 'NONE', #32089, #18615, #137874, .T. ) ;
#243274=AXIS2_PLACEMENT_3D ( 'NONE', #30249, #34125, #210165 ) ;
#243277=DIRECTION ( 'NONE',  ( 0.7071067811865474617, 0.7071067811865474617, 2.044391222244499837E-16 ) ) ;
#243290=CARTESIAN_POINT ( 'NONE',  ( -18.50000000000000000, 1.115600667400684642E-11, -67.00000000000004263 ) ) ;
#243319=CARTESIAN_POINT ( 'NONE',  ( 20.95575313997065336, 10.61455330328599089, -74.62129070194487213 ) ) ;
#243356=DIRECTION ( 'NONE',  ( -0.000000000000000000, 1.000000000000000000, 0.000000000000000000 ) ) ;
#243363=DIRECTION ( 'NONE',  ( 0.000000000000000000, 0.000000000000000000, -1.000000000000000000 ) ) ;
#243382=DIRECTION ( 'NONE',  ( -1.000000000000000000, 0.000000000000000000, 0.000000000000000000 ) ) ;
#243385=CIRCLE ( 'NONE', #97614, 0.1000000000000000472 ) ;
#243394=CARTESIAN_POINT ( 'NONE',  ( 21.05000000000000071, 5.850000000011156942, -90.36750277572211587 ) ) ;
#243406=DIRECTION ( 'NONE',  ( 0.000000000000000000, 0.000000000000000000, -1.000000000000000000 ) ) ;
#243412=AXIS2_PLACEMENT_3D ( 'NONE', #98092, #177702, #57701 ) ;
#243414=EDGE_CURVE ( 'NONE', #6865, #143962, #253536, .T. ) ;
#243439=CARTESIAN_POINT ( 'NONE',  ( -18.50000000000000000, 11.65000000001115232, -67.10000000000005116 ) ) ;
#243444=CARTESIAN_POINT ( 'NONE',  ( -18.50000000000000000, 9.350000000011156942, -88.35000000000003695 ) ) ;
#243450=DIRECTION ( 'NONE',  ( -1.000000000000000000, 0.000000000000000000, 0.000000000000000000 ) ) ;
#243491=CARTESIAN_POINT ( 'NONE',  ( 18.54286124688533732, -9.623917578786661764, -107.2412023318627377 ) ) ;
#243526=DIRECTION ( 'NONE',  ( 1.000000000000000000, 3.265361837132813093E-16, -0.000000000000000000 ) ) ;
#243569=EDGE_CURVE ( 'NONE', #154034, #20400, #20, .T. ) ;
#243605=EDGE_LOOP ( 'NONE', ( #44111, #141244, #169648, #195963, #181231 ) ) ;
#243611=CARTESIAN_POINT ( 'NONE',  ( 23.14999999999999858, 3.900000000011155432, -100.5000000000000426 ) ) ;
#243613=CARTESIAN_POINT ( 'NONE',  ( 22.46250603428203618, 0.02114417614996233138, -55.35013690265996189 ) ) ;
#243629=EDGE_CURVE ( 'NONE', #86852, #38092, #129703, .T. ) ;
#243630=FACE_OUTER_BOUND ( 'NONE', #181486, .T. ) ;
#243636=CARTESIAN_POINT ( 'NONE',  ( 23.14999999999999503, 11.65000000001116298, -88.25000000000005684 ) ) ;
#243638=EDGE_LOOP ( 'NONE', ( #99940, #30350, #159698, #212377 ) ) ;
#243694=CARTESIAN_POINT ( 'NONE',  ( -21.05000000000000071, -1.261786168553869603, -75.08649896354552311 ) ) ;
#243703=ORIENTED_EDGE ( 'NONE', *, *, #140214, .F. ) ;
#243706=CIRCLE ( 'NONE', #52332, 0.1000000000000001860 ) ;
#243722=CARTESIAN_POINT ( 'NONE',  ( -18.46856557590792391, -9.474215907775336731, -74.10198624088232577 ) ) ;
#243733=FACE_OUTER_BOUND ( 'NONE', #107496, .T. ) ;
#243744=AXIS2_PLACEMENT_3D ( 'NONE', #25108, #129000, #29915 ) ;
#243757=CARTESIAN_POINT ( 'NONE',  ( -18.50000000000000000, -9.399999999988850163, -107.4146583429697017 ) ) ;
#243813=AXIS2_PLACEMENT_3D ( 'NONE', #107747, #184713, #244679 ) ;
#243816=DIRECTION ( 'NONE',  ( 4.026293107431335996E-15, -0.8700118002898359348, 0.4930308989875165082 ) ) ;
#243830=LINE ( 'NONE', #103025, #115964 ) ;
#243862=DIRECTION ( 'NONE',  ( 0.000000000000000000, 0.01562500000001045344, 0.9998779222360096863 ) ) ;
#243871=TOROIDAL_SURFACE ( 'NONE', #131452, 12.97499999999999787, 0.1000000000000000056 ) ;
#243872=EDGE_CURVE ( 'NONE', #224664, #187777, #114537, .T. ) ;
#243873=CIRCLE ( 'NONE', #189711, 0.5000000000000004441 ) ;
#243919=AXIS2_PLACEMENT_3D ( 'NONE', #10014, #27043, #167835 ) ;
#243930=AXIS2_PLACEMENT_3D ( 'NONE', #2727, #203520, #181408 ) ;
#243935=CIRCLE ( 'NONE', #139872, 0.09999999999999939493 ) ;
#243937=CARTESIAN_POINT ( 'NONE',  ( 23.14999999999999503, 11.65000000001116298, -88.35000000000003695 ) ) ;
#243946=ADVANCED_FACE ( 'NONE', ( #217460 ), #88157, .F. ) ;
#243949=ORIENTED_EDGE ( 'NONE', *, *, #46474, .T. ) ;
#243961=CARTESIAN_POINT ( 'NONE',  ( -21.05000000000000071, 0.03175835306654922752, -60.74115287691999754 ) ) ;
#244046=CARTESIAN_POINT ( 'NONE',  ( 23.14999999999999503, 6.650000000011155876, -88.35000000000003695 ) ) ;
#244060=EDGE_CURVE ( 'NONE', #187820, #31603, #84329, .T. ) ;
#244066=ORIENTED_EDGE ( 'NONE', *, *, #68852, .F. ) ;
#244111=CARTESIAN_POINT ( 'NONE',  ( 18.59999999999999076, 10.20857864377385127, -88.35000000000003695 ) ) ;
#244116=DIRECTION ( 'NONE',  ( 3.469446951953498700E-14, -0.7899159663865300551, -0.6132151058540831201 ) ) ;
#244163=DIRECTION ( 'NONE',  ( 1.000000000000000000, 0.000000000000000000, 0.000000000000000000 ) ) ;
#244164=EDGE_LOOP ( 'NONE', ( #122607, #18651, #112304, #26769 ) ) ;
#244178=VERTEX_POINT ( 'NONE', #143060 ) ;
#244190=AXIS2_PLACEMENT_3D ( 'NONE', #66682, #163220, #146200 ) ;
#244205=CARTESIAN_POINT ( 'NONE',  ( -23.15000000000000213, 2.600000000011156054, -55.25000000000004974 ) ) ;
#244229=ORIENTED_EDGE ( 'NONE', *, *, #136652, .F. ) ;
#244235=CIRCLE ( 'NONE', #190103, 11.90000000000000746 ) ;
#244242=DIRECTION ( 'NONE',  ( 1.000000000000000000, -0.000000000000000000, -0.000000000000000000 ) ) ;
#244265=CARTESIAN_POINT ( 'NONE',  ( -22.50000000000000000, 11.75000000001115552, -67.00000000000004263 ) ) ;
#244276=SPHERICAL_SURFACE ( 'NONE', #220889, 0.1000000000000000056 ) ;
#244282=CARTESIAN_POINT ( 'NONE',  ( -20.94999999999999929, 1.115649653272650466E-11, -104.5000000000000568 ) ) ;
#244284=( BOUNDED_CURVE ( )  B_SPLINE_CURVE ( 3, ( #139418, #122459, #218966, #20800 ),
 .UNSPECIFIED., .F., .F. ) 
 B_SPLINE_CURVE_WITH_KNOTS ( ( 4, 4 ),
 ( 4.712388980384689674, 6.283185307179586232 ),
 .UNSPECIFIED. ) 
 CURVE ( )  GEOMETRIC_REPRESENTATION_ITEM ( )  RATIONAL_B_SPLINE_CURVE ( ( 1.000000000000000000, 0.8047378541243649375, 0.8047378541243649375, 1.000000000000000000 ) ) 
 REPRESENTATION_ITEM ( '' )  );
#244297=CIRCLE ( 'NONE', #131887, 0.3999999999999975797 ) ;
#244300=DIRECTION ( 'NONE',  ( 0.000000000000000000, 0.000000000000000000, 1.000000000000000000 ) ) ;
#244304=CARTESIAN_POINT ( 'NONE',  ( 21.07928932188134397, 6.328516656404468144, -66.90110485434564680 ) ) ;
#244313=EDGE_CURVE ( 'NONE', #238489, #115296, #196695, .T. ) ;
#244328=CARTESIAN_POINT ( 'NONE',  ( 22.39999999999999503, 7.790779598384535376, -66.90000000000004832 ) ) ;
#244351=CARTESIAN_POINT ( 'NONE',  ( -20.54999999999999716, 1.115600667400684642E-11, -67.00000000000004263 ) ) ;
#244365=CARTESIAN_POINT ( 'NONE',  ( 20.86777300164945004, 10.33200063080771969, -106.0931674956643320 ) ) ;
#244366=ORIENTED_EDGE ( 'NONE', *, *, #24922, .F. ) ;
#244373=ORIENTED_EDGE ( 'NONE', *, *, #23057, .T. ) ;
#244409=VERTEX_POINT ( 'NONE', #198890 ) ;
#244440=DIRECTION ( 'NONE',  ( 0.000000000000000000, 1.000000000000000000, 0.000000000000000000 ) ) ;
#244448=CARTESIAN_POINT ( 'NONE',  ( -21.05000000000000071, 6.413662734880551497, -67.08559286336239325 ) ) ;
#244500=ORIENTED_EDGE ( 'NONE', *, *, #101106, .F. ) ;
#244524=DIRECTION ( 'NONE',  ( 0.000000000000000000, 2.891205793294679805E-16, -1.000000000000000000 ) ) ;
#244535=CARTESIAN_POINT ( 'NONE',  ( 20.94999999999999929, -8.999999999988842703, -90.60603087734760663 ) ) ;
#244546=ORIENTED_EDGE ( 'NONE', *, *, #167076, .T. ) ;
#244587=ORIENTED_EDGE ( 'NONE', *, *, #201924, .F. ) ;
#244595=DIRECTION ( 'NONE',  ( 1.000000000000000000, 0.000000000000000000, 0.000000000000000000 ) ) ;
#244597=DIRECTION ( 'NONE',  ( 0.000000000000000000, 0.000000000000000000, -1.000000000000000000 ) ) ;
#244600=ORIENTED_EDGE ( 'NONE', *, *, #148405, .T. ) ;
#244616=ORIENTED_EDGE ( 'NONE', *, *, #176764, .T. ) ;
#244634=DIRECTION ( 'NONE',  ( 0.000000000000000000, -0.000000000000000000, 1.000000000000000000 ) ) ;
#244679=DIRECTION ( 'NONE',  ( 0.000000000000000000, 6.938893903907030216E-14, 1.000000000000000000 ) ) ;
#244681=DIRECTION ( 'NONE',  ( 1.000000000000000000, 0.000000000000000000, 0.000000000000000000 ) ) ;
#244699=VECTOR ( 'NONE', #106768, 1000.000000000000000 ) ;
#244718=ORIENTED_EDGE ( 'NONE', *, *, #124772, .F. ) ;
#244723=AXIS2_PLACEMENT_3D ( 'NONE', #36794, #158037, #219231 ) ;
#244737=CARTESIAN_POINT ( 'NONE',  ( -23.25000000000000000, 11.65000000001115588, -88.25000000000005684 ) ) ;
#244739=AXIS2_PLACEMENT_3D ( 'NONE', #166354, #86758, #71089 ) ;
#244750=B_SPLINE_CURVE_WITH_KNOTS ( 'NONE', 3,
 ( #81818, #21890, #204357, #121016, #64850, #140531 ),
 .UNSPECIFIED., .F., .F.,
 ( 4, 2, 4 ),
 ( 0.000000000000000000, 0.0001895189928937424410, 0.0003790379857874848820 ),
 .UNSPECIFIED. ) ;
#244768=LINE ( 'NONE', #68718, #214333 ) ;
#244790=ORIENTED_EDGE ( 'NONE', *, *, #91905, .T. ) ;
#244800=EDGE_CURVE ( 'NONE', #252694, #14463, #254665, .T. ) ;
#244806=LINE ( 'NONE', #145701, #19254 ) ;
#244904=ORIENTED_EDGE ( 'NONE', *, *, #172455, .T. ) ;
#244906=DIRECTION ( 'NONE',  ( 0.000000000000000000, 0.000000000000000000, -1.000000000000000000 ) ) ;
#244932=EDGE_CURVE ( 'NONE', #87663, #183134, #5803, .T. ) ;
#244954=CARTESIAN_POINT ( 'NONE',  ( 18.59999999999999076, 11.75000000001115907, -75.10000000000003695 ) ) ;
#244960=DIRECTION ( 'NONE',  ( -1.000000000000000000, -7.304098846218134667E-16, 0.000000000000000000 ) ) ;
#244979=DIRECTION ( 'NONE',  ( 1.000000000000000000, -0.000000000000000000, -0.000000000000000000 ) ) ;
#244989=ORIENTED_EDGE ( 'NONE', *, *, #18927, .F. ) ;
#244997=DIRECTION ( 'NONE',  ( -1.000000000000000000, 0.000000000000000000, 0.000000000000000000 ) ) ;
#245000=AXIS2_PLACEMENT_3D ( 'NONE', #89875, #12947, #50734 ) ;
#245002=CARTESIAN_POINT ( 'NONE',  ( -18.49499033040907037, -9.438148771733516185, -74.19815322592347684 ) ) ;
#245004=TOROIDAL_SURFACE ( 'NONE', #20161, 0.2000000000000000111, 0.1000000000000000056 ) ;
#245037=EDGE_CURVE ( 'NONE', #207164, #118177, #2940, .T. ) ;
#245054=ORIENTED_EDGE ( 'NONE', *, *, #177127, .F. ) ;
#245062=DIRECTION ( 'NONE',  ( 1.000000000000000000, 0.000000000000000000, 0.000000000000000000 ) ) ;
#245073=ORIENTED_EDGE ( 'NONE', *, *, #123914, .T. ) ;
#245098=ORIENTED_EDGE ( 'NONE', *, *, #93452, .F. ) ;
#245124=ADVANCED_FACE ( 'NONE', ( #51031, #88895 ), #130604, .F. ) ;
#245142=ORIENTED_EDGE ( 'NONE', *, *, #218641, .T. ) ;
#245167=DIRECTION ( 'NONE',  ( 2.694716079187272946E-16, -1.000000000000000000, 0.000000000000000000 ) ) ;
#245207=CARTESIAN_POINT ( 'NONE',  ( -23.25000000000000000, 2.000000000011154189, -87.27537807723794572 ) ) ;
#245221=CARTESIAN_POINT ( 'NONE',  ( -21.05000000000000071, 6.540656951712397138, -67.10000000000005116 ) ) ;
#245222=CYLINDRICAL_SURFACE ( 'NONE', #243930, 0.1000000000000000472 ) ;
#245224=CIRCLE ( 'NONE', #78603, 0.1000000000000028644 ) ;
#245246=EDGE_CURVE ( 'NONE', #100635, #43295, #66579, .T. ) ;
#245256=EDGE_CURVE ( 'NONE', #224195, #221121, #176900, .T. ) ;
#245310=AXIS2_PLACEMENT_3D ( 'NONE', #170533, #229175, #173095 ) ;
#245315=LINE ( 'NONE', #103205, #178652 ) ;
#245321=FACE_OUTER_BOUND ( 'NONE', #239832, .T. ) ;
#245327=ORIENTED_EDGE ( 'NONE', *, *, #28471, .F. ) ;
#245336=FACE_OUTER_BOUND ( 'NONE', #210162, .T. ) ;
#245345=CARTESIAN_POINT ( 'NONE',  ( -21.05000000000000071, 6.257814610487270279, -66.90220970869124528 ) ) ;
#245352=CIRCLE ( 'NONE', #257934, 12.77499999999999503 ) ;
#245363=CARTESIAN_POINT ( 'NONE',  ( -23.15000000000000213, 1.115600667400684642E-11, -88.70000000000004547 ) ) ;
#245368=VERTEX_POINT ( 'NONE', #135279 ) ;
#245383=CARTESIAN_POINT ( 'NONE',  ( 20.85000000000000142, 1.115600667400684642E-11, -100.5000000000000426 ) ) ;
#245387=DIRECTION ( 'NONE',  ( -1.000000000000000000, -2.952720810173289112E-16, 0.000000000000000000 ) ) ;
#245434=ORIENTED_EDGE ( 'NONE', *, *, #237688, .T. ) ;
#245480=ORIENTED_EDGE ( 'NONE', *, *, #161241, .T. ) ;
#245552=CARTESIAN_POINT ( 'NONE',  ( -20.85000000000000142, 1.115600667400684642E-11, -108.4000000000000483 ) ) ;
#245571=DIRECTION ( 'NONE',  ( 1.000000000000000000, 0.000000000000000000, 0.000000000000000000 ) ) ;
#245572=CIRCLE ( 'NONE', #233121, 0.1000000000000028644 ) ;
#245609=LINE ( 'NONE', #207786, #242868 ) ;
#245620=CARTESIAN_POINT ( 'NONE',  ( -21.05000000000000071, 1.115600667400684642E-11, -67.00000000000004263 ) ) ;
#245623=DIRECTION ( 'NONE',  ( 7.304098846218134667E-16, -1.000000000000000000, 0.000000000000000000 ) ) ;
#245628=LINE ( 'NONE', #146501, #130982 ) ;
#245629=DIRECTION ( 'NONE',  ( 0.7071359030027766224, -0.7070776581709024011, 0.000000000000000000 ) ) ;
#245644=PLANE ( 'NONE',  #50345 ) ;
#245659=CARTESIAN_POINT ( 'NONE',  ( -21.07928932188134041, 6.328516656404449492, -66.90110485434564680 ) ) ;
#245667=CARTESIAN_POINT ( 'NONE',  ( 20.94999999999999929, 5.900000000011162093, -90.28090023534366537 ) ) ;
#245684=DIRECTION ( 'NONE',  ( 0.000000000000000000, 0.000000000000000000, -1.000000000000000000 ) ) ;
#245729=ADVANCED_FACE ( 'NONE', ( #158067 ), #126431, .F. ) ;
#245749=CARTESIAN_POINT ( 'NONE',  ( -21.05000000000000071, 6.540656951712400691, -67.10000000000005116 ) ) ;
#245797=DIRECTION ( 'NONE',  ( 1.000000000000000000, 0.000000000000000000, 0.000000000000000000 ) ) ;
#245813=CARTESIAN_POINT ( 'NONE',  ( -23.15000000000000213, -8.999999999988846255, -76.89396912265249284 ) ) ;
#245861=CARTESIAN_POINT ( 'NONE',  ( 18.49999999999999289, 10.20857864377384416, -91.65000000000004832 ) ) ;
#245905=CARTESIAN_POINT ( 'NONE',  ( 20.19326291201655366, 10.15606098791449519, -74.76186180760271327 ) ) ;
#245909=CARTESIAN_POINT ( 'NONE',  ( 20.95566103547454517, 10.61824765095822087, -74.63184019298063276 ) ) ;
#245913=CIRCLE ( 'NONE', #45983, 0.1000000000000000472 ) ;
#245931=LINE ( 'NONE', #145526, #236499 ) ;
#245968=CARTESIAN_POINT ( 'NONE',  ( -21.07928932188134041, 0.09889514566555068775, -60.67148334360675221 ) ) ;
#245985=AXIS2_PLACEMENT_3D ( 'NONE', #222568, #106463, #223856 ) ;
#245995=ORIENTED_EDGE ( 'NONE', *, *, #66430, .T. ) ;
#246008=DIRECTION ( 'NONE',  ( 1.000000000000000000, -0.000000000000000000, -0.000000000000000000 ) ) ;
#246051=VERTEX_POINT ( 'NONE', #198120 ) ;
#246074=EDGE_LOOP ( 'NONE', ( #97184, #160297, #172033, #217277 ) ) ;
#246076=DIRECTION ( 'NONE',  ( -0.000000000000000000, 1.000000000000000000, -1.224646799147352961E-16 ) ) ;
#246102=CARTESIAN_POINT ( 'NONE',  ( -21.05000000000000071, 5.850000000011156942, -90.36750277572211587 ) ) ;
#246133=TOROIDAL_SURFACE ( 'NONE', #125509, 0.4000000000000003553, 0.1000000000000000056 ) ;
#246205=CIRCLE ( 'NONE', #167126, 0.09999999999999999167 ) ;
#246206=CARTESIAN_POINT ( 'NONE',  ( -20.54999999999999716, 4.250000000011156409, -79.35000000000005116 ) ) ;
#246210=LINE ( 'NONE', #29762, #20598 ) ;
#246275=DIRECTION ( 'NONE',  ( 1.000000000000000000, 0.000000000000000000, 0.000000000000000000 ) ) ;
#246285=CARTESIAN_POINT ( 'NONE',  ( 20.95595012432476523, 10.60417921308728673, -74.59576933021817524 ) ) ;
#246398=LINE ( 'NONE', #71623, #76570 ) ;
#246432=DIRECTION ( 'NONE',  ( -1.000000000000000000, 0.000000000000000000, 0.000000000000000000 ) ) ;
#246486=FACE_OUTER_BOUND ( 'NONE', #132673, .T. ) ;
#246517=ORIENTED_EDGE ( 'NONE', *, *, #176559, .T. ) ;
#246530=CARTESIAN_POINT ( 'NONE',  ( -18.59999999999999787, 5.341242990002807112, -57.19334979351202719 ) ) ;
#246542=ADVANCED_FACE ( 'NONE', ( #136530 ), #118283, .T. ) ;
#246578=CIRCLE ( 'NONE', #88147, 0.09999999999999491240 ) ;
#246582=DIRECTION ( 'NONE',  ( -1.000000000000000000, 0.000000000000000000, -0.000000000000000000 ) ) ;
#246597=VECTOR ( 'NONE', #202950, 1000.000000000000227 ) ;
#246626=FACE_OUTER_BOUND ( 'NONE', #172970, .T. ) ;
#246639=CARTESIAN_POINT ( 'NONE',  ( -21.64999999999999858, 7.350000000011155166, -79.35000000000005116 ) ) ;
#246645=ORIENTED_EDGE ( 'NONE', *, *, #68491, .F. ) ;
#246647=EDGE_CURVE ( 'NONE', #10892, #112516, #29210, .T. ) ;
#246655=DIRECTION ( 'NONE',  ( 0.000000000000000000, 0.000000000000000000, -1.000000000000000000 ) ) ;
#246666=ADVANCED_FACE ( 'NONE', ( #247191 ), #87406, .T. ) ;
#246680=VERTEX_POINT ( 'NONE', #123409 ) ;
#246687=FACE_OUTER_BOUND ( 'NONE', #133618, .T. ) ;
#246688=ORIENTED_EDGE ( 'NONE', *, *, #11897, .F. ) ;
#246753=CARTESIAN_POINT ( 'NONE',  ( -21.05000000000000071, -11.48912529306489994, -97.50000000000004263 ) ) ;
#246759=DIRECTION ( 'NONE',  ( 0.000000000000000000, 0.000000000000000000, -1.000000000000000000 ) ) ;
#246766=VERTEX_POINT ( 'NONE', #69872 ) ;
#246784=DIRECTION ( 'NONE',  ( 1.000000000000000000, -0.000000000000000000, 0.000000000000000000 ) ) ;
#246859=CARTESIAN_POINT ( 'NONE',  ( 21.13461538461538680, 8.885417037985614996, -79.35000000000005116 ) ) ;
#246876=FACE_OUTER_BOUND ( 'NONE', #39650, .T. ) ;
#246897=CARTESIAN_POINT ( 'NONE',  ( 23.15000000000000213, -8.999999999988842703, -91.10603087734760663 ) ) ;
#246922=DIRECTION ( 'NONE',  ( 0.000000000000000000, 0.000000000000000000, -1.000000000000000000 ) ) ;
#246932=CARTESIAN_POINT ( 'NONE',  ( 18.59999999999999076, -1.835859311432481045, -112.1044391687985780 ) ) ;
#246944=CARTESIAN_POINT ( 'NONE',  ( 21.05000000000000071, -0.09999999998884338825, -60.45934304829879835 ) ) ;
#246956=AXIS2_PLACEMENT_3D ( 'NONE', #48854, #227483, #31895 ) ;
#246968=DIRECTION ( 'NONE',  ( 1.000000000000000000, 0.000000000000000000, 0.000000000000000000 ) ) ;
#246972=AXIS2_PLACEMENT_3D ( 'NONE', #15168, #114254, #212089 ) ;
#246991=CARTESIAN_POINT ( 'NONE',  ( -20.54999999999999716, 4.250000000011156409, -79.25000000000004263 ) ) ;
#247030=ORIENTED_EDGE ( 'NONE', *, *, #79583, .F. ) ;
#247034=DIRECTION ( 'NONE',  ( 2.952720810173288619E-16, -1.000000000000000000, 0.000000000000000000 ) ) ;
#247069=LINE ( 'NONE', #5888, #130618 ) ;
#247123=ADVANCED_FACE ( 'NONE', ( #144893 ), #195958, .T. ) ;
#247127=CARTESIAN_POINT ( 'NONE',  ( 18.49999999999999289, 10.41716543472751688, -91.84999999941936721 ) ) ;
#247148=AXIS2_PLACEMENT_3D ( 'NONE', #130946, #94370, #111388 ) ;
#247156=EDGE_CURVE ( 'NONE', #143381, #242523, #9249, .T. ) ;
#247158=DIRECTION ( 'NONE',  ( 0.000000000000000000, 0.000000000000000000, 1.000000000000000000 ) ) ;
#247191=FACE_OUTER_BOUND ( 'NONE', #176410, .T. ) ;
#247198=VERTEX_POINT ( 'NONE', #211307 ) ;
#247203=ORIENTED_EDGE ( 'NONE', *, *, #11387, .F. ) ;
#247214=CARTESIAN_POINT ( 'NONE',  ( 23.14999999999999858, 5.900000000011162093, -90.28090023534366537 ) ) ;
#247231=CIRCLE ( 'NONE', #188804, 0.09999999999999939493 ) ;
#247250=DIRECTION ( 'NONE',  ( -0.000000000000000000, -0.1298341882519805091, -0.9915357197604881545 ) ) ;
#247259=ORIENTED_EDGE ( 'NONE', *, *, #184762, .F. ) ;
#247262=DIRECTION ( 'NONE',  ( 0.000000000000000000, -1.734723475976757554E-14, 1.000000000000000000 ) ) ;
#247277=DIRECTION ( 'NONE',  ( 1.000000000000000000, -0.000000000000000000, -0.000000000000000000 ) ) ;
#247308=EDGE_CURVE ( 'NONE', #205206, #235613, #258082, .T. ) ;
#247320=AXIS2_PLACEMENT_3D ( 'NONE', #113935, #55218, #235181 ) ;
#247367=CARTESIAN_POINT ( 'NONE',  ( -20.54999999999999716, 7.250000000011155521, -79.25000000000004263 ) ) ;
#247385=DIRECTION ( 'NONE',  ( 0.000000000000000000, 0.000000000000000000, -1.000000000000000000 ) ) ;
#247386=EDGE_CURVE ( 'NONE', #206950, #10892, #63782, .T. ) ;
#247422=ORIENTED_EDGE ( 'NONE', *, *, #103416, .F. ) ;
#247424=CARTESIAN_POINT ( 'NONE',  ( 20.85000000000000142, 7.120270961708750512, -104.1595630418393768 ) ) ;
#247473=AXIS2_PLACEMENT_3D ( 'NONE', #148564, #110711, #70340 ) ;
#247477=VECTOR ( 'NONE', #221155, 1000.000000000000000 ) ;
#247484=VERTEX_POINT ( 'NONE', #87178 ) ;
#247487=TOROIDAL_SURFACE ( 'NONE', #135023, 0.2000000000000000111, 0.1000000000000000056 ) ;
#247494=AXIS2_PLACEMENT_3D ( 'NONE', #230130, #231434, #112757 ) ;
#247513=CARTESIAN_POINT ( 'NONE',  ( -2.995603634470829482E-16, -11.74999999998884448, -88.25000000000005684 ) ) ;
#247514=DIRECTION ( 'NONE',  ( -0.000000000000000000, -0.000000000000000000, -1.000000000000000000 ) ) ;
#247518=DIRECTION ( 'NONE',  ( 1.000000000000000000, 0.000000000000000000, 0.000000000000000000 ) ) ;
#247537=ORIENTED_EDGE ( 'NONE', *, *, #214298, .F. ) ;
#247611=CARTESIAN_POINT ( 'NONE',  ( -21.93340585899104056, 1.115541036281197940E-11, -59.67585297787638865 ) ) ;
#247651=CIRCLE ( 'NONE', #222679, 0.09999999999999939493 ) ;
#247659=LINE ( 'NONE', #10350, #33289 ) ;
#247660=CARTESIAN_POINT ( 'NONE',  ( -20.64999999999999858, 1.115600667400684642E-11, -67.00000000000004263 ) ) ;
#247676=CARTESIAN_POINT ( 'NONE',  ( 21.04386569057601619, 11.75000000001104006, -93.64283735177943413 ) ) ;
#247712=CARTESIAN_POINT ( 'NONE',  ( -18.33981767444014821, -9.569575789793876908, -107.3191618437250696 ) ) ;
#247728=ORIENTED_EDGE ( 'NONE', *, *, #128319, .F. ) ;
#247732=ORIENTED_EDGE ( 'NONE', *, *, #195068, .T. ) ;
#247770=VERTEX_POINT ( 'NONE', #199133 ) ;
#247775=CARTESIAN_POINT ( 'NONE',  ( 19.80993210785486269, 11.75000000000926548, -91.76711774888731554 ) ) ;
#247790=DIRECTION ( 'NONE',  ( -1.000000000000000000, -2.952720810173289112E-16, 0.000000000000000000 ) ) ;
#247813=DIRECTION ( 'NONE',  ( -1.000000000000000000, -2.952720810173289112E-16, 0.000000000000000000 ) ) ;
#247814=DIRECTION ( 'NONE',  ( -0.000000000000000000, 0.000000000000000000, 1.000000000000000000 ) ) ;
#247817=DIRECTION ( 'NONE',  ( 0.000000000000000000, 0.000000000000000000, -1.000000000000000000 ) ) ;
#247825=DIRECTION ( 'NONE',  ( 0.000000000000000000, 0.000000000000000000, -1.000000000000000000 ) ) ;
#247835=EDGE_CURVE ( 'NONE', #27072, #80211, #217113, .T. ) ;
#247843=CARTESIAN_POINT ( 'NONE',  ( -21.44999999999999929, 7.350000000011155166, -88.15000000000004832 ) ) ;
#247847=ORIENTED_EDGE ( 'NONE', *, *, #226224, .T. ) ;
#247854=LINE ( 'NONE', #168367, #55357 ) ;
#247857=SHAPE_DEFINITION_REPRESENTATION ( #9789, #215063 ) ;
#247868=AXIS2_PLACEMENT_3D ( 'NONE', #196892, #15729, #234744 ) ;
#247886=DIRECTION ( 'NONE',  ( 0.000000000000000000, 0.000000000000000000, 1.000000000000000000 ) ) ;
#247956=DIRECTION ( 'NONE',  ( 0.000000000000000000, 0.000000000000000000, 1.000000000000000000 ) ) ;
#247974=CARTESIAN_POINT ( 'NONE',  ( -20.94999999999999929, 5.850000000011108092, -77.13249722427801203 ) ) ;
#247975=VERTEX_POINT ( 'NONE', #187290 ) ;
#248037=EDGE_LOOP ( 'NONE', ( #257339, #66224, #61701, #37296 ) ) ;
#248044=VERTEX_POINT ( 'NONE', #245968 ) ;
#248055=CARTESIAN_POINT ( 'NONE',  ( 21.14999999999999503, -0.1008583690875562017, -55.25043287651065782 ) ) ;
#248066=VERTEX_POINT ( 'NONE', #12509 ) ;
#248083=CARTESIAN_POINT ( 'NONE',  ( 23.15000000000000213, -11.48912529306489994, -97.40000000000004832 ) ) ;
#248102=CARTESIAN_POINT ( 'NONE',  ( -20.94999999999999929, 1.162701749949165642, -75.00000000000004263 ) ) ;
#248113=DIRECTION ( 'NONE',  ( 1.000000000000000000, 3.265361837132813093E-16, -0.000000000000000000 ) ) ;
#248146=CARTESIAN_POINT ( 'NONE',  ( -21.05000000000000071, -1.835341550213255957, -78.55515129256302487 ) ) ;
#248208=FACE_OUTER_BOUND ( 'NONE', #216264, .T. ) ;
#248210=VERTEX_POINT ( 'NONE', #200112 ) ;
#248253=DIRECTION ( 'NONE',  ( 1.000000000000000000, -0.000000000000000000, -0.000000000000000000 ) ) ;
#248289=ORIENTED_EDGE ( 'NONE', *, *, #19670, .T. ) ;
#248312=FACE_OUTER_BOUND ( 'NONE', #248346, .T. ) ;
#248316=DIRECTION ( 'NONE',  ( 1.000000000000000000, 0.000000000000000000, 0.000000000000000000 ) ) ;
#248346=EDGE_LOOP ( 'NONE', ( #176484, #250916, #106877, #117018 ) ) ;
#248347=CARTESIAN_POINT ( 'NONE',  ( 18.50596464788227280, 10.30632246271648889, -106.0041836778896283 ) ) ;
#248386=CARTESIAN_POINT ( 'NONE',  ( 20.85000000000000142, -11.64999999998883595, -100.5000000000000426 ) ) ;
#248388=CIRCLE ( 'NONE', #135950, 11.74999999999999645 ) ;
#248390=CARTESIAN_POINT ( 'NONE',  ( 20.94999999999999574, 1.851028230152016674, -78.65391326942254580 ) ) ;
#248451=TOROIDAL_SURFACE ( 'NONE', #160983, 11.65000000000000036, 0.1000000000000000056 ) ;
#248455=ADVANCED_FACE ( 'NONE', ( #176412 ), #137254, .T. ) ;
#248461=DIRECTION ( 'NONE',  ( 1.000000000000000000, 0.000000000000000000, 0.000000000000000000 ) ) ;
#248485=ORIENTED_EDGE ( 'NONE', *, *, #209698, .F. ) ;
#248504=DIRECTION ( 'NONE',  ( -1.000000000000000000, -3.265361837132813093E-16, 0.000000000000000000 ) ) ;
#248542=LINE ( 'NONE', #191164, #25679 ) ;
#248560=AXIS2_PLACEMENT_3D ( 'NONE', #224385, #221799, #223102 ) ;
#248571=LINE ( 'NONE', #69960, #141591 ) ;
#248578=CARTESIAN_POINT ( 'NONE',  ( 20.94999999999999574, -1.851028230129704522, -78.65391326942254580 ) ) ;
#248586=EDGE_LOOP ( 'NONE', ( #150663, #248936, #28606, #126446 ) ) ;
#248615=CARTESIAN_POINT ( 'NONE',  ( 20.85000000000000142, -11.74999999998883560, -97.50000000000004263 ) ) ;
#248624=ORIENTED_EDGE ( 'NONE', *, *, #10623, .T. ) ;
#248666=ORIENTED_EDGE ( 'NONE', *, *, #189465, .F. ) ;
#248700=VERTEX_POINT ( 'NONE', #134051 ) ;
#248720=AXIS2_PLACEMENT_3D ( 'NONE', #247513, #68893, #188816 ) ;
#248732=CARTESIAN_POINT ( 'NONE',  ( -21.05000000000000071, 1.115600667400684642E-11, -67.00000000000004263 ) ) ;
#248739=ADVANCED_FACE ( 'NONE', ( #15420 ), #253999, .T. ) ;
#248798=ORIENTED_EDGE ( 'NONE', *, *, #214867, .F. ) ;
#248830=LINE ( 'NONE', #110586, #196781 ) ;
#248835=CIRCLE ( 'NONE', #111443, 0.1000000000000028644 ) ;
#248880=LINE ( 'NONE', #87210, #81544 ) ;
#248931=AXIS2_PLACEMENT_3D ( 'NONE', #41605, #200659, #227919 ) ;
#248936=ORIENTED_EDGE ( 'NONE', *, *, #70103, .F. ) ;
#248938=AXIS2_PLACEMENT_3D ( 'NONE', #244328, #125673, #245629 ) ;
#248963=LINE ( 'NONE', #152447, #139491 ) ;
#248972=CARTESIAN_POINT ( 'NONE',  ( 18.59999999999999432, 1.728086936805619311, -53.88443500516780915 ) ) ;
#248995=AXIS2_PLACEMENT_3D ( 'NONE', #230555, #194003, #51882 ) ;
#249032=EDGE_LOOP ( 'NONE', ( #180979, #249351, #76478, #79115 ) ) ;
#249049=LINE ( 'NONE', #49548, #255061 ) ;
#249056=CYLINDRICAL_SURFACE ( 'NONE', #215663, 0.1000000000000028644 ) ;
#249113=ORIENTED_EDGE ( 'NONE', *, *, #135063, .F. ) ;
#249141=CIRCLE ( 'NONE', #194979, 0.1000000000000002554 ) ;
#249148=CARTESIAN_POINT ( 'NONE',  ( -18.59999999999999787, -1.162701749926853712, -75.10000000000003695 ) ) ;
#249156=ADVANCED_FACE ( 'NONE', ( #129470 ), #188161, .F. ) ;
#249165=DIRECTION ( 'NONE',  ( 0.7071067811865474617, 0.7071067811865474617, 0.000000000000000000 ) ) ;
#249186=DIRECTION ( 'NONE',  ( -1.000000000000000000, 0.000000000000000000, 0.000000000000000000 ) ) ;
#249219=CIRCLE ( 'NONE', #32770, 0.09999999999999939493 ) ;
#249228=EDGE_CURVE ( 'NONE', #178346, #137777, #146368, .T. ) ;
#249229=CARTESIAN_POINT ( 'NONE',  ( -20.64999999999999858, 7.250000000011155521, -79.35000000000005116 ) ) ;
#249246=CIRCLE ( 'NONE', #228582, 0.09999999999999939493 ) ;
#249253=VECTOR ( 'NONE', #169708, 1000.000000000000000 ) ;
#249255=CARTESIAN_POINT ( 'NONE',  ( 20.94999999999999574, 14.00000000001115730, -72.42709253038259476 ) ) ;
#249258=EDGE_LOOP ( 'NONE', ( #230764, #13174, #250904, #44220, #65692 ) ) ;
#249310=CARTESIAN_POINT ( 'NONE',  ( -23.25000000000000000, -1.851617760457748618, -112.1031897196037050 ) ) ;
#249311=ORIENTED_EDGE ( 'NONE', *, *, #181674, .T. ) ;
#249318=ADVANCED_FACE ( 'NONE', ( #125987 ), #159073, .T. ) ;
#249329=ORIENTED_EDGE ( 'NONE', *, *, #58462, .F. ) ;
#249351=ORIENTED_EDGE ( 'NONE', *, *, #257521, .F. ) ;
#249355=DIRECTION ( 'NONE',  ( 1.000000000000000000, 0.000000000000000000, 0.000000000000000000 ) ) ;
#249364=B_SPLINE_CURVE_WITH_KNOTS ( 'NONE', 3,
 ( #102454, #218568, #219866, #123346, #43808, #257646 ),
 .UNSPECIFIED., .F., .F.,
 ( 4, 2, 4 ),
 ( 0.000000000000000000, 0.0002113392456165989763, 0.0004226784912331979526 ),
 .UNSPECIFIED. ) ;
#249379=AXIS2_PLACEMENT_3D ( 'NONE', #241386, #190409, #30058 ) ;
#249403=CARTESIAN_POINT ( 'NONE',  ( -23.15000000000000213, 1.115600667400684642E-11, -100.5000000000000426 ) ) ;
#249438=AXIS2_PLACEMENT_3D ( 'NONE', #208467, #244997, #87187 ) ;
#249457=CARTESIAN_POINT ( 'NONE',  ( 21.04105312098515057, 8.875332623054768888, -79.32850674721208861 ) ) ;
#249459=EDGE_CURVE ( 'NONE', #113090, #233410, #250615, .T. ) ;
#249481=AXIS2_PLACEMENT_3D ( 'NONE', #48090, #229315, #58333 ) ;
#249508=ADVANCED_FACE ( 'NONE', ( #108988 ), #230230, .F. ) ;
#249511=ORIENTED_EDGE ( 'NONE', *, *, #87094, .T. ) ;
#249529=ORIENTED_EDGE ( 'NONE', *, *, #116944, .T. ) ;
#249530=CARTESIAN_POINT ( 'NONE',  ( 20.85882249326303040, 10.33248238083634796, -106.0948465439131922 ) ) ;
#249567=EDGE_CURVE ( 'NONE', #224643, #63408, #155854, .T. ) ;
#249572=ORIENTED_EDGE ( 'NONE', *, *, #106331, .F. ) ;
#249575=FACE_OUTER_BOUND ( 'NONE', #214707, .T. ) ;
#249612=ORIENTED_EDGE ( 'NONE', *, *, #90594, .F. ) ;
#249635=LINE ( 'NONE', #128393, #171377 ) ;
#249640=CARTESIAN_POINT ( 'NONE',  ( 23.24999999999999645, 5.600000000011153389, -79.40526601891313874 ) ) ;
#249643=FACE_OUTER_BOUND ( 'NONE', #180055, .T. ) ;
#249647=DIRECTION ( 'NONE',  ( 0.000000000000000000, 0.000000000000000000, -1.000000000000000000 ) ) ;
#249667=CARTESIAN_POINT ( 'NONE',  ( -21.12230431290520016, 6.457566653304167126, -66.99479014831103996 ) ) ;
#249701=CARTESIAN_POINT ( 'NONE',  ( -21.05000000000000071, -11.29603075032412463, -97.45210084033617193 ) ) ;
#249709=CYLINDRICAL_SURFACE ( 'NONE', #144134, 0.09999999999999811817 ) ;
#249724=CARTESIAN_POINT ( 'NONE',  ( 20.94999999999999574, 8.926614585098251453, -75.47168301922316402 ) ) ;
#249738=CARTESIAN_POINT ( 'NONE',  ( 21.05000000000000071, -8.999999999988842703, -90.60603087734760663 ) ) ;
#249742=DIRECTION ( 'NONE',  ( -1.000000000000000000, 0.000000000000000000, 0.000000000000000000 ) ) ;
#249748=CARTESIAN_POINT ( 'NONE',  ( 20.30531438145591139, 10.09690106110208596, -74.79601780727338678 ) ) ;
#249755=CARTESIAN_POINT ( 'NONE',  ( 21.05000000000000071, 1.115625160336667635E-11, -98.50000000000004263 ) ) ;
#249768=FACE_OUTER_BOUND ( 'NONE', #193995, .T. ) ;
#249791=DIRECTION ( 'NONE',  ( -1.000000000000000000, 0.000000000000000000, 0.000000000000000000 ) ) ;
#249798=CARTESIAN_POINT ( 'NONE',  ( -23.25000000000000000, 1.115600667400684642E-11, -100.5000000000000426 ) ) ;
#249799=EDGE_CURVE ( 'NONE', #150463, #217530, #52564, .T. ) ;
#249826=DIRECTION ( 'NONE',  ( 0.000000000000000000, 0.000000000000000000, -1.000000000000000000 ) ) ;
#249827=CARTESIAN_POINT ( 'NONE',  ( 21.12802099929860944, 8.780552590233368093, -79.24818998493165623 ) ) ;
#249839=CIRCLE ( 'NONE', #145769, 0.1000000000000028644 ) ;
#249914=ORIENTED_EDGE ( 'NONE', *, *, #244800, .F. ) ;
#249919=ORIENTED_EDGE ( 'NONE', *, *, #205326, .F. ) ;
#249948=ORIENTED_EDGE ( 'NONE', *, *, #73916, .T. ) ;
#249958=ORIENTED_EDGE ( 'NONE', *, *, #54167, .F. ) ;
#249967=VECTOR ( 'NONE', #181240, 1000.000000000000000 ) ;
#249973=DIRECTION ( 'NONE',  ( 0.000000000000000000, 1.000000000000000000, 0.000000000000000000 ) ) ;
#249980=DIRECTION ( 'NONE',  ( 0.000000000000000000, 0.000000000000000000, -1.000000000000000000 ) ) ;
#249982=VECTOR ( 'NONE', #247825, 1000.000000000000000 ) ;
#249989=VERTEX_POINT ( 'NONE', #141111 ) ;
#249992=ORIENTED_EDGE ( 'NONE', *, *, #50577, .F. ) ;
#250023=DIRECTION ( 'NONE',  ( -1.000000000000000000, 3.469446951953635015E-14, 0.000000000000000000 ) ) ;
#250035=EDGE_CURVE ( 'NONE', #202477, #75011, #161972, .T. ) ;
#250043=VERTEX_POINT ( 'NONE', #245345 ) ;
#250058=ORIENTED_EDGE ( 'NONE', *, *, #28836, .T. ) ;
#250068=EDGE_CURVE ( 'NONE', #169584, #211426, #201071, .T. ) ;
#250088=CYLINDRICAL_SURFACE ( 'NONE', #158607, 0.1000000000000028644 ) ;
#250097=ORIENTED_EDGE ( 'NONE', *, *, #3109, .T. ) ;
#250109=CARTESIAN_POINT ( 'NONE',  ( 21.14999999999999858, 0.09779029131994770863, -60.74218538952391810 ) ) ;
#250131=EDGE_LOOP ( 'NONE', ( #127929, #15376, #64564, #70199, #34612 ) ) ;
#250141=DIRECTION ( 'NONE',  ( 1.000000000000000000, 0.000000000000000000, 0.000000000000000000 ) ) ;
#250163=ORIENTED_EDGE ( 'NONE', *, *, #136399, .T. ) ;
#250167=VERTEX_POINT ( 'NONE', #9289 ) ;
#250176=CARTESIAN_POINT ( 'NONE',  ( -21.29999999999995808, 1.115600667400684642E-11, -67.00000000000004263 ) ) ;
#250183=CIRCLE ( 'NONE', #200288, 0.1000000000000028644 ) ;
#250194=CARTESIAN_POINT ( 'NONE',  ( -20.94999999999999929, 1.115600667400684642E-11, -100.5000000000000426 ) ) ;
#250217=CARTESIAN_POINT ( 'NONE',  ( -18.59999999999999787, 11.75000000001115197, -55.25000000000004974 ) ) ;
#250224=VERTEX_POINT ( 'NONE', #109658 ) ;
#250242=CARTESIAN_POINT ( 'NONE',  ( 20.96428641294244599, 11.75000000001149836, -93.67489317794097303 ) ) ;
#250253=DIRECTION ( 'NONE',  ( 0.000000000000000000, 1.000000000000000000, 0.000000000000000000 ) ) ;
#250260=CIRCLE ( 'NONE', #83620, 1.899999999999999023 ) ;
#250272=LINE ( 'NONE', #216263, #96893 ) ;
#250295=ORIENTED_EDGE ( 'NONE', *, *, #204459, .T. ) ;
#250299=AXIS2_PLACEMENT_3D ( 'NONE', #57971, #20165, #137509 ) ;
#250323=DIRECTION ( 'NONE',  ( 1.000000000000000000, 0.000000000000000000, -0.000000000000000000 ) ) ;
#250342=CIRCLE ( 'NONE', #179620, 0.1000000000000028644 ) ;
#250362=CARTESIAN_POINT ( 'NONE',  ( 20.94999999999999929, 1.115600667400684642E-11, -100.5000000000000426 ) ) ;
#250371=CARTESIAN_POINT ( 'NONE',  ( -18.50000000000000000, -1.164121893230052995, -108.4148480855716485 ) ) ;
#250381=CARTESIAN_POINT ( 'NONE',  ( -23.25000000000000000, -1.736705739456431807, -112.0174225876237699 ) ) ;
#250391=CARTESIAN_POINT ( 'NONE',  ( 22.60000000000000142, 1.115600667400684642E-11, -67.00000000000004263 ) ) ;
#250445=CARTESIAN_POINT ( 'NONE',  ( 23.14999999999999858, 1.115600667400684642E-11, -100.5000000000000426 ) ) ;
#250580=AXIS2_PLACEMENT_3D ( 'NONE', #179873, #239842, #45479 ) ;
#250615=CIRCLE ( 'NONE', #59050, 3.900000000000000799 ) ;
#250616=EDGE_LOOP ( 'NONE', ( #165295, #247537, #212958, #26204 ) ) ;
#250621=ORIENTED_EDGE ( 'NONE', *, *, #65152, .F. ) ;
#250631=CARTESIAN_POINT ( 'NONE',  ( 23.14999999999999503, 6.550000000011156231, -88.15000000000004832 ) ) ;
#250707=FACE_OUTER_BOUND ( 'NONE', #235549, .T. ) ;
#250713=DIRECTION ( 'NONE',  ( -1.000000000000000000, 9.012599976028471648E-15, 6.882867235861662930E-14 ) ) ;
#250727=AXIS2_PLACEMENT_3D ( 'NONE', #234653, #195553, #233398 ) ;
#250765=CARTESIAN_POINT ( 'NONE',  ( 22.50014994444007499, 11.74971973190315389, -66.91691984328092246 ) ) ;
#250776=EDGE_LOOP ( 'NONE', ( #181219, #202700 ) ) ;
#250785=DIRECTION ( 'NONE',  ( 0.000000000000000000, 0.000000000000000000, -1.000000000000000000 ) ) ;
#250790=CARTESIAN_POINT ( 'NONE',  ( 23.25000000000000000, -11.74999999998883560, -55.25000000000004974 ) ) ;
#250829=ORIENTED_EDGE ( 'NONE', *, *, #20837, .F. ) ;
#250882=TOROIDAL_SURFACE ( 'NONE', #96740, 0.2000000000000000111, 0.1000000000000000056 ) ;
#250888=EDGE_CURVE ( 'NONE', #199698, #76744, #46493, .T. ) ;
#250901=CARTESIAN_POINT ( 'NONE',  ( 22.40000000000020819, -0.1008583690885111045, -55.25043287651034518 ) ) ;
#250904=ORIENTED_EDGE ( 'NONE', *, *, #68852, .T. ) ;
#250916=ORIENTED_EDGE ( 'NONE', *, *, #121800, .T. ) ;
#250944=EDGE_LOOP ( 'NONE', ( #186214, #227414, #8523, #134374 ) ) ;
#250970=DIRECTION ( 'NONE',  ( 2.952720810173289112E-16, -1.000000000000000000, -0.000000000000000000 ) ) ;
#250984=DIRECTION ( 'NONE',  ( 0.000000000000000000, 0.000000000000000000, -1.000000000000000000 ) ) ;
#251002=CARTESIAN_POINT ( 'NONE',  ( 23.25000000000000000, -8.596261682231833845, -76.45012751715033517 ) ) ;
#251012=EDGE_CURVE ( 'NONE', #139104, #225893, #105581, .T. ) ;
#251014=TOROIDAL_SURFACE ( 'NONE', #30291, 0.2000000000000000111, 0.1000000000000000056 ) ;
#251037=FACE_OUTER_BOUND ( 'NONE', #243638, .T. ) ;
#251044=AXIS2_PLACEMENT_3D ( 'NONE', #116194, #211423, #155335 ) ;
#251052=EDGE_CURVE ( 'NONE', #237092, #198825, #18130, .T. ) ;
#251127=AXIS2_PLACEMENT_3D ( 'NONE', #78098, #175958, #57241 ) ;
#251164=DIRECTION ( 'NONE',  ( 0.000000000000000000, 0.000000000000000000, -1.000000000000000000 ) ) ;
#251178=DIRECTION ( 'NONE',  ( -0.7071067811865388020, 0.7071067811865561215, 0.000000000000000000 ) ) ;
#251200=ORIENTED_EDGE ( 'NONE', *, *, #132732, .F. ) ;
#251207=CARTESIAN_POINT ( 'NONE',  ( 21.05000000000000071, 1.349084418638171412, -74.98649896354552880 ) ) ;
#251218=DIRECTION ( 'NONE',  ( 0.000000000000000000, 0.000000000000000000, -1.000000000000000000 ) ) ;
#251241=CIRCLE ( 'NONE', #201373, 0.1000000000000028644 ) ;
#251244=CARTESIAN_POINT ( 'NONE',  ( 21.05000000000000071, -0.09999999998884338825, -67.00000000000004263 ) ) ;
#251248=ORIENTED_EDGE ( 'NONE', *, *, #49790, .F. ) ;
#251288=AXIS2_PLACEMENT_3D ( 'NONE', #112643, #90494, #89214 ) ;
#251323=ORIENTED_EDGE ( 'NONE', *, *, #182513, .T. ) ;
#251336=EDGE_CURVE ( 'NONE', #64371, #140759, #187980, .T. ) ;
#251354=EDGE_CURVE ( 'NONE', #190057, #193140, #22612, .T. ) ;
#251372=DIRECTION ( 'NONE',  ( -0.000000000000000000, 0.1350103645451904977, 0.9908441862701597991 ) ) ;
#251378=AXIS2_PLACEMENT_3D ( 'NONE', #153360, #214559, #131172 ) ;
#251403=TOROIDAL_SURFACE ( 'NONE', #68061, 0.6000000000000006439, 0.1000000000000000056 ) ;
#251408=CARTESIAN_POINT ( 'NONE',  ( 22.60000000000000142, 11.74956712350054744, -66.89914163090134025 ) ) ;
#251430=CARTESIAN_POINT ( 'NONE',  ( -20.96077737575343392, 11.62390063401577933, -93.64079195710642978 ) ) ;
#251441=ORIENTED_EDGE ( 'NONE', *, *, #166807, .F. ) ;
#251456=LINE ( 'NONE', #147223, #179075 ) ;
#251460=FACE_OUTER_BOUND ( 'NONE', #186493, .T. ) ;
#251483=FACE_OUTER_BOUND ( 'NONE', #180369, .T. ) ;
#251487=EDGE_CURVE ( 'NONE', #11297, #202894, #77002, .T. ) ;
#251504=FACE_OUTER_BOUND ( 'NONE', #74633, .T. ) ;
#251527=CARTESIAN_POINT ( 'NONE',  ( 21.05000000000000071, 1.115653327213047955E-11, -71.30000000000006821 ) ) ;
#251534=AXIS2_PLACEMENT_3D ( 'NONE', #168465, #13197, #48454 ) ;
#251537=CIRCLE ( 'NONE', #59991, 2.000000000000001776 ) ;
#251579=AXIS2_PLACEMENT_3D ( 'NONE', #159092, #179932, #199500 ) ;
#251583=VERTEX_POINT ( 'NONE', #181266 ) ;
#251606=ORIENTED_EDGE ( 'NONE', *, *, #62311, .F. ) ;
#251608=CIRCLE ( 'NONE', #139143, 0.09999999999999939493 ) ;
#251620=ORIENTED_EDGE ( 'NONE', *, *, #103497, .T. ) ;
#251649=CYLINDRICAL_SURFACE ( 'NONE', #250727, 11.80000000000000426 ) ;
#251663=CARTESIAN_POINT ( 'NONE',  ( -23.25000000000000000, 4.150000000011156764, -88.15000000000004832 ) ) ;
#251677=DIRECTION ( 'NONE',  ( 0.000000000000000000, -0.9915357197604853789, 0.1298341882520022694 ) ) ;
#251683=ADVANCED_FACE ( 'NONE', ( #32477 ), #109390, .T. ) ;
#251746=EDGE_CURVE ( 'NONE', #6498, #224664, #189194, .T. ) ;
#251779=ORIENTED_EDGE ( 'NONE', *, *, #87621, .F. ) ;
#251839=CARTESIAN_POINT ( 'NONE',  ( -18.49513951962167368, -9.437725026666544892, -107.2780725750291850 ) ) ;
#251876=VECTOR ( 'NONE', #115778, 1000.000000000000000 ) ;
#251890=EDGE_CURVE ( 'NONE', #237092, #39976, #93693, .T. ) ;
#251929=DIRECTION ( 'NONE',  ( 2.952720810173289112E-16, -1.000000000000000000, 0.000000000000000000 ) ) ;
#251942=( BOUNDED_CURVE ( )  B_SPLINE_CURVE ( 3, ( #11116, #88046, #110196, #249724 ),
 .UNSPECIFIED., .F., .F. ) 
 B_SPLINE_CURVE_WITH_KNOTS ( ( 4, 4 ),
 ( 0.06456096931748307732, 3.077031684272310219 ),
 .UNSPECIFIED. ) 
 CURVE ( )  GEOMETRIC_REPRESENTATION_ITEM ( )  RATIONAL_B_SPLINE_CURVE ( ( 1.000000000000000000, 0.3763440860215093164, 0.3763440860215093164, 1.000000000000000000 ) ) 
 REPRESENTATION_ITEM ( '' )  );
#251971=CARTESIAN_POINT ( 'NONE',  ( -1.820710678118658388, -9.929289321870186313, -91.65000000000004832 ) ) ;
#251993=EDGE_CURVE ( 'NONE', #13227, #55890, #232886, .T. ) ;
#251997=DIRECTION ( 'NONE',  ( -2.952720810173289112E-16, 1.000000000000000000, 0.000000000000000000 ) ) ;
#252007=EDGE_LOOP ( 'NONE', ( #86624, #3247, #102315, #251606 ) ) ;
#252014=AXIS2_PLACEMENT_3D ( 'NONE', #226192, #162421, #227504 ) ;
#252075=DIRECTION ( 'NONE',  ( 0.000000000000000000, 1.000000000000000000, -6.308085367188393199E-16 ) ) ;
#252139=DIRECTION ( 'NONE',  ( 0.000000000000000000, 0.000000000000000000, -1.000000000000000000 ) ) ;
#252145=CARTESIAN_POINT ( 'NONE',  ( -21.05000000000000071, 6.540656951712397138, -67.10000000000005116 ) ) ;
#252181=DIRECTION ( 'NONE',  ( 1.000000000000000000, -0.000000000000000000, -0.000000000000000000 ) ) ;
#252200=EDGE_CURVE ( 'NONE', #54519, #73858, #27274, .T. ) ;
#252230=VERTEX_POINT ( 'NONE', #153400 ) ;
#252248=CARTESIAN_POINT ( 'NONE',  ( 23.14999999999999858, 1.115600667400684642E-11, -102.5000000000000426 ) ) ;
#252296=AXIS2_PLACEMENT_3D ( 'NONE', #168593, #29071, #211526 ) ;
#252349=DIRECTION ( 'NONE',  ( 1.000000000000000000, -0.000000000000000000, -0.000000000000000000 ) ) ;
#252351=ORIENTED_EDGE ( 'NONE', *, *, #204163, .T. ) ;
#252353=AXIS2_PLACEMENT_3D ( 'NONE', #56727, #22809, #237963 ) ;
#252368=ORIENTED_EDGE ( 'NONE', *, *, #102265, .F. ) ;
#252374=ORIENTED_EDGE ( 'NONE', *, *, #255791, .T. ) ;
#252384=ORIENTED_EDGE ( 'NONE', *, *, #25772, .F. ) ;
#252396=CARTESIAN_POINT ( 'NONE',  ( -20.64999999999999858, -9.499999999988846255, -90.60603087734760663 ) ) ;
#252398=TOROIDAL_SURFACE ( 'NONE', #56747, 11.65000000000000036, 0.1000000000000000056 ) ;
#252405=LINE ( 'NONE', #73819, #216615 ) ;
#252406=ORIENTED_EDGE ( 'NONE', *, *, #46474, .F. ) ;
#252408=LINE ( 'NONE', #153377, #207265 ) ;
#252423=CARTESIAN_POINT ( 'NONE',  ( 20.95512820512820440, 8.876151316299273120, -75.55862899514100661 ) ) ;
#252424=ORIENTED_EDGE ( 'NONE', *, *, #35582, .F. ) ;
#252433=CARTESIAN_POINT ( 'NONE',  ( 21.14999999999999858, 11.75000000001116263, -79.15000000000004832 ) ) ;
#252482=ORIENTED_EDGE ( 'NONE', *, *, #31560, .F. ) ;
#252521=VECTOR ( 'NONE', #221192, 1000.000000000000000 ) ;
#252552=CARTESIAN_POINT ( 'NONE',  ( -20.94999999999999929, -11.64999999998884306, -97.40000000000004832 ) ) ;
#252553=CARTESIAN_POINT ( 'NONE',  ( 21.05000000000000071, 8.876614585098254295, -75.38508047884472774 ) ) ;
#252555=ORIENTED_EDGE ( 'NONE', *, *, #12500, .T. ) ;
#252560=DIRECTION ( 'NONE',  ( 0.000000000000000000, 0.000000000000000000, 1.000000000000000000 ) ) ;
#252611=FACE_OUTER_BOUND ( 'NONE', #25710, .T. ) ;
#252613=VERTEX_POINT ( 'NONE', #201030 ) ;
#252622=ORIENTED_EDGE ( 'NONE', *, *, #69036, .F. ) ;
#252638=EDGE_LOOP ( 'NONE', ( #44856, #24433, #2161, #28364 ) ) ;
#252646=FACE_OUTER_BOUND ( 'NONE', #68001, .T. ) ;
#252694=VERTEX_POINT ( 'NONE', #105750 ) ;
#252699=CARTESIAN_POINT ( 'NONE',  ( 21.14999999999999858, 10.71339244341104013, -79.25000000000005684 ) ) ;
#252704=CARTESIAN_POINT ( 'NONE',  ( -20.94999999999999929, -1.164121893230052995, -108.4148480855716485 ) ) ;
#252728=CARTESIAN_POINT ( 'NONE',  ( -22.47071067811865319, 0.09909245471376178227, -59.27992525550197911 ) ) ;
#252744=CARTESIAN_POINT ( 'NONE',  ( 21.05000000000000071, 4.850467289730776344, -88.46573259099837117 ) ) ;
#252763=FACE_OUTER_BOUND ( 'NONE', #196415, .T. ) ;
#252768=DIRECTION ( 'NONE',  ( -1.000000000000000000, 0.000000000000000000, 0.000000000000000000 ) ) ;
#252770=FACE_OUTER_BOUND ( 'NONE', #238004, .T. ) ;
#252779=EDGE_LOOP ( 'NONE', ( #172066, #234269, #145694, #119345 ) ) ;
#252791=CARTESIAN_POINT ( 'NONE',  ( -18.59999999999999787, 7.021664781911246322, -104.3335654018973315 ) ) ;
#252880=ORIENTED_EDGE ( 'NONE', *, *, #217117, .F. ) ;
#252914=VECTOR ( 'NONE', #211745, 1000.000000000000000 ) ;
#252927=DIRECTION ( 'NONE',  ( 2.879366945564059217E-14, -0.9875055080513751582, 0.1575844902526747915 ) ) ;
#252950=FACE_OUTER_BOUND ( 'NONE', #156285, .T. ) ;
#252982=ADVANCED_FACE ( 'NONE', ( #107862 ), #24503, .F. ) ;
#253021=CARTESIAN_POINT ( 'NONE',  ( 18.49999999999999289, 6.650000000011155876, -88.35000000000003695 ) ) ;
#253033=ADVANCED_FACE ( 'NONE', ( #4885 ), #103988, .T. ) ;
#253049=ORIENTED_EDGE ( 'NONE', *, *, #28260, .F. ) ;
#253054=ORIENTED_EDGE ( 'NONE', *, *, #15154, .T. ) ;
#253055=ORIENTED_EDGE ( 'NONE', *, *, #33845, .F. ) ;
#253069=ORIENTED_EDGE ( 'NONE', *, *, #255650, .T. ) ;
#253076=ADVANCED_FACE ( 'NONE', ( #212119 ), #231686, .F. ) ;
#253081=CIRCLE ( 'NONE', #257313, 0.1000000000000033223 ) ;
#253094=CARTESIAN_POINT ( 'NONE',  ( 21.05000000000000071, 1.115486826172573664E-11, -60.45934304829880546 ) ) ;
#253099=VERTEX_POINT ( 'NONE', #54300 ) ;
#253111=EDGE_CURVE ( 'NONE', #149634, #246680, #131282, .T. ) ;
#253133=ORIENTED_EDGE ( 'NONE', *, *, #236787, .T. ) ;
#253145=TOROIDAL_SURFACE ( 'NONE', #203273, 0.4000000000000012990, 0.1000000000000000056 ) ;
#253148=TOROIDAL_SURFACE ( 'NONE', #7448, 3.899999999999999467, 0.1000000000000000056 ) ;
#253230=EDGE_LOOP ( 'NONE', ( #145274, #138385, #154681, #69517, #140378, #64018, #101480, #51601, #251779, #169120, #80167, #92381 ) ) ;
#253247=CARTESIAN_POINT ( 'NONE',  ( -20.54999999999999716, -8.999999999988844479, -90.60603087734760663 ) ) ;
#253262=ORIENTED_EDGE ( 'NONE', *, *, #28288, .T. ) ;
#253266=CARTESIAN_POINT ( 'NONE',  ( 22.32929514600007792, 7.578647565387638174, -66.90092432188612293 ) ) ;
#253275=LINE ( 'NONE', #39408, #57973 ) ;
#253285=ORIENTED_EDGE ( 'NONE', *, *, #107610, .T. ) ;
#253292=AXIS2_PLACEMENT_3D ( 'NONE', #190651, #12011, #94079 ) ;
#253294=DIRECTION ( 'NONE',  ( 1.000000000000000000, 3.265361837132813093E-16, -0.000000000000000000 ) ) ;
#253339=AXIS2_PLACEMENT_3D ( 'NONE', #209916, #172098, #234591 ) ;
#253355=DIRECTION ( 'NONE',  ( 1.000000000000000000, 0.000000000000000000, -0.000000000000000000 ) ) ;
#253372=CARTESIAN_POINT ( 'NONE',  ( -23.15000000000000213, -11.64999999998884483, -55.25000000000004974 ) ) ;
#253406=CARTESIAN_POINT ( 'NONE',  ( -21.14999999999999858, 1.115600667400684642E-11, -60.45934304829880546 ) ) ;
#253413=CIRCLE ( 'NONE', #95205, 7.900000000000000355 ) ;
#253437=CYLINDRICAL_SURFACE ( 'NONE', #88931, 0.1000000000000028644 ) ;
#253466=ADVANCED_FACE ( 'NONE', ( #154438 ), #33211, .T. ) ;
#253478=ORIENTED_EDGE ( 'NONE', *, *, #213624, .F. ) ;
#253486=DIRECTION ( 'NONE',  ( 1.734723475976817507E-14, -1.000000000000000000, 0.000000000000000000 ) ) ;
#253536=B_SPLINE_CURVE_WITH_KNOTS ( 'NONE', 3,
 ( #82721, #179317, #123178, #102284, #164875, #623, #161024, #181867, #224826, #162314, #222242, #99724, #180580, #202703, #241827, #198848 ),
 .UNSPECIFIED., .F., .F.,
 ( 4, 3, 3, 3, 3, 4 ),
 ( 0.000000000000000000, 3.357088238232317244E-05, 6.714213034886757942E-05, 0.0001007408646120921551, 0.0001343627955914185768, 0.0001573956632895995484 ),
 .UNSPECIFIED. ) ;
#253556=( BOUNDED_SURFACE ( )  B_SPLINE_SURFACE ( 3, 2, ( 
 ( #9062, #31244, #126441 ),
 ( #205982, #11653, #91169 ),
 ( #226824, #247676, #108177 ),
 ( #185135, #186434, #48185 ),
 ( #168185, #250242, #127742 ),
 ( #165589, #27389, #125173 ) ),
 .UNSPECIFIED., .F., .F., .T. ) 
 B_SPLINE_SURFACE_WITH_KNOTS ( ( 4, 2, 4 ),
 ( 3, 3 ),
 ( -1.776356839400250465E-15, 0.7853981633974468357, 1.570796326794895448 ),
 ( 0.000000000000000000, 1.000000000000000000 ),
 .UNSPECIFIED. ) 
 GEOMETRIC_REPRESENTATION_ITEM ( )  RATIONAL_B_SPLINE_SURFACE ( (
 ( 1.000000000000000000, 0.4999999999999960587, 1.000000000000000000),
 ( 1.000000000000000000, 0.4993418825332500144, 1.000000000000000000),
 ( 1.000000000000000000, 0.5278258667060371501, 1.000000000000000000),
 ( 1.000000000000000000, 0.6092287576694621620, 1.000000000000000000),
 ( 1.000000000000000000, 0.6611148371779838051, 1.000000000000000000),
 ( 1.000000000000000000, 0.7071067811865719976, 1.000000000000000000) ) ) 
 REPRESENTATION_ITEM ( '' )  SURFACE ( )  );
#253559=ADVANCED_FACE ( 'NONE', ( #160839 ), #180390, .F. ) ;
#253570=ORIENTED_EDGE ( 'NONE', *, *, #225931, .F. ) ;
#253590=DIRECTION ( 'NONE',  ( -1.000000000000000000, -0.000000000000000000, -0.000000000000000000 ) ) ;
#253630=ORIENTED_EDGE ( 'NONE', *, *, #119452, .T. ) ;
#253671=FACE_OUTER_BOUND ( 'NONE', #136904, .T. ) ;
#253688=CIRCLE ( 'NONE', #66276, 0.1000000000000028644 ) ;
#253714=CARTESIAN_POINT ( 'NONE',  ( -18.50000000000000000, 10.29288807859935950, -105.9580020160122302 ) ) ;
#253726=AXIS2_PLACEMENT_3D ( 'NONE', #208977, #228558, #206412 ) ;
#253744=AXIS2_PLACEMENT_3D ( 'NONE', #49528, #189037, #243862 ) ;
#253782=TOROIDAL_SURFACE ( 'NONE', #258045, 12.77499999999999858, 0.1000000000000000056 ) ;
#253786=EDGE_LOOP ( 'NONE', ( #249311, #245098, #243067, #115573 ) ) ;
#253790=ORIENTED_EDGE ( 'NONE', *, *, #121649, .F. ) ;
#253793=AXIS2_PLACEMENT_3D ( 'NONE', #234710, #53502, #114761 ) ;
#253799=AXIS2_PLACEMENT_3D ( 'NONE', #138967, #80277, #218513 ) ;
#253815=ORIENTED_EDGE ( 'NONE', *, *, #1169, .F. ) ;
#253851=CARTESIAN_POINT ( 'NONE',  ( -22.39999999999999858, 0.1000000000111554016, -59.20922040162664501 ) ) ;
#253854=ADVANCED_FACE ( 'NONE', ( #14607 ), #109816, .T. ) ;
#253870=AXIS2_PLACEMENT_3D ( 'NONE', #195011, #97126, #176728 ) ;
#253874=DIRECTION ( 'NONE',  ( 1.000000000000000000, 0.000000000000000000, 0.000000000000000000 ) ) ;
#253894=VERTEX_POINT ( 'NONE', #32905 ) ;
#253901=CARTESIAN_POINT ( 'NONE',  ( 21.00000000000000000, 9.750000000011153745, -79.35000000000005116 ) ) ;
#253921=CARTESIAN_POINT ( 'NONE',  ( 20.85000000000000142, 7.070967871809997973, -104.2465642218683541 ) ) ;
#253976=CARTESIAN_POINT ( 'NONE',  ( -21.44999999999999929, 7.150000000011155876, -79.25000000000004263 ) ) ;
#253986=DIRECTION ( 'NONE',  ( 0.000000000000000000, 0.000000000000000000, -1.000000000000000000 ) ) ;
#253990=DIRECTION ( 'NONE',  ( 0.000000000000000000, 1.000000000000000000, 0.000000000000000000 ) ) ;
#253999=SPHERICAL_SURFACE ( 'NONE', #92214, 0.1000000000000000056 ) ;
#254011=DIRECTION ( 'NONE',  ( -4.391705002472929091E-16, 1.000000000000000000, 0.000000000000000000 ) ) ;
#254016=CARTESIAN_POINT ( 'NONE',  ( 21.05000000000000071, 5.000000000011153745, -88.49473398108695221 ) ) ;
#254017=CYLINDRICAL_SURFACE ( 'NONE', #56879, 0.09999999999999939493 ) ;
#254027=CARTESIAN_POINT ( 'NONE',  ( -20.00857864376270001, 9.250000000011157297, -88.25000000000005684 ) ) ;
#254052=ORIENTED_EDGE ( 'NONE', *, *, #79073, .F. ) ;
#254060=ADVANCED_FACE ( 'NONE', ( #24879 ), #202209, .T. ) ;
#254101=ORIENTED_EDGE ( 'NONE', *, *, #85531, .F. ) ;
#254131=FACE_OUTER_BOUND ( 'NONE', #112562, .T. ) ;
#254132=ORIENTED_EDGE ( 'NONE', *, *, #148405, .F. ) ;
#254146=CARTESIAN_POINT ( 'NONE',  ( 18.31325810956244382, -9.536388475995861924, -107.3684402063055074 ) ) ;
#254162=DIRECTION ( 'NONE',  ( 0.000000000000000000, 0.000000000000000000, -1.000000000000000000 ) ) ;
#254172=CARTESIAN_POINT ( 'NONE',  ( 23.24999999999999289, 11.65000000001116298, -67.10000000000005116 ) ) ;
#254233=AXIS2_PLACEMENT_3D ( 'NONE', #119662, #201745, #102617 ) ;
#254253=ORIENTED_EDGE ( 'NONE', *, *, #126909, .T. ) ;
#254260=ORIENTED_EDGE ( 'NONE', *, *, #145991, .T. ) ;
#254271=CARTESIAN_POINT ( 'NONE',  ( 21.30000000000002558, 1.115600667400684642E-11, -67.00000000000004263 ) ) ;
#254290=( BOUNDED_SURFACE ( )  B_SPLINE_SURFACE ( 3, 2, ( 
 ( #109467, #148631, #226860 ),
 ( #169506, #28715, #127776 ),
 ( #165626, #105604, #187758 ),
 ( #6526, #206024, #9106 ),
 ( #49518, #247712, #46921 ),
 ( #69093, #186464, #228159 ),
 ( #27423, #48224, #129057 ),
 ( #144741, #110762, #208606 ),
 ( #29978, #26111, #224291 ),
 ( #106908, #189026, #190325 ) ),
 .UNSPECIFIED., .F., .F., .F. ) 
 B_SPLINE_SURFACE_WITH_KNOTS ( ( 4, 2, 2, 2, 4 ),
 ( 3, 3 ),
 ( 0.0001836757140119193922, 0.0004000170051583608419, 0.0005081876507315815803, 0.0005622729735181920038, 0.0006163582963048023187 ),
 ( 0.000000000000000000, 1.000000000000000000 ),
 .UNSPECIFIED. ) 
 GEOMETRIC_REPRESENTATION_ITEM ( )  RATIONAL_B_SPLINE_SURFACE ( (
 ( 1.000000000000000000, 0.7071067811865135999, 1.000000000000000000),
 ( 1.000000000000000000, 0.6461995200032549791, 1.000000000000000000),
 ( 1.000000000000000000, 0.5776453529546025090, 1.000000000000000000),
 ( 1.000000000000000000, 0.4585233068353464780, 1.000000000000000000),
 ( 1.000000000000000000, 0.4154092989903095390, 1.000000000000000000),
 ( 1.000000000000000000, 0.3550093145854532617, 1.000000000000000000),
 ( 1.000000000000000000, 0.3354498651685169364, 1.000000000000000000),
 ( 1.000000000000000000, 0.3060347992257099192, 1.000000000000000000),
 ( 1.000000000000000000, 0.2963555829624704985, 1.000000000000000000),
 ( 1.000000000000000000, 0.2966190024560417804, 1.000000000000000000) ) ) 
 REPRESENTATION_ITEM ( '' )  SURFACE ( )  );
#254302=ADVANCED_FACE ( 'NONE', ( #173400 ), #240693, .F. ) ;
#254308=VERTEX_POINT ( 'NONE', #14300 ) ;
#254310=CARTESIAN_POINT ( 'NONE',  ( -20.64999999999999858, 7.250000000011155521, -79.25000000000004263 ) ) ;
#254330=ORIENTED_EDGE ( 'NONE', *, *, #114067, .F. ) ;
#254338=DIRECTION ( 'NONE',  ( 2.952720810173289112E-16, -1.000000000000000000, -0.000000000000000000 ) ) ;
#254340=ORIENTED_EDGE ( 'NONE', *, *, #215716, .T. ) ;
#254359=ORIENTED_EDGE ( 'NONE', *, *, #249799, .F. ) ;
#254365=DIRECTION ( 'NONE',  ( 1.000000000000000000, 3.265361837132813093E-16, -0.000000000000000000 ) ) ;
#254376=AXIS2_PLACEMENT_3D ( 'NONE', #71162, #192374, #174137 ) ;
#254391=CIRCLE ( 'NONE', #141991, 0.1000000000000028644 ) ;
#254404=EDGE_CURVE ( 'NONE', #155368, #248700, #44170, .T. ) ;
#254405=VERTEX_POINT ( 'NONE', #234598 ) ;
#254430=FACE_OUTER_BOUND ( 'NONE', #13457, .T. ) ;
#254514=DIRECTION ( 'NONE',  ( 0.7071067811865475727, 0.7071067811865475727, 0.000000000000000000 ) ) ;
#254529=ORIENTED_EDGE ( 'NONE', *, *, #142615, .T. ) ;
#254533=ORIENTED_EDGE ( 'NONE', *, *, #227136, .T. ) ;
#254563=EDGE_CURVE ( 'NONE', #60863, #101410, #227668, .T. ) ;
#254578=CARTESIAN_POINT ( 'NONE',  ( -21.55000000000000071, 7.350000000011155166, -79.35000000000005116 ) ) ;
#254587=CARTESIAN_POINT ( 'NONE',  ( 21.14999999999999858, 6.650000000011155876, -79.15000000000004832 ) ) ;
#254614=CARTESIAN_POINT ( 'NONE',  ( -18.59999999999999787, 9.250000000011157297, -88.15000000000004832 ) ) ;
#254662=CARTESIAN_POINT ( 'NONE',  ( 21.08078803292165659, 6.333012964448272442, -66.92081401284225706 ) ) ;
#254665=LINE ( 'NONE', #117766, #189184 ) ;
#254668=EDGE_LOOP ( 'NONE', ( #135612, #241581, #37328, #213165 ) ) ;
#254703=CIRCLE ( 'NONE', #171406, 11.80000000000000426 ) ;
#254718=ORIENTED_EDGE ( 'NONE', *, *, #120521, .F. ) ;
#254724=DIRECTION ( 'NONE',  ( 1.000000000000000000, 2.952720810173289112E-16, -0.000000000000000000 ) ) ;
#254741=CARTESIAN_POINT ( 'NONE',  ( -20.85000000000000142, 1.115600667400684642E-11, -100.5000000000000426 ) ) ;
#254747=CARTESIAN_POINT ( 'NONE',  ( -23.15000000000000213, 11.65000000001115588, -88.35000000000003695 ) ) ;
#254786=CARTESIAN_POINT ( 'NONE',  ( -23.25000000000000000, -8.596261682231832069, -91.04987248284976431 ) ) ;
#254790=DIRECTION ( 'NONE',  ( -1.000000000000000000, -0.000000000000000000, 0.000000000000000000 ) ) ;
#254796=CIRCLE ( 'NONE', #204768, 4.049999999999998934 ) ;
#254812=DIRECTION ( 'NONE',  ( 0.000000000000000000, 0.000000000000000000, -1.000000000000000000 ) ) ;
#254848=CARTESIAN_POINT ( 'NONE',  ( -22.59999999999999787, 11.74956712350054744, -66.89914163090134025 ) ) ;
#254888=ORIENTED_EDGE ( 'NONE', *, *, #156655, .F. ) ;
#254908=VECTOR ( 'NONE', #176004, 1000.000000000000000 ) ;
#254966=EDGE_CURVE ( 'NONE', #95156, #157348, #202727, .T. ) ;
#254983=EDGE_CURVE ( 'NONE', #113968, #143581, #19586, .T. ) ;
#254992=CARTESIAN_POINT ( 'NONE',  ( -21.13498764882296044, 0.001656394742485162381, -60.50438185652610912 ) ) ;
#254996=DIRECTION ( 'NONE',  ( 1.000000000000000000, -0.000000000000000000, -0.000000000000000000 ) ) ;
#255017=DIRECTION ( 'NONE',  ( 0.000000000000000000, 0.1350103645451876666, 0.9908441862701600211 ) ) ;
#255049=CIRCLE ( 'NONE', #38644, 0.09999999999999939493 ) ;
#255061=VECTOR ( 'NONE', #206053, 999.9999999999998863 ) ;
#255068=EDGE_CURVE ( 'NONE', #4905, #123588, #95242, .T. ) ;
#255076=ORIENTED_EDGE ( 'NONE', *, *, #229538, .T. ) ;
#255100=LINE ( 'NONE', #76508, #238442 ) ;
#255102=VERTEX_POINT ( 'NONE', #23647 ) ;
#255128=DIRECTION ( 'NONE',  ( 0.000000000000000000, -0.1350103645451876944, 0.9908441862701601321 ) ) ;
#255189=FACE_OUTER_BOUND ( 'NONE', #33795, .T. ) ;
#255197=EDGE_CURVE ( 'NONE', #237745, #224664, #20240, .T. ) ;
#255213=CARTESIAN_POINT ( 'NONE',  ( 21.00000000000000000, 9.750000000011153745, -88.15000000000004832 ) ) ;
#255226=CARTESIAN_POINT ( 'NONE',  ( -23.15000000000000213, 11.75000000001115552, -97.40000000000004832 ) ) ;
#255243=EDGE_CURVE ( 'NONE', #254308, #218145, #91143, .T. ) ;
#255254=DIRECTION ( 'NONE',  ( 0.000000000000000000, 0.000000000000000000, 1.000000000000000000 ) ) ;
#255286=TOROIDAL_SURFACE ( 'NONE', #197066, 11.70000000000000639, 0.1000000000000000056 ) ;
#255323=CARTESIAN_POINT ( 'NONE',  ( 18.45036689428334853, -9.490184143317749843, -74.01269582748609821 ) ) ;
#255331=FACE_OUTER_BOUND ( 'NONE', #223033, .T. ) ;
#255342=CIRCLE ( 'NONE', #80393, 0.3999999999999975797 ) ;
#255361=ORIENTED_EDGE ( 'NONE', *, *, #75920, .T. ) ;
#255371=CARTESIAN_POINT ( 'NONE',  ( -18.59999999999999787, 9.350000000011156942, -79.35000000000005116 ) ) ;
#255377=ORIENTED_EDGE ( 'NONE', *, *, #11392, .F. ) ;
#255378=CIRCLE ( 'NONE', #76350, 0.6000000000000033085 ) ;
#255390=DIRECTION ( 'NONE',  ( -0.000000000000000000, -0.1298341882519737922, -0.9915357197604890427 ) ) ;
#255395=FACE_OUTER_BOUND ( 'NONE', #6452, .T. ) ;
#255454=AXIS2_PLACEMENT_3D ( 'NONE', #16829, #32562, #91220 ) ;
#255550=ORIENTED_EDGE ( 'NONE', *, *, #69771, .T. ) ;
#255552=CIRCLE ( 'NONE', #139035, 0.5000000000000004441 ) ;
#255592=CARTESIAN_POINT ( 'NONE',  ( 23.15000000000000213, -11.74999999998883737, -79.25000000000004263 ) ) ;
#255595=CARTESIAN_POINT ( 'NONE',  ( -20.64999999999999858, 7.250000000011155521, -88.15000000000004832 ) ) ;
#255599=ORIENTED_EDGE ( 'NONE', *, *, #182778, .T. ) ;
#255650=EDGE_CURVE ( 'NONE', #24665, #219149, #212227, .T. ) ;
#255651=DIRECTION ( 'NONE',  ( -0.000000000000000000, 1.000000000000000000, 0.000000000000000000 ) ) ;
#255655=FACE_OUTER_BOUND ( 'NONE', #166635, .T. ) ;
#255657=CARTESIAN_POINT ( 'NONE',  ( -21.05000000000000071, 11.62071067812980907, -73.86841665234109655 ) ) ;
#255674=ORIENTED_EDGE ( 'NONE', *, *, #68831, .F. ) ;
#255680=DIRECTION ( 'NONE',  ( 0.000000000000000000, -2.862293735361729181E-14, -1.000000000000000000 ) ) ;
#255691=ADVANCED_FACE ( 'NONE', ( #147081 ), #191394, .T. ) ;
#255709=ORIENTED_EDGE ( 'NONE', *, *, #219565, .F. ) ;
#255764=CIRCLE ( 'NONE', #85078, 0.1000000000000028644 ) ;
#255791=EDGE_CURVE ( 'NONE', #86923, #221912, #56946, .T. ) ;
#255823=LINE ( 'NONE', #78500, #227772 ) ;
#255838=CARTESIAN_POINT ( 'NONE',  ( 23.14999999999999858, 1.115600667400684642E-11, -100.5000000000000426 ) ) ;
#255874=DIRECTION ( 'NONE',  ( 0.000000000000000000, 0.000000000000000000, -1.000000000000000000 ) ) ;
#255890=CYLINDRICAL_SURFACE ( 'NONE', #8301, 0.09999999999999939493 ) ;
#255925=ADVANCED_FACE ( 'NONE', ( #64678 ), #130329, .T. ) ;
#255935=ADVANCED_FACE ( 'NONE', ( #180792 ), #242759, .F. ) ;
#255948=AXIS2_PLACEMENT_3D ( 'NONE', #156659, #154104, #159210 ) ;
#255960=EDGE_CURVE ( 'NONE', #55997, #239916, #101055, .T. ) ;
#255986=CARTESIAN_POINT ( 'NONE',  ( -18.49719636458545224, -9.446365359216978064, -74.07161386988313723 ) ) ;
#255998=ORIENTED_EDGE ( 'NONE', *, *, #222824, .T. ) ;
#256020=CARTESIAN_POINT ( 'NONE',  ( -21.14999999999999858, 6.540656951712397138, -67.00000000000004263 ) ) ;
#256095=DIRECTION ( 'NONE',  ( 0.000000000000000000, 1.000000000000000000, 0.000000000000000000 ) ) ;
#256133=DIRECTION ( 'NONE',  ( -1.000000000000000000, 0.000000000000000000, 0.000000000000000000 ) ) ;
#256138=AXIS2_PLACEMENT_3D ( 'NONE', #222581, #180921, #240896 ) ;
#256145=EDGE_CURVE ( 'NONE', #133216, #80211, #118919, .T. ) ;
#256148=ORIENTED_EDGE ( 'NONE', *, *, #75208, .T. ) ;
#256149=EDGE_CURVE ( 'NONE', #133700, #150237, #36834, .T. ) ;
#256156=ORIENTED_EDGE ( 'NONE', *, *, #152678, .F. ) ;
#256180=ORIENTED_EDGE ( 'NONE', *, *, #68692, .F. ) ;
#256184=CIRCLE ( 'NONE', #68836, 0.2000000000000057288 ) ;
#256223=AXIS2_PLACEMENT_3D ( 'NONE', #189675, #253486, #231381 ) ;
#256246=EDGE_CURVE ( 'NONE', #205206, #203901, #176339, .T. ) ;
#256256=VERTEX_POINT ( 'NONE', #15527 ) ;
#256264=AXIS2_PLACEMENT_3D ( 'NONE', #225773, #144958, #5435 ) ;
#256280=ORIENTED_EDGE ( 'NONE', *, *, #57314, .F. ) ;
#256332=EDGE_CURVE ( 'NONE', #74117, #111464, #191604, .T. ) ;
#256352=LINE ( 'NONE', #234278, #7655 ) ;
#256365=ORIENTED_EDGE ( 'NONE', *, *, #137292, .F. ) ;
#256399=DIRECTION ( 'NONE',  ( 0.000000000000000000, 0.000000000000000000, -1.000000000000000000 ) ) ;
#256412=CIRCLE ( 'NONE', #73355, 4.150000000000001243 ) ;
#256428=AXIS2_PLACEMENT_3D ( 'NONE', #255838, #117660, #158120 ) ;
#256435=DIRECTION ( 'NONE',  ( 0.000000000000000000, -0.1568667991644714932, 0.9876197685951274563 ) ) ;
#256436=VERTEX_POINT ( 'NONE', #80573 ) ;
#256454=ORIENTED_EDGE ( 'NONE', *, *, #103416, .T. ) ;
#256473=LINE ( 'NONE', #20519, #28834 ) ;
#256497=CARTESIAN_POINT ( 'NONE',  ( 21.13461538461538325, 10.61458296203669427, -79.35000000000006537 ) ) ;
#256513=CIRCLE ( 'NONE', #40133, 0.1000000000000028644 ) ;
#256516=EDGE_CURVE ( 'NONE', #20400, #18191, #159571, .T. ) ;
#256538=ORIENTED_EDGE ( 'NONE', *, *, #93029, .T. ) ;
#256546=ADVANCED_FACE ( 'NONE', ( #86018 ), #34881, .F. ) ;
#256551=AXIS2_PLACEMENT_3D ( 'NONE', #34805, #11364, #249973 ) ;
#256558=EDGE_LOOP ( 'NONE', ( #21940, #77630, #51552, #5800 ) ) ;
#256572=FACE_OUTER_BOUND ( 'NONE', #210492, .T. ) ;
#256594=VECTOR ( 'NONE', #103573, 1000.000000000000000 ) ;
#256603=CARTESIAN_POINT ( 'NONE',  ( 18.51565452909393983, -9.352859338825888713, -74.19490932123386528 ) ) ;
#256631=EDGE_CURVE ( 'NONE', #237980, #43295, #126614, .T. ) ;
#256646=VERTEX_POINT ( 'NONE', #11673 ) ;
#256666=EDGE_CURVE ( 'NONE', #10085, #120362, #84877, .T. ) ;
#256721=ORIENTED_EDGE ( 'NONE', *, *, #67626, .F. ) ;
#256762=DIRECTION ( 'NONE',  ( 0.000000000000000000, 1.000000000000000000, 0.000000000000000000 ) ) ;
#256771=CARTESIAN_POINT ( 'NONE',  ( -20.85000000000000142, -1.249999999988843369, -108.3004807544151333 ) ) ;
#256783=CARTESIAN_POINT ( 'NONE',  ( 23.14999999999998437, 1.115650265596050101E-11, -62.95000000000004547 ) ) ;
#256814=DIRECTION ( 'NONE',  ( 1.000000000000000000, 0.000000000000000000, 0.000000000000000000 ) ) ;
#256870=DIRECTION ( 'NONE',  ( 0.000000000000000000, 0.000000000000000000, -1.000000000000000000 ) ) ;
#256891=AXIS2_PLACEMENT_3D ( 'NONE', #51083, #207650, #10719 ) ;
#256901=ORIENTED_EDGE ( 'NONE', *, *, #243569, .F. ) ;
#256908=CARTESIAN_POINT ( 'NONE',  ( 21.09107601085565165, 0.03930716472848838627, -60.63612202464012313 ) ) ;
#256950=FACE_OUTER_BOUND ( 'NONE', #168957, .T. ) ;
#256955=AXIS2_PLACEMENT_3D ( 'NONE', #245620, #185646, #66974 ) ;
#256991=ORIENTED_EDGE ( 'NONE', *, *, #69886, .T. ) ;
#257038=ORIENTED_EDGE ( 'NONE', *, *, #24989, .F. ) ;
#257046=AXIS2_PLACEMENT_3D ( 'NONE', #94185, #217648, #239823 ) ;
#257070=ORIENTED_EDGE ( 'NONE', *, *, #108273, .T. ) ;
#257072=CARTESIAN_POINT ( 'NONE',  ( -23.15000000000000213, -11.74999999998884448, -55.25000000000004974 ) ) ;
#257127=ORIENTED_EDGE ( 'NONE', *, *, #23221, .T. ) ;
#257134=LINE ( 'NONE', #53857, #38427 ) ;
#257146=ORIENTED_EDGE ( 'NONE', *, *, #157099, .F. ) ;
#257156=FACE_OUTER_BOUND ( 'NONE', #56087, .T. ) ;
#257160=CARTESIAN_POINT ( 'NONE',  ( -18.59999999999999787, 1.851028230152016674, -78.65391326942254580 ) ) ;
#257162=ORIENTED_EDGE ( 'NONE', *, *, #23221, .F. ) ;
#257191=CARTESIAN_POINT ( 'NONE',  ( 18.49999999999999645, 5.699452464332751767, -54.45772604343021328 ) ) ;
#257205=ORIENTED_EDGE ( 'NONE', *, *, #99747, .F. ) ;
#257229=DIRECTION ( 'NONE',  ( 0.000000000000000000, -1.000000000000000000, -0.000000000000000000 ) ) ;
#257233=CONICAL_SURFACE ( 'NONE', #7302, 4.299999999999956302, 0.7853981633974466137 ) ;
#257234=AXIS2_PLACEMENT_3D ( 'NONE', #6273, #229201, #187519 ) ;
#257251=DIRECTION ( 'NONE',  ( -0.000000000000000000, 0.8660254037844383745, -0.5000000000000003331 ) ) ;
#257270=ORIENTED_EDGE ( 'NONE', *, *, #86762, .T. ) ;
#257279=DIRECTION ( 'NONE',  ( 0.000000000000000000, 1.000000000000000000, 2.891205793294679805E-16 ) ) ;
#257303=CARTESIAN_POINT ( 'NONE',  ( -20.85000000000000142, 11.65000000001115232, -93.71613433702194129 ) ) ;
#257313=AXIS2_PLACEMENT_3D ( 'NONE', #130846, #85267, #164849 ) ;
#257339=ORIENTED_EDGE ( 'NONE', *, *, #150518, .T. ) ;
#257372=CIRCLE ( 'NONE', #40990, 0.1000000000000028644 ) ;
#257390=ORIENTED_EDGE ( 'NONE', *, *, #100027, .F. ) ;
#257437=VECTOR ( 'NONE', #181943, 1000.000000000000000 ) ;
#257488=EDGE_LOOP ( 'NONE', ( #160414, #128982, #235964, #120250 ) ) ;
#257521=EDGE_CURVE ( 'NONE', #114655, #111692, #174977, .T. ) ;
#257530=AXIS2_PLACEMENT_3D ( 'NONE', #106371, #98980, #184640 ) ;
#257532=DIRECTION ( 'NONE',  ( -3.265361837132813093E-16, 1.000000000000000000, 0.000000000000000000 ) ) ;
#257552=ORIENTED_EDGE ( 'NONE', *, *, #228523, .T. ) ;
#257568=CYLINDRICAL_SURFACE ( 'NONE', #240215, 0.1000000000000028644 ) ;
#257574=EDGE_LOOP ( 'NONE', ( #8581, #45116, #22936, #175687 ) ) ;
#257595=ORIENTED_EDGE ( 'NONE', *, *, #42908, .F. ) ;
#257601=LINE ( 'NONE', #96009, #1460 ) ;
#257638=CARTESIAN_POINT ( 'NONE',  ( -21.76363531954647357, 0.09900187431060442078, -59.98706345212830371 ) ) ;
#257645=LINE ( 'NONE', #118206, #99921 ) ;
#257646=CARTESIAN_POINT ( 'NONE',  ( 21.05000000000000071, 10.72371710471867701, -74.66491356908764487 ) ) ;
#257662=DIRECTION ( 'NONE',  ( 0.000000000000000000, -1.000000000000000000, 0.000000000000000000 ) ) ;
#257670=AXIS2_PLACEMENT_3D ( 'NONE', #8151, #168553, #6856 ) ;
#257679=AXIS2_PLACEMENT_3D ( 'NONE', #56591, #176599, #194878 ) ;
#257686=DIRECTION ( 'NONE',  ( 0.000000000000000000, 0.000000000000000000, 1.000000000000000000 ) ) ;
#257689=CYLINDRICAL_SURFACE ( 'NONE', #228183, 0.1000000000000000472 ) ;
#257714=EDGE_LOOP ( 'NONE', ( #4935, #5766, #190637 ) ) ;
#257719=EDGE_LOOP ( 'NONE', ( #199041, #130561, #183501, #225966 ) ) ;
#257729=VERTEX_POINT ( 'NONE', #130342 ) ;
#257743=FACE_OUTER_BOUND ( 'NONE', #275, .T. ) ;
#257749=AXIS2_PLACEMENT_3D ( 'NONE', #173225, #14119, #93632 ) ;
#257765=DIRECTION ( 'NONE',  ( -1.000000000000000000, 0.000000000000000000, 0.000000000000000000 ) ) ;
#257826=CIRCLE ( 'NONE', #53885, 0.1000000000000028644 ) ;
#257850=AXIS2_PLACEMENT_3D ( 'NONE', #16357, #231544, #73771 ) ;
#257867=FACE_OUTER_BOUND ( 'NONE', #43527, .T. ) ;
#257895=VERTEX_POINT ( 'NONE', #213740 ) ;
#257897=DIRECTION ( 'NONE',  ( 0.000000000000000000, 0.000000000000000000, 1.000000000000000000 ) ) ;
#257898=DIRECTION ( 'NONE',  ( 0.000000000000000000, -1.000000000000000000, 0.000000000000000000 ) ) ;
#257922=VERTEX_POINT ( 'NONE', #257952 ) ;
#257934=AXIS2_PLACEMENT_3D ( 'NONE', #175339, #254790, #235270 ) ;
#257936=AXIS2_PLACEMENT_3D ( 'NONE', #165350, #160240, #225289 ) ;
#257952=CARTESIAN_POINT ( 'NONE',  ( 19.75857864376268935, 11.75000000001115907, -91.85000000000003695 ) ) ;
#258004=CARTESIAN_POINT ( 'NONE',  ( -20.94999999999999929, -11.41227409413852811, -97.60000000000005116 ) ) ;
#258014=CARTESIAN_POINT ( 'NONE',  ( -22.57320508075687115, 11.75000000001115552, -67.00000000000007105 ) ) ;
#258032=EDGE_CURVE ( 'NONE', #160493, #232467, #230428, .T. ) ;
#258045=AXIS2_PLACEMENT_3D ( 'NONE', #89449, #170333, #249826 ) ;
#258082=LINE ( 'NONE', #80757, #4553 ) ;
#258086=VERTEX_POINT ( 'NONE', #208320 ) ;
#258095=DIRECTION ( 'NONE',  ( 1.000000000000000000, -0.000000000000000000, -0.000000000000000000 ) ) ;
ENDSEC;
END-ISO-10303-21;
